ISO-10303-21;
HEADER;
FILE_DESCRIPTION (('STEP AP214'),
    '1' );
FILE_NAME ('Injection Molded Chain Links 13.step',
    '2026-10-08T22:59:04',
    ( '' ),
    ( '' ),
    'SwSTEP 2.0',
    'SolidWorks 2020',
    '' );
FILE_SCHEMA (( 'AUTOMOTIVE_DESIGN' ));
ENDSEC;

DATA;
#6=CARTESIAN_POINT ( 'NONE',  ( 20.11144452914042802, 66.06638914889212799, -128.6328140305745933 ) ) ;
#111=CARTESIAN_POINT ( 'NONE',  ( -20.94999999999999929, 87.48912529308798014, -105.9231074845242091 ) ) ;
#115=ORIENTED_EDGE ( 'NONE', *, *, #108700, .T. ) ;
#132=AXIS2_PLACEMENT_3D ( 'NONE', #200037, #1808, #61804 ) ;
#138=ORIENTED_EDGE ( 'NONE', *, *, #133333, .T. ) ;
#170=VECTOR ( 'NONE', #232496, 1000.000000000000000 ) ;
#175=ORIENTED_EDGE ( 'NONE', *, *, #85520, .F. ) ;
#233=ORIENTED_EDGE ( 'NONE', *, *, #144291, .F. ) ;
#259=ORIENTED_EDGE ( 'NONE', *, *, #102586, .T. ) ;
#274=FACE_OUTER_BOUND ( 'NONE', #244850, .T. ) ;
#291=CYLINDRICAL_SURFACE ( 'NONE', #124370, 0.1000000000000028644 ) ;
#304=ORIENTED_EDGE ( 'NONE', *, *, #196870, .F. ) ;
#309=AXIS2_PLACEMENT_3D ( 'NONE', #21762, #240801, #38751 ) ;
#318=DIRECTION ( 'NONE',  ( 0.000000000000000000, 0.6728971962616412394, -0.7397360091703134577 ) ) ;
#361=DIRECTION ( 'NONE',  ( 0.000000000000000000, 0.6728971962617102953, 0.7397360091702507301 ) ) ;
#377=EDGE_LOOP ( 'NONE', ( #153054, #45410, #48839 ) ) ;
#388=AXIS2_PLACEMENT_3D ( 'NONE', #182068, #137780, #103776 ) ;
#396=DIRECTION ( 'NONE',  ( 0.000000000000000000, 1.000000000000000000, 6.982962677686266711E-15 ) ) ;
#425=CARTESIAN_POINT ( 'NONE',  ( 21.05000000000000071, 65.27628289530457550, -128.8581939154367717 ) ) ;
#442=VERTEX_POINT ( 'NONE', #204323 ) ;
#473=DIRECTION ( 'NONE',  ( -1.000000000000000000, -0.000000000000000000, -0.000000000000000000 ) ) ;
#488=CARTESIAN_POINT ( 'NONE',  ( -20.94999999999999929, 69.15387683765929694, -99.28538121767448388 ) ) ;
#519=CIRCLE ( 'NONE', #54870, 0.1000000000000028644 ) ;
#525=VECTOR ( 'NONE', #181803, 1000.000000000000000 ) ;
#537=DIRECTION ( 'NONE',  ( 1.000000000000000000, 0.000000000000000000, -0.000000000000000000 ) ) ;
#538=DIRECTION ( 'NONE',  ( 1.000000000000000000, 0.000000000000000000, 0.000000000000000000 ) ) ;
#609=LINE ( 'NONE', #234103, #72056 ) ;
#613=DIRECTION ( 'NONE',  ( 0.000000000000000000, -6.982962677686266711E-15, 1.000000000000000000 ) ) ;
#624=EDGE_CURVE ( 'NONE', #224260, #121586, #254952, .T. ) ;
#631=ORIENTED_EDGE ( 'NONE', *, *, #65245, .T. ) ;
#652=ORIENTED_EDGE ( 'NONE', *, *, #252109, .F. ) ;
#688=ORIENTED_EDGE ( 'NONE', *, *, #183122, .T. ) ;
#760=LINE ( 'NONE', #80294, #188466 ) ;
#768=ORIENTED_EDGE ( 'NONE', *, *, #108329, .T. ) ;
#813=ORIENTED_EDGE ( 'NONE', *, *, #63724, .F. ) ;
#832=DIRECTION ( 'NONE',  ( 1.000000000000000000, -7.304098846218134667E-16, -5.100424963727256530E-30 ) ) ;
#852=CARTESIAN_POINT ( 'NONE',  ( 21.30000000000002558, 76.00000000001213607, -136.5231074845242745 ) ) ;
#855=CARTESIAN_POINT ( 'NONE',  ( 21.05000000000000071, 69.74218538953603286, -136.6208977758331287 ) ) ;
#860=CARTESIAN_POINT ( 'NONE',  ( -21.05000000000000071, 74.14897176987119565, -124.8691942151018139 ) ) ;
#863=CARTESIAN_POINT ( 'NONE',  ( 21.05000000000000071, 70.50000000001205080, -124.1178414656112352 ) ) ;
#869=ORIENTED_EDGE ( 'NONE', *, *, #89409, .F. ) ;
#901=DIRECTION ( 'NONE',  ( 1.000000000000000000, -2.952720810173289112E-16, -2.061873921506763405E-30 ) ) ;
#902=FACE_OUTER_BOUND ( 'NONE', #56191, .T. ) ;
#907=LINE ( 'NONE', #247242, #149676 ) ;
#918=DIRECTION ( 'NONE',  ( -1.000000000000000000, 7.304098846218134667E-16, 5.100424963727256530E-30 ) ) ;
#933=CIRCLE ( 'NONE', #167593, 0.1000000000000028644 ) ;
#935=DIRECTION ( 'NONE',  ( -0.000000000000000000, 1.000000000000000000, 6.982962677686267499E-15 ) ) ;
#949=DIRECTION ( 'NONE',  ( 1.000000000000000000, 0.000000000000000000, 0.000000000000000000 ) ) ;
#966=AXIS2_PLACEMENT_3D ( 'NONE', #7756, #245072, #225483 ) ;
#968=CARTESIAN_POINT ( 'NONE',  ( -21.05000000000000071, 87.65000000001192859, -106.1231074845242262 ) ) ;
#987=SPHERICAL_SURFACE ( 'NONE', #235532, 0.1000000000000000056 ) ;
#992=CIRCLE ( 'NONE', #105215, 12.97499999999999964 ) ;
#996=DIRECTION ( 'NONE',  ( -1.000000000000000000, 2.952720810173289112E-16, 2.061873921506763405E-30 ) ) ;
#1059=CARTESIAN_POINT ( 'NONE',  ( -21.65000000000000213, 68.29142135624935861, -124.2731074845243597 ) ) ;
#1085=AXIS2_PLACEMENT_3D ( 'NONE', #149356, #48937, #73678 ) ;
#1097=DIRECTION ( 'NONE',  ( -1.000000000000000000, 0.000000000000000000, -0.000000000000000000 ) ) ;
#1109=ORIENTED_EDGE ( 'NONE', *, *, #21363, .F. ) ;
#1120=DIRECTION ( 'NONE',  ( 0.000000000000000000, 1.000000000000000000, 6.982962677686266711E-15 ) ) ;
#1149=EDGE_CURVE ( 'NONE', #115956, #185096, #224248, .T. ) ;
#1150=ORIENTED_EDGE ( 'NONE', *, *, #62827, .T. ) ;
#1155=VERTEX_POINT ( 'NONE', #161747 ) ;
#1166=AXIS2_PLACEMENT_3D ( 'NONE', #61305, #43035, #117434 ) ;
#1174=CARTESIAN_POINT ( 'NONE',  ( -22.47071067811865319, 75.90090754530959316, -144.2431822290223522 ) ) ;
#1179=AXIS2_PLACEMENT_3D ( 'NONE', #169114, #67404, #208218 ) ;
#1182=DIRECTION ( 'NONE',  ( -1.000000000000000000, -0.000000000000000000, -0.000000000000000000 ) ) ;
#1194=DIRECTION ( 'NONE',  ( 0.000000000000000000, 0.000000000000000000, 1.000000000000000000 ) ) ;
#1212=CARTESIAN_POINT ( 'NONE',  ( -22.49510344025093644, 75.93287232181796753, -148.1730775896385808 ) ) ;
#1229=FACE_OUTER_BOUND ( 'NONE', #124610, .T. ) ;
#1282=CARTESIAN_POINT ( 'NONE',  ( 20.74625933824082580, 67.11708647892778856, -127.9679364604012477 ) ) ;
#1302=CARTESIAN_POINT ( 'NONE',  ( 21.07971444708685738, 69.67020791838558580, -136.6109309208422644 ) ) ;
#1310=ORIENTED_EDGE ( 'NONE', *, *, #34015, .F. ) ;
#1322=ORIENTED_EDGE ( 'NONE', *, *, #36825, .T. ) ;
#1374=ORIENTED_EDGE ( 'NONE', *, *, #27708, .F. ) ;
#1375=DIRECTION ( 'NONE',  ( -1.000000000000000000, 2.952720810173289112E-16, 2.061873921506763405E-30 ) ) ;
#1403=ORIENTED_EDGE ( 'NONE', *, *, #157105, .F. ) ;
#1405=DIRECTION ( 'NONE',  ( 3.616040088954490704E-32, 7.105427357601001859E-15, -1.000000000000000000 ) ) ;
#1451=DIRECTION ( 'NONE',  ( 0.000000000000000000, -1.000000000000000000, 0.000000000000000000 ) ) ;
#1474=FACE_OUTER_BOUND ( 'NONE', #212469, .T. ) ;
#1482=VERTEX_POINT ( 'NONE', #62306 ) ;
#1508=AXIS2_PLACEMENT_3D ( 'NONE', #56459, #216827, #96854 ) ;
#1531=AXIS2_PLACEMENT_3D ( 'NONE', #39502, #197251, #58994 ) ;
#1553=CARTESIAN_POINT ( 'NONE',  ( 22.40000000000010516, 76.00000000001315925, -148.2735403769831919 ) ) ;
#1561=CARTESIAN_POINT ( 'NONE',  ( 18.49999999999999289, 64.25000000001220712, -148.2731074845243882 ) ) ;
#1601=DIRECTION ( 'NONE',  ( 0.000000000000000000, -1.000000000000000000, -6.982962677686265922E-15 ) ) ;
#1620=VERTEX_POINT ( 'NONE', #165255 ) ;
#1648=CARTESIAN_POINT ( 'NONE',  ( -18.43599941264928077, 85.51932742860607561, -129.5501306950018261 ) ) ;
#1671=TOROIDAL_SURFACE ( 'NONE', #18441, 11.90000000000000391, 0.1000000000000000056 ) ;
#1700=DIRECTION ( 'NONE',  ( 0.000000000000000000, 0.000000000000000000, -1.000000000000000000 ) ) ;
#1717=AXIS2_PLACEMENT_3D ( 'NONE', #156925, #76069, #154373 ) ;
#1737=DIRECTION ( 'NONE',  ( -1.000000000000000000, -0.000000000000000000, -0.000000000000000000 ) ) ;
#1743=DIRECTION ( 'NONE',  ( -1.000000000000000000, 0.000000000000000000, 0.000000000000000000 ) ) ;
#1755=TOROIDAL_SURFACE ( 'NONE', #214163, 0.4000000000000009104, 0.1000000000000000056 ) ;
#1757=LINE ( 'NONE', #203820, #24029 ) ;
#1808=DIRECTION ( 'NONE',  ( 1.836970198721029934E-16, 1.000000000000000000, 6.982962677686266711E-15 ) ) ;
#1820=VERTEX_POINT ( 'NONE', #104926 ) ;
#1867=DIRECTION ( 'NONE',  ( 1.000000000000000000, 0.000000000000000000, 0.000000000000000000 ) ) ;
#1899=ADVANCED_FACE ( 'NONE', ( #67126 ), #109557, .T. ) ;
#1902=CARTESIAN_POINT ( 'NONE',  ( 20.94999999999999574, 67.07338541492499928, -128.0514244653012383 ) ) ;
#1905=TOROIDAL_SURFACE ( 'NONE', #255779, 0.2000000000000000111, 0.1000000000000000056 ) ;
#1927=VECTOR ( 'NONE', #206610, 1000.000000000000000 ) ;
#1930=EDGE_CURVE ( 'NONE', #157880, #236445, #248331, .T. ) ;
#1938=EDGE_CURVE ( 'NONE', #192475, #210448, #69715, .T. ) ;
#1942=CARTESIAN_POINT ( 'NONE',  ( -18.50000000000001066, 85.41920341803874805, -129.2753216740955509 ) ) ;
#1957=DIRECTION ( 'NONE',  ( 0.000000000000000000, 0.4999999999999088507, -0.8660254037844913322 ) ) ;
#1960=EDGE_CURVE ( 'NONE', #37312, #186227, #89247, .T. ) ;
#1968=EDGE_CURVE ( 'NONE', #143912, #15448, #101125, .T. ) ;
#1980=ORIENTED_EDGE ( 'NONE', *, *, #49123, .T. ) ;
#1987=ADVANCED_FACE ( 'NONE', ( #31882 ), #172701, .T. ) ;
#1990=CARTESIAN_POINT ( 'NONE',  ( -20.64999999999999858, 85.50000000001207923, -126.6291383618717816 ) ) ;
#2028=FACE_OUTER_BOUND ( 'NONE', #209242, .T. ) ;
#2031=EDGE_CURVE ( 'NONE', #227184, #229125, #238749, .T. ) ;
#2034=ORIENTED_EDGE ( 'NONE', *, *, #224184, .F. ) ;
#2038=COLOUR_RGB ( '', 0.72549020, 0.75294118, 0.79215686) ;
#2048=CARTESIAN_POINT ( 'NONE',  ( -21.05000000000000071, 76.10000000001220144, -143.0637644362255401 ) ) ;
#2065=CARTESIAN_POINT ( 'NONE',  ( -21.05000000000000071, 64.35000000001214460, -136.4231074845243938 ) ) ;
#2085=AXIS2_PLACEMENT_3D ( 'NONE', #968, #120985, #200495 ) ;
#2089=CARTESIAN_POINT ( 'NONE',  ( -22.50000000000000000, 76.00000000001213607, -136.5231074845242745 ) ) ;
#2097=DIRECTION ( 'NONE',  ( 1.000000000000000000, -0.000000000000000000, -0.000000000000000000 ) ) ;
#2100=ORIENTED_EDGE ( 'NONE', *, *, #71790, .T. ) ;
#2152=CIRCLE ( 'NONE', #110487, 0.1000000000000028644 ) ;
#2165=DIRECTION ( 'NONE',  ( 0.000000000000000000, -0.8660254037844419273, 0.4999999999999942824 ) ) ;
#2194=PRODUCT_DEFINITION ( 'UNKNOWN', '', #98794, #60944 ) ;
#2216=EDGE_CURVE ( 'NONE', #139066, #12375, #192974, .T. ) ;
#2235=CIRCLE ( 'NONE', #43948, 0.1000000000000028644 ) ;
#2238=CARTESIAN_POINT ( 'NONE',  ( 21.14999999999999858, 64.25000000001213607, -136.4231074845243938 ) ) ;
#2261=CARTESIAN_POINT ( 'NONE',  ( 22.39999999999999503, 76.10085836911093793, -148.2726746080136877 ) ) ;
#2268=TOROIDAL_SURFACE ( 'NONE', #247986, 2.100000000000002309, 0.1000000000000000056 ) ;
#2311=ADVANCED_FACE ( 'NONE', ( #25157 ), #227174, .T. ) ;
#2341=EDGE_CURVE ( 'NONE', #80343, #8664, #126314, .T. ) ;
#2359=CIRCLE ( 'NONE', #10762, 3.900000000000000799 ) ;
#2362=FACE_OUTER_BOUND ( 'NONE', #103503, .T. ) ;
#2369=EDGE_LOOP ( 'NONE', ( #246721, #113564, #221007, #28489 ) ) ;
#2382=ORIENTED_EDGE ( 'NONE', *, *, #5338, .F. ) ;
#2425=AXIS2_PLACEMENT_3D ( 'NONE', #153513, #135160, #16531 ) ;
#2441=ORIENTED_EDGE ( 'NONE', *, *, #117503, .T. ) ;
#2446=CIRCLE ( 'NONE', #148194, 11.65000000000000746 ) ;
#2466=CARTESIAN_POINT ( 'NONE',  ( -18.59999999999999787, 77.83585931145546510, -91.51866831572576189 ) ) ;
#2492=TOROIDAL_SURFACE ( 'NONE', #52568, 0.2000000000000000111, 0.1000000000000000056 ) ;
#2502=ORIENTED_EDGE ( 'NONE', *, *, #189485, .F. ) ;
#2514=AXIS2_PLACEMENT_3D ( 'NONE', #52057, #252836, #131610 ) ;
#2517=FACE_OUTER_BOUND ( 'NONE', #218625, .T. ) ;
#2523=DIRECTION ( 'NONE',  ( 0.000000000000000000, 0.9908441862701605762, -0.1350103645451835310 ) ) ;
#2574=LINE ( 'NONE', #182534, #181703 ) ;
#2576=CIRCLE ( 'NONE', #152651, 0.1000000000000028644 ) ;
#2579=CARTESIAN_POINT ( 'NONE',  ( 21.05000000000000071, 64.35000000001204512, -124.3731074845243825 ) ) ;
#2590=CARTESIAN_POINT ( 'NONE',  ( 21.08621493067296271, 69.65070570884047640, -136.5793023240004516 ) ) ;
#2611=DIRECTION ( 'NONE',  ( 1.000000000000000000, 0.000000000000000000, 0.000000000000000000 ) ) ;
#2614=DIRECTION ( 'NONE',  ( 0.000000000000000000, -7.109473446599835262E-15, 1.000000000000000000 ) ) ;
#2636=VERTEX_POINT ( 'NONE', #186191 ) ;
#2654=CARTESIAN_POINT ( 'NONE',  ( 18.49999999999999289, 65.79142135624952914, -148.2731074845243882 ) ) ;
#2669=CIRCLE ( 'NONE', #19250, 0.1000000000000028644 ) ;
#2677=ORIENTED_EDGE ( 'NONE', *, *, #225088, .T. ) ;
#2705=VERTEX_POINT ( 'NONE', #188744 ) ;
#2738=ORIENTED_EDGE ( 'NONE', *, *, #83930, .T. ) ;
#2755=ORIENTED_EDGE ( 'NONE', *, *, #163487, .F. ) ;
#2764=CIRCLE ( 'NONE', #86316, 0.1000000000000028644 ) ;
#2771=DIRECTION ( 'NONE',  ( 1.000000000000000000, 0.000000000000000000, 0.000000000000000000 ) ) ;
#2855=EDGE_CURVE ( 'NONE', #38011, #172986, #255817, .T. ) ;
#2869=VECTOR ( 'NONE', #140765, 1000.000000000000000 ) ;
#2874=EDGE_CURVE ( 'NONE', #24275, #199005, #159911, .T. ) ;
#2875=ORIENTED_EDGE ( 'NONE', *, *, #17361, .T. ) ;
#2881=AXIS2_PLACEMENT_3D ( 'NONE', #18555, #237603, #39428 ) ;
#2888=EDGE_CURVE ( 'NONE', #207855, #252068, #18546, .T. ) ;
#2896=CIRCLE ( 'NONE', #248607, 0.09999999999999939493 ) ;
#2909=FACE_OUTER_BOUND ( 'NONE', #250237, .T. ) ;
#2926=CARTESIAN_POINT ( 'NONE',  ( -23.25000000000000000, 76.00000000001213607, -136.5231074845242745 ) ) ;
#2937=ORIENTED_EDGE ( 'NONE', *, *, #140716, .F. ) ;
#2975=FACE_OUTER_BOUND ( 'NONE', #65005, .T. ) ;
#2981=VERTEX_POINT ( 'NONE', #187177 ) ;
#3015=ORIENTED_EDGE ( 'NONE', *, *, #62731, .F. ) ;
#3052=DIRECTION ( 'NONE',  ( 0.000000000000000000, 0.000000000000000000, 1.000000000000000000 ) ) ;
#3058=DIRECTION ( 'NONE',  ( 1.000000000000000000, 0.000000000000000000, 0.000000000000000000 ) ) ;
#3059=CARTESIAN_POINT ( 'NONE',  ( -18.40000000000000213, 85.50000000001192291, -96.10095763519393586 ) ) ;
#3077=FACE_OUTER_BOUND ( 'NONE', #184933, .T. ) ;
#3082=VERTEX_POINT ( 'NONE', #153200 ) ;
#3119=EDGE_CURVE ( 'NONE', #253291, #144360, #147534, .T. ) ;
#3148=LINE ( 'NONE', #162265, #65679 ) ;
#3160=VECTOR ( 'NONE', #84787, 1000.000000000000000 ) ;
#3176=CIRCLE ( 'NONE', #94767, 0.09999999999999939493 ) ;
#3184=DIRECTION ( 'NONE',  ( 1.000000000000000000, 0.000000000000000000, 0.000000000000000000 ) ) ;
#3185=VERTEX_POINT ( 'NONE', #110175 ) ;
#3232=FACE_OUTER_BOUND ( 'NONE', #130749, .T. ) ;
#3276=DIRECTION ( 'NONE',  ( 0.000000000000000000, -0.01562499999999307672, 0.9998779222360100194 ) ) ;
#3277=ORIENTED_EDGE ( 'NONE', *, *, #253791, .T. ) ;
#3286=FACE_OUTER_BOUND ( 'NONE', #114005, .T. ) ;
#3317=EDGE_CURVE ( 'NONE', #147707, #22276, #128205, .T. ) ;
#3318=( BOUNDED_SURFACE ( )  B_SPLINE_SURFACE ( 3, 2, ( 
 ( #250457, #11879, #228340 ),
 ( #130504, #9282, #52241 ),
 ( #247891, #229623, #88794 ),
 ( #54812, #230921, #151384 ),
 ( #69275, #13147, #91396 ),
 ( #131795, #170978, #74433 ) ),
 .UNSPECIFIED., .F., .F., .F. ) 
 B_SPLINE_SURFACE_WITH_KNOTS ( ( 4, 2, 4 ),
 ( 3, 3 ),
 ( 4.712388980384689674, 5.497787143782137953, 6.283185307179586232 ),
 ( 0.000000000000000000, 1.000000000000000000 ),
 .UNSPECIFIED. ) 
 GEOMETRIC_REPRESENTATION_ITEM ( )  RATIONAL_B_SPLINE_SURFACE ( (
 ( 1.000000000000000000, 0.7071067811865475727, 1.000000000000000000),
 ( 1.000000000000000000, 0.7727932973487801060, 1.000000000000000000),
 ( 1.000000000000000000, 0.8282379607654416498, 1.000000000000000000),
 ( 1.000000000000000000, 0.9038128468035157015, 1.000000000000000000),
 ( 1.000000000000000000, 0.9240297172246855206, 1.000000000000000000),
 ( 1.000000000000000000, 0.9238795325112961754, 1.000000000000000000) ) ) 
 REPRESENTATION_ITEM ( '' )  SURFACE ( )  );
#3352=SPHERICAL_SURFACE ( 'NONE', #4676, 0.1000000000000000056 ) ;
#3360=DIRECTION ( 'NONE',  ( -1.000000000000000000, 0.000000000000000000, 0.000000000000000000 ) ) ;
#3363=VERTEX_POINT ( 'NONE', #40952 ) ;
#3379=CARTESIAN_POINT ( 'NONE',  ( 23.25000000000000000, 87.65000000001192859, -106.1231074845242262 ) ) ;
#3383=AXIS2_PLACEMENT_3D ( 'NONE', #216656, #120169, #1451 ) ;
#3404=CARTESIAN_POINT ( 'NONE',  ( 21.05000000000000071, 65.27628289530454708, -124.3731074845243825 ) ) ;
#3406=EDGE_CURVE ( 'NONE', #87320, #174077, #146417, .T. ) ;
#3427=CARTESIAN_POINT ( 'NONE',  ( 18.49999999999999645, 74.36282728704168221, -124.9409541190522930 ) ) ;
#3444=CARTESIAN_POINT ( 'NONE',  ( -21.05000000000000071, 69.70000000001212470, -136.4231074845243654 ) ) ;
#3455=ORIENTED_EDGE ( 'NONE', *, *, #196481, .T. ) ;
#3489=CARTESIAN_POINT ( 'NONE',  ( -23.15000000000000213, 64.35000000001195986, -110.0379132551783385 ) ) ;
#3512=CARTESIAN_POINT ( 'NONE',  ( 18.59999999999999076, 70.05000000001213323, -126.2174051794894893 ) ) ;
#3515=ADVANCED_FACE ( 'NONE', ( #193286 ), #10790, .T. ) ;
#3529=VECTOR ( 'NONE', #32726, 1000.000000000000000 ) ;
#3530=AXIS2_PLACEMENT_3D ( 'NONE', #224361, #202239, #103111 ) ;
#3535=AXIS2_PLACEMENT_3D ( 'NONE', #250930, #150574, #129718 ) ;
#3536=CARTESIAN_POINT ( 'NONE',  ( 20.94999999999999929, 87.29603075034721371, -106.0710066441880883 ) ) ;
#3548=LINE ( 'NONE', #184755, #102058 ) ;
#3556=CARTESIAN_POINT ( 'NONE',  ( 18.49999999999999645, 77.63717271298244782, -124.9409541190522788 ) ) ;
#3566=ORIENTED_EDGE ( 'NONE', *, *, #101725, .F. ) ;
#3567=DIRECTION ( 'NONE',  ( -0.000000000000000000, 7.272083257015735086E-15, -1.000000000000000000 ) ) ;
#3584=DIRECTION ( 'NONE',  ( 0.000000000000000000, -1.000000000000000000, -6.982962677686265922E-15 ) ) ;
#3601=VERTEX_POINT ( 'NONE', #94161 ) ;
#3607=CIRCLE ( 'NONE', #32711, 0.09999999999999520384 ) ;
#3624=DIRECTION ( 'NONE',  ( 0.000000000000000000, 1.000000000000000000, 6.982962677686266711E-15 ) ) ;
#3626=CARTESIAN_POINT ( 'NONE',  ( -18.59999999999999787, 68.97833521811179480, -99.18954208262705663 ) ) ;
#3633=VECTOR ( 'NONE', #143905, 1000.000000000000000 ) ;
#3652=FACE_OUTER_BOUND ( 'NONE', #75740, .T. ) ;
#3683=EDGE_CURVE ( 'NONE', #63258, #88307, #177154, .T. ) ;
#3702=AXIS2_PLACEMENT_3D ( 'NONE', #237308, #118663, #57358 ) ;
#3723=ORIENTED_EDGE ( 'NONE', *, *, #164192, .T. ) ;
#3732=CARTESIAN_POINT ( 'NONE',  ( -22.50000000000000000, 76.00000000001213607, -136.5231074845242745 ) ) ;
#3756=ORIENTED_EDGE ( 'NONE', *, *, #27419, .F. ) ;
#3768=CARTESIAN_POINT ( 'NONE',  ( -21.44999999999999929, 68.85000000001200249, -115.3731074845243540 ) ) ;
#3773=CARTESIAN_POINT ( 'NONE',  ( -18.59999999999999787, 65.66751761918668251, -97.42826094061121012 ) ) ;
#3785=DIRECTION ( 'NONE',  ( 0.000000000000000000, 0.000000000000000000, 1.000000000000000000 ) ) ;
#3799=ORIENTED_EDGE ( 'NONE', *, *, #36730, .T. ) ;
#3816=ORIENTED_EDGE ( 'NONE', *, *, #140021, .T. ) ;
#3849=AXIS2_PLACEMENT_3D ( 'NONE', #227179, #228489, #109795 ) ;
#3860=EDGE_LOOP ( 'NONE', ( #233354, #254636, #169036, #209580 ) ) ;
#3882=CARTESIAN_POINT ( 'NONE',  ( 21.05000000000000071, 77.16270174995010223, -128.6231074845242972 ) ) ;
#3887=DIRECTION ( 'NONE',  ( -0.000000000000000000, 0.1350103645451807555, 0.9908441862701610203 ) ) ;
#3906=ORIENTED_EDGE ( 'NONE', *, *, #25606, .T. ) ;
#3949=AXIS2_PLACEMENT_3D ( 'NONE', #96722, #255786, #137164 ) ;
#3954=DIRECTION ( 'NONE',  ( 1.000000000000000000, -1.836970198721029934E-16, -1.282749433769087582E-30 ) ) ;
#3963=ORIENTED_EDGE ( 'NONE', *, *, #30172, .T. ) ;
#4010=VERTEX_POINT ( 'NONE', #217321 ) ;
#4025=AXIS2_PLACEMENT_3D ( 'NONE', #10207, #28519, #144551 ) ;
#4026=LINE ( 'NONE', #83533, #145039 ) ;
#4030=FACE_OUTER_BOUND ( 'NONE', #48518, .T. ) ;
#4034=ORIENTED_EDGE ( 'NONE', *, *, #172720, .T. ) ;
#4051=TOROIDAL_SURFACE ( 'NONE', #120778, 0.2000000000000000111, 0.1000000000000000056 ) ;
#4066=CARTESIAN_POINT ( 'NONE',  ( -23.25000000000000000, 77.83585931145546510, -91.41866831572575336 ) ) ;
#4108=CARTESIAN_POINT ( 'NONE',  ( -18.59999999999999787, 64.35000000001208775, -129.5083017138703667 ) ) ;
#4174=ORIENTED_EDGE ( 'NONE', *, *, #158792, .F. ) ;
#4198=EDGE_CURVE ( 'NONE', #73777, #33295, #248030, .T. ) ;
#4206=ORIENTED_EDGE ( 'NONE', *, *, #65773, .F. ) ;
#4220=DIRECTION ( 'NONE',  ( 0.000000000000000000, -6.467318590049456648E-15, 1.000000000000000000 ) ) ;
#4273=LINE ( 'NONE', #83780, #222849 ) ;
#4313=DIRECTION ( 'NONE',  ( 0.000000000000000000, -1.000000000000000000, -6.352154140967427193E-15 ) ) ;
#4336=EDGE_CURVE ( 'NONE', #102291, #145138, #146428, .T. ) ;
#4341=FACE_OUTER_BOUND ( 'NONE', #74736, .T. ) ;
#4351=DIRECTION ( 'NONE',  ( -1.000000000000000000, -0.000000000000000000, -0.000000000000000000 ) ) ;
#4364=DIRECTION ( 'NONE',  ( -1.000000000000000000, 0.000000000000000000, -0.000000000000000000 ) ) ;
#4367=EDGE_CURVE ( 'NONE', #14895, #145261, #133645, .T. ) ;
#4373=VERTEX_POINT ( 'NONE', #217017 ) ;
#4381=EDGE_CURVE ( 'NONE', #175608, #105012, #100619, .T. ) ;
#4430=CARTESIAN_POINT ( 'NONE',  ( 21.05000000000000071, 69.55000000001207638, -126.5060803140843291 ) ) ;
#4437=ORIENTED_EDGE ( 'NONE', *, *, #100995, .T. ) ;
#4507=EDGE_CURVE ( 'NONE', #154018, #102756, #203882, .T. ) ;
#4526=EDGE_CURVE ( 'NONE', #89014, #40840, #196516, .T. ) ;
#4532=EDGE_CURVE ( 'NONE', #61324, #88196, #133977, .T. ) ;
#4589=ORIENTED_EDGE ( 'NONE', *, *, #231552, .F. ) ;
#4602=ORIENTED_EDGE ( 'NONE', *, *, #239549, .F. ) ;
#4641=CARTESIAN_POINT ( 'NONE',  ( 20.90851465518106167, 65.67467670974416194, -97.45317318268841689 ) ) ;
#4646=DIRECTION ( 'NONE',  ( 0.000000000000000000, -1.000000000000000000, -6.982962677686266711E-15 ) ) ;
#4652=ADVANCED_FACE ( 'NONE', ( #94203 ), #34277, .F. ) ;
#4676=AXIS2_PLACEMENT_3D ( 'NONE', #41251, #22970, #236843 ) ;
#4679=ORIENTED_EDGE ( 'NONE', *, *, #44245, .F. ) ;
#4723=DIRECTION ( 'NONE',  ( 6.938893903907224433E-15, 1.000000000000000000, 7.272083257015735086E-15 ) ) ;
#4729=ADVANCED_FACE ( 'NONE', ( #21127 ), #98030, .F. ) ;
#4737=CARTESIAN_POINT ( 'NONE',  ( 20.94999999999999574, 87.65000000001212754, -133.6231074845242119 ) ) ;
#4772=DIRECTION ( 'NONE',  ( 0.000000000000000000, 6.982962677686267499E-15, -1.000000000000000000 ) ) ;
#4789=DIRECTION ( 'NONE',  ( 0.000000000000000000, 0.000000000000000000, 1.000000000000000000 ) ) ;
#4799=EDGE_LOOP ( 'NONE', ( #91549, #131922 ) ) ;
#4818=FACE_OUTER_BOUND ( 'NONE', #36515, .T. ) ;
#4836=DIRECTION ( 'NONE',  ( -0.000000000000000000, -6.982962677686266711E-15, 1.000000000000000000 ) ) ;
#4844=DIRECTION ( 'NONE',  ( 1.000000000000000000, -6.938893903907222067E-15, -4.845403715540888588E-29 ) ) ;
#4894=ADVANCED_FACE ( 'NONE', ( #232156 ), #96719, .F. ) ;
#4906=ORIENTED_EDGE ( 'NONE', *, *, #143097, .T. ) ;
#4977=ORIENTED_EDGE ( 'NONE', *, *, #107367, .F. ) ;
#4989=CARTESIAN_POINT ( 'NONE',  ( -20.54999999999999716, 74.00000000001199396, -115.8477294072864083 ) ) ;
#5024=EDGE_CURVE ( 'NONE', #177416, #254300, #176071, .T. ) ;
#5043=CIRCLE ( 'NONE', #38389, 0.5000000000000004441 ) ;
#5098=VECTOR ( 'NONE', #103092, 1000.000000000000000 ) ;
#5106=DIRECTION ( 'NONE',  ( 0.000000000000000000, 6.853228547068871147E-15, -1.000000000000000000 ) ) ;
#5115=CARTESIAN_POINT ( 'NONE',  ( 20.53930447208010790, 67.02285131248707728, -128.0806003429518967 ) ) ;
#5142=CARTESIAN_POINT ( 'NONE',  ( -18.59999999999999787, 76.00000000001190870, -103.0231074845243029 ) ) ;
#5262=CIRCLE ( 'NONE', #122000, 0.1000000000000016431 ) ;
#5288=AXIS2_PLACEMENT_3D ( 'NONE', #6576, #69150, #148680 ) ;
#5291=ORIENTED_EDGE ( 'NONE', *, *, #144515, .F. ) ;
#5325=CARTESIAN_POINT ( 'NONE',  ( 20.94999999999999929, 74.16465844978765176, -124.9679561919613207 ) ) ;
#5337=VECTOR ( 'NONE', #70660, 1000.000000000000000 ) ;
#5338=EDGE_CURVE ( 'NONE', #108560, #45688, #219167, .T. ) ;
#5340=EDGE_CURVE ( 'NONE', #128962, #161509, #256529, .T. ) ;
#5379=CARTESIAN_POINT ( 'NONE',  ( 21.05000000000000071, 64.25000000001195133, -110.0379132551783243 ) ) ;
#5392=CARTESIAN_POINT ( 'NONE',  ( -21.03571358705756467, 64.25000000001209344, -129.6980006624665123 ) ) ;
#5412=AXIS2_PLACEMENT_3D ( 'NONE', #127689, #11600, #188938 ) ;
#5434=ORIENTED_EDGE ( 'NONE', *, *, #76568, .T. ) ;
#5458=ORIENTED_EDGE ( 'NONE', *, *, #77598, .T. ) ;
#5476=DIRECTION ( 'NONE',  ( 1.000000000000000000, 0.000000000000000000, 0.000000000000000000 ) ) ;
#5486=FACE_OUTER_BOUND ( 'NONE', #100643, .T. ) ;
#5559=EDGE_LOOP ( 'NONE', ( #184908, #121556, #8120, #6395 ) ) ;
#5563=VERTEX_POINT ( 'NONE', #10882 ) ;
#5579=CYLINDRICAL_SURFACE ( 'NONE', #230350, 2.000000000000001776 ) ;
#5604=CIRCLE ( 'NONE', #151405, 0.1000000000000028644 ) ;
#5624=LINE ( 'NONE', #147743, #27863 ) ;
#5637=ORIENTED_EDGE ( 'NONE', *, *, #44504, .T. ) ;
#5655=AXIS2_PLACEMENT_3D ( 'NONE', #250337, #71720, #32617 ) ;
#5658=DIRECTION ( 'NONE',  ( 0.000000000000000000, 0.5000000000000729417, 0.8660254037843965191 ) ) ;
#5662=EDGE_CURVE ( 'NONE', #23751, #207855, #135963, .T. ) ;
#5671=CARTESIAN_POINT ( 'NONE',  ( 18.59999999999999787, 74.13328508995475374, -124.7704322382423072 ) ) ;
#5694=CARTESIAN_POINT ( 'NONE',  ( -18.50000000000000000, 64.25000000001215028, -136.4231074845243938 ) ) ;
#5697=CARTESIAN_POINT ( 'NONE',  ( -18.59999999999999787, 77.83585931145546510, -91.51866831572576189 ) ) ;
#5719=ORIENTED_EDGE ( 'NONE', *, *, #166631, .F. ) ;
#5758=CARTESIAN_POINT ( 'NONE',  ( 22.60000000000000142, 76.00000000001213607, -136.5231074845242745 ) ) ;
#5765=DIRECTION ( 'NONE',  ( 1.000000000000000000, 0.000000000000000000, 0.000000000000000000 ) ) ;
#5768=ADVANCED_FACE ( 'NONE', ( #210368 ), #21591, .F. ) ;
#5777=EDGE_LOOP ( 'NONE', ( #43621, #52826, #235891, #20818 ) ) ;
#5793=FACE_OUTER_BOUND ( 'NONE', #103559, .T. ) ;
#5827=CARTESIAN_POINT ( 'NONE',  ( -21.59142135623730852, 68.15000000001205649, -124.2731074845243597 ) ) ;
#5850=VECTOR ( 'NONE', #8636, 1000.000000000000000 ) ;
#5851=FACE_OUTER_BOUND ( 'NONE', #133371, .T. ) ;
#5908=CARTESIAN_POINT ( 'NONE',  ( 23.14999999999999858, 76.00000000001188027, -99.02310748452428868 ) ) ;
#5923=CARTESIAN_POINT ( 'NONE',  ( 20.89878130938411616, 65.67252876774529113, -97.44570419949944551 ) ) ;
#5971=AXIS2_PLACEMENT_3D ( 'NONE', #189833, #230237, #11197 ) ;
#5974=CARTESIAN_POINT ( 'NONE',  ( 18.59999999999999076, 74.16465844978765176, -124.8679561919613263 ) ) ;
#5989=AXIS2_PLACEMENT_3D ( 'NONE', #157843, #198201, #58671 ) ;
#5994=AXIS2_PLACEMENT_3D ( 'NONE', #96587, #176178, #87171 ) ;
#6056=DIRECTION ( 'NONE',  ( 0.000000000000000000, -6.240597636138643358E-14, -1.000000000000000000 ) ) ;
#6063=CARTESIAN_POINT ( 'NONE',  ( 23.14999999999999858, 71.22429906543263201, -124.6743393804783722 ) ) ;
#6068=CARTESIAN_POINT ( 'NONE',  ( -21.14999999999999858, 76.00000000001217870, -142.7816861282870207 ) ) ;
#6086=CARTESIAN_POINT ( 'NONE',  ( -23.25000000000000000, 87.65000000001214175, -136.5231074845242176 ) ) ;
#6090=ADVANCED_FACE ( 'NONE', ( #201900 ), #84464, .F. ) ;
#6104=DIRECTION ( 'NONE',  ( 1.000000000000000000, 0.000000000000000000, 0.000000000000000000 ) ) ;
#6106=VERTEX_POINT ( 'NONE', #59789 ) ;
#6111=ORIENTED_EDGE ( 'NONE', *, *, #170334, .F. ) ;
#6129=FACE_OUTER_BOUND ( 'NONE', #14252, .T. ) ;
#6168=AXIS2_PLACEMENT_3D ( 'NONE', #129587, #229963, #13497 ) ;
#6169=AXIS2_PLACEMENT_3D ( 'NONE', #161352, #935, #60939 ) ;
#6199=ORIENTED_EDGE ( 'NONE', *, *, #96140, .F. ) ;
#6201=FACE_OUTER_BOUND ( 'NONE', #134189, .T. ) ;
#6233=ORIENTED_EDGE ( 'NONE', *, *, #7821, .F. ) ;
#6234=ORIENTED_EDGE ( 'NONE', *, *, #60981, .F. ) ;
#6286=DIRECTION ( 'NONE',  ( 0.000000000000000000, 0.000000000000000000, 1.000000000000000000 ) ) ;
#6328=CARTESIAN_POINT ( 'NONE',  ( 19.92426406871192412, 64.25000000001196554, -111.6731074845243938 ) ) ;
#6333=CARTESIAN_POINT ( 'NONE',  ( -21.00023020733438628, 69.60913075474442735, -136.5231074845243597 ) ) ;
#6344=DIRECTION ( 'NONE',  ( 0.000000000000000000, -1.000000000000000000, -6.982962677686265922E-15 ) ) ;
#6391=EDGE_CURVE ( 'NONE', #54263, #230368, #227356, .T. ) ;
#6395=ORIENTED_EDGE ( 'NONE', *, *, #145586, .F. ) ;
#6446=CARTESIAN_POINT ( 'NONE',  ( 21.14250536705908345, 69.48182782313142525, -136.5231074845243313 ) ) ;
#6474=ORIENTED_EDGE ( 'NONE', *, *, #218509, .F. ) ;
#6480=AXIS2_PLACEMENT_3D ( 'NONE', #71215, #13790, #54188 ) ;
#6508=EDGE_CURVE ( 'NONE', #1155, #152762, #206692, .T. ) ;
#6509=FACE_OUTER_BOUND ( 'NONE', #52436, .T. ) ;
#6531=CARTESIAN_POINT ( 'NONE',  ( -22.50000000000000000, 64.25000000001215028, -136.5231074845243597 ) ) ;
#6542=DIRECTION ( 'NONE',  ( 0.000000000000000000, -0.8660254037844377084, -0.5000000000000016653 ) ) ;
#6544=ORIENTED_EDGE ( 'NONE', *, *, #136042, .F. ) ;
#6576=CARTESIAN_POINT ( 'NONE',  ( -20.94999999999999929, 77.36087058720413268, -128.4501095574333362 ) ) ;
#6589=DIRECTION ( 'NONE',  ( 0.000000000000000000, -0.8660254037844420383, 0.4999999999999943379 ) ) ;
#6627=DIRECTION ( 'NONE',  ( 0.000000000000000000, -8.267618268485210697E-15, 1.000000000000000000 ) ) ;
#6679=PRESENTATION_STYLE_ASSIGNMENT (( #107059 ) ) ;
#6680=ADVANCED_FACE ( 'NONE', ( #204469 ), #7565, .T. ) ;
#6739=DIRECTION ( 'NONE',  ( 1.000000000000000000, 0.000000000000000000, 0.000000000000000000 ) ) ;
#6766=EDGE_CURVE ( 'NONE', #13648, #89168, #2669, .T. ) ;
#6807=VERTEX_POINT ( 'NONE', #234306 ) ;
#6842=TOROIDAL_SURFACE ( 'NONE', #31986, 7.800000000000000711, 0.1000000000000000056 ) ;
#6862=ORIENTED_EDGE ( 'NONE', *, *, #45278, .F. ) ;
#6926=EDGE_LOOP ( 'NONE', ( #195686, #46359, #248366 ) ) ;
#6929=CARTESIAN_POINT ( 'NONE',  ( -18.40000000000000213, 85.50000000001186606, -96.42291809330220076 ) ) ;
#6965=EDGE_CURVE ( 'NONE', #74752, #126029, #94437, .T. ) ;
#7000=TOROIDAL_SURFACE ( 'NONE', #61179, 1.900000000000002576, 0.1000000000000000056 ) ;
#7010=CARTESIAN_POINT ( 'NONE',  ( -21.05000000000000071, 76.00000000001213607, -136.5231074845242745 ) ) ;
#7023=FACE_OUTER_BOUND ( 'NONE', #90596, .T. ) ;
#7051=CARTESIAN_POINT ( 'NONE',  ( -18.59999999999999787, 61.95000000001210338, -131.0094124137634140 ) ) ;
#7101=CARTESIAN_POINT ( 'NONE',  ( -20.54999999999999716, 74.00000000001199396, -116.2477294072864140 ) ) ;
#7109=AXIS2_PLACEMENT_3D ( 'NONE', #211838, #171456, #51434 ) ;
#7164=FACE_OUTER_BOUND ( 'NONE', #187489, .T. ) ;
#7180=CARTESIAN_POINT ( 'NONE',  ( 18.59999999999999787, 77.26327546522911405, -95.12124281777788326 ) ) ;
#7181=EDGE_CURVE ( 'NONE', #86370, #155283, #202595, .T. ) ;
#7194=DIRECTION ( 'NONE',  ( 7.304098846218134667E-16, -1.000000000000000000, -6.982962677686267499E-15 ) ) ;
#7215=CARTESIAN_POINT ( 'NONE',  ( 20.93302460841142931, 65.68434038414356735, -97.48668807260655456 ) ) ;
#7221=CARTESIAN_POINT ( 'NONE',  ( -18.59999999999999787, 64.25000000001199396, -115.2731074845243739 ) ) ;
#7231=AXIS2_PLACEMENT_3D ( 'NONE', #246042, #67396, #189916 ) ;
#7265=AXIS2_PLACEMENT_3D ( 'NONE', #241260, #122598, #142137 ) ;
#7272=LINE ( 'NONE', #176648, #234115 ) ;
#7300=EDGE_CURVE ( 'NONE', #15679, #53074, #219248, .T. ) ;
#7343=EDGE_CURVE ( 'NONE', #126029, #74752, #223596, .T. ) ;
#7414=ORIENTED_EDGE ( 'NONE', *, *, #221548, .F. ) ;
#7432=LINE ( 'NONE', #28329, #25634 ) ;
#7453=CIRCLE ( 'NONE', #69839, 0.09999999999999459321 ) ;
#7536=VERTEX_POINT ( 'NONE', #207421 ) ;
#7565=SPHERICAL_SURFACE ( 'NONE', #173438, 0.1000000000000000056 ) ;
#7573=DIRECTION ( 'NONE',  ( 1.000000000000000000, 0.000000000000000000, 0.000000000000000000 ) ) ;
#7585=FACE_OUTER_BOUND ( 'NONE', #102189, .T. ) ;
#7598=CARTESIAN_POINT ( 'NONE',  ( 20.84999999999999787, 64.25000000001195133, -109.9422547304830857 ) ) ;
#7628=ADVANCED_FACE ( 'NONE', ( #54739 ), #235940, .F. ) ;
#7630=CARTESIAN_POINT ( 'NONE',  ( 20.04142135623730070, 64.25000000001196554, -111.8731074845243825 ) ) ;
#7642=DIRECTION ( 'NONE',  ( 0.000000000000000000, -7.429790795770644761E-15, 1.000000000000000000 ) ) ;
#7653=EDGE_CURVE ( 'NONE', #74720, #206067, #111381, .T. ) ;
#7658=VERTEX_POINT ( 'NONE', #118594 ) ;
#7667=AXIS2_PLACEMENT_3D ( 'NONE', #75990, #142372, #103230 ) ;
#7715=CARTESIAN_POINT ( 'NONE',  ( -18.59999999999999787, 76.00000000001190870, -103.0231074845243029 ) ) ;
#7756=CARTESIAN_POINT ( 'NONE',  ( 20.85000000000000142, 76.00000000001190870, -103.0231074845243029 ) ) ;
#7759=CIRCLE ( 'NONE', #99304, 4.049999999999998046 ) ;
#7763=SPHERICAL_SURFACE ( 'NONE', #73218, 0.1000000000000000056 ) ;
#7771=AXIS2_PLACEMENT_3D ( 'NONE', #186684, #68002, #25055 ) ;
#7817=CIRCLE ( 'NONE', #66054, 11.70000000000000284 ) ;
#7821=EDGE_CURVE ( 'NONE', #60670, #157942, #236278, .T. ) ;
#7849=VERTEX_POINT ( 'NONE', #164129 ) ;
#7864=EDGE_LOOP ( 'NONE', ( #127313, #8381, #67814, #233894 ) ) ;
#7877=FACE_OUTER_BOUND ( 'NONE', #162128, .T. ) ;
#7919=ORIENTED_EDGE ( 'NONE', *, *, #222706, .F. ) ;
#7940=LINE ( 'NONE', #129167, #162321 ) ;
#7963=EDGE_CURVE ( 'NONE', #67101, #163770, #110553, .T. ) ;
#7985=( LENGTH_UNIT ( ) NAMED_UNIT ( * ) SI_UNIT ( .MILLI., .METRE. ) );
#7991=CARTESIAN_POINT ( 'NONE',  ( 21.13461538461538325, 65.38541703798651383, -124.2731074845243739 ) ) ;
#8003=AXIS2_PLACEMENT_3D ( 'NONE', #51252, #75987, #53858 ) ;
#8020=AXIS2_PLACEMENT_3D ( 'NONE', #82296, #161890, #62768 ) ;
#8030=AXIS2_PLACEMENT_3D ( 'NONE', #171208, #250684, #49920 ) ;
#8053=CARTESIAN_POINT ( 'NONE',  ( 20.95512820512820085, 65.37615131630020926, -128.8581939154367717 ) ) ;
#8057=AXIS2_PLACEMENT_3D ( 'NONE', #75337, #94856, #133985 ) ;
#8111=DIRECTION ( 'NONE',  ( 1.000000000000000000, 0.000000000000000000, 0.000000000000000000 ) ) ;
#8120=ORIENTED_EDGE ( 'NONE', *, *, #189483, .F. ) ;
#8123=DIRECTION ( 'NONE',  ( 0.000000000000000000, 0.1350103645451807555, 0.9908441862701609093 ) ) ;
#8128=ORIENTED_EDGE ( 'NONE', *, *, #5340, .F. ) ;
#8132=ORIENTED_EDGE ( 'NONE', *, *, #140855, .T. ) ;
#8134=VERTEX_POINT ( 'NONE', #171859 ) ;
#8135=ORIENTED_EDGE ( 'NONE', *, *, #204998, .F. ) ;
#8137=CARTESIAN_POINT ( 'NONE',  ( -20.64999999999999858, 73.60000000001200249, -116.2477294072864140 ) ) ;
#8147=EDGE_LOOP ( 'NONE', ( #249487, #118290, #43417, #15641 ) ) ;
#8186=CIRCLE ( 'NONE', #153980, 0.09999999999999459321 ) ;
#8189=VERTEX_POINT ( 'NONE', #60841 ) ;
#8196=CARTESIAN_POINT ( 'NONE',  ( 21.00000000000000000, 66.25000000001199396, -115.3731074845243683 ) ) ;
#8200=DIRECTION ( 'NONE',  ( 0.000000000000000000, 0.8777080977375072424, -0.4791956752371691608 ) ) ;
#8231=CARTESIAN_POINT ( 'NONE',  ( -23.25000000000000000, 76.00000000001190870, -103.0231074845243029 ) ) ;
#8238=DIRECTION ( 'NONE',  ( 0.000000000000000000, -6.938893903907222067E-15, 1.000000000000000000 ) ) ;
#8245=CARTESIAN_POINT ( 'NONE',  ( 18.43565242384934066, 85.51932773110452501, -129.5501311079648872 ) ) ;
#8290=CYLINDRICAL_SURFACE ( 'NONE', #92832, 0.09999999999999939493 ) ;
#8304=DIRECTION ( 'NONE',  ( 0.000000000000000000, 4.163336342344217877E-13, -1.000000000000000000 ) ) ;
#8334=VERTEX_POINT ( 'NONE', #189794 ) ;
#8342=ORIENTED_EDGE ( 'NONE', *, *, #13770, .F. ) ;
#8355=CARTESIAN_POINT ( 'NONE',  ( 21.14999999999999858, 65.28660755661216797, -124.2731074845243739 ) ) ;
#8357=VECTOR ( 'NONE', #28806, 1000.000000000000000 ) ;
#8363=CARTESIAN_POINT ( 'NONE',  ( -21.05000000000000071, 87.48912529308798014, -105.9231074845242091 ) ) ;
#8381=ORIENTED_EDGE ( 'NONE', *, *, #243551, .T. ) ;
#8400=DIRECTION ( 'NONE',  ( -1.000000000000000000, 3.265361837132813093E-16, 2.280189983783949500E-30 ) ) ;
#8412=DIRECTION ( 'NONE',  ( 1.000000000000000000, 0.000000000000000000, 0.000000000000000000 ) ) ;
#8419=ORIENTED_EDGE ( 'NONE', *, *, #17361, .F. ) ;
#8422=LINE ( 'NONE', #204038, #217879 ) ;
#8456=CYLINDRICAL_SURFACE ( 'NONE', #257573, 0.1000000000000028644 ) ;
#8476=DIRECTION ( 'NONE',  ( 0.000000000000000000, 1.000000000000000000, 0.000000000000000000 ) ) ;
#8479=ADVANCED_FACE ( 'NONE', ( #174123 ), #218310, .F. ) ;
#8495=AXIS2_PLACEMENT_3D ( 'NONE', #47074, #186622, #90058 ) ;
#8498=CYLINDRICAL_SURFACE ( 'NONE', #3535, 0.09999999999999520384 ) ;
#8508=CARTESIAN_POINT ( 'NONE',  ( 21.05000000000000071, 74.65091558138507821, -128.5366085209788309 ) ) ;
#8525=LINE ( 'NONE', #167616, #92328 ) ;
#8544=DIRECTION ( 'NONE',  ( 0.000000000000000000, 0.000000000000000000, -1.000000000000000000 ) ) ;
#8547=DIRECTION ( 'NONE',  ( 0.000000000000000000, -6.982962677686266711E-15, 1.000000000000000000 ) ) ;
#8564=AXIS2_PLACEMENT_3D ( 'NONE', #22063, #25911, #203248 ) ;
#8586=ORIENTED_EDGE ( 'NONE', *, *, #73518, .F. ) ;
#8589=ORIENTED_EDGE ( 'NONE', *, *, #17279, .T. ) ;
#8611=FACE_OUTER_BOUND ( 'NONE', #73596, .T. ) ;
#8614=DIRECTION ( 'NONE',  ( -1.000000000000000000, -0.000000000000000000, -0.000000000000000000 ) ) ;
#8615=ADVANCED_FACE ( 'NONE', ( #257399 ), #183075, .F. ) ;
#8636=DIRECTION ( 'NONE',  ( -0.000000000000000000, 6.982962677686266711E-15, -1.000000000000000000 ) ) ;
#8640=VERTEX_POINT ( 'NONE', #193027 ) ;
#8657=CARTESIAN_POINT ( 'NONE',  ( 18.52351027002948669, 85.64216290470703541, -96.30806053401445865 ) ) ;
#8660=VECTOR ( 'NONE', #53853, 1000.000000000000000 ) ;
#8664=VERTEX_POINT ( 'NONE', #46109 ) ;
#8682=AXIS2_PLACEMENT_3D ( 'NONE', #126977, #164827, #224775 ) ;
#8692=DIRECTION ( 'NONE',  ( -1.000000000000000000, 0.000000000000000000, -0.000000000000000000 ) ) ;
#8693=DIRECTION ( 'NONE',  ( 0.000000000000000000, -7.487053152578127080E-15, 1.000000000000000000 ) ) ;
#8707=VECTOR ( 'NONE', #57630, 1000.000000000000000 ) ;
#8722=FACE_OUTER_BOUND ( 'NONE', #158128, .T. ) ;
#8735=EDGE_CURVE ( 'NONE', #124002, #56789, #24664, .T. ) ;
#8771=VERTEX_POINT ( 'NONE', #76910 ) ;
#8796=LINE ( 'NONE', #25788, #10927 ) ;
#8802=AXIS2_PLACEMENT_3D ( 'NONE', #75305, #16608, #213493 ) ;
#8807=ORIENTED_EDGE ( 'NONE', *, *, #53836, .F. ) ;
#8816=CARTESIAN_POINT ( 'NONE',  ( -21.05000000000000071, 87.39257802171779588, -133.4491579046922709 ) ) ;
#8845=AXIS2_PLACEMENT_3D ( 'NONE', #100596, #41969, #61518 ) ;
#8855=DIRECTION ( 'NONE',  ( 1.000000000000000000, 0.000000000000000000, 0.000000000000000000 ) ) ;
#8870=VERTEX_POINT ( 'NONE', #138154 ) ;
#8881=CARTESIAN_POINT ( 'NONE',  ( -21.05000000000000071, 77.83534155023646406, -124.9679561919613064 ) ) ;
#8903=DIRECTION ( 'NONE',  ( 0.000000000000000000, 0.000000000000000000, 1.000000000000000000 ) ) ;
#8932=VECTOR ( 'NONE', #225502, 1000.000000000000000 ) ;
#9009=CARTESIAN_POINT ( 'NONE',  ( -20.94999999999999929, 64.25000000001210765, -129.5083017138703667 ) ) ;
#9016=CARTESIAN_POINT ( 'NONE',  ( -21.55000000000000426, 68.29142135624935861, -124.1731074845243512 ) ) ;
#9045=EDGE_LOOP ( 'NONE', ( #137340, #63394, #88915, #65293, #46744, #5458, #156315, #196128, #118082, #17668 ) ) ;
#9078=CARTESIAN_POINT ( 'NONE',  ( 18.59999999999996945, 68.97833521811179480, -99.18954208262705663 ) ) ;
#9088=FACE_OUTER_BOUND ( 'NONE', #175262, .T. ) ;
#9103=ORIENTED_EDGE ( 'NONE', *, *, #114700, .T. ) ;
#9124=DIRECTION ( 'NONE',  ( -1.000000000000000000, -0.000000000000000000, -0.000000000000000000 ) ) ;
#9138=ORIENTED_EDGE ( 'NONE', *, *, #207473, .F. ) ;
#9142=ORIENTED_EDGE ( 'NONE', *, *, #172806, .F. ) ;
#9169=DIRECTION ( 'NONE',  ( 0.000000000000000000, 0.000000000000000000, 1.000000000000000000 ) ) ;
#9213=DIRECTION ( 'NONE',  ( -1.000000000000000000, 0.000000000000000000, -0.000000000000000000 ) ) ;
#9251=AXIS2_PLACEMENT_3D ( 'NONE', #37350, #157307, #122985 ) ;
#9264=FACE_OUTER_BOUND ( 'NONE', #74650, .T. ) ;
#9266=AXIS2_PLACEMENT_3D ( 'NONE', #102322, #103618, #243152 ) ;
#9267=VECTOR ( 'NONE', #125258, 1000.000000000000000 ) ;
#9282=CARTESIAN_POINT ( 'NONE',  ( 19.80993210785465308, 64.25000000001242029, -111.7559897356370868 ) ) ;
#9298=ORIENTED_EDGE ( 'NONE', *, *, #200597, .F. ) ;
#9305=EDGE_CURVE ( 'NONE', #37875, #76136, #70639, .T. ) ;
#9329=DIRECTION ( 'NONE',  ( 0.000000000000000000, -1.000000000000000000, -6.982962677686266711E-15 ) ) ;
#9376=CIRCLE ( 'NONE', #26156, 12.87499999999999822 ) ;
#9395=LINE ( 'NONE', #126783, #251614 ) ;
#9399=EDGE_LOOP ( 'NONE', ( #90694, #116474, #251369, #160808, #204547 ) ) ;
#9414=CARTESIAN_POINT ( 'NONE',  ( 18.49999999999999289, 65.62657994473188694, -111.7573193598984176 ) ) ;
#9462=CARTESIAN_POINT ( 'NONE',  ( -21.14999999999999858, 64.35000000001208775, -129.7392418215462158 ) ) ;
#9545=CARTESIAN_POINT ( 'NONE',  ( 18.59999999999999076, 65.79142135624930177, -115.1731074845243796 ) ) ;
#9571=SPHERICAL_SURFACE ( 'NONE', #175486, 0.1000000000000000056 ) ;
#9572=ORIENTED_EDGE ( 'NONE', *, *, #140285, .T. ) ;
#9617=ORIENTED_EDGE ( 'NONE', *, *, #5024, .F. ) ;
#9626=CARTESIAN_POINT ( 'NONE',  ( 23.14999999999999147, 76.00000000001213607, -136.5231074845242745 ) ) ;
#9638=ADVANCED_FACE ( 'NONE', ( #198810 ), #12542, .T. ) ;
#9645=ADVANCED_FACE ( 'NONE', ( #24054 ), #143967, .T. ) ;
#9661=CARTESIAN_POINT ( 'NONE',  ( 22.47071067811865319, 68.27992525551410097, -136.6221999392269595 ) ) ;
#9697=DIRECTION ( 'NONE',  ( -1.000000000000000000, -0.000000000000000000, -0.000000000000000000 ) ) ;
#9711=FACE_OUTER_BOUND ( 'NONE', #223953, .T. ) ;
#9722=CARTESIAN_POINT ( 'NONE',  ( 20.95346350065193519, 67.11282275083759430, -128.0113755374889877 ) ) ;
#9729=LINE ( 'NONE', #89263, #19195 ) ;
#9766=CARTESIAN_POINT ( 'NONE',  ( -18.50000000000000000, 66.85000000001205933, -124.1731074845243512 ) ) ;
#9784=AXIS2_PLACEMENT_3D ( 'NONE', #95411, #255723, #116276 ) ;
#9792=ORIENTED_EDGE ( 'NONE', *, *, #21908, .F. ) ;
#9803=VERTEX_POINT ( 'NONE', #185679 ) ;
#9864=EDGE_CURVE ( 'NONE', #213961, #192664, #195889, .T. ) ;
#9870=DIRECTION ( 'NONE',  ( 1.000000000000000000, 0.000000000000000000, 0.000000000000000000 ) ) ;
#9873=FACE_OUTER_BOUND ( 'NONE', #132751, .T. ) ;
#9892=AXIS2_PLACEMENT_3D ( 'NONE', #164581, #105851, #201123 ) ;
#9907=ADVANCED_FACE ( 'NONE', ( #132127 ), #36914, .F. ) ;
#9953=DIRECTION ( 'NONE',  ( 1.000000000000000000, 0.000000000000000000, 0.000000000000000000 ) ) ;
#9955=ADVANCED_FACE ( 'NONE', ( #31775 ), #16816, .F. ) ;
#9956=AXIS2_PLACEMENT_3D ( 'NONE', #46819, #87232, #166827 ) ;
#9968=AXIS2_PLACEMENT_3D ( 'NONE', #214519, #231541, #111586 ) ;
#10048=CARTESIAN_POINT ( 'NONE',  ( -21.37071067811865532, 67.92928932189340685, -124.2731074845243597 ) ) ;
#10049=EDGE_CURVE ( 'NONE', #235860, #47181, #198417, .T. ) ;
#10067=ADVANCED_FACE ( 'NONE', ( #240125 ), #61481, .T. ) ;
#10131=LINE ( 'NONE', #12723, #214180 ) ;
#10143=EDGE_CURVE ( 'NONE', #85966, #181206, #254711, .T. ) ;
#10161=LINE ( 'NONE', #171835, #104893 ) ;
#10176=DIRECTION ( 'NONE',  ( 0.000000000000000000, 0.000000000000000000, -1.000000000000000000 ) ) ;
#10178=DIRECTION ( 'NONE',  ( -1.000000000000000000, 1.836970198721029934E-16, 1.282749433769087757E-30 ) ) ;
#10186=ORIENTED_EDGE ( 'NONE', *, *, #127665, .T. ) ;
#10207=CARTESIAN_POINT ( 'NONE',  ( 18.59999999999999787, 87.75000000001195133, -111.6731074845242233 ) ) ;
#10214=CARTESIAN_POINT ( 'NONE',  ( -21.07094088545304444, 69.67983277809565834, -136.6220011870765632 ) ) ;
#10243=EDGE_CURVE ( 'NONE', #216369, #247118, #217131, .T. ) ;
#10354=CARTESIAN_POINT ( 'NONE',  ( 22.59080734064468388, 64.25000000001215028, -136.5538571926214502 ) ) ;
#10356=CARTESIAN_POINT ( 'NONE',  ( 23.15000000000000213, 87.48912529308798014, -106.1231074845242262 ) ) ;
#10407=EDGE_LOOP ( 'NONE', ( #105848, #211786, #79026, #81256 ) ) ;
#10433=DIRECTION ( 'NONE',  ( 0.000000000000000000, -6.608470384673558123E-15, 1.000000000000000000 ) ) ;
#10443=CIRCLE ( 'NONE', #247759, 0.1000000000000070832 ) ;
#10462=DIRECTION ( 'NONE',  ( -1.000000000000000000, 0.000000000000000000, 0.000000000000000000 ) ) ;
#10474=CARTESIAN_POINT ( 'NONE',  ( 20.94999999999999929, 70.60000000001200249, -115.4283735034374274 ) ) ;
#10477=VERTEX_POINT ( 'NONE', #218952 ) ;
#10501=EDGE_CURVE ( 'NONE', #197779, #144144, #159111, .T. ) ;
#10523=FACE_OUTER_BOUND ( 'NONE', #84759, .T. ) ;
#10550=ADVANCED_FACE ( 'NONE', ( #39064 ), #163375, .T. ) ;
#10551=CARTESIAN_POINT ( 'NONE',  ( 21.05000000000000071, 87.48912529308798014, -106.1231074845242262 ) ) ;
#10578=ORIENTED_EDGE ( 'NONE', *, *, #72708, .F. ) ;
#10609=CARTESIAN_POINT ( 'NONE',  ( -21.05000000000000071, 76.00000000001210765, -132.2231074845243199 ) ) ;
#10627=AXIS2_PLACEMENT_3D ( 'NONE', #102644, #3567, #123528 ) ;
#10639=CARTESIAN_POINT ( 'NONE',  ( -18.50000000000000000, 77.86671491006937629, -124.7704322382422788 ) ) ;
#10659=VECTOR ( 'NONE', #122565, 1000.000000000000000 ) ;
#10660=CARTESIAN_POINT ( 'NONE',  ( -21.05000000000000071, 76.10000000001222986, -148.1731074845243086 ) ) ;
#10736=DIRECTION ( 'NONE',  ( 0.000000000000000000, 0.000000000000000000, -1.000000000000000000 ) ) ;
#10744=AXIS2_PLACEMENT_3D ( 'NONE', #257988, #97658, #41590 ) ;
#10762=AXIS2_PLACEMENT_3D ( 'NONE', #8231, #68196, #107311 ) ;
#10765=ORIENTED_EDGE ( 'NONE', *, *, #27840, .T. ) ;
#10785=DIRECTION ( 'NONE',  ( 0.000000000000000000, -0.9654727137038715545, -0.2605042016806676242 ) ) ;
#10790=PLANE ( 'NONE',  #168615 ) ;
#10808=CARTESIAN_POINT ( 'NONE',  ( -21.10257677756356642, 69.60161825747941577, -136.5480582340923661 ) ) ;
#10817=EDGE_CURVE ( 'NONE', #214648, #224952, #111861, .T. ) ;
#10842=CARTESIAN_POINT ( 'NONE',  ( 23.14999999999999858, 70.40000000001199965, -115.4283735034374274 ) ) ;
#10852=CIRCLE ( 'NONE', #173211, 7.900000000000003908 ) ;
#10855=FACE_OUTER_BOUND ( 'NONE', #95417, .T. ) ;
#10882=CARTESIAN_POINT ( 'NONE',  ( -22.48660254037843487, 64.35000000001214460, -136.5731074845243711 ) ) ;
#10894=TOROIDAL_SURFACE ( 'NONE', #77479, 2.100000000000002309, 0.1000000000000000056 ) ;
#10897=DIRECTION ( 'NONE',  ( 0.000000000000000000, -6.982962677686266711E-15, 1.000000000000000000 ) ) ;
#10924=CARTESIAN_POINT ( 'NONE',  ( 20.46382478191414833, 65.40137955871470865, -128.8452930151789531 ) ) ;
#10927=VECTOR ( 'NONE', #147000, 1000.000000000000000 ) ;
#10932=CARTESIAN_POINT ( 'NONE',  ( 18.59999999999999076, 69.35000000001200249, -115.2731074845243455 ) ) ;
#10944=DIRECTION ( 'NONE',  ( -1.000000000000000000, 0.000000000000000000, 0.000000000000000000 ) ) ;
#10964=DIRECTION ( 'NONE',  ( 1.000000000000000000, -0.000000000000000000, 0.000000000000000000 ) ) ;
#10968=AXIS2_PLACEMENT_3D ( 'NONE', #256681, #57224, #212492 ) ;
#10996=ORIENTED_EDGE ( 'NONE', *, *, #257115, .T. ) ;
#11028=EDGE_CURVE ( 'NONE', #88364, #144144, #225871, .T. ) ;
#11096=DIRECTION ( 'NONE',  ( 0.000000000000000000, 0.000000000000000000, 1.000000000000000000 ) ) ;
#11097=ORIENTED_EDGE ( 'NONE', *, *, #14494, .F. ) ;
#11102=CARTESIAN_POINT ( 'NONE',  ( -23.25000000000000000, 85.00000000001197975, -112.3170766071766735 ) ) ;
#11110=AXIS2_PLACEMENT_3D ( 'NONE', #208370, #70150, #14007 ) ;
#11119=DIRECTION ( 'NONE',  ( 1.000000000000000000, 0.000000000000000000, 0.000000000000000000 ) ) ;
#11141=CYLINDRICAL_SURFACE ( 'NONE', #49979, 0.09999999999999939493 ) ;
#11188=DIRECTION ( 'NONE',  ( 0.000000000000000000, 0.000000000000000000, 1.000000000000000000 ) ) ;
#11197=DIRECTION ( 'NONE',  ( 0.000000000000000000, -6.982962677686266711E-15, 1.000000000000000000 ) ) ;
#11235=EDGE_LOOP ( 'NONE', ( #41089, #161365, #49130, #67436 ) ) ;
#11236=EDGE_CURVE ( 'NONE', #127492, #197068, #256114, .T. ) ;
#11251=VERTEX_POINT ( 'NONE', #117950 ) ;
#11281=DIRECTION ( 'NONE',  ( 0.000000000000000000, -1.000000000000000000, -6.982962677686266711E-15 ) ) ;
#11286=AXIS2_PLACEMENT_3D ( 'NONE', #185304, #45789, #204847 ) ;
#11287=AXIS2_PLACEMENT_3D ( 'NONE', #184298, #83876, #60489 ) ;
#11292=EDGE_LOOP ( 'NONE', ( #127477, #154441, #2937, #23887 ) ) ;
#11306=ORIENTED_EDGE ( 'NONE', *, *, #140522, .F. ) ;
#11308=DIRECTION ( 'NONE',  ( 1.000000000000000000, 0.000000000000000000, 0.000000000000000000 ) ) ;
#11327=ORIENTED_EDGE ( 'NONE', *, *, #69183, .F. ) ;
#11345=DIRECTION ( 'NONE',  ( -1.000000000000000000, 0.000000000000000000, -0.000000000000000000 ) ) ;
#11347=ORIENTED_EDGE ( 'NONE', *, *, #32657, .T. ) ;
#11360=ORIENTED_EDGE ( 'NONE', *, *, #231316, .F. ) ;
#11373=ORIENTED_EDGE ( 'NONE', *, *, #105586, .T. ) ;
#11379=EDGE_LOOP ( 'NONE', ( #145302, #221518, #255487 ) ) ;
#11391=DIRECTION ( 'NONE',  ( 2.952720810173289112E-16, 1.000000000000000000, 6.308085367188367561E-15 ) ) ;
#11420=CIRCLE ( 'NONE', #157182, 0.09999999999999939493 ) ;
#11421=ORIENTED_EDGE ( 'NONE', *, *, #200652, .F. ) ;
#11429=EDGE_LOOP ( 'NONE', ( #206593, #215876, #53054, #191035 ) ) ;
#11501=FACE_BOUND ( 'NONE', #14365, .T. ) ;
#11600=DIRECTION ( 'NONE',  ( 1.000000000000000000, -7.304098846218134667E-16, -5.100424963727255829E-30 ) ) ;
#11629=EDGE_CURVE ( 'NONE', #145638, #210448, #242839, .T. ) ;
#11646=CARTESIAN_POINT ( 'NONE',  ( -18.45140287520618116, 85.48607773954142885, -96.38258435783812672 ) ) ;
#11650=DIRECTION ( 'NONE',  ( -1.000000000000000000, -0.000000000000000000, -0.000000000000000000 ) ) ;
#11659=DIRECTION ( 'NONE',  ( 0.000000000000000000, -0.4999999999999943379, -0.8660254037844420383 ) ) ;
#11671=VECTOR ( 'NONE', #45174, 1000.000000000000000 ) ;
#11699=DIRECTION ( 'NONE',  ( 1.000000000000000000, 0.000000000000000000, 0.000000000000000000 ) ) ;
#11708=EDGE_CURVE ( 'NONE', #154018, #76954, #25767, .T. ) ;
#11735=EDGE_LOOP ( 'NONE', ( #169451, #189621, #12126, #38704, #220882 ) ) ;
#11794=DIRECTION ( 'NONE',  ( 0.000000000000000000, -1.000000000000000000, -6.860497997771531562E-15 ) ) ;
#11796=ORIENTED_EDGE ( 'NONE', *, *, #252109, .T. ) ;
#11810=CARTESIAN_POINT ( 'NONE',  ( 18.49999999999999289, 65.50857864377465489, -111.6731074845243796 ) ) ;
#11826=SPHERICAL_SURFACE ( 'NONE', #154749, 0.1000000000000000056 ) ;
#11850=FACE_OUTER_BOUND ( 'NONE', #80631, .T. ) ;
#11860=CARTESIAN_POINT ( 'NONE',  ( -20.94999999999999929, 74.16465844978765176, -124.9679561919613207 ) ) ;
#11879=CARTESIAN_POINT ( 'NONE',  ( 19.75857864376268935, 64.25000000001196554, -111.7731074845243882 ) ) ;
#11908=AXIS2_PLACEMENT_3D ( 'NONE', #41848, #161796, #122663 ) ;
#11911=ORIENTED_EDGE ( 'NONE', *, *, #248792, .F. ) ;
#11927=DIRECTION ( 'NONE',  ( 0.000000000000000000, -6.982962677686266711E-15, 1.000000000000000000 ) ) ;
#11944=ORIENTED_EDGE ( 'NONE', *, *, #39954, .F. ) ;
#11981=VECTOR ( 'NONE', #93219, 1000.000000000000000 ) ;
#11986=CIRCLE ( 'NONE', #45280, 0.1000000000000028644 ) ;
#11997=CARTESIAN_POINT ( 'NONE',  ( 23.24999999999999289, 69.35000000001205933, -124.3731074845243540 ) ) ;
#12030=ORIENTED_EDGE ( 'NONE', *, *, #238390, .F. ) ;
#12031=DIRECTION ( 'NONE',  ( 1.000000000000000000, 0.000000000000000000, 0.000000000000000000 ) ) ;
#12044=VECTOR ( 'NONE', #43566, 1000.000000000000000 ) ;
#12059=DIRECTION ( 'NONE',  ( 0.000000000000000000, -1.000000000000000000, -6.982962677686266711E-15 ) ) ;
#12060=DIRECTION ( 'NONE',  ( 1.000000000000000000, 0.000000000000000000, 0.000000000000000000 ) ) ;
#12072=EDGE_CURVE ( 'NONE', #56619, #67927, #38778, .T. ) ;
#12082=ORIENTED_EDGE ( 'NONE', *, *, #208396, .T. ) ;
#12092=DIRECTION ( 'NONE',  ( 0.000000000000000000, -0.2605042016806740079, 0.9654727137038698892 ) ) ;
#12126=ORIENTED_EDGE ( 'NONE', *, *, #183866, .F. ) ;
#12156=FACE_OUTER_BOUND ( 'NONE', #116191, .T. ) ;
#12174=LINE ( 'NONE', #91686, #117030 ) ;
#12183=CARTESIAN_POINT ( 'NONE',  ( 21.46681500593474112, 69.14248884062944001, -136.5231074845243597 ) ) ;
#12190=VERTEX_POINT ( 'NONE', #204249 ) ;
#12211=CARTESIAN_POINT ( 'NONE',  ( -23.25000000000000000, 70.05000000001196270, -113.3288097895591591 ) ) ;
#12229=EDGE_LOOP ( 'NONE', ( #768, #80937, #233887, #99345 ) ) ;
#12265=EDGE_CURVE ( 'NONE', #2981, #155807, #86856, .T. ) ;
#12266=CARTESIAN_POINT ( 'NONE',  ( -20.94999999999999929, 76.00000000001190870, -103.0231074845243029 ) ) ;
#12286=DIRECTION ( 'NONE',  ( 1.000000000000000000, 0.000000000000000000, 0.000000000000000000 ) ) ;
#12295=CARTESIAN_POINT ( 'NONE',  ( 21.93340585900768858, 76.00000000001219291, -143.8472545066313728 ) ) ;
#12305=ADVANCED_FACE ( 'NONE', ( #52877 ), #105805, .T. ) ;
#12367=FACE_OUTER_BOUND ( 'NONE', #52133, .T. ) ;
#12375=VERTEX_POINT ( 'NONE', #75057 ) ;
#12377=ORIENTED_EDGE ( 'NONE', *, *, #186952, .T. ) ;
#12416=EDGE_LOOP ( 'NONE', ( #157603, #56927, #56875, #117432 ) ) ;
#12425=VECTOR ( 'NONE', #2614, 1000.000000000000000 ) ;
#12443=DIRECTION ( 'NONE',  ( 0.000000000000000000, -6.982962677686266711E-15, 1.000000000000000000 ) ) ;
#12447=DIRECTION ( 'NONE',  ( 0.000000000000000000, 1.000000000000000000, 6.982962677686266711E-15 ) ) ;
#12457=FACE_OUTER_BOUND ( 'NONE', #63915, .T. ) ;
#12481=AXIS2_PLACEMENT_3D ( 'NONE', #37147, #137486, #191427 ) ;
#12532=CARTESIAN_POINT ( 'NONE',  ( 18.39999999999999858, 85.68240343348826116, -96.36626410711143365 ) ) ;
#12542=TOROIDAL_SURFACE ( 'NONE', #116574, 0.2000000000000000111, 0.1000000000000000056 ) ;
#12565=DIRECTION ( 'NONE',  ( 1.000000000000000000, 0.000000000000000000, 0.000000000000000000 ) ) ;
#12573=AXIS2_PLACEMENT_3D ( 'NONE', #225812, #43362, #126739 ) ;
#12626=EDGE_CURVE ( 'NONE', #153145, #206536, #243381, .T. ) ;
#12648=DIRECTION ( 'NONE',  ( 1.000000000000000000, 0.000000000000000000, 0.000000000000000000 ) ) ;
#12669=CARTESIAN_POINT ( 'NONE',  ( 23.14999999999999858, 76.00000000001193712, -107.0231074845243029 ) ) ;
#12704=DIRECTION ( 'NONE',  ( 0.000000000000000000, 0.000000000000000000, 1.000000000000000000 ) ) ;
#12706=CARTESIAN_POINT ( 'NONE',  ( 23.14999999999999503, 64.25000000001220712, -148.2731074845243882 ) ) ;
#12723=CARTESIAN_POINT ( 'NONE',  ( -20.94999999999999929, 87.48912529308798014, -106.0231074845242176 ) ) ;
#12774=CARTESIAN_POINT ( 'NONE',  ( -23.25000000000000000, 69.01799029515544248, -99.32695536626806643 ) ) ;
#12791=EDGE_CURVE ( 'NONE', #153790, #121700, #39415, .T. ) ;
#12798=DIRECTION ( 'NONE',  ( -4.701977403289178058E-30, -2.433019743745433765E-14, 1.000000000000000000 ) ) ;
#12803=DIRECTION ( 'NONE',  ( 7.304098846218134667E-16, 1.000000000000000000, 6.982962677686267499E-15 ) ) ;
#12823=EDGE_CURVE ( 'NONE', #17520, #53190, #99392, .T. ) ;
#12841=DIRECTION ( 'NONE',  ( 0.000000000000000000, 0.000000000000000000, 1.000000000000000000 ) ) ;
#12864=EDGE_CURVE ( 'NONE', #74720, #52643, #47164, .T. ) ;
#12886=ORIENTED_EDGE ( 'NONE', *, *, #199779, .T. ) ;
#12889=ADVANCED_FACE ( 'NONE', ( #120307 ), #17327, .T. ) ;
#12934=CARTESIAN_POINT ( 'NONE',  ( 22.57320508075687115, 64.25000000001215028, -136.5231074845243597 ) ) ;
#12942=CARTESIAN_POINT ( 'NONE',  ( -23.25000000000000000, 71.65000000001199965, -115.3731074845243256 ) ) ;
#12954=LINE ( 'NONE', #151168, #105889 ) ;
#12964=DIRECTION ( 'NONE',  ( 1.000000000000000000, 0.000000000000000000, 0.000000000000000000 ) ) ;
#12993=CARTESIAN_POINT ( 'NONE',  ( 20.94999999999999929, 76.00000000001193712, -107.0231074845243029 ) ) ;
#13011=VERTEX_POINT ( 'NONE', #67988 ) ;
#13018=DIRECTION ( 'NONE',  ( 1.000000000000000000, 0.000000000000000000, 0.000000000000000000 ) ) ;
#13022=ORIENTED_EDGE ( 'NONE', *, *, #115843, .F. ) ;
#13025=CARTESIAN_POINT ( 'NONE',  ( 18.48413544395646113, 85.66430403363958135, -96.34000249148589035 ) ) ;
#13051=DIRECTION ( 'NONE',  ( 0.000000000000000000, -6.688090509790120484E-15, 1.000000000000000000 ) ) ;
#13107=DIRECTION ( 'NONE',  ( 0.000000000000000000, 0.000000000000000000, 1.000000000000000000 ) ) ;
#13108=ORIENTED_EDGE ( 'NONE', *, *, #164199, .T. ) ;
#13130=EDGE_CURVE ( 'NONE', #224814, #153656, #217852, .T. ) ;
#13147=CARTESIAN_POINT ( 'NONE',  ( 19.99999999738052736, 64.25000000001196554, -111.8359355348916893 ) ) ;
#13187=CARTESIAN_POINT ( 'NONE',  ( 21.04999999999999716, 65.45624872451648457, -128.9667196758603041 ) ) ;
#13193=ORIENTED_EDGE ( 'NONE', *, *, #4198, .T. ) ;
#13245=FACE_OUTER_BOUND ( 'NONE', #163392, .T. ) ;
#13252=EDGE_LOOP ( 'NONE', ( #218592, #215534, #95883, #132333 ) ) ;
#13258=ORIENTED_EDGE ( 'NONE', *, *, #85587, .F. ) ;
#13281=FACE_OUTER_BOUND ( 'NONE', #90176, .T. ) ;
#13284=EDGE_LOOP ( 'NONE', ( #28475, #250576, #238204, #188342, #176312 ) ) ;
#13286=VERTEX_POINT ( 'NONE', #244691 ) ;
#13292=ORIENTED_EDGE ( 'NONE', *, *, #198169, .T. ) ;
#13325=CARTESIAN_POINT ( 'NONE',  ( 20.95561247346651967, 65.40499263480853642, -128.9293247175427268 ) ) ;
#13333=CARTESIAN_POINT ( 'NONE',  ( 22.49806830649814060, 75.92253568368671779, -148.1729971393633889 ) ) ;
#13368=VERTEX_POINT ( 'NONE', #187320 ) ;
#13416=EDGE_CURVE ( 'NONE', #62401, #76270, #92047, .T. ) ;
#13440=ORIENTED_EDGE ( 'NONE', *, *, #136531, .T. ) ;
#13456=CARTESIAN_POINT ( 'NONE',  ( -18.47140463609787986, 85.67147468523276643, -96.35034702625016223 ) ) ;
#13467=CYLINDRICAL_SURFACE ( 'NONE', #80904, 0.1000000000000064587 ) ;
#13497=DIRECTION ( 'NONE',  ( 0.000000000000000000, 0.000000000000000000, -1.000000000000000000 ) ) ;
#13499=CARTESIAN_POINT ( 'NONE',  ( 23.24999999999999289, 64.35000000001213039, -136.5231074845243597 ) ) ;
#13539=CARTESIAN_POINT ( 'NONE',  ( -21.17356465864818560, 69.57719687377041851, -136.6220187255381973 ) ) ;
#13547=CARTESIAN_POINT ( 'NONE',  ( 21.05000000000000071, 67.17357026049489832, -128.1090527715806502 ) ) ;
#13561=AXIS2_PLACEMENT_3D ( 'NONE', #218339, #15046, #197505 ) ;
#13608=CARTESIAN_POINT ( 'NONE',  ( 20.85000000000000142, 64.25000000001195133, -109.8069731475024753 ) ) ;
#13643=CIRCLE ( 'NONE', #51029, 0.2000000000000057288 ) ;
#13644=AXIS2_PLACEMENT_3D ( 'NONE', #30924, #227797, #110420 ) ;
#13648=VERTEX_POINT ( 'NONE', #57606 ) ;
#13664=AXIS2_PLACEMENT_3D ( 'NONE', #215044, #156390, #36437 ) ;
#13684=VERTEX_POINT ( 'NONE', #231151 ) ;
#13693=CARTESIAN_POINT ( 'NONE',  ( -23.15000000000000213, 76.00000000001213607, -136.5231074845242745 ) ) ;
#13733=VECTOR ( 'NONE', #239984, 1000.000000000000000 ) ;
#13748=DIRECTION ( 'NONE',  ( 2.557131231893037478E-16, 0.8660254037844420383, -0.4999999999999943379 ) ) ;
#13754=FACE_OUTER_BOUND ( 'NONE', #208246, .T. ) ;
#13761=VERTEX_POINT ( 'NONE', #92692 ) ;
#13770=EDGE_CURVE ( 'NONE', #78926, #151026, #143413, .T. ) ;
#13790=DIRECTION ( 'NONE',  ( 8.673617379884087537E-15, 6.982962677686266711E-15, -1.000000000000000000 ) ) ;
#13808=VERTEX_POINT ( 'NONE', #210101 ) ;
#13844=AXIS2_PLACEMENT_3D ( 'NONE', #196460, #161206, #80341 ) ;
#13861=DIRECTION ( 'NONE',  ( 0.000000000000000000, -7.086529944415894657E-15, 1.000000000000000000 ) ) ;
#13873=CYLINDRICAL_SURFACE ( 'NONE', #215067, 0.1000000000000072220 ) ;
#13908=DIRECTION ( 'NONE',  ( 1.000000000000000000, 0.000000000000000000, 0.000000000000000000 ) ) ;
#13945=CONICAL_SURFACE ( 'NONE', #176281, 7.750000000000034639, 0.7853981633974531640 ) ;
#13963=CARTESIAN_POINT ( 'NONE',  ( 23.14999999999999858, 76.00000000001190870, -103.0231074845243029 ) ) ;
#13973=PLANE ( 'NONE',  #141716 ) ;
#14007=DIRECTION ( 'NONE',  ( 1.000000000000000000, 0.000000000000000000, 0.000000000000000000 ) ) ;
#14010=AXIS2_PLACEMENT_3D ( 'NONE', #72777, #251370, #34934 ) ;
#14025=VERTEX_POINT ( 'NONE', #182532 ) ;
#14038=CARTESIAN_POINT ( 'NONE',  ( -20.94999999999999929, 87.39257802171779588, -133.4491579046922709 ) ) ;
#14097=DIRECTION ( 'NONE',  ( 1.000000000000000000, 0.000000000000000000, 0.000000000000000000 ) ) ;
#14103=CIRCLE ( 'NONE', #130784, 0.09999999999998898659 ) ;
#14113=CYLINDRICAL_SURFACE ( 'NONE', #90535, 0.1000000000000028644 ) ;
#14115=EDGE_CURVE ( 'NONE', #16570, #207709, #193496, .T. ) ;
#14158=CARTESIAN_POINT ( 'NONE',  ( -18.39999999999999858, 85.60000000001210196, -129.4910380878245633 ) ) ;
#14173=ORIENTED_EDGE ( 'NONE', *, *, #57886, .F. ) ;
#14216=AXIS2_PLACEMENT_3D ( 'NONE', #30884, #50384, #32162 ) ;
#14226=AXIS2_PLACEMENT_3D ( 'NONE', #218396, #181869, #21522 ) ;
#14233=ORIENTED_EDGE ( 'NONE', *, *, #143097, .F. ) ;
#14252=EDGE_LOOP ( 'NONE', ( #214428, #94687, #23233, #234168 ) ) ;
#14291=VERTEX_POINT ( 'NONE', #74149 ) ;
#14320=CARTESIAN_POINT ( 'NONE',  ( -23.15000000000000213, 85.50000000001207923, -126.6291383618717816 ) ) ;
#14325=ORIENTED_EDGE ( 'NONE', *, *, #68806, .T. ) ;
#14333=DIRECTION ( 'NONE',  ( 0.000000000000000000, 0.8777080977375072424, -0.4791956752371691608 ) ) ;
#14354=EDGE_LOOP ( 'NONE', ( #58600, #57235, #249519, #116451 ) ) ;
#14361=ADVANCED_FACE ( 'NONE', ( #143052 ), #225149, .T. ) ;
#14365=EDGE_LOOP ( 'NONE', ( #91977, #104907 ) ) ;
#14381=DIRECTION ( 'NONE',  ( -1.000000000000000000, 0.000000000000000000, -0.000000000000000000 ) ) ;
#14409=ORIENTED_EDGE ( 'NONE', *, *, #239585, .T. ) ;
#14435=EDGE_CURVE ( 'NONE', #217189, #22276, #3548, .T. ) ;
#14465=CARTESIAN_POINT ( 'NONE',  ( -21.14999999999999858, 76.00000000001213607, -136.5231074845242745 ) ) ;
#14494=EDGE_CURVE ( 'NONE', #28335, #6807, #32137, .T. ) ;
#14504=AXIS2_PLACEMENT_3D ( 'NONE', #92036, #226392, #206856 ) ;
#14505=CARTESIAN_POINT ( 'NONE',  ( 18.49999999999998934, 65.70711192142361767, -97.56510546851221477 ) ) ;
#14587=VERTEX_POINT ( 'NONE', #254943 ) ;
#14594=VERTEX_POINT ( 'NONE', #135035 ) ;
#14596=AXIS2_PLACEMENT_3D ( 'NONE', #244781, #183546, #162705 ) ;
#14614=LINE ( 'NONE', #30315, #225540 ) ;
#14624=FACE_OUTER_BOUND ( 'NONE', #212236, .T. ) ;
#14661=EDGE_CURVE ( 'NONE', #170158, #21653, #245407, .T. ) ;
#14665=DIRECTION ( 'NONE',  ( 1.000000000000000000, 0.000000000000000000, 0.000000000000000000 ) ) ;
#14709=CARTESIAN_POINT ( 'NONE',  ( 18.44364597020196328, 85.49048731717437022, -129.4651295948404197 ) ) ;
#14713=FACE_OUTER_BOUND ( 'NONE', #211737, .T. ) ;
#14732=CARTESIAN_POINT ( 'NONE',  ( 18.59999999999999076, 65.50857864377465489, -111.7731074845243739 ) ) ;
#14746=DIRECTION ( 'NONE',  ( 0.000000000000000000, 6.982962677686266711E-15, -1.000000000000000000 ) ) ;
#14795=CARTESIAN_POINT ( 'NONE',  ( 20.12500000000000355, 65.75804927292941215, -128.6629037574382721 ) ) ;
#14832=DIRECTION ( 'NONE',  ( 0.000000000000000000, 0.1568667991644355497, -0.9876197685951332295 ) ) ;
#14851=CARTESIAN_POINT ( 'NONE',  ( 20.94999999999999574, 74.83729825007408465, -128.4231074845243086 ) ) ;
#14872=VERTEX_POINT ( 'NONE', #94010 ) ;
#14881=EDGE_CURVE ( 'NONE', #192091, #112369, #95870, .T. ) ;
#14889=VERTEX_POINT ( 'NONE', #116174 ) ;
#14895=VERTEX_POINT ( 'NONE', #20939 ) ;
#14896=ORIENTED_EDGE ( 'NONE', *, *, #201184, .T. ) ;
#14958=CARTESIAN_POINT ( 'NONE',  ( -18.41817142474038960, 85.49870306661395603, -96.41914199688721965 ) ) ;
#14992=EDGE_LOOP ( 'NONE', ( #74267, #112887, #59412 ) ) ;
#15011=DIRECTION ( 'NONE',  ( 0.000000000000000000, -6.982962677686266711E-15, 1.000000000000000000 ) ) ;
#15034=AXIS2_PLACEMENT_3D ( 'NONE', #136973, #112297, #54854 ) ;
#15046=DIRECTION ( 'NONE',  ( 0.000000000000000000, -0.5000000000000016653, 0.8660254037844377084 ) ) ;
#15061=DIRECTION ( 'NONE',  ( 1.000000000000000000, 0.000000000000000000, 0.000000000000000000 ) ) ;
#15073=EDGE_LOOP ( 'NONE', ( #113178, #56437, #18692, #169849 ) ) ;
#15106=DIRECTION ( 'NONE',  ( -1.000000000000000000, 0.000000000000000000, 0.000000000000000000 ) ) ;
#15118=LINE ( 'NONE', #35971, #193014 ) ;
#15140=ORIENTED_EDGE ( 'NONE', *, *, #154765, .F. ) ;
#15142=VECTOR ( 'NONE', #156678, 1000.000000000000114 ) ;
#15183=AXIS2_PLACEMENT_3D ( 'NONE', #146506, #184358, #29201 ) ;
#15208=CARTESIAN_POINT ( 'NONE',  ( -18.59999999999999787, 77.16270174995010223, -128.4231074845242802 ) ) ;
#15223=DIRECTION ( 'NONE',  ( 0.000000000000000000, 6.982962677686266711E-15, -1.000000000000000000 ) ) ;
#15251=ORIENTED_EDGE ( 'NONE', *, *, #227436, .F. ) ;
#15302=ORIENTED_EDGE ( 'NONE', *, *, #147899, .T. ) ;
#15313=CARTESIAN_POINT ( 'NONE',  ( -18.50000000000000000, 66.75000000001199396, -115.2731074845243597 ) ) ;
#15324=DIRECTION ( 'NONE',  ( 1.000000000000000000, 0.000000000000000000, 0.000000000000000000 ) ) ;
#15361=DIRECTION ( 'NONE',  ( 1.000000000000000000, 0.000000000000000000, 0.000000000000000000 ) ) ;
#15380=VECTOR ( 'NONE', #136910, 1000.000000000000000 ) ;
#15396=DIRECTION ( 'NONE',  ( -1.000000000000000000, 1.836970198721029934E-16, 1.601412966608202925E-30 ) ) ;
#15445=DIRECTION ( 'NONE',  ( 0.000000000000000000, -6.938893903907270030E-14, 1.000000000000000000 ) ) ;
#15448=VERTEX_POINT ( 'NONE', #83094 ) ;
#15454=CIRCLE ( 'NONE', #40416, 0.1000000000000028644 ) ;
#15460=ORIENTED_EDGE ( 'NONE', *, *, #164799, .F. ) ;
#15462=LINE ( 'NONE', #254039, #106439 ) ;
#15492=CARTESIAN_POINT ( 'NONE',  ( 20.85000000000000142, 87.65000000001192859, -105.9231074845242091 ) ) ;
#15524=ADVANCED_FACE ( 'NONE', ( #229076 ), #13873, .F. ) ;
#15532=DIRECTION ( 'NONE',  ( 1.000000000000000000, 0.000000000000000000, 0.000000000000000000 ) ) ;
#15557=ORIENTED_EDGE ( 'NONE', *, *, #78794, .F. ) ;
#15562=ORIENTED_EDGE ( 'NONE', *, *, #163064, .T. ) ;
#15576=ORIENTED_EDGE ( 'NONE', *, *, #50600, .F. ) ;
#15593=ADVANCED_FACE ( 'NONE', ( #70016, #30900 ), #127405, .F. ) ;
#15619=CYLINDRICAL_SURFACE ( 'NONE', #78202, 0.1000000000000033362 ) ;
#15641=ORIENTED_EDGE ( 'NONE', *, *, #31968, .F. ) ;
#15662=DIRECTION ( 'NONE',  ( 1.000000000000000000, 7.304098846218134667E-16, 5.100424963727256530E-30 ) ) ;
#15663=CARTESIAN_POINT ( 'NONE',  ( 18.59999999999999432, 77.83585931145546510, -91.51866831572576189 ) ) ;
#15673=AXIS2_PLACEMENT_3D ( 'NONE', #83185, #45377, #166647 ) ;
#15679=VERTEX_POINT ( 'NONE', #59374 ) ;
#15685=CIRCLE ( 'NONE', #161417, 12.87499999999999822 ) ;
#15743=CARTESIAN_POINT ( 'NONE',  ( -23.25000000000000000, 85.00000000001207923, -126.6291383618717816 ) ) ;
#15748=VECTOR ( 'NONE', #65913, 1000.000000000000000 ) ;
#15760=CARTESIAN_POINT ( 'NONE',  ( 21.40925344232283223, 75.90104981139253937, -143.1816263439147292 ) ) ;
#15783=CARTESIAN_POINT ( 'NONE',  ( 20.94999999999999929, 68.87972903831429505, -99.36354444268502561 ) ) ;
#15829=ORIENTED_EDGE ( 'NONE', *, *, #128080, .F. ) ;
#15849=AXIS2_PLACEMENT_3D ( 'NONE', #126860, #205088, #207696 ) ;
#15877=CIRCLE ( 'NONE', #199000, 0.1000000000000009492 ) ;
#15970=VECTOR ( 'NONE', #201059, 1000.000000000000000 ) ;
#15972=AXIS2_PLACEMENT_3D ( 'NONE', #101103, #181992, #103699 ) ;
#15974=CARTESIAN_POINT ( 'NONE',  ( -21.07946286933444924, 69.67096268100443979, -136.5997913277807925 ) ) ;
#15983=EDGE_CURVE ( 'NONE', #255544, #16182, #67116, .T. ) ;
#16018=ADVANCED_FACE ( 'NONE', ( #230045 ), #138088, .T. ) ;
#16071=AXIS2_PLACEMENT_3D ( 'NONE', #76731, #57150, #153769 ) ;
#16075=VERTEX_POINT ( 'NONE', #134769 ) ;
#16092=EDGE_CURVE ( 'NONE', #119534, #3185, #198670, .T. ) ;
#16142=ADVANCED_FACE ( 'NONE', ( #2975 ), #118308, .T. ) ;
#16145=DIRECTION ( 'NONE',  ( 2.952720810173289112E-16, 1.000000000000000000, -6.088138035986627436E-46 ) ) ;
#16149=CIRCLE ( 'NONE', #195220, 11.65000000000000746 ) ;
#16156=EDGE_LOOP ( 'NONE', ( #222120, #112422, #116970, #83913 ) ) ;
#16164=CARTESIAN_POINT ( 'NONE',  ( 18.43473516226069364, 85.49494228277033869, -129.4772088011747257 ) ) ;
#16169=ORIENTED_EDGE ( 'NONE', *, *, #56557, .F. ) ;
#16171=CARTESIAN_POINT ( 'NONE',  ( 20.85000000000000142, 77.83585931145546510, -91.51866831572576189 ) ) ;
#16182=VERTEX_POINT ( 'NONE', #103354 ) ;
#16203=AXIS2_PLACEMENT_3D ( 'NONE', #47705, #145525, #225051 ) ;
#16252=CARTESIAN_POINT ( 'NONE',  ( -18.44204374631839016, 85.49103638961018703, -96.39690621430322892 ) ) ;
#16257=CARTESIAN_POINT ( 'NONE',  ( -20.85000000000000142, 75.83895117929318985, -103.3072973288845162 ) ) ;
#16332=ORIENTED_EDGE ( 'NONE', *, *, #43215, .F. ) ;
#16343=ADVANCED_FACE ( 'NONE', ( #27730 ), #186784, .F. ) ;
#16365=CARTESIAN_POINT ( 'NONE',  ( 23.14999999999999503, 64.35000000001197407, -115.1731074845243796 ) ) ;
#16375=ORIENTED_EDGE ( 'NONE', *, *, #67315, .F. ) ;
#16411=ADVANCED_FACE ( 'NONE', ( #158893 ), #19820, .F. ) ;
#16481=EDGE_LOOP ( 'NONE', ( #117317, #241452, #143571, #86998 ) ) ;
#16486=CARTESIAN_POINT ( 'NONE',  ( 18.59999999999999076, 65.79142135624930177, -115.2731074845243597 ) ) ;
#16488=CARTESIAN_POINT ( 'NONE',  ( -18.50000000000000000, 85.40000000001209912, -129.2258477248609552 ) ) ;
#16500=TOROIDAL_SURFACE ( 'NONE', #203916, 0.9750000000000019762, 0.1000000000000000056 ) ;
#16524=CARTESIAN_POINT ( 'NONE',  ( -20.85000000000000142, 64.25000000001196554, -109.8647081744214375 ) ) ;
#16531=DIRECTION ( 'NONE',  ( 1.000000000000000000, 0.000000000000000000, 0.000000000000000000 ) ) ;
#16544=CARTESIAN_POINT ( 'NONE',  ( -18.50000000000000000, 74.83729825007408465, -128.4231074845243086 ) ) ;
#16556=CARTESIAN_POINT ( 'NONE',  ( -20.54999999999999716, 76.00000000001192291, -105.0231074845243029 ) ) ;
#16565=ORIENTED_EDGE ( 'NONE', *, *, #69648, .T. ) ;
#16570=VERTEX_POINT ( 'NONE', #186131 ) ;
#16589=EDGE_LOOP ( 'NONE', ( #73188, #126947, #76049, #228109 ) ) ;
#16600=CYLINDRICAL_SURFACE ( 'NONE', #244926, 0.1000000000000052097 ) ;
#16608=DIRECTION ( 'NONE',  ( 2.557131231893037478E-16, 0.8660254037844420383, -0.4999999999999942824 ) ) ;
#16616=FACE_OUTER_BOUND ( 'NONE', #31292, .T. ) ;
#16625=VECTOR ( 'NONE', #3954, 1000.000000000000000 ) ;
#16637=DIRECTION ( 'NONE',  ( 0.000000000000000000, -1.000000000000000000, 0.000000000000000000 ) ) ;
#16641=CARTESIAN_POINT ( 'NONE',  ( 21.07199075132371746, 67.22505500089597774, -124.3095753229114990 ) ) ;
#16663=AXIS2_PLACEMENT_3D ( 'NONE', #163919, #6104, #85618 ) ;
#16685=CIRCLE ( 'NONE', #83278, 0.1000000000000067224 ) ;
#16701=CIRCLE ( 'NONE', #125032, 0.2000000000000057288 ) ;
#16784=DIRECTION ( 'NONE',  ( 0.000000000000000000, -7.304098846218139203E-15, 1.000000000000000000 ) ) ;
#16816=CONICAL_SURFACE ( 'NONE', #208365, 4.049999999999998046, 0.7853981633974604915 ) ;
#16840=VERTEX_POINT ( 'NONE', #256302 ) ;
#16863=CARTESIAN_POINT ( 'NONE',  ( 18.46932045258648358, 85.67068520027757472, -96.34924711152753218 ) ) ;
#16875=ORIENTED_EDGE ( 'NONE', *, *, #196405, .T. ) ;
#16911=AXIS2_PLACEMENT_3D ( 'NONE', #98149, #76054, #14832 ) ;
#16918=CARTESIAN_POINT ( 'NONE',  ( -21.05000000000000071, 74.16465844978765176, -124.9679561919613207 ) ) ;
#16929=DIRECTION ( 'NONE',  ( 0.000000000000000000, -6.982962677686266711E-15, 1.000000000000000000 ) ) ;
#16943=CARTESIAN_POINT ( 'NONE',  ( -18.59999999999999787, 64.35000000001208775, -129.5083017138703667 ) ) ;
#16957=CIRCLE ( 'NONE', #8564, 0.1000000000000028644 ) ;
#16961=EDGE_LOOP ( 'NONE', ( #37168, #228849, #123456, #66845 ) ) ;
#16966=ORIENTED_EDGE ( 'NONE', *, *, #109434, .T. ) ;
#17045=EDGE_CURVE ( 'NONE', #82597, #62401, #22484, .T. ) ;
#17056=AXIS2_PLACEMENT_3D ( 'NONE', #107041, #92296, #86179 ) ;
#17060=EDGE_CURVE ( 'NONE', #164329, #58209, #111738, .T. ) ;
#17079=ADVANCED_FACE ( 'NONE', ( #125422 ), #153483, .F. ) ;
#17100=ORIENTED_EDGE ( 'NONE', *, *, #95246, .F. ) ;
#17114=ORIENTED_EDGE ( 'NONE', *, *, #247190, .T. ) ;
#17136=ORIENTED_EDGE ( 'NONE', *, *, #29106, .F. ) ;
#17137=ORIENTED_EDGE ( 'NONE', *, *, #222637, .T. ) ;
#17154=VERTEX_POINT ( 'NONE', #219524 ) ;
#17194=FACE_OUTER_BOUND ( 'NONE', #179496, .T. ) ;
#17234=CARTESIAN_POINT ( 'NONE',  ( -20.15000000000000568, 66.70857864377474300, -124.1731074845243654 ) ) ;
#17279=EDGE_CURVE ( 'NONE', #119976, #71875, #57558, .T. ) ;
#17287=DIRECTION ( 'NONE',  ( 0.000000000000000000, -0.1350103645451974088, 0.9908441862701587999 ) ) ;
#17313=DIRECTION ( 'NONE',  ( 0.000000000000000000, 6.467318590049456648E-15, -1.000000000000000000 ) ) ;
#17327=CYLINDRICAL_SURFACE ( 'NONE', #230335, 0.09999999999999939493 ) ;
#17329=DIRECTION ( 'NONE',  ( 0.000000000000000000, 0.000000000000000000, 1.000000000000000000 ) ) ;
#17345=ORIENTED_EDGE ( 'NONE', *, *, #139454, .F. ) ;
#17351=EDGE_CURVE ( 'NONE', #216955, #19089, #194599, .T. ) ;
#17361=EDGE_CURVE ( 'NONE', #133367, #160229, #227884, .T. ) ;
#17375=ADVANCED_FACE ( 'NONE', ( #134544 ), #177587, .T. ) ;
#17381=DIRECTION ( 'NONE',  ( 0.000000000000000000, -7.086529944415894657E-15, 1.000000000000000000 ) ) ;
#17383=FACE_OUTER_BOUND ( 'NONE', #92708, .T. ) ;
#17384=CARTESIAN_POINT ( 'NONE',  ( -18.47079683080343315, 85.47166410525701963, -129.4142469435320209 ) ) ;
#17421=CARTESIAN_POINT ( 'NONE',  ( -20.54999999999999716, 76.00000000001190870, -103.0231074845243029 ) ) ;
#17455=ORIENTED_EDGE ( 'NONE', *, *, #90033, .F. ) ;
#17456=CIRCLE ( 'NONE', #133982, 12.87499999999999822 ) ;
#17490=VECTOR ( 'NONE', #170886, 1000.000000000000000 ) ;
#17494=EDGE_CURVE ( 'NONE', #1482, #105325, #115446, .T. ) ;
#17498=CARTESIAN_POINT ( 'NONE',  ( -18.46154800491001424, 85.48020627425391638, -96.36565664614275306 ) ) ;
#17500=CYLINDRICAL_SURFACE ( 'NONE', #224841, 0.09999999999999939493 ) ;
#17520=VERTEX_POINT ( 'NONE', #101829 ) ;
#17521=ORIENTED_EDGE ( 'NONE', *, *, #159230, .F. ) ;
#17539=VERTEX_POINT ( 'NONE', #44471 ) ;
#17542=ORIENTED_EDGE ( 'NONE', *, *, #57355, .F. ) ;
#17581=DIRECTION ( 'NONE',  ( 1.000000000000000000, 0.000000000000000000, 0.000000000000000000 ) ) ;
#17653=EDGE_LOOP ( 'NONE', ( #123656, #232742, #195357 ) ) ;
#17662=ORIENTED_EDGE ( 'NONE', *, *, #196481, .F. ) ;
#17668=ORIENTED_EDGE ( 'NONE', *, *, #249108, .T. ) ;
#17682=VERTEX_POINT ( 'NONE', #110842 ) ;
#17704=ORIENTED_EDGE ( 'NONE', *, *, #95180, .F. ) ;
#17718=CARTESIAN_POINT ( 'NONE',  ( -20.99551997958453953, 64.25000000001158185, -109.8714483468347538 ) ) ;
#17737=CIRCLE ( 'NONE', #88656, 0.1000000000000028644 ) ;
#17739=DIRECTION ( 'NONE',  ( -1.000000000000000000, -0.000000000000000000, -0.000000000000000000 ) ) ;
#17757=CARTESIAN_POINT ( 'NONE',  ( -21.05000000000000071, 76.08579911628621062, -142.9370863660131761 ) ) ;
#17765=DIRECTION ( 'NONE',  ( -1.000000000000000000, -0.000000000000000000, -0.000000000000000000 ) ) ;
#17824=ORIENTED_EDGE ( 'NONE', *, *, #39306, .T. ) ;
#17884=VERTEX_POINT ( 'NONE', #138095 ) ;
#17894=CARTESIAN_POINT ( 'NONE',  ( 21.05095171578076574, 67.22382012124101891, -124.3572342078864779 ) ) ;
#17984=DIRECTION ( 'NONE',  ( 2.952720810173289112E-16, 1.000000000000000000, 6.982962677686266711E-15 ) ) ;
#17996=DIRECTION ( 'NONE',  ( -1.000000000000000000, 0.000000000000000000, 0.000000000000000000 ) ) ;
#17997=AXIS2_PLACEMENT_3D ( 'NONE', #6531, #245156, #27428 ) ;
#18004=CARTESIAN_POINT ( 'NONE',  ( -22.49436431346200038, 64.35004905235869899, -136.5900110142466417 ) ) ;
#18015=LINE ( 'NONE', #97520, #183199 ) ;
#18033=DIRECTION ( 'NONE',  ( -0.000000000000000000, 1.000000000000000000, 6.982962677686266711E-15 ) ) ;
#18065=EDGE_CURVE ( 'NONE', #237888, #156851, #207077, .T. ) ;
#18067=EDGE_LOOP ( 'NONE', ( #183759, #152798, #62884, #11421, #235777, #81441, #227077, #31086, #125338, #97668, #126497, #58550, #105387, #49134, #164218, #246183 ) ) ;
#18104=AXIS2_PLACEMENT_3D ( 'NONE', #165968, #125530, #206361 ) ;
#18110=ORIENTED_EDGE ( 'NONE', *, *, #168509, .F. ) ;
#18116=CIRCLE ( 'NONE', #68191, 0.09999999999998898659 ) ;
#18132=CARTESIAN_POINT ( 'NONE',  ( 18.37172112093835352, 85.57096165225564732, -96.20637303104089710 ) ) ;
#18133=AXIS2_PLACEMENT_3D ( 'NONE', #20840, #216438, #239875 ) ;
#18181=VECTOR ( 'NONE', #35494, 1000.000000000000000 ) ;
#18192=CARTESIAN_POINT ( 'NONE',  ( 21.14999999999999503, 76.00000000001213607, -136.5231074845242745 ) ) ;
#18209=( BOUNDED_CURVE ( )  B_SPLINE_CURVE ( 3, ( #71295, #188645, #145659, #208233 ),
 .UNSPECIFIED., .F., .T. ) 
 B_SPLINE_CURVE_WITH_KNOTS ( ( 4, 4 ),
 ( 3.192897208853993085, 4.712388980384689674 ),
 .UNSPECIFIED. ) 
 CURVE ( )  GEOMETRIC_REPRESENTATION_ITEM ( )  RATIONAL_B_SPLINE_CURVE ( ( 1.000000000000000000, 0.8166740347213228279, 0.8166740347213228279, 1.000000000000000000 ) ) 
 REPRESENTATION_ITEM ( '' )  );
#18221=EDGE_CURVE ( 'NONE', #102756, #155438, #111724, .T. ) ;
#18229=DIRECTION ( 'NONE',  ( -1.000000000000000000, 2.952720810173289112E-16, 2.061873921506763405E-30 ) ) ;
#18233=VERTEX_POINT ( 'NONE', #3404 ) ;
#18247=CARTESIAN_POINT ( 'NONE',  ( 18.59999999999999787, 85.40000000001185754, -96.14106563635155567 ) ) ;
#18248=ORIENTED_EDGE ( 'NONE', *, *, #140649, .F. ) ;
#18253=FACE_OUTER_BOUND ( 'NONE', #3860, .T. ) ;
#18256=CYLINDRICAL_SURFACE ( 'NONE', #132920, 0.09999999999999939493 ) ;
#18264=CIRCLE ( 'NONE', #234742, 0.1999999999999987899 ) ;
#18279=CIRCLE ( 'NONE', #14216, 0.09999999999999939493 ) ;
#18303=ORIENTED_EDGE ( 'NONE', *, *, #137818, .F. ) ;
#18316=AXIS2_PLACEMENT_3D ( 'NONE', #234403, #901, #197847 ) ;
#18318=LINE ( 'NONE', #156584, #89030 ) ;
#18343=CARTESIAN_POINT ( 'NONE',  ( 23.14999999999999858, 74.00000000001190870, -103.0231074845243171 ) ) ;
#18408=ORIENTED_EDGE ( 'NONE', *, *, #207622, .F. ) ;
#18414=VERTEX_POINT ( 'NONE', #88061 ) ;
#18420=VERTEX_POINT ( 'NONE', #73695 ) ;
#18434=VERTEX_POINT ( 'NONE', #74978 ) ;
#18441=AXIS2_PLACEMENT_3D ( 'NONE', #143560, #82273, #240108 ) ;
#18454=FACE_OUTER_BOUND ( 'NONE', #226452, .T. ) ;
#18461=EDGE_CURVE ( 'NONE', #236918, #101582, #94500, .T. ) ;
#18463=CARTESIAN_POINT ( 'NONE',  ( 22.43288208788031568, 75.99510014512684108, -148.1727593282433872 ) ) ;
#18476=DIRECTION ( 'NONE',  ( 0.000000000000000000, 7.056502275159890043E-15, -1.000000000000000000 ) ) ;
#18482=SHAPE_REPRESENTATION_RELATIONSHIP ( 'NONE' , 'NONE' ,  #171686, #179045 ) ;
#18510=CARTESIAN_POINT ( 'NONE',  ( 20.94999999999999929, 71.18691588786246882, -114.9646252410481537 ) ) ;
#18529=CARTESIAN_POINT ( 'NONE',  ( -18.50016250449483479, 65.70233904877011355, -97.54874109119680270 ) ) ;
#18534=DIRECTION ( 'NONE',  ( 0.000000000000000000, -1.000000000000000000, 0.000000000000000000 ) ) ;
#18542=CARTESIAN_POINT ( 'NONE',  ( 18.59999999999999076, 64.25000000001207923, -128.4231074845243654 ) ) ;
#18546=CIRCLE ( 'NONE', #189236, 0.09999999999998898659 ) ;
#18555=CARTESIAN_POINT ( 'NONE',  ( -23.25000000000000000, 76.00000000001213607, -136.5231074845242745 ) ) ;
#18576=ORIENTED_EDGE ( 'NONE', *, *, #56872, .T. ) ;
#18602=ORIENTED_EDGE ( 'NONE', *, *, #186278, .T. ) ;
#18610=CARTESIAN_POINT ( 'NONE',  ( 18.49999999999999289, 69.15387683765929694, -99.28538121767448388 ) ) ;
#18631=AXIS2_PLACEMENT_3D ( 'NONE', #189267, #249243, #187983 ) ;
#18634=CARTESIAN_POINT ( 'NONE',  ( 20.85000000106584750, 64.25000000001195133, -109.8676028280505790 ) ) ;
#18664=CARTESIAN_POINT ( 'NONE',  ( -18.60000000000000142, 85.32100840337339775, -129.2871692354463562 ) ) ;
#18692=ORIENTED_EDGE ( 'NONE', *, *, #182802, .F. ) ;
#18699=DIRECTION ( 'NONE',  ( 0.000000000000000000, 1.000000000000000000, 6.982962677686266711E-15 ) ) ;
#18740=ORIENTED_EDGE ( 'NONE', *, *, #39306, .F. ) ;
#18778=CARTESIAN_POINT ( 'NONE',  ( -21.05000000000000071, 64.40000000001195701, -109.9513107147998880 ) ) ;
#18780=CARTESIAN_POINT ( 'NONE',  ( -18.50000000000000000, 85.48068669529084218, -96.08199231576638510 ) ) ;
#18788=FACE_OUTER_BOUND ( 'NONE', #231203, .T. ) ;
#18805=ORIENTED_EDGE ( 'NONE', *, *, #101475, .T. ) ;
#18806=DIRECTION ( 'NONE',  ( 1.000000000000000000, 0.000000000000000000, 0.000000000000000000 ) ) ;
#18831=FACE_OUTER_BOUND ( 'NONE', #67298, .T. ) ;
#18853=VECTOR ( 'NONE', #149222, 1000.000000000000000 ) ;
#18856=EDGE_CURVE ( 'NONE', #207360, #229115, #174511, .T. ) ;
#18869=ORIENTED_EDGE ( 'NONE', *, *, #11708, .T. ) ;
#18942=LINE ( 'NONE', #239292, #190526 ) ;
#18993=CARTESIAN_POINT ( 'NONE',  ( -18.59999999999999787, 76.00000000001190870, -103.0231074845243029 ) ) ;
#18997=ADVANCED_FACE ( 'NONE', ( #119907 ), #224892, .F. ) ;
#19028=CARTESIAN_POINT ( 'NONE',  ( -21.05000000000000071, 76.00000000001213607, -136.5231074845242745 ) ) ;
#19059=DIRECTION ( 'NONE',  ( 1.000000000000000000, -7.304098846218134667E-16, -5.100424963727255829E-30 ) ) ;
#19089=VERTEX_POINT ( 'NONE', #33664 ) ;
#19112=VERTEX_POINT ( 'NONE', #153610 ) ;
#19119=LINE ( 'NONE', #55640, #93534 ) ;
#19151=EDGE_CURVE ( 'NONE', #206067, #239754, #128669, .T. ) ;
#19160=DIRECTION ( 'NONE',  ( 0.000000000000000000, 0.000000000000000000, 1.000000000000000000 ) ) ;
#19195=VECTOR ( 'NONE', #168858, 999.9999999999998863 ) ;
#19199=ORIENTED_EDGE ( 'NONE', *, *, #74493, .T. ) ;
#19200=CARTESIAN_POINT ( 'NONE',  ( -20.85000000000000142, 64.25000000001196554, -109.8069731475024895 ) ) ;
#19216=ORIENTED_EDGE ( 'NONE', *, *, #49673, .T. ) ;
#19221=DIRECTION ( 'NONE',  ( -0.000000000000000000, -1.000000000000000000, -6.982962677686266711E-15 ) ) ;
#19250=AXIS2_PLACEMENT_3D ( 'NONE', #154810, #212204, #210902 ) ;
#19260=CYLINDRICAL_SURFACE ( 'NONE', #91214, 7.900000000000003908 ) ;
#19287=DIRECTION ( 'NONE',  ( 0.000000000000000000, -7.026728003956683390E-15, 1.000000000000000000 ) ) ;
#19317=LINE ( 'NONE', #257874, #94928 ) ;
#19321=ADVANCED_FACE ( 'NONE', ( #159999 ), #75364, .T. ) ;
#19334=EDGE_CURVE ( 'NONE', #235551, #156427, #196133, .T. ) ;
#19370=EDGE_LOOP ( 'NONE', ( #60146, #118366, #121942, #85736 ) ) ;
#19391=ORIENTED_EDGE ( 'NONE', *, *, #78794, .T. ) ;
#19409=ORIENTED_EDGE ( 'NONE', *, *, #229048, .F. ) ;
#19415=PLANE ( 'NONE',  #207393 ) ;
#19446=CIRCLE ( 'NONE', #194428, 0.1000000000000033362 ) ;
#19489=DIRECTION ( 'NONE',  ( -1.000000000000000000, 0.000000000000000000, -0.000000000000000000 ) ) ;
#19494=EDGE_CURVE ( 'NONE', #125207, #70458, #128550, .T. ) ;
#19500=ORIENTED_EDGE ( 'NONE', *, *, #22389, .T. ) ;
#19506=EDGE_LOOP ( 'NONE', ( #180394, #112059, #250658, #207530 ) ) ;
#19510=DIRECTION ( 'NONE',  ( -1.000000000000000000, -0.000000000000000000, -0.000000000000000000 ) ) ;
#19523=ORIENTED_EDGE ( 'NONE', *, *, #57886, .T. ) ;
#19559=ORIENTED_EDGE ( 'NONE', *, *, #113844, .T. ) ;
#19563=CIRCLE ( 'NONE', #178352, 0.5000000000000004441 ) ;
#19581=CARTESIAN_POINT ( 'NONE',  ( 20.94999999999999929, 76.00000000001190870, -103.0231074845243029 ) ) ;
#19614=CIRCLE ( 'NONE', #7109, 0.09999999999999971412 ) ;
#19630=VECTOR ( 'NONE', #141021, 1000.000000000000000 ) ;
#19632=DIRECTION ( 'NONE',  ( 0.000000000000000000, 6.982962677686266711E-15, -1.000000000000000000 ) ) ;
#19667=CARTESIAN_POINT ( 'NONE',  ( -23.15000000000000213, 85.50000000001207923, -126.6291383618717816 ) ) ;
#19674=AXIS2_PLACEMENT_3D ( 'NONE', #37812, #18229, #258069 ) ;
#19685=LINE ( 'NONE', #103037, #16625 ) ;
#19704=CARTESIAN_POINT ( 'NONE',  ( -21.05000000000000071, 77.83534155023646406, -124.9679561919612922 ) ) ;
#19706=ORIENTED_EDGE ( 'NONE', *, *, #241626, .T. ) ;
#19711=( BOUNDED_SURFACE ( )  B_SPLINE_SURFACE ( 3, 2, ( 
 ( #237684, #175191, #176447 ),
 ( #139847, #60315, #38214 ),
 ( #215542, #156893, #138549 ),
 ( #42069, #199861, #21233 ),
 ( #57744, #197269, #18634 ),
 ( #19936, #76036, #141158 ) ),
 .UNSPECIFIED., .F., .F., .F. ) 
 B_SPLINE_SURFACE_WITH_KNOTS ( ( 4, 2, 4 ),
 ( 3, 3 ),
 ( -1.776356839400250465E-15, 0.7853981633974468357, 1.570796326794895448 ),
 ( 0.000000000000000000, 1.000000000000000000 ),
 .UNSPECIFIED. ) 
 GEOMETRIC_REPRESENTATION_ITEM ( )  RATIONAL_B_SPLINE_SURFACE ( (
 ( 1.000000000000000000, 0.5000000000000154321, 1.000000000000000000),
 ( 1.000000000000000000, 0.4993418825323190369, 1.000000000000000000),
 ( 1.000000000000000000, 0.5278258667072365240, 1.000000000000000000),
 ( 1.000000000000000000, 0.6092287576681939543, 1.000000000000000000),
 ( 1.000000000000000000, 0.6611148371789450362, 1.000000000000000000),
 ( 1.000000000000000000, 0.7071067811865597852, 1.000000000000000000) ) ) 
 REPRESENTATION_ITEM ( '' )  SURFACE ( )  );
#19712=EDGE_LOOP ( 'NONE', ( #205396, #58710, #31284, #89260 ) ) ;
#19723=VERTEX_POINT ( 'NONE', #206495 ) ;
#19728=ORIENTED_EDGE ( 'NONE', *, *, #137818, .T. ) ;
#19730=AXIS2_PLACEMENT_3D ( 'NONE', #158731, #199108, #240809 ) ;
#19739=ADVANCED_FACE ( 'NONE', ( #65695 ), #9571, .T. ) ;
#19741=AXIS2_PLACEMENT_3D ( 'NONE', #37586, #175813, #58380 ) ;
#19745=ORIENTED_EDGE ( 'NONE', *, *, #23579, .F. ) ;
#19753=DIRECTION ( 'NONE',  ( 0.000000000000000000, 0.000000000000000000, -1.000000000000000000 ) ) ;
#19757=DIRECTION ( 'NONE',  ( 1.000000000000000000, 0.000000000000000000, 0.000000000000000000 ) ) ;
#19767=EDGE_LOOP ( 'NONE', ( #159755, #149827, #238151, #42704 ) ) ;
#19771=VERTEX_POINT ( 'NONE', #106081 ) ;
#19779=CARTESIAN_POINT ( 'NONE',  ( 18.59999999999998366, 76.00000000001190870, -103.0231074845243029 ) ) ;
#19803=AXIS2_PLACEMENT_3D ( 'NONE', #69477, #228543, #49888 ) ;
#19814=CIRCLE ( 'NONE', #86388, 0.5000000000000004441 ) ;
#19820=TOROIDAL_SURFACE ( 'NONE', #40691, 0.4000000000000005773, 0.1000000000000000056 ) ;
#19826=AXIS2_PLACEMENT_3D ( 'NONE', #180602, #98441, #175482 ) ;
#19836=CARTESIAN_POINT ( 'NONE',  ( -23.25000000000000000, 76.00000000001190870, -103.0231074845243029 ) ) ;
#19853=ORIENTED_EDGE ( 'NONE', *, *, #108175, .T. ) ;
#19870=DIRECTION ( 'NONE',  ( 0.000000000000000000, 0.000000000000000000, 1.000000000000000000 ) ) ;
#19893=ORIENTED_EDGE ( 'NONE', *, *, #39652, .F. ) ;
#19915=LINE ( 'NONE', #158173, #20722 ) ;
#19936=CARTESIAN_POINT ( 'NONE',  ( 20.94999999999999929, 64.35000000001195986, -109.8069731475024753 ) ) ;
#19941=DIRECTION ( 'NONE',  ( 0.000000000000000000, -1.000000000000000000, -6.982962677686266711E-15 ) ) ;
#19961=DIRECTION ( 'NONE',  ( 1.000000000000000000, 0.000000000000000000, 0.000000000000000000 ) ) ;
#19975=EDGE_CURVE ( 'NONE', #210448, #139103, #12174, .T. ) ;
#19993=ADVANCED_FACE ( 'NONE', ( #78528 ), #118966, .T. ) ;
#20006=CARTESIAN_POINT ( 'NONE',  ( 21.14999999999999858, 69.45934304831089889, -136.5231074845243313 ) ) ;
#20013=EDGE_CURVE ( 'NONE', #182615, #235424, #144658, .T. ) ;
#20034=ORIENTED_EDGE ( 'NONE', *, *, #167574, .F. ) ;
#20040=ORIENTED_EDGE ( 'NONE', *, *, #79671, .F. ) ;
#20041=ORIENTED_EDGE ( 'NONE', *, *, #149771, .F. ) ;
#20049=ADVANCED_FACE ( 'NONE', ( #178967 ), #257045, .T. ) ;
#20069=LINE ( 'NONE', #123016, #32425 ) ;
#20077=DIRECTION ( 'NONE',  ( 1.000000000000000000, 0.000000000000000000, 0.000000000000000000 ) ) ;
#20119=VECTOR ( 'NONE', #163092, 1000.000000000000000 ) ;
#20144=DIRECTION ( 'NONE',  ( -1.000000000000000000, -0.000000000000000000, -0.000000000000000000 ) ) ;
#20183=DIRECTION ( 'NONE',  ( 0.000000000000000000, -6.982962677686266711E-15, 1.000000000000000000 ) ) ;
#20188=CARTESIAN_POINT ( 'NONE',  ( 21.14999999999999858, 64.35000000001204512, -124.3731074845243825 ) ) ;
#20192=DIRECTION ( 'NONE',  ( -1.000000000000000000, 2.952720810173289112E-16, 2.061873921506763405E-30 ) ) ;
#20214=EDGE_CURVE ( 'NONE', #162766, #56965, #86212, .T. ) ;
#20220=CARTESIAN_POINT ( 'NONE',  ( -18.59999999999999787, 76.00000000001185185, -95.12310748452429721 ) ) ;
#20222=CARTESIAN_POINT ( 'NONE',  ( 21.05000000000000071, 87.29603075034721371, -106.0710066441880883 ) ) ;
#20258=ORIENTED_EDGE ( 'NONE', *, *, #228080, .F. ) ;
#20263=EDGE_CURVE ( 'NONE', #17682, #221833, #240526, .T. ) ;
#20295=VERTEX_POINT ( 'NONE', #224008 ) ;
#20365=FACE_BOUND ( 'NONE', #134320, .T. ) ;
#20391=VERTEX_POINT ( 'NONE', #222720 ) ;
#20409=CIRCLE ( 'NONE', #203913, 0.09999999999999939493 ) ;
#20427=EDGE_CURVE ( 'NONE', #172315, #206383, #144837, .T. ) ;
#20439=LINE ( 'NONE', #201618, #254453 ) ;
#20451=ORIENTED_EDGE ( 'NONE', *, *, #144833, .F. ) ;
#20461=AXIS2_PLACEMENT_3D ( 'NONE', #233322, #62370, #239722 ) ;
#20468=DIRECTION ( 'NONE',  ( 1.000000000000000000, 0.000000000000000000, 0.000000000000000000 ) ) ;
#20497=DIRECTION ( 'NONE',  ( -1.000000000000000000, 1.836970198721029934E-16, 1.282749433769087757E-30 ) ) ;
#20520=EDGE_CURVE ( 'NONE', #182465, #172315, #103139, .T. ) ;
#20526=DIRECTION ( 'NONE',  ( 1.713247197920696616E-14, -0.9876197685951263461, 0.1568667991644794590 ) ) ;
#20557=CARTESIAN_POINT ( 'NONE',  ( 20.94999999999999929, 77.16412189325305349, -95.10825939895268277 ) ) ;
#20581=ORIENTED_EDGE ( 'NONE', *, *, #125864, .F. ) ;
#20617=CARTESIAN_POINT ( 'NONE',  ( 18.59999999999999076, 69.01799029515542827, -99.32695536626805222 ) ) ;
#20650=EDGE_CURVE ( 'NONE', #14587, #211151, #203736, .T. ) ;
#20670=CARTESIAN_POINT ( 'NONE',  ( -23.25000000000000000, 77.14957036958755054, -95.20719500002232394 ) ) ;
#20687=AXIS2_PLACEMENT_3D ( 'NONE', #160096, #239618, #240900 ) ;
#20722=VECTOR ( 'NONE', #251097, 1000.000000000000000 ) ;
#20741=CARTESIAN_POINT ( 'NONE',  ( 20.94999999999999929, 87.65000000001190017, -103.0231074845242318 ) ) ;
#20760=CARTESIAN_POINT ( 'NONE',  ( -21.05000000000000071, 87.48912529308817909, -133.4231074845242233 ) ) ;
#20763=CARTESIAN_POINT ( 'NONE',  ( -18.59999999999999787, 64.25000000001199396, -115.1731074845243796 ) ) ;
#20802=CARTESIAN_POINT ( 'NONE',  ( 21.05000000000000071, 71.00000000001199396, -115.4283735034374274 ) ) ;
#20806=CIRCLE ( 'NONE', #245645, 0.2000000000000057288 ) ;
#20816=CARTESIAN_POINT ( 'NONE',  ( 21.14999999999999858, 69.45934304831089889, -136.5231074845243313 ) ) ;
#20818=ORIENTED_EDGE ( 'NONE', *, *, #75800, .F. ) ;
#20822=EDGE_CURVE ( 'NONE', #73853, #216955, #249283, .T. ) ;
#20825=DIRECTION ( 'NONE',  ( 0.000000000000000000, -0.9908441862701605762, 0.1350103645451835310 ) ) ;
#20840=CARTESIAN_POINT ( 'NONE',  ( 22.39999999999999503, 64.25000000001215028, -136.6231074845243825 ) ) ;
#20866=CARTESIAN_POINT ( 'NONE',  ( -20.94999999999999929, 76.00000000001190870, -103.0231074845243029 ) ) ;
#20879=CIRCLE ( 'NONE', #170753, 0.1000000000000028644 ) ;
#20896=CARTESIAN_POINT ( 'NONE',  ( 20.13684514580103624, 66.50414460725946242, -128.3800757988350938 ) ) ;
#20905=DIRECTION ( 'NONE',  ( -1.000000000000000000, 3.265361837132813093E-16, 2.280189983783949500E-30 ) ) ;
#20915=CARTESIAN_POINT ( 'NONE',  ( 21.13498764882293557, 69.50438185653827361, -136.5247638792556586 ) ) ;
#20916=ORIENTED_EDGE ( 'NONE', *, *, #41763, .T. ) ;
#20924=FACE_OUTER_BOUND ( 'NONE', #6926, .T. ) ;
#20928=DIRECTION ( 'NONE',  ( -1.000000000000000000, 0.000000000000000000, 0.000000000000000000 ) ) ;
#20939=CARTESIAN_POINT ( 'NONE',  ( 21.05000000000000071, 64.40000000001194280, -109.9513107147998880 ) ) ;
#20960=TOROIDAL_SURFACE ( 'NONE', #233333, 0.2000000000000000111, 0.1000000000000000056 ) ;
#20972=ORIENTED_EDGE ( 'NONE', *, *, #162558, .F. ) ;
#20996=ORIENTED_EDGE ( 'NONE', *, *, #109447, .T. ) ;
#21000=DIRECTION ( 'NONE',  ( -1.000000000000000000, 0.000000000000000000, 0.000000000000000000 ) ) ;
#21007=CARTESIAN_POINT ( 'NONE',  ( -20.64999999999999858, 85.50000000001197975, -112.9170766071766820 ) ) ;
#21022=ORIENTED_EDGE ( 'NONE', *, *, #119507, .F. ) ;
#21026=CARTESIAN_POINT ( 'NONE',  ( -20.94999999999999929, 76.00000000001190870, -103.0231074845243029 ) ) ;
#21037=DIRECTION ( 'NONE',  ( 2.952720810173289112E-16, 1.000000000000000000, 6.938893903907229955E-15 ) ) ;
#21040=CIRCLE ( 'NONE', #120998, 0.5000000000000004441 ) ;
#21042=ADVANCED_FACE ( 'NONE', ( #196368 ), #243671, .T. ) ;
#21043=ORIENTED_EDGE ( 'NONE', *, *, #46488, .F. ) ;
#21065=AXIS2_PLACEMENT_3D ( 'NONE', #59543, #82954, #257721 ) ;
#21076=DIRECTION ( 'NONE',  ( 1.000000000000000000, -3.265361837132813093E-16, -2.280189983783949500E-30 ) ) ;
#21097=DIRECTION ( 'NONE',  ( 0.000000000000000000, 6.853228547068871147E-15, -1.000000000000000000 ) ) ;
#21099=CARTESIAN_POINT ( 'NONE',  ( 18.57071067811864040, 65.82071067813065213, -115.1731074845243796 ) ) ;
#21119=TOROIDAL_SURFACE ( 'NONE', #250231, 6.258578643762700899, 0.1000000000000000056 ) ;
#21127=FACE_OUTER_BOUND ( 'NONE', #74818, .T. ) ;
#21130=CARTESIAN_POINT ( 'NONE',  ( -21.59142135623730852, 68.15000000001199965, -115.3731074845243540 ) ) ;
#21142=ORIENTED_EDGE ( 'NONE', *, *, #200167, .T. ) ;
#21164=CARTESIAN_POINT ( 'NONE',  ( 22.59999999999999432, 75.89914163091350474, -148.2726746080136877 ) ) ;
#21171=CARTESIAN_POINT ( 'NONE',  ( -21.00219873199083054, 64.39461131213550971, -129.6104600562298401 ) ) ;
#21229=ADVANCED_FACE ( 'NONE', ( #128398 ), #8456, .T. ) ;
#21233=CARTESIAN_POINT ( 'NONE',  ( 20.87155475150661132, 64.25000000001195133, -109.9275209553671147 ) ) ;
#21277=EDGE_CURVE ( 'NONE', #221570, #159137, #128113, .T. ) ;
#21284=EDGE_CURVE ( 'NONE', #13808, #121455, #167550, .T. ) ;
#21346=CARTESIAN_POINT ( 'NONE',  ( -23.15000000000000213, 85.00000000001197975, -112.9170766071766820 ) ) ;
#21363=EDGE_CURVE ( 'NONE', #23492, #88928, #235209, .T. ) ;
#21374=DIRECTION ( 'NONE',  ( -1.000000000000000000, 0.000000000000000000, 0.000000000000000000 ) ) ;
#21396=DIRECTION ( 'NONE',  ( 0.000000000000000000, -6.853228547068871147E-15, 1.000000000000000000 ) ) ;
#21412=EDGE_LOOP ( 'NONE', ( #179093, #54668, #32942, #201880 ) ) ;
#21417=ORIENTED_EDGE ( 'NONE', *, *, #256871, .F. ) ;
#21421=VERTEX_POINT ( 'NONE', #73592 ) ;
#21435=DIRECTION ( 'NONE',  ( 0.000000000000000000, -1.000000000000000000, 0.000000000000000000 ) ) ;
#21458=ADVANCED_FACE ( 'NONE', ( #132249 ), #81239, .T. ) ;
#21462=CARTESIAN_POINT ( 'NONE',  ( -21.05000000000000071, 87.48912529308798014, -106.1231074845242262 ) ) ;
#21464=DIRECTION ( 'NONE',  ( -1.000000000000000000, 2.952720810173289112E-16, 2.061873921506763405E-30 ) ) ;
#21476=FACE_OUTER_BOUND ( 'NONE', #136572, .T. ) ;
#21508=DIRECTION ( 'NONE',  ( 0.000000000000000000, 0.1455152366551500653, 0.9893560106964507384 ) ) ;
#21522=DIRECTION ( 'NONE',  ( 0.000000000000000000, -0.4999999999999088507, 0.8660254037844913322 ) ) ;
#21529=EDGE_CURVE ( 'NONE', #243534, #51864, #183983, .T. ) ;
#21555=TOROIDAL_SURFACE ( 'NONE', #83484, 0.2000000000000000111, 0.1000000000000000056 ) ;
#21559=DIRECTION ( 'NONE',  ( -1.000000000000000000, 0.000000000000000000, 0.000000000000000000 ) ) ;
#21572=DIRECTION ( 'NONE',  ( -1.000000000000000000, 0.000000000000000000, -0.000000000000000000 ) ) ;
#21580=ADVANCED_FACE ( 'NONE', ( #119117 ), #219831, .T. ) ;
#21591=( BOUNDED_SURFACE ( )  B_SPLINE_SURFACE ( 3, 2, ( 
 ( #233785, #193383, #253324 ),
 ( #111263, #51249, #91693 ),
 ( #115110, #75983, #12183 ),
 ( #155554, #214216, #35606 ) ),
 .UNSPECIFIED., .F., .F., .T. ) 
 B_SPLINE_SURFACE_WITH_KNOTS ( ( 4, 4 ),
 ( 3, 3 ),
 ( 0.04058434257139476031, 0.04256401539001599538 ),
 ( 0.000000000000000000, 1.000000000000000000 ),
 .UNSPECIFIED. ) 
 GEOMETRIC_REPRESENTATION_ITEM ( )  RATIONAL_B_SPLINE_SURFACE ( (
 ( 1.000000000000000000, 0.7103081912007810361, 1.000000000000000000),
 ( 1.000000000000000000, 0.7104998333556750145, 1.000000000000000000),
 ( 1.000000000000000000, 0.7107238315754048630, 1.000000000000000000),
 ( 1.000000000000000000, 0.7110073749539779220, 1.000000000000000000) ) ) 
 REPRESENTATION_ITEM ( '' )  SURFACE ( )  );
#21622=EDGE_LOOP ( 'NONE', ( #60268, #226761, #55929, #40017 ) ) ;
#21624=DIRECTION ( 'NONE',  ( 1.000000000000000000, 0.000000000000000000, 0.000000000000000000 ) ) ;
#21652=EDGE_CURVE ( 'NONE', #37720, #144144, #7453, .T. ) ;
#21653=VERTEX_POINT ( 'NONE', #83784 ) ;
#21661=ORIENTED_EDGE ( 'NONE', *, *, #120290, .T. ) ;
#21679=CARTESIAN_POINT ( 'NONE',  ( 23.14999999999999503, 64.25000000001199396, -115.2731074845243739 ) ) ;
#21686=CARTESIAN_POINT ( 'NONE',  ( 20.02499999999999858, 66.25000000001199396, -115.3731074845243683 ) ) ;
#21731=ADVANCED_FACE ( 'NONE', ( #48552 ), #144819, .T. ) ;
#21737=DIRECTION ( 'NONE',  ( 0.000000000000000000, 0.000000000000000000, 1.000000000000000000 ) ) ;
#21759=ORIENTED_EDGE ( 'NONE', *, *, #196998, .F. ) ;
#21762=CARTESIAN_POINT ( 'NONE',  ( -18.59999999999999787, 77.16412189325305349, -95.10825939895268277 ) ) ;
#21780=AXIS2_PLACEMENT_3D ( 'NONE', #162305, #241820, #146553 ) ;
#21800=DIRECTION ( 'NONE',  ( 1.000000000000000000, 0.000000000000000000, 0.000000000000000000 ) ) ;
#21839=DIRECTION ( 'NONE',  ( 0.000000000000000000, 0.1350103645451946055, -0.9908441862701591329 ) ) ;
#21908=EDGE_CURVE ( 'NONE', #70177, #102921, #253344, .T. ) ;
#21915=EDGE_LOOP ( 'NONE', ( #233605, #228488, #44989, #91581 ) ) ;
#21938=EDGE_CURVE ( 'NONE', #185471, #177518, #142208, .T. ) ;
#21958=CARTESIAN_POINT ( 'NONE',  ( -21.29999999999995808, 76.00000000001216449, -140.5731074845242858 ) ) ;
#21981=ORIENTED_EDGE ( 'NONE', *, *, #71112, .T. ) ;
#22015=DIRECTION ( 'NONE',  ( -1.000000000000000000, 3.265361837132813093E-16, 2.280189983783949500E-30 ) ) ;
#22019=DIRECTION ( 'NONE',  ( 0.000000000000000000, -6.982962677686266711E-15, 1.000000000000000000 ) ) ;
#22028=ORIENTED_EDGE ( 'NONE', *, *, #238390, .T. ) ;
#22045=DIRECTION ( 'NONE',  ( 0.000000000000000000, -1.000000000000000000, -6.982962677686266711E-15 ) ) ;
#22063=CARTESIAN_POINT ( 'NONE',  ( -23.15000000000000213, 64.35000000001198828, -115.1731074845243796 ) ) ;
#22073=ORIENTED_EDGE ( 'NONE', *, *, #160038, .T. ) ;
#22083=DIRECTION ( 'NONE',  ( 0.000000000000000000, 0.000000000000000000, -1.000000000000000000 ) ) ;
#22199=CARTESIAN_POINT ( 'NONE',  ( -20.64999999999999858, 85.00000000001207923, -127.1291383618717816 ) ) ;
#22206=DIRECTION ( 'NONE',  ( 0.000000000000000000, -6.938893903907222067E-15, 1.000000000000000000 ) ) ;
#22224=CARTESIAN_POINT ( 'NONE',  ( 18.49999999999999645, 77.29973367124300410, -146.4949779616548824 ) ) ;
#22242=DIRECTION ( 'NONE',  ( -1.000000000000000000, 1.836970198721029934E-16, 1.282749433769087757E-30 ) ) ;
#22266=CIRCLE ( 'NONE', #173289, 0.1000000000000028644 ) ;
#22270=CYLINDRICAL_SURFACE ( 'NONE', #105456, 0.09999999999998898659 ) ;
#22276=VERTEX_POINT ( 'NONE', #165797 ) ;
#22311=DIRECTION ( 'NONE',  ( 0.000000000000000000, 1.000000000000000000, 6.982962677686266711E-15 ) ) ;
#22315=TOROIDAL_SURFACE ( 'NONE', #184591, 0.4000000000000009104, 0.1000000000000000056 ) ;
#22340=DIRECTION ( 'NONE',  ( 0.000000000000000000, -6.938893903907229955E-15, 1.000000000000000000 ) ) ;
#22359=DIRECTION ( 'NONE',  ( 0.000000000000000000, 0.000000000000000000, 1.000000000000000000 ) ) ;
#22360=DIRECTION ( 'NONE',  ( -1.000000000000000000, 0.000000000000000000, 0.000000000000000000 ) ) ;
#22369=CARTESIAN_POINT ( 'NONE',  ( -21.45000000000000284, 68.29142135624935861, -124.2731074845243597 ) ) ;
#22389=EDGE_CURVE ( 'NONE', #21421, #254127, #53626, .T. ) ;
#22391=CIRCLE ( 'NONE', #1508, 2.000000000000001776 ) ;
#22397=EDGE_CURVE ( 'NONE', #65006, #21421, #91380, .T. ) ;
#22405=EDGE_LOOP ( 'NONE', ( #183645, #154834, #80275, #82327 ) ) ;
#22445=CARTESIAN_POINT ( 'NONE',  ( -21.05000000000000071, 64.25000000001209344, -129.7392418215462442 ) ) ;
#22463=DIRECTION ( 'NONE',  ( -1.000000000000000000, 0.000000000000000000, -0.000000000000000000 ) ) ;
#22478=AXIS2_PLACEMENT_3D ( 'NONE', #63474, #42638, #24383 ) ;
#22484=LINE ( 'NONE', #223212, #124229 ) ;
#22487=EDGE_LOOP ( 'NONE', ( #138303, #242618, #184300, #246209 ) ) ;
#22494=VERTEX_POINT ( 'NONE', #170965 ) ;
#22512=CYLINDRICAL_SURFACE ( 'NONE', #9892, 0.1000000000000028644 ) ;
#22515=AXIS2_PLACEMENT_3D ( 'NONE', #196030, #213006, #95621 ) ;
#22532=DIRECTION ( 'NONE',  ( 0.000000000000000000, 8.326672684688666480E-14, 1.000000000000000000 ) ) ;
#22550=CIRCLE ( 'NONE', #139019, 0.1000000000000028644 ) ;
#22551=LINE ( 'NONE', #110737, #38859 ) ;
#22591=CARTESIAN_POINT ( 'NONE',  ( 21.05000000000000426, 65.43724016256105358, -129.0662935266057900 ) ) ;
#22598=ADVANCED_FACE ( 'NONE', ( #196883 ), #18256, .T. ) ;
#22753=FACE_OUTER_BOUND ( 'NONE', #248687, .T. ) ;
#22773=CARTESIAN_POINT ( 'NONE',  ( -18.59999999999999787, 64.35000000001208775, -129.5083017138703667 ) ) ;
#22780=CIRCLE ( 'NONE', #39545, 0.1000000000000028644 ) ;
#22790=ORIENTED_EDGE ( 'NONE', *, *, #4532, .T. ) ;
#22794=VERTEX_POINT ( 'NONE', #51911 ) ;
#22806=CARTESIAN_POINT ( 'NONE',  ( 18.39999999999999858, 85.60000000001210196, -129.4910380878245633 ) ) ;
#22813=SPHERICAL_SURFACE ( 'NONE', #114490, 0.1000000000000000056 ) ;
#22827=AXIS2_PLACEMENT_3D ( 'NONE', #254677, #189628, #35709 ) ;
#22842=CIRCLE ( 'NONE', #213792, 0.09999999999999939493 ) ;
#22844=ORIENTED_EDGE ( 'NONE', *, *, #154202, .T. ) ;
#22908=AXIS2_PLACEMENT_3D ( 'NONE', #219797, #119438, #238076 ) ;
#22909=AXIS2_PLACEMENT_3D ( 'NONE', #81998, #118618, #159036 ) ;
#22944=CARTESIAN_POINT ( 'NONE',  ( -21.05000000000000071, 75.94867256767049923, -142.8232908207915273 ) ) ;
#22947=CARTESIAN_POINT ( 'NONE',  ( 23.14999999999999858, 76.00000000001190870, -103.0231074845243029 ) ) ;
#22951=AXIS2_PLACEMENT_3D ( 'NONE', #122200, #201724, #102590 ) ;
#22967=EDGE_LOOP ( 'NONE', ( #168073, #196341, #148766, #228189 ) ) ;
#22970=DIRECTION ( 'NONE',  ( 0.000000000000000000, -1.000000000000000000, -6.982962677686265922E-15 ) ) ;
#22979=CARTESIAN_POINT ( 'NONE',  ( -23.25000000000000000, 76.10000000001222986, -148.1726782920690937 ) ) ;
#22995=EDGE_CURVE ( 'NONE', #43436, #14594, #80444, .T. ) ;
#22997=CARTESIAN_POINT ( 'NONE',  ( -20.54999999999999716, 76.00000000001213607, -136.5231074845242745 ) ) ;
#23013=ORIENTED_EDGE ( 'NONE', *, *, #248898, .F. ) ;
#23037=DIRECTION ( 'NONE',  ( 1.000000000000000000, 0.000000000000000000, 0.000000000000000000 ) ) ;
#23048=EDGE_CURVE ( 'NONE', #153127, #122858, #153994, .T. ) ;
#23049=LINE ( 'NONE', #860, #154521 ) ;
#23054=AXIS2_PLACEMENT_3D ( 'NONE', #245829, #86725, #155439 ) ;
#23075=DIRECTION ( 'NONE',  ( 0.000000000000000000, -1.000000000000000000, 0.000000000000000000 ) ) ;
#23083=EDGE_CURVE ( 'NONE', #131694, #167228, #187278, .T. ) ;
#23105=CARTESIAN_POINT ( 'NONE',  ( -21.45000000000000284, 68.29142135624930177, -115.3731074845243540 ) ) ;
#23109=AXIS2_PLACEMENT_3D ( 'NONE', #123089, #202614, #227307 ) ;
#23115=DIRECTION ( 'NONE',  ( 0.000000000000000000, -0.4999999999999088507, 0.8660254037844913322 ) ) ;
#23232=FACE_OUTER_BOUND ( 'NONE', #219466, .T. ) ;
#23233=ORIENTED_EDGE ( 'NONE', *, *, #87811, .T. ) ;
#23269=CARTESIAN_POINT ( 'NONE',  ( -21.44999999999999929, 68.85000000001205933, -124.2731074845243455 ) ) ;
#23271=CARTESIAN_POINT ( 'NONE',  ( -21.05000000000000071, 69.74115727647293284, -136.5551211777123797 ) ) ;
#23274=DIRECTION ( 'NONE',  ( 2.952720810173289112E-16, 1.000000000000000000, -6.088138035986627436E-46 ) ) ;
#23286=ORIENTED_EDGE ( 'NONE', *, *, #201265, .T. ) ;
#23313=FACE_OUTER_BOUND ( 'NONE', #237816, .T. ) ;
#23380=DIRECTION ( 'NONE',  ( -1.000000000000000000, 2.952720810173289112E-16, 2.061873921506763405E-30 ) ) ;
#23383=CARTESIAN_POINT ( 'NONE',  ( -20.64999999999999858, 74.00000000001199396, -116.2477294072864140 ) ) ;
#23395=CARTESIAN_POINT ( 'NONE',  ( 21.51976009735019346, 69.08954155835293420, -136.5231074845243313 ) ) ;
#23431=CIRCLE ( 'NONE', #35883, 11.80000000000000426 ) ;
#23447=VERTEX_POINT ( 'NONE', #183149 ) ;
#23449=DIRECTION ( 'NONE',  ( 0.000000000000000000, -6.938893903907222067E-15, 1.000000000000000000 ) ) ;
#23485=EDGE_CURVE ( 'NONE', #225917, #79334, #158259, .T. ) ;
#23492=VERTEX_POINT ( 'NONE', #93969 ) ;
#23494=VECTOR ( 'NONE', #193677, 1000.000000000000000 ) ;
#23514=LINE ( 'NONE', #83416, #12425 ) ;
#23523=AXIS2_PLACEMENT_3D ( 'NONE', #76088, #253434, #36995 ) ;
#23550=CARTESIAN_POINT ( 'NONE',  ( 20.94999999999999574, 65.52661458509918191, -128.9444530202758301 ) ) ;
#23552=CIRCLE ( 'NONE', #35990, 0.09999999999999939493 ) ;
#23553=ORIENTED_EDGE ( 'NONE', *, *, #217480, .F. ) ;
#23554=CARTESIAN_POINT ( 'NONE',  ( -20.94999999999999929, 68.97833521811179480, -99.18954208262705663 ) ) ;
#23579=EDGE_CURVE ( 'NONE', #26810, #224301, #20879, .T. ) ;
#23589=DIRECTION ( 'NONE',  ( 0.000000000000000000, -0.5000000000000016653, 0.8660254037844377084 ) ) ;
#23650=CARTESIAN_POINT ( 'NONE',  ( -21.13498764882296044, 75.99834360528086563, -143.0187256279982364 ) ) ;
#23654=CARTESIAN_POINT ( 'NONE',  ( 19.75857864376268935, 64.35000000001197407, -111.6731074845243796 ) ) ;
#23711=CARTESIAN_POINT ( 'NONE',  ( 21.05000000000000071, 67.18479819544440090, -128.1025699878376827 ) ) ;
#23727=DIRECTION ( 'NONE',  ( 0.000000000000000000, 0.000000000000000000, 1.000000000000000000 ) ) ;
#23739=CARTESIAN_POINT ( 'NONE',  ( -20.94999999999999929, 64.25000000001209344, -129.5083017138703667 ) ) ;
#23751=VERTEX_POINT ( 'NONE', #211638 ) ;
#23755=FACE_OUTER_BOUND ( 'NONE', #232277, .T. ) ;
#23764=EDGE_CURVE ( 'NONE', #165453, #60977, #90381, .T. ) ;
#23769=AXIS2_PLACEMENT_3D ( 'NONE', #178640, #116079, #239878 ) ;
#23787=DIRECTION ( 'NONE',  ( 1.000000000000000000, 0.000000000000000000, 0.000000000000000000 ) ) ;
#23791=DIRECTION ( 'NONE',  ( 1.000000000000000000, 0.000000000000000000, 0.000000000000000000 ) ) ;
#23801=AXIS2_PLACEMENT_3D ( 'NONE', #209306, #131059, #188465 ) ;
#23817=ORIENTED_EDGE ( 'NONE', *, *, #163792, .F. ) ;
#23833=AXIS2_PLACEMENT_3D ( 'NONE', #31651, #109852, #212835 ) ;
#23867=ORIENTED_EDGE ( 'NONE', *, *, #207160, .F. ) ;
#23887=ORIENTED_EDGE ( 'NONE', *, *, #94759, .T. ) ;
#23896=AXIS2_PLACEMENT_3D ( 'NONE', #25908, #226650, #84533 ) ;
#23922=VECTOR ( 'NONE', #44716, 1000.000000000000000 ) ;
#23944=VECTOR ( 'NONE', #250151, 1000.000000000000000 ) ;
#23984=DIRECTION ( 'NONE',  ( -1.000000000000000000, 1.836970198721029934E-16, 1.282749433769087757E-30 ) ) ;
#23986=AXIS2_PLACEMENT_3D ( 'NONE', #246989, #68372, #44953 ) ;
#23993=CARTESIAN_POINT ( 'NONE',  ( -23.15000000000000213, 76.00000000001205080, -123.6481074845242887 ) ) ;
#24013=DIRECTION ( 'NONE',  ( 1.000000000000000000, 0.000000000000000000, 0.000000000000000000 ) ) ;
#24021=DIRECTION ( 'NONE',  ( 0.000000000000000000, 6.982962677686266711E-15, -1.000000000000000000 ) ) ;
#24029=VECTOR ( 'NONE', #239107, 1000.000000000000000 ) ;
#24054=FACE_OUTER_BOUND ( 'NONE', #81944, .T. ) ;
#24066=FACE_OUTER_BOUND ( 'NONE', #182662, .T. ) ;
#24084=CARTESIAN_POINT ( 'NONE',  ( 21.05000000000000071, 67.22371710471961137, -127.9644784893834100 ) ) ;
#24098=CIRCLE ( 'NONE', #128125, 0.1000000000000028644 ) ;
#24120=CARTESIAN_POINT ( 'NONE',  ( -23.25000000000000000, 87.75000000001222134, -148.2731074845242176 ) ) ;
#24133=CYLINDRICAL_SURFACE ( 'NONE', #98442, 0.1000000000000064587 ) ;
#24169=CARTESIAN_POINT ( 'NONE',  ( -18.59999999999999787, 74.75000000001207923, -128.5231074845243029 ) ) ;
#24175=DIRECTION ( 'NONE',  ( 1.000000000000000000, 0.000000000000000000, 0.000000000000000000 ) ) ;
#24187=EDGE_LOOP ( 'NONE', ( #56263, #230378, #133390, #83051 ) ) ;
#24192=AXIS2_PLACEMENT_3D ( 'NONE', #193388, #190836, #214222 ) ;
#24214=PLANE ( 'NONE',  #15972 ) ;
#24249=VERTEX_POINT ( 'NONE', #196967 ) ;
#24275=VERTEX_POINT ( 'NONE', #134413 ) ;
#24296=CYLINDRICAL_SURFACE ( 'NONE', #27539, 0.1000000000000028644 ) ;
#24365=ADVANCED_FACE ( 'NONE', ( #180002 ), #239972, .T. ) ;
#24383=DIRECTION ( 'NONE',  ( 0.000000000000000000, -0.1568667991644355497, -0.9876197685951332295 ) ) ;
#24399=EDGE_CURVE ( 'NONE', #50227, #122858, #145984, .T. ) ;
#24408=DIRECTION ( 'NONE',  ( -0.000000000000000000, 0.1298341882520009927, 0.9915357197604854900 ) ) ;
#24466=ORIENTED_EDGE ( 'NONE', *, *, #92462, .T. ) ;
#24472=FACE_OUTER_BOUND ( 'NONE', #254375, .T. ) ;
#24473=CARTESIAN_POINT ( 'NONE',  ( -21.55000000000000426, 68.25000000001199396, -115.2731074845243455 ) ) ;
#24476=ORIENTED_EDGE ( 'NONE', *, *, #151863, .T. ) ;
#24484=ORIENTED_EDGE ( 'NONE', *, *, #120290, .F. ) ;
#24492=DIRECTION ( 'NONE',  ( 0.000000000000000000, 0.000000000000000000, 1.000000000000000000 ) ) ;
#24502=EDGE_CURVE ( 'NONE', #24275, #76825, #33580, .T. ) ;
#24512=TOROIDAL_SURFACE ( 'NONE', #36991, 0.4000000000000012990, 0.1000000000000000056 ) ;
#24538=CARTESIAN_POINT ( 'NONE',  ( -22.50000000000094147, 75.90000000001231228, -148.1726782920691221 ) ) ;
#24580=EDGE_CURVE ( 'NONE', #107664, #200718, #167180, .T. ) ;
#24628=ORIENTED_EDGE ( 'NONE', *, *, #193568, .F. ) ;
#24629=CARTESIAN_POINT ( 'NONE',  ( 21.05000000000000071, 69.74218538953603286, -136.6208977758331287 ) ) ;
#24646=DIRECTION ( 'NONE',  ( -0.000000000000000000, 1.000000000000000000, 6.982962677686266711E-15 ) ) ;
#24664=CIRCLE ( 'NONE', #41220, 0.4000000000000114575 ) ;
#24682=CARTESIAN_POINT ( 'NONE',  ( -22.45372860728439690, 75.98507938046373056, -148.1729046192281771 ) ) ;
#24690=EDGE_CURVE ( 'NONE', #246496, #4373, #213671, .T. ) ;
#24733=EDGE_CURVE ( 'NONE', #45688, #108560, #222014, .T. ) ;
#24743=CARTESIAN_POINT ( 'NONE',  ( 20.94999999999999929, 74.16465844978765176, -124.9679561919613207 ) ) ;
#24754=CARTESIAN_POINT ( 'NONE',  ( -20.95000000000000284, 64.35000000001195986, -110.0379132551783243 ) ) ;
#24764=AXIS2_PLACEMENT_3D ( 'NONE', #98273, #20077, #77441 ) ;
#24818=LINE ( 'NONE', #182592, #164485 ) ;
#24834=VERTEX_POINT ( 'NONE', #144366 ) ;
#24855=DIRECTION ( 'NONE',  ( 0.000000000000000000, -6.467318590049456648E-15, 1.000000000000000000 ) ) ;
#24859=VERTEX_POINT ( 'NONE', #221342 ) ;
#24878=EDGE_LOOP ( 'NONE', ( #180737, #93788, #64240, #17542 ) ) ;
#24900=CARTESIAN_POINT ( 'NONE',  ( 20.94999999999999929, 70.15000000001198543, -113.1556047088022581 ) ) ;
#24902=EDGE_CURVE ( 'NONE', #231942, #28671, #85664, .T. ) ;
#24906=DIRECTION ( 'NONE',  ( 1.000000000000000000, 0.000000000000000000, 0.000000000000000000 ) ) ;
#24917=ADVANCED_FACE ( 'NONE', ( #128698 ), #106528, .T. ) ;
#24920=CARTESIAN_POINT ( 'NONE',  ( -21.11927991906891222, 75.99091632053830381, -142.9716006030158155 ) ) ;
#24961=VECTOR ( 'NONE', #114822, 1000.000000000000000 ) ;
#24969=AXIS2_PLACEMENT_3D ( 'NONE', #22806, #102272, #82710 ) ;
#24986=CARTESIAN_POINT ( 'NONE',  ( 21.05000000000000071, 67.22371710471961137, -127.9644784893834100 ) ) ;
#24988=DIRECTION ( 'NONE',  ( -1.000000000000000000, 3.265361837132813093E-16, 2.280189983783949500E-30 ) ) ;
#24992=CARTESIAN_POINT ( 'NONE',  ( -21.64999999999999858, 68.75000000001199396, -115.2731074845243455 ) ) ;
#24994=CARTESIAN_POINT ( 'NONE',  ( -23.15000000000000213, 74.00000000001205080, -123.2984855617622060 ) ) ;
#24998=DIRECTION ( 'NONE',  ( 1.000000000000000000, 0.000000000000000000, 0.000000000000000000 ) ) ;
#25015=CARTESIAN_POINT ( 'NONE',  ( -21.14999999893415250, 64.25000000001209344, -129.6786121409976715 ) ) ;
#25031=ORIENTED_EDGE ( 'NONE', *, *, #220105, .T. ) ;
#25045=CARTESIAN_POINT ( 'NONE',  ( 22.14074124539698829, 68.60992214896839414, -136.6221603803684275 ) ) ;
#25055=DIRECTION ( 'NONE',  ( 0.000000000000000000, 0.000000000000000000, -1.000000000000000000 ) ) ;
#25063=( BOUNDED_SURFACE ( )  B_SPLINE_SURFACE ( 3, 2, ( 
 ( #110080, #84371, #33160 ),
 ( #12295, #91810, #171389 ),
 ( #124850, #63573, #72257 ),
 ( #163981, #143104, #112663 ) ),
 .UNSPECIFIED., .F., .F., .F. ) 
 B_SPLINE_SURFACE_WITH_KNOTS ( ( 4, 4 ),
 ( 3, 3 ),
 ( -3.469446951953614189E-18, 0.001979672783031532438 ),
 ( 0.000000000000000000, 1.000000000000000000 ),
 .UNSPECIFIED. ) 
 GEOMETRIC_REPRESENTATION_ITEM ( )  RATIONAL_B_SPLINE_SURFACE ( (
 ( 1.000000000000000000, 0.7103081912008384347, 1.000000000000000000),
 ( 1.000000000000000000, 0.7104998333558356638, 1.000000000000000000),
 ( 1.000000000000000000, 0.7107238315755363134, 1.000000000000000000),
 ( 1.000000000000000000, 0.7110073749539295163, 1.000000000000000000) ) ) 
 REPRESENTATION_ITEM ( '' )  SURFACE ( )  );
#25068=CARTESIAN_POINT ( 'NONE',  ( 21.30000000000002558, 76.00000000001213607, -136.5231074845242745 ) ) ;
#25096=VERTEX_POINT ( 'NONE', #1990 ) ;
#25112=CIRCLE ( 'NONE', #199891, 0.5000000000000004441 ) ;
#25133=CYLINDRICAL_SURFACE ( 'NONE', #129629, 0.1000000000000033362 ) ;
#25145=CARTESIAN_POINT ( 'NONE',  ( 21.05000000000000071, 69.52244781751869596, -136.4231075192252547 ) ) ;
#25152=CIRCLE ( 'NONE', #54159, 7.800000000000001599 ) ;
#25157=FACE_OUTER_BOUND ( 'NONE', #114589, .T. ) ;
#25164=DIRECTION ( 'NONE',  ( 0.000000000000000000, -7.172728831056617961E-15, 1.000000000000000000 ) ) ;
#25181=DIRECTION ( 'NONE',  ( 0.000000000000000000, -1.000000000000000000, -8.717686153663073805E-15 ) ) ;
#25194=FACE_OUTER_BOUND ( 'NONE', #16589, .T. ) ;
#25205=DIRECTION ( 'NONE',  ( -2.602085213965226419E-14, -6.982962677686266711E-15, 1.000000000000000000 ) ) ;
#25220=CARTESIAN_POINT ( 'NONE',  ( 18.49999999999999289, 65.79142135624927334, -111.8731074845243683 ) ) ;
#25294=FACE_BOUND ( 'NONE', #231470, .T. ) ;
#25330=DIRECTION ( 'NONE',  ( 0.000000000000000000, 0.000000000000000000, 1.000000000000000000 ) ) ;
#25358=ORIENTED_EDGE ( 'NONE', *, *, #23083, .F. ) ;
#25410=DIRECTION ( 'NONE',  ( -1.000000000000000000, -0.000000000000000000, -0.000000000000000000 ) ) ;
#25421=CIRCLE ( 'NONE', #8845, 0.09999999999999939493 ) ;
#25464=ORIENTED_EDGE ( 'NONE', *, *, #57608, .T. ) ;
#25481=AXIS2_PLACEMENT_3D ( 'NONE', #56736, #39814, #58033 ) ;
#25497=CARTESIAN_POINT ( 'NONE',  ( -21.05000000000000071, 76.00000000001199396, -114.7231074845243057 ) ) ;
#25526=CARTESIAN_POINT ( 'NONE',  ( 20.86777300164945004, 65.66799936921530900, -97.42993998886008455 ) ) ;
#25531=CARTESIAN_POINT ( 'NONE',  ( -20.54999999999999716, 66.65000000001198543, -115.3731074845243683 ) ) ;
#25574=DIRECTION ( 'NONE',  ( 0.000000000000000000, -6.982962677686266711E-15, 1.000000000000000000 ) ) ;
#25606=EDGE_CURVE ( 'NONE', #105012, #13011, #56772, .T. ) ;
#25634=VECTOR ( 'NONE', #88231, 1000.000000000000000 ) ;
#25668=VERTEX_POINT ( 'NONE', #183074 ) ;
#25671=CARTESIAN_POINT ( 'NONE',  ( 23.24999999999999645, 76.00000000001213607, -136.5231074845242745 ) ) ;
#25709=ORIENTED_EDGE ( 'NONE', *, *, #194990, .F. ) ;
#25751=VERTEX_POINT ( 'NONE', #47382 ) ;
#25760=CARTESIAN_POINT ( 'NONE',  ( 18.49999999999999289, 64.25000000001196554, -111.6731074845243796 ) ) ;
#25767=B_SPLINE_CURVE_WITH_KNOTS ( 'NONE', 3,
 ( #119940, #84571, #143308, #179893, #1212, #222838, #58624, #140747, #101583, #203290, #24682, #178623, #138158, #39105, #239860, #161625 ),
 .UNSPECIFIED., .F., .F.,
 ( 4, 3, 3, 3, 3, 4 ),
 ( 0.000000000000000000, 2.209075297431620268E-05, 5.594258369009776820E-05, 8.979524372341989448E-05, 0.0001236472815274614490, 0.0001574990747609543082 ),
 .UNSPECIFIED. ) ;
#25768=TOROIDAL_SURFACE ( 'NONE', #171550, 0.6000000000000004219, 0.1000000000000000056 ) ;
#25788=CARTESIAN_POINT ( 'NONE',  ( 21.05000000000000071, 76.00000000001205080, -124.3731074845242972 ) ) ;
#25797=EDGE_CURVE ( 'NONE', #1620, #82189, #251047, .T. ) ;
#25805=VERTEX_POINT ( 'NONE', #48675 ) ;
#25807=ADVANCED_FACE ( 'NONE', ( #190801 ), #8290, .T. ) ;
#25846=AXIS2_PLACEMENT_3D ( 'NONE', #178384, #220051, #41435 ) ;
#25881=CARTESIAN_POINT ( 'NONE',  ( 22.48660254037843842, 64.25000000001213607, -136.5731074845243995 ) ) ;
#25889=DIRECTION ( 'NONE',  ( 0.000000000000000000, -0.01562499999996560217, -0.9998779222360102414 ) ) ;
#25902=DIRECTION ( 'NONE',  ( 0.000000000000000000, 1.000000000000000000, 6.982962677686266711E-15 ) ) ;
#25908=CARTESIAN_POINT ( 'NONE',  ( -21.14999999999999858, 76.10000000001222986, -148.1726782920690937 ) ) ;
#25911=DIRECTION ( 'NONE',  ( 1.000000000000000000, -0.000000000000000000, 0.000000000000000000 ) ) ;
#26001=DIRECTION ( 'NONE',  ( -1.000000000000000000, 0.000000000000000000, 0.000000000000000000 ) ) ;
#26015=DIRECTION ( 'NONE',  ( 0.000000000000000000, -0.9908441862701605762, 0.1350103645451835310 ) ) ;
#26017=FACE_OUTER_BOUND ( 'NONE', #249224, .T. ) ;
#26026=DIRECTION ( 'NONE',  ( 1.000000000000000000, 0.000000000000000000, 0.000000000000000000 ) ) ;
#26032=CIRCLE ( 'NONE', #9266, 0.3999999999999975797 ) ;
#26042=CARTESIAN_POINT ( 'NONE',  ( 18.59999999999999076, 69.45000000001206786, -126.5060803140843291 ) ) ;
#26063=AXIS2_PLACEMENT_3D ( 'NONE', #187663, #33749, #248908 ) ;
#26076=FACE_OUTER_BOUND ( 'NONE', #204314, .T. ) ;
#26097=MANIFOLD_SOLID_BREP ( 'Stock-MAS-200-1', #223943 ) ;
#26100=ORIENTED_EDGE ( 'NONE', *, *, #7181, .F. ) ;
#26101=ORIENTED_EDGE ( 'NONE', *, *, #48804, .T. ) ;
#26134=ORIENTED_EDGE ( 'NONE', *, *, #142171, .F. ) ;
#26156=AXIS2_PLACEMENT_3D ( 'NONE', #94975, #179667, #143071 ) ;
#26168=ORIENTED_EDGE ( 'NONE', *, *, #103265, .F. ) ;
#26173=DIRECTION ( 'NONE',  ( 1.000000000000000000, 0.000000000000000000, 0.000000000000000000 ) ) ;
#26186=EDGE_LOOP ( 'NONE', ( #167203, #205061, #38641, #144411 ) ) ;
#26213=CARTESIAN_POINT ( 'NONE',  ( -18.59999999999999787, 77.83534155023646406, -124.8679561919613121 ) ) ;
#26227=DIRECTION ( 'NONE',  ( 0.000000000000000000, -0.9274965247785555977, 0.3738317757009190223 ) ) ;
#26232=VECTOR ( 'NONE', #221698, 1000.000000000000000 ) ;
#26244=DIRECTION ( 'NONE',  ( -1.000000000000000000, -0.000000000000000000, -0.000000000000000000 ) ) ;
#26258=CARTESIAN_POINT ( 'NONE',  ( 21.05000000000000071, 67.12338541492499644, -128.1380270056797031 ) ) ;
#26267=SPHERICAL_SURFACE ( 'NONE', #250655, 0.1000000000000000056 ) ;
#26286=EDGE_CURVE ( 'NONE', #139066, #56206, #243046, .T. ) ;
#26299=ORIENTED_EDGE ( 'NONE', *, *, #17279, .F. ) ;
#26399=CARTESIAN_POINT ( 'NONE',  ( -21.05000000000000071, 74.73821383144705521, -128.4366085209788366 ) ) ;
#26418=ORIENTED_EDGE ( 'NONE', *, *, #142171, .T. ) ;
#26427=VECTOR ( 'NONE', #217497, 999.9999999999998863 ) ;
#26434=ORIENTED_EDGE ( 'NONE', *, *, #253302, .F. ) ;
#26485=ORIENTED_EDGE ( 'NONE', *, *, #144457, .F. ) ;
#26496=EDGE_CURVE ( 'NONE', #189309, #64533, #122453, .T. ) ;
#26500=FACE_OUTER_BOUND ( 'NONE', #243447, .T. ) ;
#26520=FACE_OUTER_BOUND ( 'NONE', #52391, .T. ) ;
#26522=CARTESIAN_POINT ( 'NONE',  ( 18.59999999999999432, 77.16270174995010223, -128.4231074845242802 ) ) ;
#26528=CARTESIAN_POINT ( 'NONE',  ( 18.58685178364169843, 85.40673308381636275, -129.3986870154365363 ) ) ;
#26597=AXIS2_PLACEMENT_3D ( 'NONE', #169026, #211978, #33367 ) ;
#26612=CARTESIAN_POINT ( 'NONE',  ( 20.94999999999999929, 77.13501884592203339, -95.30613060109196510 ) ) ;
#26642=DIRECTION ( 'NONE',  ( 1.000000000000000000, 0.000000000000000000, 0.000000000000000000 ) ) ;
#26644=CARTESIAN_POINT ( 'NONE',  ( 21.05193202509564543, 65.27606398031487345, -124.3505728811986017 ) ) ;
#26677=CIRCLE ( 'NONE', #59952, 0.1000000000000028644 ) ;
#26701=CARTESIAN_POINT ( 'NONE',  ( -18.59999999999999787, 64.35000000001198828, -115.1731074845243796 ) ) ;
#26703=CYLINDRICAL_SURFACE ( 'NONE', #171800, 0.5000000000000004441 ) ;
#26753=CARTESIAN_POINT ( 'NONE',  ( 20.95159278453404283, 67.09210366206302467, -128.0383872994151204 ) ) ;
#26771=ORIENTED_EDGE ( 'NONE', *, *, #17494, .F. ) ;
#26775=CYLINDRICAL_SURFACE ( 'NONE', #35572, 4.049999999999998046 ) ;
#26783=CIRCLE ( 'NONE', #193374, 3.900000000000000799 ) ;
#26810=VERTEX_POINT ( 'NONE', #211677 ) ;
#26915=CARTESIAN_POINT ( 'NONE',  ( -21.05000000000000071, 62.00000000001195133, -108.4502000149068834 ) ) ;
#26919=DIRECTION ( 'NONE',  ( 0.000000000000000000, -5.214354714482146219E-14, 1.000000000000000000 ) ) ;
#26925=FACE_OUTER_BOUND ( 'NONE', #157205, .T. ) ;
#26933=ADVANCED_FACE ( 'NONE', ( #192119 ), #13467, .T. ) ;
#26964=LINE ( 'NONE', #146855, #148136 ) ;
#27010=B_SPLINE_CURVE_WITH_KNOTS ( 'NONE', 3,
 ( #202855, #62076, #25526, #183307, #142860, #200301, #5923, #4641, #185864, #85444, #7215, #182024, #141603, #82877, #86746, #46343, #243258, #81595, #162473 ),
 .UNSPECIFIED., .F., .F.,
 ( 4, 3, 3, 3, 3, 3, 4 ),
 ( 1.387778780781445676E-17, 2.646747978909012316E-05, 5.271166642128706850E-05, 9.008788829884963154E-05, 0.0001426648776560992193, 0.0001897378458659761016, 0.0001917382627806360094 ),
 .UNSPECIFIED. ) ;
#27055=ORIENTED_EDGE ( 'NONE', *, *, #84122, .F. ) ;
#27088=DIRECTION ( 'NONE',  ( 0.000000000000000000, 0.000000000000000000, -1.000000000000000000 ) ) ;
#27120=AXIS2_PLACEMENT_3D ( 'NONE', #203552, #49612, #129159 ) ;
#27151=ORIENTED_EDGE ( 'NONE', *, *, #157892, .T. ) ;
#27180=SURFACE_SIDE_STYLE ('',( #180136 ) ) ;
#27221=CYLINDRICAL_SURFACE ( 'NONE', #4025, 0.09999999999999939493 ) ;
#27271=AXIS2_PLACEMENT_3D ( 'NONE', #23105, #4772, #242120 ) ;
#27286=ORIENTED_EDGE ( 'NONE', *, *, #26496, .T. ) ;
#27354=TOROIDAL_SURFACE ( 'NONE', #10744, 12.97499999999999787, 0.1000000000000000056 ) ;
#27385=CARTESIAN_POINT ( 'NONE',  ( -18.59999999999999787, 77.16412189325305349, -95.20825939895267709 ) ) ;
#27409=AXIS2_PLACEMENT_3D ( 'NONE', #135269, #15361, #115727 ) ;
#27419=EDGE_CURVE ( 'NONE', #147468, #247369, #185347, .T. ) ;
#27428=DIRECTION ( 'NONE',  ( 0.000000000000000000, -1.000000000000000000, -6.352154140967427193E-15 ) ) ;
#27479=ADVANCED_FACE ( 'NONE', ( #89460 ), #51595, .F. ) ;
#27489=EDGE_CURVE ( 'NONE', #174398, #105079, #171615, .T. ) ;
#27514=ORIENTED_EDGE ( 'NONE', *, *, #195574, .T. ) ;
#27539=AXIS2_PLACEMENT_3D ( 'NONE', #45120, #80363, #135544 ) ;
#27541=TOROIDAL_SURFACE ( 'NONE', #173290, 1.900000000000002576, 0.1000000000000000056 ) ;
#27571=CARTESIAN_POINT ( 'NONE',  ( 22.50000000000000000, 76.00000000001213607, -136.5231074845242745 ) ) ;
#27577=DIRECTION ( 'NONE',  ( 0.000000000000000000, 0.000000000000000000, 1.000000000000000000 ) ) ;
#27582=CARTESIAN_POINT ( 'NONE',  ( 21.04116576186320486, 65.37533692126069695, -124.1945257158966029 ) ) ;
#27600=DIRECTION ( 'NONE',  ( -0.000000000000000000, 6.982962677686266711E-15, -1.000000000000000000 ) ) ;
#27602=DIRECTION ( 'NONE',  ( 0.000000000000000000, 0.8660254037844377084, 0.5000000000000015543 ) ) ;
#27623=DIRECTION ( 'NONE',  ( 0.000000000000000000, 0.000000000000000000, 1.000000000000000000 ) ) ;
#27662=ADVANCED_FACE ( 'NONE', ( #254904 ), #118913, .T. ) ;
#27673=ADVANCED_FACE ( 'NONE', ( #80142 ), #139721, .F. ) ;
#27686=ORIENTED_EDGE ( 'NONE', *, *, #145628, .T. ) ;
#27708=EDGE_CURVE ( 'NONE', #15679, #99499, #122997, .T. ) ;
#27724=VERTEX_POINT ( 'NONE', #106150 ) ;
#27730=FACE_OUTER_BOUND ( 'NONE', #55761, .T. ) ;
#27745=CARTESIAN_POINT ( 'NONE',  ( 18.49999999999999289, 65.58283456529555622, -111.6731074851050494 ) ) ;
#27768=AXIS2_PLACEMENT_3D ( 'NONE', #211835, #98250, #73627 ) ;
#27803=DIRECTION ( 'NONE',  ( 0.000000000000000000, 6.982962677686266711E-15, -1.000000000000000000 ) ) ;
#27827=LINE ( 'NONE', #162191, #249129 ) ;
#27840=EDGE_CURVE ( 'NONE', #74814, #201537, #142710, .T. ) ;
#27863=VECTOR ( 'NONE', #207728, 1000.000000000000114 ) ;
#27864=ORIENTED_EDGE ( 'NONE', *, *, #7300, .F. ) ;
#27879=DIRECTION ( 'NONE',  ( 1.000000000000000000, 0.000000000000000000, 0.000000000000000000 ) ) ;
#27895=CARTESIAN_POINT ( 'NONE',  ( -20.94403535211772294, 65.69367753730655579, -97.51892380663478832 ) ) ;
#27896=DIRECTION ( 'NONE',  ( 0.000000000000000000, -1.000000000000000000, -6.982962677686265922E-15 ) ) ;
#27915=DIRECTION ( 'NONE',  ( 0.000000000000000000, 6.982962677686267499E-15, -1.000000000000000000 ) ) ;
#27941=CARTESIAN_POINT ( 'NONE',  ( 21.13507111622890022, 65.28231661301367694, -124.2739388981635926 ) ) ;
#28033=DIRECTION ( 'NONE',  ( 1.000000000000000000, 0.000000000000000000, 0.000000000000000000 ) ) ;
#28060=CARTESIAN_POINT ( 'NONE',  ( -23.25000000000000000, 76.00000000001213607, -136.5231074845242745 ) ) ;
#28081=AXIS2_PLACEMENT_3D ( 'NONE', #125454, #204961, #165877 ) ;
#28099=CIRCLE ( 'NONE', #94701, 0.1000000000000028644 ) ;
#28112=DIRECTION ( 'NONE',  ( 0.000000000000000000, 0.000000000000000000, 1.000000000000000000 ) ) ;
#28117=B_SPLINE_CURVE_WITH_KNOTS ( 'NONE', 3,
 ( #211920, #231481, #95785, #56639, #132363, #33307 ),
 .UNSPECIFIED., .F., .F.,
 ( 4, 2, 4 ),
 ( 0.000000000000000000, 0.0001569047307838633283, 0.0003138094615677266565 ),
 .UNSPECIFIED. ) ;
#28123=CIRCLE ( 'NONE', #182227, 0.1000000000000028644 ) ;
#28137=CIRCLE ( 'NONE', #44862, 0.1000000000000028644 ) ;
#28146=CIRCLE ( 'NONE', #236405, 0.1000000000000028644 ) ;
#28204=CARTESIAN_POINT ( 'NONE',  ( 20.94999999999999574, 87.75000000001210765, -133.4231074845242233 ) ) ;
#28205=CYLINDRICAL_SURFACE ( 'NONE', #68022, 0.5000000000000004441 ) ;
#28237=EDGE_CURVE ( 'NONE', #172986, #14872, #173105, .T. ) ;
#28269=ORIENTED_EDGE ( 'NONE', *, *, #14661, .F. ) ;
#28279=ADVANCED_FACE ( 'NONE', ( #190557 ), #87562, .F. ) ;
#28280=ORIENTED_EDGE ( 'NONE', *, *, #153326, .F. ) ;
#28324=ADVANCED_FACE ( 'NONE', ( #156582 ), #196943, .F. ) ;
#28325=VECTOR ( 'NONE', #166090, 1000.000000000000000 ) ;
#28329=CARTESIAN_POINT ( 'NONE',  ( -20.94999999999999929, 87.39257802171759693, -106.0970570643561501 ) ) ;
#28335=VERTEX_POINT ( 'NONE', #15783 ) ;
#28344=CIRCLE ( 'NONE', #144812, 0.09999999999999799327 ) ;
#28349=AXIS2_PLACEMENT_3D ( 'NONE', #61705, #158277, #196083 ) ;
#28372=DIRECTION ( 'NONE',  ( -1.000000000000000000, -0.000000000000000000, -0.000000000000000000 ) ) ;
#28377=ORIENTED_EDGE ( 'NONE', *, *, #249733, .F. ) ;
#28378=DIRECTION ( 'NONE',  ( 1.000000000000000000, 0.000000000000000000, 0.000000000000000000 ) ) ;
#28386=CARTESIAN_POINT ( 'NONE',  ( -21.05000000000000071, 76.00000000001213607, -136.5231074845242745 ) ) ;
#28388=EDGE_CURVE ( 'NONE', #253291, #198296, #23431, .T. ) ;
#28402=ADVANCED_FACE ( 'NONE', ( #134388 ), #173597, .F. ) ;
#28412=ORIENTED_EDGE ( 'NONE', *, *, #2855, .T. ) ;
#28418=AXIS2_PLACEMENT_3D ( 'NONE', #42998, #57396, #37878 ) ;
#28458=DIRECTION ( 'NONE',  ( 0.000000000000000000, -1.000000000000000000, -6.982962677686265922E-15 ) ) ;
#28475=ORIENTED_EDGE ( 'NONE', *, *, #110319, .F. ) ;
#28489=ORIENTED_EDGE ( 'NONE', *, *, #204143, .T. ) ;
#28504=EDGE_CURVE ( 'NONE', #171429, #192475, #161701, .T. ) ;
#28515=CARTESIAN_POINT ( 'NONE',  ( -22.59999999999999787, 64.25043287652275126, -136.6239658536230763 ) ) ;
#28519=DIRECTION ( 'NONE',  ( -3.265361837132813093E-16, -1.000000000000000000, -6.982962677686266711E-15 ) ) ;
#28542=CIRCLE ( 'NONE', #111689, 0.1000000000000017680 ) ;
#28559=CARTESIAN_POINT ( 'NONE',  ( -21.05000000000000071, 76.00000000001210765, -132.2231074845243199 ) ) ;
#28577=DIRECTION ( 'NONE',  ( 0.000000000000000000, 0.000000000000000000, 1.000000000000000000 ) ) ;
#28584=CIRCLE ( 'NONE', #32850, 0.2000000000000057288 ) ;
#28589=ORIENTED_EDGE ( 'NONE', *, *, #163974, .F. ) ;
#28599=FACE_OUTER_BOUND ( 'NONE', #82476, .T. ) ;
#28670=EDGE_LOOP ( 'NONE', ( #43972, #253723, #118299, #238949 ) ) ;
#28671=VERTEX_POINT ( 'NONE', #88534 ) ;
#28675=DIRECTION ( 'NONE',  ( 0.000000000000000000, -0.008583690987162452199, 0.9999631594459053030 ) ) ;
#28729=ADVANCED_FACE ( 'NONE', ( #254940 ), #7000, .F. ) ;
#28736=DIRECTION ( 'NONE',  ( 1.000000000000000000, 0.000000000000000000, 0.000000000000000000 ) ) ;
#28738=ORIENTED_EDGE ( 'NONE', *, *, #207473, .T. ) ;
#28758=CARTESIAN_POINT ( 'NONE',  ( -22.50000000000000000, 76.00000000001213607, -136.6231074845242972 ) ) ;
#28806=DIRECTION ( 'NONE',  ( -0.000000000000000000, 6.982962677686266711E-15, -1.000000000000000000 ) ) ;
#28859=CARTESIAN_POINT ( 'NONE',  ( -20.94999999999999929, 76.00000000001213607, -136.5231074845242745 ) ) ;
#28877=CARTESIAN_POINT ( 'NONE',  ( 18.59999999999998721, 56.14960075277857499, -134.2428044267230689 ) ) ;
#28911=EDGE_CURVE ( 'NONE', #58001, #93827, #252696, .T. ) ;
#28927=ADVANCED_FACE ( 'NONE', ( #3232 ), #82748, .F. ) ;
#28928=EDGE_LOOP ( 'NONE', ( #162778, #76303, #48819, #236124 ) ) ;
#28934=VERTEX_POINT ( 'NONE', #123204 ) ;
#28938=CARTESIAN_POINT ( 'NONE',  ( 21.05000000000000071, 65.43728505328409994, -129.0663053788799175 ) ) ;
#28948=CIRCLE ( 'NONE', #241297, 0.9750000000000036415 ) ;
#28957=CARTESIAN_POINT ( 'NONE',  ( -18.59999999999999787, 66.65000000001205649, -124.2731074845243597 ) ) ;
#28973=ORIENTED_EDGE ( 'NONE', *, *, #79876, .T. ) ;
#28996=AXIS2_PLACEMENT_3D ( 'NONE', #49576, #129116, #110822 ) ;
#29023=LINE ( 'NONE', #52369, #143959 ) ;
#29043=CARTESIAN_POINT ( 'NONE',  ( 21.05000000000000071, 76.00000000001189449, -101.1231074845242972 ) ) ;
#29084=EDGE_CURVE ( 'NONE', #128325, #31427, #145135, .T. ) ;
#29097=ORIENTED_EDGE ( 'NONE', *, *, #10243, .F. ) ;
#29098=ORIENTED_EDGE ( 'NONE', *, *, #34408, .T. ) ;
#29106=EDGE_CURVE ( 'NONE', #231809, #177416, #115198, .T. ) ;
#29118=CARTESIAN_POINT ( 'NONE',  ( -23.15000000000000213, 84.66355140188112216, -112.5472086025915388 ) ) ;
#29119=AXIS2_PLACEMENT_3D ( 'NONE', #14851, #133486, #35703 ) ;
#29136=ORIENTED_EDGE ( 'NONE', *, *, #241293, .T. ) ;
#29157=CARTESIAN_POINT ( 'NONE',  ( -21.64999999999999858, 68.65000000001205649, -124.1731074845243512 ) ) ;
#29201=DIRECTION ( 'NONE',  ( -1.000000000000000000, 0.000000000000000000, 0.000000000000000000 ) ) ;
#29217=ORIENTED_EDGE ( 'NONE', *, *, #129528, .F. ) ;
#29218=DIRECTION ( 'NONE',  ( 0.000000000000000000, -0.9915357197604804940, 0.1298341882520397950 ) ) ;
#29255=ADVANCED_FACE ( 'NONE', ( #203724 ), #119635, .T. ) ;
#29281=DIRECTION ( 'NONE',  ( -0.000000000000000000, -6.982962677686266711E-15, 1.000000000000000000 ) ) ;
#29293=DIRECTION ( 'NONE',  ( -0.000000000000000000, 0.8660254037844377084, 0.5000000000000016653 ) ) ;
#29298=VECTOR ( 'NONE', #224283, 1000.000000000000000 ) ;
#29316=ORIENTED_EDGE ( 'NONE', *, *, #122709, .T. ) ;
#29330=CARTESIAN_POINT ( 'NONE',  ( -21.05000000000000071, 76.00000000001213607, -136.5231074845242745 ) ) ;
#29337=DIRECTION ( 'NONE',  ( 0.000000000000000000, 0.000000000000000000, 1.000000000000000000 ) ) ;
#29351=DIRECTION ( 'NONE',  ( 0.000000000000000000, 0.000000000000000000, 1.000000000000000000 ) ) ;
#29355=ORIENTED_EDGE ( 'NONE', *, *, #166904, .T. ) ;
#29376=FACE_OUTER_BOUND ( 'NONE', #169281, .T. ) ;
#29378=CARTESIAN_POINT ( 'NONE',  ( 20.95512820512820440, 67.12384868372396340, -127.9644784893834100 ) ) ;
#29408=DIRECTION ( 'NONE',  ( 0.000000000000000000, 0.000000000000000000, 1.000000000000000000 ) ) ;
#29426=ORIENTED_EDGE ( 'NONE', *, *, #187529, .T. ) ;
#29480=DIRECTION ( 'NONE',  ( 0.000000000000000000, 0.000000000000000000, -1.000000000000000000 ) ) ;
#29489=VERTEX_POINT ( 'NONE', #92745 ) ;
#29492=CARTESIAN_POINT ( 'NONE',  ( -23.15000000000000213, 64.35000000001198828, -115.1731074845243796 ) ) ;
#29499=CARTESIAN_POINT ( 'NONE',  ( -20.54999999999999716, 71.65000000001199965, -115.2731074845243171 ) ) ;
#29540=ORIENTED_EDGE ( 'NONE', *, *, #96198, .F. ) ;
#29545=ORIENTED_EDGE ( 'NONE', *, *, #223409, .T. ) ;
#29552=CARTESIAN_POINT ( 'NONE',  ( 20.84999999999999432, 68.97833521811179480, -99.18954208262705663 ) ) ;
#29562=TOROIDAL_SURFACE ( 'NONE', #8682, 0.2000000000000000111, 0.1000000000000000056 ) ;
#29595=AXIS2_PLACEMENT_3D ( 'NONE', #78291, #58716, #22206 ) ;
#29664=EDGE_CURVE ( 'NONE', #235865, #207855, #224249, .T. ) ;
#29686=CARTESIAN_POINT ( 'NONE',  ( -18.59999999999999787, 64.35000000001191722, -103.0231074845243882 ) ) ;
#29696=ORIENTED_EDGE ( 'NONE', *, *, #257165, .T. ) ;
#29735=CARTESIAN_POINT ( 'NONE',  ( -20.64999999999999858, 74.00000000001205080, -123.7984855617622060 ) ) ;
#29752=CARTESIAN_POINT ( 'NONE',  ( 22.39999999999999503, 64.25000000001215028, -136.5231074845243597 ) ) ;
#29781=DIRECTION ( 'NONE',  ( 0.000000000000000000, 0.000000000000000000, 1.000000000000000000 ) ) ;
#29784=DIRECTION ( 'NONE',  ( -0.000000000000000000, 1.000000000000000000, 6.982962677686266711E-15 ) ) ;
#29789=CARTESIAN_POINT ( 'NONE',  ( -20.64999999999999858, 71.65000000001207070, -124.1731074845243228 ) ) ;
#29794=ADVANCED_FACE ( 'NONE', ( #26076 ), #147288, .F. ) ;
#29804=AXIS2_PLACEMENT_3D ( 'NONE', #58404, #256580, #76701 ) ;
#29825=CARTESIAN_POINT ( 'NONE',  ( 20.94999999999999929, 77.83534155023646406, -124.9679561919612922 ) ) ;
#29827=CARTESIAN_POINT ( 'NONE',  ( 20.95512820512820440, 67.12384868372387814, -115.2731074845243597 ) ) ;
#29828=ORIENTED_EDGE ( 'NONE', *, *, #189483, .T. ) ;
#29845=ORIENTED_EDGE ( 'NONE', *, *, #29084, .T. ) ;
#29851=TOROIDAL_SURFACE ( 'NONE', #133859, 0.2000000000000000111, 0.1000000000000000056 ) ;
#29874=CARTESIAN_POINT ( 'NONE',  ( 21.30000000000002558, 76.00000000001213607, -136.5231074845242745 ) ) ;
#29923=VERTEX_POINT ( 'NONE', #211120 ) ;
#29926=VERTEX_POINT ( 'NONE', #194143 ) ;
#29974=ORIENTED_EDGE ( 'NONE', *, *, #224641, .T. ) ;
#29991=ORIENTED_EDGE ( 'NONE', *, *, #196405, .F. ) ;
#30053=ORIENTED_EDGE ( 'NONE', *, *, #100995, .F. ) ;
#30098=EDGE_CURVE ( 'NONE', #85966, #224260, #181002, .T. ) ;
#30106=DIRECTION ( 'NONE',  ( -1.000000000000000000, 0.000000000000000000, 0.000000000000000000 ) ) ;
#30111=DIRECTION ( 'NONE',  ( -0.000000000000000000, 7.109473446599835262E-15, -1.000000000000000000 ) ) ;
#30117=CARTESIAN_POINT ( 'NONE',  ( 23.24999999999999289, 69.55000000001199112, -115.3731074845243398 ) ) ;
#30120=VECTOR ( 'NONE', #222964, 1000.000000000000000 ) ;
#30132=CARTESIAN_POINT ( 'NONE',  ( 18.39999999999999858, 85.50000000001185185, -96.42291809330220076 ) ) ;
#30172=EDGE_CURVE ( 'NONE', #206647, #71756, #68727, .T. ) ;
#30180=CARTESIAN_POINT ( 'NONE',  ( 21.14999999999999858, 87.75000000001205080, -124.2731074845242176 ) ) ;
#30185=ORIENTED_EDGE ( 'NONE', *, *, #210064, .F. ) ;
#30193=CARTESIAN_POINT ( 'NONE',  ( 21.05000000000000071, 65.31570632562440437, -128.9964335458868447 ) ) ;
#30226=LINE ( 'NONE', #108466, #41405 ) ;
#30315=CARTESIAN_POINT ( 'NONE',  ( -21.05000000000000071, 70.10000000001197407, -113.2422072491806944 ) ) ;
#30339=CIRCLE ( 'NONE', #138439, 0.1000000000000072220 ) ;
#30363=AXIS2_PLACEMENT_3D ( 'NONE', #96495, #173544, #234747 ) ;
#30365=DIRECTION ( 'NONE',  ( 0.000000000000000000, -6.982962677686266711E-15, 1.000000000000000000 ) ) ;
#30368=EDGE_CURVE ( 'NONE', #50227, #16840, #172850, .T. ) ;
#30374=EDGE_CURVE ( 'NONE', #235865, #81327, #247816, .T. ) ;
#30376=DIRECTION ( 'NONE',  ( 1.000000000000000000, 0.000000000000000000, 0.000000000000000000 ) ) ;
#30390=DIRECTION ( 'NONE',  ( 0.000000000000000000, -1.000000000000000000, -8.717686153663073805E-15 ) ) ;
#30396=EDGE_LOOP ( 'NONE', ( #170779, #68535, #4602, #209987, #168653 ) ) ;
#30408=DIRECTION ( 'NONE',  ( -0.000000000000000000, -0.6132151058540604716, 0.7899159663865477077 ) ) ;
#30443=CARTESIAN_POINT ( 'NONE',  ( -20.90851465518106167, 65.67467670974416194, -97.45317318268841689 ) ) ;
#30492=CARTESIAN_POINT ( 'NONE',  ( -18.50000000000000000, 66.85000000001200249, -115.3731074845243683 ) ) ;
#30511=CIRCLE ( 'NONE', #176256, 0.5000000000000004441 ) ;
#30543=CARTESIAN_POINT ( 'NONE',  ( 18.49999999999999645, 77.16412189325305349, -95.10825939895268277 ) ) ;
#30551=ADVANCED_FACE ( 'NONE', ( #231048 ), #48529, .F. ) ;
#30557=ORIENTED_EDGE ( 'NONE', *, *, #155034, .F. ) ;
#30560=DIRECTION ( 'NONE',  ( 1.000000000000000000, 0.000000000000000000, 0.000000000000000000 ) ) ;
#30583=CIRCLE ( 'NONE', #63883, 0.09999999999999939493 ) ;
#30586=EDGE_LOOP ( 'NONE', ( #27286, #254296, #181780, #149024, #36427 ) ) ;
#30589=AXIS2_PLACEMENT_3D ( 'NONE', #176782, #35983, #94647 ) ;
#30596=DIRECTION ( 'NONE',  ( -1.000000000000000000, -0.000000000000000000, 0.000000000000000000 ) ) ;
#30654=AXIS2_PLACEMENT_3D ( 'NONE', #197072, #121437, #19753 ) ;
#30656=CARTESIAN_POINT ( 'NONE',  ( 21.00000000000000000, 66.25000000001199396, -115.3731074845243683 ) ) ;
#30669=DIRECTION ( 'NONE',  ( 0.000000000000000000, -7.116814260417668513E-15, 1.000000000000000000 ) ) ;
#30685=CARTESIAN_POINT ( 'NONE',  ( 22.50000000000000000, 64.35042919246734527, -136.6231074845243825 ) ) ;
#30703=DIRECTION ( 'NONE',  ( 1.000000000000000000, 0.000000000000000000, 0.000000000000000000 ) ) ;
#30771=LINE ( 'NONE', #29499, #248125 ) ;
#30772=CARTESIAN_POINT ( 'NONE',  ( -21.05000000000000071, 77.85102823015292017, -124.8691942151017855 ) ) ;
#30778=AXIS2_PLACEMENT_3D ( 'NONE', #35386, #69350, #232287 ) ;
#30800=ADVANCED_FACE ( 'NONE', ( #243851 ), #2268, .T. ) ;
#30833=CARTESIAN_POINT ( 'NONE',  ( 20.94999999999999574, 77.25000000001209344, -128.5231074845242745 ) ) ;
#30863=DIRECTION ( 'NONE',  ( 1.000000000000000000, -0.000000000000000000, 0.000000000000000000 ) ) ;
#30872=CARTESIAN_POINT ( 'NONE',  ( -21.14999999999999858, 76.00000000001219291, -143.0637644362255401 ) ) ;
#30882=VERTEX_POINT ( 'NONE', #237006 ) ;
#30884=CARTESIAN_POINT ( 'NONE',  ( 18.59999999999999076, 65.79142135624930177, -115.1731074845243796 ) ) ;
#30895=DIRECTION ( 'NONE',  ( 0.000000000000000000, -1.000000000000000000, -6.982962677686265922E-15 ) ) ;
#30900=FACE_BOUND ( 'NONE', #4799, .T. ) ;
#30901=EDGE_LOOP ( 'NONE', ( #11306, #210744, #252912 ) ) ;
#30908=ORIENTED_EDGE ( 'NONE', *, *, #187841, .F. ) ;
#30924=CARTESIAN_POINT ( 'NONE',  ( 20.94999999999999574, 77.16270174995010223, -128.4231074845242802 ) ) ;
#30926=CARTESIAN_POINT ( 'NONE',  ( -23.15000000000000213, 76.00000000001190870, -103.0231074845243029 ) ) ;
#30933=LINE ( 'NONE', #10048, #175566 ) ;
#30941=VERTEX_POINT ( 'NONE', #156206 ) ;
#30954=CARTESIAN_POINT ( 'NONE',  ( -23.25000000000000000, 76.00000000001213607, -136.5231074845242745 ) ) ;
#30963=DIRECTION ( 'NONE',  ( 0.000000000000000000, -7.147358527629759053E-15, 1.000000000000000000 ) ) ;
#30975=ORIENTED_EDGE ( 'NONE', *, *, #61730, .F. ) ;
#31039=DIRECTION ( 'NONE',  ( 2.952720810173289112E-16, 1.000000000000000000, 6.982962677686266711E-15 ) ) ;
#31083=ORIENTED_EDGE ( 'NONE', *, *, #226588, .F. ) ;
#31085=CARTESIAN_POINT ( 'NONE',  ( -21.53752568617692020, 69.21319212550827160, -136.6220819458086737 ) ) ;
#31086=ORIENTED_EDGE ( 'NONE', *, *, #233606, .T. ) ;
#31097=ADVANCED_FACE ( 'NONE', ( #163888 ), #64639, .F. ) ;
#31141=AXIS2_PLACEMENT_3D ( 'NONE', #190563, #109704, #228396 ) ;
#31153=ORIENTED_EDGE ( 'NONE', *, *, #224184, .T. ) ;
#31156=DIRECTION ( 'NONE',  ( -1.000000000000000000, 0.000000000000000000, -0.000000000000000000 ) ) ;
#31159=AXIS2_PLACEMENT_3D ( 'NONE', #2089, #238135, #161188 ) ;
#31184=DIRECTION ( 'NONE',  ( 0.000000000000000000, 0.1350103645451974088, -0.9908441862701587999 ) ) ;
#31190=CIRCLE ( 'NONE', #14596, 0.1000000000000028644 ) ;
#31230=CARTESIAN_POINT ( 'NONE',  ( 22.59999999999999076, 64.25012875563564307, -136.5885370755380563 ) ) ;
#31236=CARTESIAN_POINT ( 'NONE',  ( -18.42637059832564006, 85.49694546190156075, -96.41403017472441661 ) ) ;
#31266=DIRECTION ( 'NONE',  ( 1.000000000000000000, 0.000000000000000000, 0.000000000000000000 ) ) ;
#31267=ADVANCED_FACE ( 'NONE', ( #213901 ), #252251, .T. ) ;
#31284=ORIENTED_EDGE ( 'NONE', *, *, #12864, .F. ) ;
#31292=EDGE_LOOP ( 'NONE', ( #193123, #90992, #26434, #24466 ) ) ;
#31310=CARTESIAN_POINT ( 'NONE',  ( 22.50000000000000000, 75.90000000001222702, -148.1726782920690937 ) ) ;
#31313=VERTEX_POINT ( 'NONE', #196902 ) ;
#31349=EDGE_LOOP ( 'NONE', ( #176389, #216597, #154719, #251365 ) ) ;
#31350=CIRCLE ( 'NONE', #22951, 0.1000000000000028783 ) ;
#31367=CIRCLE ( 'NONE', #64625, 0.2000000000000057288 ) ;
#31384=CARTESIAN_POINT ( 'NONE',  ( 23.14999999999999858, 72.10000000001190301, -103.0231074845243313 ) ) ;
#31392=EDGE_CURVE ( 'NONE', #188797, #127805, #140787, .T. ) ;
#31408=DIRECTION ( 'NONE',  ( 1.000000000000000000, 0.000000000000000000, 0.000000000000000000 ) ) ;
#31412=FACE_OUTER_BOUND ( 'NONE', #63767, .T. ) ;
#31414=ORIENTED_EDGE ( 'NONE', *, *, #76410, .F. ) ;
#31417=CARTESIAN_POINT ( 'NONE',  ( -21.05000000000000071, 69.74218538953603286, -136.6208977758331287 ) ) ;
#31427=VERTEX_POINT ( 'NONE', #183768 ) ;
#31450=EDGE_CURVE ( 'NONE', #156427, #75842, #248181, .T. ) ;
#31459=ADVANCED_FACE ( 'NONE', ( #28599 ), #135739, .T. ) ;
#31488=CARTESIAN_POINT ( 'NONE',  ( 20.95429693346638800, 65.45669512011652103, -128.9622249462114496 ) ) ;
#31529=FACE_OUTER_BOUND ( 'NONE', #217209, .T. ) ;
#31533=EDGE_LOOP ( 'NONE', ( #189331, #127851 ) ) ;
#31554=EDGE_CURVE ( 'NONE', #181206, #208002, #235145, .T. ) ;
#31591=VECTOR ( 'NONE', #156085, 1000.000000000000000 ) ;
#31595=DIRECTION ( 'NONE',  ( -1.000000000000000000, 0.000000000000000000, -0.000000000000000000 ) ) ;
#31597=AXIS2_PLACEMENT_3D ( 'NONE', #75966, #91671, #252024 ) ;
#31613=ORIENTED_EDGE ( 'NONE', *, *, #248898, .T. ) ;
#31621=FACE_OUTER_BOUND ( 'NONE', #250605, .T. ) ;
#31629=CARTESIAN_POINT ( 'NONE',  ( 20.95265033839679347, 65.48774916754493347, -128.9573437284944077 ) ) ;
#31651=CARTESIAN_POINT ( 'NONE',  ( -20.54999999999999716, 74.00000000001205080, -123.2984855617622060 ) ) ;
#31662=DIRECTION ( 'NONE',  ( 1.000000000000000000, 0.000000000000000000, 0.000000000000000000 ) ) ;
#31703=CARTESIAN_POINT ( 'NONE',  ( -18.50000000000000000, 64.25000000001222134, -148.2731074845243882 ) ) ;
#31722=CARTESIAN_POINT ( 'NONE',  ( -20.85000000000000142, 68.97833521811179480, -99.18954208262705663 ) ) ;
#31775=FACE_OUTER_BOUND ( 'NONE', #175558, .T. ) ;
#31780=AXIS2_PLACEMENT_3D ( 'NONE', #215772, #193669, #37176 ) ;
#31792=ORIENTED_EDGE ( 'NONE', *, *, #69145, .T. ) ;
#31806=LINE ( 'NONE', #69628, #194324 ) ;
#31808=EDGE_CURVE ( 'NONE', #152762, #76270, #118642, .T. ) ;
#31822=EDGE_CURVE ( 'NONE', #153127, #49212, #22780, .T. ) ;
#31832=CARTESIAN_POINT ( 'NONE',  ( 21.05000000000000071, 85.00000000001207923, -126.6291383618717816 ) ) ;
#31836=CYLINDRICAL_SURFACE ( 'NONE', #72717, 0.09999999999999976963 ) ;
#31841=ORIENTED_EDGE ( 'NONE', *, *, #132163, .T. ) ;
#31845=CARTESIAN_POINT ( 'NONE',  ( -21.05000000000000071, 76.00000000001213607, -136.5231074845242745 ) ) ;
#31857=CYLINDRICAL_SURFACE ( 'NONE', #105981, 0.1000000000000028644 ) ;
#31859=VERTEX_POINT ( 'NONE', #10932 ) ;
#31860=DIRECTION ( 'NONE',  ( 0.000000000000000000, 0.000000000000000000, 1.000000000000000000 ) ) ;
#31882=FACE_OUTER_BOUND ( 'NONE', #377, .T. ) ;
#31888=AXIS2_PLACEMENT_3D ( 'NONE', #133579, #35792, #193567 ) ;
#31907=ORIENTED_EDGE ( 'NONE', *, *, #78011, .T. ) ;
#31928=CARTESIAN_POINT ( 'NONE',  ( -20.94999999999999929, 74.83729825007408465, -128.5231074845243029 ) ) ;
#31933=CIRCLE ( 'NONE', #186027, 0.1000000000000072220 ) ;
#31941=EDGE_CURVE ( 'NONE', #190104, #29489, #73052, .T. ) ;
#31968=EDGE_CURVE ( 'NONE', #148869, #212214, #189546, .T. ) ;
#31985=ORIENTED_EDGE ( 'NONE', *, *, #6766, .F. ) ;
#31986=AXIS2_PLACEMENT_3D ( 'NONE', #76241, #112817, #251019 ) ;
#31998=ADVANCED_FACE ( 'NONE', ( #235112 ), #164602, .T. ) ;
#32000=DIRECTION ( 'NONE',  ( 0.000000000000000000, -6.982962677686266711E-15, 1.000000000000000000 ) ) ;
#32033=DIRECTION ( 'NONE',  ( 0.000000000000000000, 7.086529944415894657E-15, -1.000000000000000000 ) ) ;
#32059=DIRECTION ( 'NONE',  ( 0.000000000000000000, -1.000000000000000000, 0.000000000000000000 ) ) ;
#32078=CIRCLE ( 'NONE', #131831, 0.1000000000000033362 ) ;
#32133=EDGE_CURVE ( 'NONE', #121455, #172986, #44612, .T. ) ;
#32137=LINE ( 'NONE', #152083, #206144 ) ;
#32143=DIRECTION ( 'NONE',  ( -0.000000000000000000, 0.1350103645451974088, -0.9908441862701587999 ) ) ;
#32162=DIRECTION ( 'NONE',  ( 1.000000000000000000, 0.000000000000000000, 0.000000000000000000 ) ) ;
#32179=CARTESIAN_POINT ( 'NONE',  ( 23.15000000000000213, 88.41227409416160299, -106.0231074845242176 ) ) ;
#32232=DIRECTION ( 'NONE',  ( 0.000000000000000000, 0.000000000000000000, 1.000000000000000000 ) ) ;
#32245=AXIS2_PLACEMENT_3D ( 'NONE', #213982, #35379, #216538 ) ;
#32258=ORIENTED_EDGE ( 'NONE', *, *, #3683, .T. ) ;
#32266=CARTESIAN_POINT ( 'NONE',  ( -20.05000000000000426, 66.75000000001199396, -115.3731074845243683 ) ) ;
#32288=CARTESIAN_POINT ( 'NONE',  ( -21.05000000000000071, 64.35000000001214460, -136.4231074845243938 ) ) ;
#32324=ADVANCED_FACE ( 'NONE', ( #47142, #206250 ), #107135, .T. ) ;
#32353=FACE_OUTER_BOUND ( 'NONE', #129175, .T. ) ;
#32376=CARTESIAN_POINT ( 'NONE',  ( 21.14999999999999858, 67.21339244341194785, -124.2731074845243597 ) ) ;
#32381=CIRCLE ( 'NONE', #244703, 11.65000000000000746 ) ;
#32406=CARTESIAN_POINT ( 'NONE',  ( -23.25000000000000000, 68.97833521811179480, -99.18954208262705663 ) ) ;
#32412=EDGE_CURVE ( 'NONE', #130620, #230224, #239941, .T. ) ;
#32425=VECTOR ( 'NONE', #224662, 1000.000000000000000 ) ;
#32514=CARTESIAN_POINT ( 'NONE',  ( -18.46907102845853288, 85.47372736477593946, -96.34707274578771319 ) ) ;
#32528=DIRECTION ( 'NONE',  ( 0.000000000000000000, 0.8660254037844420383, -0.4999999999999943379 ) ) ;
#32604=CARTESIAN_POINT ( 'NONE',  ( 18.31325810956227684, 85.53638847601904160, -96.15466727821856807 ) ) ;
#32612=EDGE_LOOP ( 'NONE', ( #120994, #207395, #84500 ) ) ;
#32617=DIRECTION ( 'NONE',  ( 0.000000000000000000, 1.000000000000000000, 0.000000000000000000 ) ) ;
#32625=DIRECTION ( 'NONE',  ( 0.000000000000000000, -6.982962677686266711E-15, 1.000000000000000000 ) ) ;
#32642=FACE_OUTER_BOUND ( 'NONE', #121705, .T. ) ;
#32645=ORIENTED_EDGE ( 'NONE', *, *, #230502, .F. ) ;
#32653=DIRECTION ( 'NONE',  ( 0.000000000000000000, 0.000000000000000000, -1.000000000000000000 ) ) ;
#32657=EDGE_CURVE ( 'NONE', #147024, #187556, #48138, .T. ) ;
#32707=DIRECTION ( 'NONE',  ( 0.000000000000000000, -0.1350103645451945777, 0.9908441862701590219 ) ) ;
#32711=AXIS2_PLACEMENT_3D ( 'NONE', #216166, #37560, #157536 ) ;
#32716=CYLINDRICAL_SURFACE ( 'NONE', #87930, 0.5000000000000004441 ) ;
#32724=CARTESIAN_POINT ( 'NONE',  ( 20.94999999999999574, 87.65000000001212754, -133.6231074845242119 ) ) ;
#32726=DIRECTION ( 'NONE',  ( 1.000000000000000000, 0.000000000000000000, 0.000000000000000000 ) ) ;
#32746=EDGE_LOOP ( 'NONE', ( #235895, #42147, #63179, #40969 ) ) ;
#32750=ORIENTED_EDGE ( 'NONE', *, *, #4381, .T. ) ;
#32769=CARTESIAN_POINT ( 'NONE',  ( 18.59999999999999076, 74.16465844978765176, -124.9679561919613207 ) ) ;
#32790=LINE ( 'NONE', #210120, #72825 ) ;
#32793=CARTESIAN_POINT ( 'NONE',  ( 18.55121869061587958, 65.67252876774529113, -97.44570419949944551 ) ) ;
#32833=PRODUCT ( 'Injection Molded Chain Links 13', 'Injection Molded Chain Links 13', '', ( #95206 ) ) ;
#32850=AXIS2_PLACEMENT_3D ( 'NONE', #256815, #78226, #237319 ) ;
#32858=FACE_OUTER_BOUND ( 'NONE', #98511, .T. ) ;
#32861=ORIENTED_EDGE ( 'NONE', *, *, #5340, .T. ) ;
#32868=B_SPLINE_CURVE_WITH_KNOTS ( 'NONE', 3,
 ( #223184, #161964, #139791, #241483, #44566, #142369 ),
 .UNSPECIFIED., .F., .F.,
 ( 4, 2, 4 ),
 ( 0.000000000000000000, 0.0001497467027049222718, 0.0002994934054098445436 ),
 .UNSPECIFIED. ) ;
#32889=CARTESIAN_POINT ( 'NONE',  ( 18.49999999999999645, 74.13328508995475374, -124.7704322382423072 ) ) ;
#32894=CARTESIAN_POINT ( 'NONE',  ( 20.94999999999999929, 71.00000000001199396, -114.9283735034374274 ) ) ;
#32895=EDGE_CURVE ( 'NONE', #156851, #155989, #85808, .T. ) ;
#32926=CARTESIAN_POINT ( 'NONE',  ( 20.95378194480896639, 65.46508800846929432, -128.9580533363765369 ) ) ;
#32929=CYLINDRICAL_SURFACE ( 'NONE', #114767, 0.5000000000000004441 ) ;
#32942=ORIENTED_EDGE ( 'NONE', *, *, #92473, .F. ) ;
#32953=DIRECTION ( 'NONE',  ( 0.000000000000000000, 1.000000000000000000, 6.982962677686266711E-15 ) ) ;
#32981=CARTESIAN_POINT ( 'NONE',  ( 20.04142135623730070, 64.35000000001198828, -115.1731074845243796 ) ) ;
#32993=ADVANCED_FACE ( 'NONE', ( #81785 ), #240904, .F. ) ;
#33005=CARTESIAN_POINT ( 'NONE',  ( 20.12500000000000000, 66.25000000001205080, -115.3731074845243683 ) ) ;
#33081=DIRECTION ( 'NONE',  ( 0.000000000000000000, -7.147358527629766941E-15, 1.000000000000000000 ) ) ;
#33124=EDGE_CURVE ( 'NONE', #160229, #254598, #169465, .T. ) ;
#33160=CARTESIAN_POINT ( 'NONE',  ( 22.47071067811864964, 75.90090754530959316, -144.2431822290223522 ) ) ;
#33166=DIRECTION ( 'NONE',  ( 1.000000000000000000, -0.000000000000000000, 0.000000000000000000 ) ) ;
#33167=ORIENTED_EDGE ( 'NONE', *, *, #69806, .F. ) ;
#33174=DIRECTION ( 'NONE',  ( 0.000000000000000000, -7.034366652768095332E-15, 1.000000000000000000 ) ) ;
#33179=VECTOR ( 'NONE', #238463, 1000.000000000000000 ) ;
#33201=VERTEX_POINT ( 'NONE', #56781 ) ;
#33236=AXIS2_PLACEMENT_3D ( 'NONE', #233967, #239115, #60455 ) ;
#33241=ORIENTED_EDGE ( 'NONE', *, *, #171438, .F. ) ;
#33281=EDGE_CURVE ( 'NONE', #81327, #188797, #65176, .T. ) ;
#33295=VERTEX_POINT ( 'NONE', #77637 ) ;
#33307=CARTESIAN_POINT ( 'NONE',  ( 22.39999999999999503, 76.10085836911093793, -148.2726746080136877 ) ) ;
#33317=ADVANCED_FACE ( 'NONE', ( #48803 ), #24133, .T. ) ;
#33319=CARTESIAN_POINT ( 'NONE',  ( -21.65000000000000213, 68.29142135624930177, -115.2731074845243455 ) ) ;
#33332=DIRECTION ( 'NONE',  ( 1.000000000000000000, -3.265361837132813093E-16, -2.280189983783949500E-30 ) ) ;
#33363=ORIENTED_EDGE ( 'NONE', *, *, #180403, .F. ) ;
#33366=VECTOR ( 'NONE', #60962, 1000.000000000000000 ) ;
#33367=DIRECTION ( 'NONE',  ( 0.000000000000000000, 0.000000000000000000, 1.000000000000000000 ) ) ;
#33375=DIRECTION ( 'NONE',  ( 0.000000000000000000, 0.000000000000000000, 1.000000000000000000 ) ) ;
#33383=DIRECTION ( 'NONE',  ( 1.000000000000000000, 0.000000000000000000, 0.000000000000000000 ) ) ;
#33398=CARTESIAN_POINT ( 'NONE',  ( -22.45305610364635385, 76.10085836911093793, -148.2726746080136593 ) ) ;
#33401=ORIENTED_EDGE ( 'NONE', *, *, #160748, .T. ) ;
#33418=CARTESIAN_POINT ( 'NONE',  ( 21.10257677756356998, 75.97504925044421498, -142.9214892270570658 ) ) ;
#33464=VECTOR ( 'NONE', #256455, 1000.000000000000114 ) ;
#33472=DIRECTION ( 'NONE',  ( -1.000000000000000000, 2.952720810173289112E-16, 2.061873921506763405E-30 ) ) ;
#33475=DIRECTION ( 'NONE',  ( 0.000000000000000000, -0.8660254037844377084, -0.5000000000000016653 ) ) ;
#33508=CYLINDRICAL_SURFACE ( 'NONE', #206066, 0.09999999999999939493 ) ;
#33525=VECTOR ( 'NONE', #180914, 1000.000000000000000 ) ;
#33532=ADVANCED_FACE ( 'NONE', ( #37943, #129631 ), #255630, .T. ) ;
#33545=VECTOR ( 'NONE', #63750, 1000.000000000000000 ) ;
#33580=B_SPLINE_CURVE_WITH_KNOTS ( 'NONE', 3,
 ( #12934, #10354, #31230, #70346 ),
 .UNSPECIFIED., .F., .F.,
 ( 4, 4 ),
 ( 3.469446951953614189E-18, 0.0001058379652594603572 ),
 .UNSPECIFIED. ) ;
#33621=LINE ( 'NONE', #149691, #165375 ) ;
#33664=CARTESIAN_POINT ( 'NONE',  ( -23.25000000000000000, 74.08971962618021223, -115.6544753397232626 ) ) ;
#33681=ORIENTED_EDGE ( 'NONE', *, *, #135274, .F. ) ;
#33685=SURFACE_SIDE_STYLE ('',( #153638 ) ) ;
#33711=DIRECTION ( 'NONE',  ( 1.000000000000000000, 0.000000000000000000, 0.000000000000000000 ) ) ;
#33713=AXIS2_PLACEMENT_3D ( 'NONE', #99104, #238645, #100385 ) ;
#33742=DIRECTION ( 'NONE',  ( 0.000000000000000000, 0.000000000000000000, 1.000000000000000000 ) ) ;
#33743=CARTESIAN_POINT ( 'NONE',  ( 21.06086055315979522, 67.22529248505583155, -124.3207853293703664 ) ) ;
#33749=DIRECTION ( 'NONE',  ( 0.5000000000001141309, -6.047423072554455661E-15, 0.8660254037843729824 ) ) ;
#33760=CARTESIAN_POINT ( 'NONE',  ( -18.59999999999999787, 74.25000000001205080, -124.8535959266226598 ) ) ;
#33778=AXIS2_PLACEMENT_3D ( 'NONE', #82924, #158680, #222436 ) ;
#33786=CARTESIAN_POINT ( 'NONE',  ( -18.59999999999999787, 76.00000000001190870, -103.0231074845243029 ) ) ;
#33799=EDGE_CURVE ( 'NONE', #3185, #163770, #152885, .T. ) ;
#33835=CARTESIAN_POINT ( 'NONE',  ( 23.14999999999999858, 76.00000000001190870, -103.0231074845243029 ) ) ;
#33840=ADVANCED_FACE ( 'NONE', ( #148581 ), #127737, .F. ) ;
#33842=ORIENTED_EDGE ( 'NONE', *, *, #174455, .F. ) ;
#33849=ORIENTED_EDGE ( 'NONE', *, *, #99640, .F. ) ;
#33903=CIRCLE ( 'NONE', #204701, 11.74999999999999645 ) ;
#33908=AXIS2_PLACEMENT_3D ( 'NONE', #169858, #34186, #214070 ) ;
#33982=CARTESIAN_POINT ( 'NONE',  ( 21.04999999999998650, 69.35000000001205933, -124.2731074845243455 ) ) ;
#34015=EDGE_CURVE ( 'NONE', #70035, #238178, #153079, .T. ) ;
#34055=EDGE_LOOP ( 'NONE', ( #185725, #255830, #227092, #8128 ) ) ;
#34106=EDGE_LOOP ( 'NONE', ( #160542, #166684, #136393, #80693 ) ) ;
#34108=EDGE_LOOP ( 'NONE', ( #53454, #245602, #63984, #85470 ) ) ;
#34131=AXIS2_PLACEMENT_3D ( 'NONE', #10551, #230893, #247864 ) ;
#34142=ADVANCED_FACE ( 'NONE', ( #86967 ), #107423, .T. ) ;
#34150=AXIS2_PLACEMENT_3D ( 'NONE', #206146, #50890, #130453 ) ;
#34174=DIRECTION ( 'NONE',  ( 0.000000000000000000, 0.9893560106964510714, -0.1455152366551481502 ) ) ;
#34186=DIRECTION ( 'NONE',  ( 0.000000000000000000, -0.1350103645451945777, 0.9908441862701591329 ) ) ;
#34195=ORIENTED_EDGE ( 'NONE', *, *, #59038, .T. ) ;
#34198=CARTESIAN_POINT ( 'NONE',  ( 20.95539060131842746, 65.37613784235644232, -128.8693736708681854 ) ) ;
#34219=ORIENTED_EDGE ( 'NONE', *, *, #71642, .F. ) ;
#34236=CARTESIAN_POINT ( 'NONE',  ( -20.64999999999999858, 84.73084112150739600, -126.9250327655398962 ) ) ;
#34239=CIRCLE ( 'NONE', #179970, 0.1000000000000028644 ) ;
#34251=CARTESIAN_POINT ( 'NONE',  ( -23.15000000000000213, 76.00000000001210765, -132.4731074845242915 ) ) ;
#34262=AXIS2_PLACEMENT_3D ( 'NONE', #60543, #24021, #103514 ) ;
#34277=CYLINDRICAL_SURFACE ( 'NONE', #175879, 0.5000000000000004441 ) ;
#34287=CYLINDRICAL_SURFACE ( 'NONE', #250162, 0.09999999999999939493 ) ;
#34292=ORIENTED_EDGE ( 'NONE', *, *, #236806, .F. ) ;
#34310=CIRCLE ( 'NONE', #180035, 0.1000000000000028644 ) ;
#34323=EDGE_CURVE ( 'NONE', #193833, #155848, #44890, .T. ) ;
#34345=AXIS2_PLACEMENT_3D ( 'NONE', #74221, #11659, #32528 ) ;
#34369=VECTOR ( 'NONE', #203944, 1000.000000000000000 ) ;
#34376=DIRECTION ( 'NONE',  ( -1.836970198721029934E-16, -1.000000000000000000, -6.982962677686266711E-15 ) ) ;
#34387=ORIENTED_EDGE ( 'NONE', *, *, #181317, .T. ) ;
#34396=CARTESIAN_POINT ( 'NONE',  ( 21.05000000000000071, 64.35000000001213039, -136.5231074845243597 ) ) ;
#34402=DIRECTION ( 'NONE',  ( 1.000000000000000000, 0.000000000000000000, 0.000000000000000000 ) ) ;
#34404=CARTESIAN_POINT ( 'NONE',  ( -21.78635804494510708, 68.96433851485896582, -136.6221125500320284 ) ) ;
#34408=EDGE_CURVE ( 'NONE', #128325, #53595, #15877, .T. ) ;
#34419=VERTEX_POINT ( 'NONE', #218471 ) ;
#34455=EDGE_CURVE ( 'NONE', #8771, #109129, #149261, .T. ) ;
#34461=ORIENTED_EDGE ( 'NONE', *, *, #100688, .T. ) ;
#34469=ORIENTED_EDGE ( 'NONE', *, *, #145216, .T. ) ;
#34489=EDGE_CURVE ( 'NONE', #127497, #145638, #90838, .T. ) ;
#34498=CARTESIAN_POINT ( 'NONE',  ( -23.15000000000000213, 85.00000000001207923, -126.6291383618717816 ) ) ;
#34505=CIRCLE ( 'NONE', #142780, 0.1000000000000046685 ) ;
#34512=B_SPLINE_CURVE_WITH_KNOTS ( 'NONE', 3,
 ( #149108, #126958, #48693, #147817, #106078, #124399, #27895, #205191, #228649, #184349, #146496, #30443, #245625, #108679, #90390, #129533, #109953, #107384, #85223 ),
 .UNSPECIFIED., .F., .F.,
 ( 4, 3, 3, 3, 3, 3, 4 ),
 ( -2.000416914659873068E-06, 0.000000000000000000, 4.714008503744566487E-05, 9.979203887777271477E-05, 0.0001372215519229485938, 0.0001635031576220933387, 0.0001900083748504131887 ),
 .UNSPECIFIED. ) ;
#34514=CIRCLE ( 'NONE', #13644, 0.09999999999998898659 ) ;
#34519=DIRECTION ( 'NONE',  ( 0.000000000000000000, 1.000000000000000000, 8.717686153663073805E-15 ) ) ;
#34531=AXIS2_PLACEMENT_3D ( 'NONE', #84938, #22463, #45850 ) ;
#34578=EDGE_CURVE ( 'NONE', #54998, #211151, #195114, .T. ) ;
#34583=VERTEX_POINT ( 'NONE', #203635 ) ;
#34623=DIRECTION ( 'NONE',  ( 1.000000000000000000, 0.000000000000000000, 0.000000000000000000 ) ) ;
#34640=ADVANCED_FACE ( 'NONE', ( #61564 ), #291, .T. ) ;
#34665=EDGE_LOOP ( 'NONE', ( #111568, #233409, #5719, #131872 ) ) ;
#34668=ORIENTED_EDGE ( 'NONE', *, *, #258052, .F. ) ;
#34694=DIRECTION ( 'NONE',  ( 1.000000000000000000, -7.304098846218134667E-16, -5.100424963727256530E-30 ) ) ;
#34756=ORIENTED_EDGE ( 'NONE', *, *, #58447, .T. ) ;
#34790=DIRECTION ( 'NONE',  ( 0.000000000000000000, 6.982962677686266711E-15, -1.000000000000000000 ) ) ;
#34813=DIRECTION ( 'NONE',  ( -0.000000000000000000, 6.982962677686266711E-15, -1.000000000000000000 ) ) ;
#34815=ORIENTED_EDGE ( 'NONE', *, *, #31941, .T. ) ;
#34836=DIRECTION ( 'NONE',  ( 1.000000000000000000, 0.000000000000000000, 0.000000000000000000 ) ) ;
#34895=ADVANCED_FACE ( 'NONE', ( #12367 ), #8498, .T. ) ;
#34896=DIRECTION ( 'NONE',  ( 0.000000000000000000, 0.000000000000000000, 1.000000000000000000 ) ) ;
#34934=DIRECTION ( 'NONE',  ( 1.000000000000000000, 0.000000000000000000, 0.000000000000000000 ) ) ;
#34958=( BOUNDED_SURFACE ( )  B_SPLINE_SURFACE ( 3, 2, ( 
 ( #139766, #138476, #219318 ),
 ( #39441, #40728, #155540 ),
 ( #96777, #81080, #216751 ),
 ( #195934, #160668, #134629 ) ),
 .UNSPECIFIED., .F., .F., .F. ) 
 B_SPLINE_SURFACE_WITH_KNOTS ( ( 4, 4 ),
 ( 3, 3 ),
 ( -1.908195823574487804E-17, 0.001979672783031562362 ),
 ( 0.000000000000000000, 1.000000000000000000 ),
 .UNSPECIFIED. ) 
 GEOMETRIC_REPRESENTATION_ITEM ( )  RATIONAL_B_SPLINE_SURFACE ( (
 ( 1.000000000000000000, 0.7103081912008383236, 1.000000000000000000),
 ( 1.000000000000000000, 0.7104998333558345536, 1.000000000000000000),
 ( 1.000000000000000000, 0.7107238315755375346, 1.000000000000000000),
 ( 1.000000000000000000, 0.7110073749539294052, 1.000000000000000000) ) ) 
 REPRESENTATION_ITEM ( '' )  SURFACE ( )  );
#35017=CARTESIAN_POINT ( 'NONE',  ( 21.05000005001280527, 67.12872030824186709, -124.3451598962785738 ) ) ;
#35032=ORIENTED_EDGE ( 'NONE', *, *, #159760, .T. ) ;
#35079=AXIS2_PLACEMENT_3D ( 'NONE', #238338, #218762, #217477 ) ;
#35080=AXIS2_PLACEMENT_3D ( 'NONE', #62036, #198956, #217222 ) ;
#35100=DIRECTION ( 'NONE',  ( 0.000000000000000000, 0.000000000000000000, 1.000000000000000000 ) ) ;
#35172=FACE_OUTER_BOUND ( 'NONE', #174743, .T. ) ;
#35207=CARTESIAN_POINT ( 'NONE',  ( -18.50000000000000000, 64.25000000001222134, -148.2731074845243882 ) ) ;
#35209=DIRECTION ( 'NONE',  ( 0.000000000000000000, 0.000000000000000000, 1.000000000000000000 ) ) ;
#35228=CARTESIAN_POINT ( 'NONE',  ( 21.05000000000000071, 77.25000000001209344, -128.6231074845242972 ) ) ;
#35230=CYLINDRICAL_SURFACE ( 'NONE', #87322, 0.09999999999999976963 ) ;
#35241=CARTESIAN_POINT ( 'NONE',  ( 21.14999999999999858, 64.35000000001204512, -124.3731074845243825 ) ) ;
#35299=DIRECTION ( 'NONE',  ( -0.000000000000000000, -1.000000000000000000, -7.272083257015735086E-15 ) ) ;
#35301=ORIENTED_EDGE ( 'NONE', *, *, #100830, .T. ) ;
#35302=VERTEX_POINT ( 'NONE', #131981 ) ;
#35303=CARTESIAN_POINT ( 'NONE',  ( -21.05000000000000071, 77.25000000001209344, -128.5231074845242745 ) ) ;
#35310=CARTESIAN_POINT ( 'NONE',  ( -18.59999999999999787, 77.83534155023646406, -124.9679561919613064 ) ) ;
#35317=ORIENTED_EDGE ( 'NONE', *, *, #138443, .T. ) ;
#35322=TOROIDAL_SURFACE ( 'NONE', #72722, 0.6000000000000006439, 0.1000000000000000056 ) ;
#35329=CARTESIAN_POINT ( 'NONE',  ( 22.01447462590973458, 75.90096299995266804, -143.7869076857541870 ) ) ;
#35336=ORIENTED_EDGE ( 'NONE', *, *, #59183, .T. ) ;
#35341=ORIENTED_EDGE ( 'NONE', *, *, #199125, .F. ) ;
#35369=EDGE_CURVE ( 'NONE', #161400, #76954, #74622, .T. ) ;
#35379=DIRECTION ( 'NONE',  ( 1.000000000000000000, 0.000000000000000000, 0.000000000000000000 ) ) ;
#35386=CARTESIAN_POINT ( 'NONE',  ( 18.59999999999999787, 76.00000000001213607, -136.5231074845242745 ) ) ;
#35397=EDGE_LOOP ( 'NONE', ( #244513, #142949, #152800, #29355, #37732, #82866 ) ) ;
#35435=AXIS2_PLACEMENT_3D ( 'NONE', #119801, #144445, #23274 ) ;
#35452=ORIENTED_EDGE ( 'NONE', *, *, #198268, .T. ) ;
#35458=EDGE_LOOP ( 'NONE', ( #21759, #193279, #254171, #216148 ) ) ;
#35467=AXIS2_PLACEMENT_3D ( 'NONE', #198929, #176827, #78958 ) ;
#35483=CARTESIAN_POINT ( 'NONE',  ( 20.95035502843362707, 65.52236167323562199, -128.9468077757879882 ) ) ;
#35494=DIRECTION ( 'NONE',  ( 5.603264701231745086E-32, 7.172728831056619538E-15, -1.000000000000000000 ) ) ;
#35517=ORIENTED_EDGE ( 'NONE', *, *, #106028, .T. ) ;
#35553=DIRECTION ( 'NONE',  ( 0.000000000000000000, -0.1298341882519953583, -0.9915357197604862671 ) ) ;
#35567=DIRECTION ( 'NONE',  ( -1.000000000000000000, 0.000000000000000000, 0.000000000000000000 ) ) ;
#35572=AXIS2_PLACEMENT_3D ( 'NONE', #28060, #142812, #185817 ) ;
#35573=AXIS2_PLACEMENT_3D ( 'NONE', #201989, #23380, #147136 ) ;
#35606=CARTESIAN_POINT ( 'NONE',  ( 21.00023020733438273, 69.60913075474442735, -136.5231074845243597 ) ) ;
#35650=CARTESIAN_POINT ( 'NONE',  ( 21.05000000000000071, 74.83729825007408465, -128.4231074845243086 ) ) ;
#35651=DIRECTION ( 'NONE',  ( -1.000000000000000000, 2.952720810173289112E-16, 2.061873921506763405E-30 ) ) ;
#35703=DIRECTION ( 'NONE',  ( 0.000000000000000000, 0.000000000000000000, 1.000000000000000000 ) ) ;
#35709=DIRECTION ( 'NONE',  ( 0.000000000000000000, -0.4999999999999088507, 0.8660254037844913322 ) ) ;
#35722=ORIENTED_EDGE ( 'NONE', *, *, #66590, .F. ) ;
#35761=DIRECTION ( 'NONE',  ( 1.000000000000000000, 0.000000000000000000, 0.000000000000000000 ) ) ;
#35792=DIRECTION ( 'NONE',  ( -4.408576920032447972E-17, -0.1350103645451946055, 0.9908441862701591329 ) ) ;
#35798=ORIENTED_EDGE ( 'NONE', *, *, #220336, .F. ) ;
#35802=CIRCLE ( 'NONE', #169101, 0.8750000000000007772 ) ;
#35858=CARTESIAN_POINT ( 'NONE',  ( -20.85000000000000142, 77.83585931145546510, -91.51866831572576189 ) ) ;
#35883=AXIS2_PLACEMENT_3D ( 'NONE', #93987, #236075, #57424 ) ;
#35912=ORIENTED_EDGE ( 'NONE', *, *, #108523, .F. ) ;
#35917=FACE_OUTER_BOUND ( 'NONE', #100679, .T. ) ;
#35933=VERTEX_POINT ( 'NONE', #183321 ) ;
#35959=CIRCLE ( 'NONE', #131626, 0.5000000000000004441 ) ;
#35971=CARTESIAN_POINT ( 'NONE',  ( -1.739115166359751801E-14, 64.35000000001205933, -124.2731074845243739 ) ) ;
#35974=EDGE_LOOP ( 'NONE', ( #150330, #42668, #244903, #20581 ) ) ;
#35983=DIRECTION ( 'NONE',  ( -0.000000000000000000, -0.1350103645451718737, 0.9908441862701622416 ) ) ;
#35990=AXIS2_PLACEMENT_3D ( 'NONE', #129979, #72618, #252499 ) ;
#36071=AXIS2_PLACEMENT_3D ( 'NONE', #157093, #63096, #103499 ) ;
#36113=ADVANCED_FACE ( 'NONE', ( #18788 ), #37065, .T. ) ;
#36126=AXIS2_PLACEMENT_3D ( 'NONE', #255272, #233228, #19287 ) ;
#36184=CARTESIAN_POINT ( 'NONE',  ( 20.94999999999999929, 85.00000000001197975, -112.4170766071766678 ) ) ;
#36230=ADVANCED_FACE ( 'NONE', ( #205118 ), #125599, .F. ) ;
#36288=CARTESIAN_POINT ( 'NONE',  ( -23.25000000000000000, 73.40000000001205649, -123.2984855617622202 ) ) ;
#36322=ORIENTED_EDGE ( 'NONE', *, *, #65338, .T. ) ;
#36330=DIRECTION ( 'NONE',  ( 0.000000000000000000, -1.000000000000000000, -7.272083257015735086E-15 ) ) ;
#36341=AXIS2_PLACEMENT_3D ( 'NONE', #219435, #162070, #182914 ) ;
#36363=ORIENTED_EDGE ( 'NONE', *, *, #14661, .T. ) ;
#36370=B_SPLINE_CURVE_WITH_KNOTS ( 'NONE', 3,
 ( #42033, #144945, #202373, #250168, #25045, #224494, #71550, #45861, #121589, #64149 ),
 .UNSPECIFIED., .F., .F.,
 ( 4, 3, 3, 4 ),
 ( 0.000000000000000000, 0.0002000000000002908468, 0.001000000000045115191, 0.001967863649472098748 ),
 .UNSPECIFIED. ) ;
#36379=CARTESIAN_POINT ( 'NONE',  ( -23.25000000000000000, 77.25000000001185185, -95.22262673010921219 ) ) ;
#36406=DIRECTION ( 'NONE',  ( 1.000000000000000000, 0.000000000000000000, 0.000000000000000000 ) ) ;
#36427=ORIENTED_EDGE ( 'NONE', *, *, #136565, .F. ) ;
#36437=DIRECTION ( 'NONE',  ( 0.000000000000000000, -1.000000000000000000, -7.272083257015735086E-15 ) ) ;
#36468=AXIS2_PLACEMENT_3D ( 'NONE', #201389, #96185, #103556 ) ;
#36487=CARTESIAN_POINT ( 'NONE',  ( -20.64999999999999858, 74.05981308412415842, -115.8522266955776416 ) ) ;
#36504=ADVANCED_FACE ( 'NONE', ( #111184 ), #178730, .F. ) ;
#36515=EDGE_LOOP ( 'NONE', ( #238762, #15576, #251619, #206031 ) ) ;
#36519=EDGE_CURVE ( 'NONE', #20391, #69086, #212859, .T. ) ;
#36560=VECTOR ( 'NONE', #83223, 1000.000000000000000 ) ;
#36601=CARTESIAN_POINT ( 'NONE',  ( 23.24999999999999645, 76.00000000001190870, -103.0231074845243029 ) ) ;
#36608=CARTESIAN_POINT ( 'NONE',  ( -21.05000000000000071, 77.83534155023646406, -124.9679561919613064 ) ) ;
#36610=LINE ( 'NONE', #174853, #24961 ) ;
#36660=AXIS2_PLACEMENT_3D ( 'NONE', #204760, #81263, #105645 ) ;
#36690=DIRECTION ( 'NONE',  ( 0.000000000000000000, 0.000000000000000000, 1.000000000000000000 ) ) ;
#36713=FACE_OUTER_BOUND ( 'NONE', #44328, .T. ) ;
#36719=ORIENTED_EDGE ( 'NONE', *, *, #200167, .F. ) ;
#36730=EDGE_CURVE ( 'NONE', #104197, #99499, #40678, .T. ) ;
#36737=EDGE_CURVE ( 'NONE', #185852, #163770, #57856, .T. ) ;
#36738=CIRCLE ( 'NONE', #182470, 0.1000000000000028644 ) ;
#36748=DIRECTION ( 'NONE',  ( -4.391705002472927119E-16, -1.000000000000000000, -7.026728003956683390E-15 ) ) ;
#36759=EDGE_CURVE ( 'NONE', #1820, #64056, #53789, .T. ) ;
#36772=EDGE_CURVE ( 'NONE', #8189, #203841, #237131, .T. ) ;
#36775=DIRECTION ( 'NONE',  ( 0.000000000000000000, -6.982962677686266711E-15, 1.000000000000000000 ) ) ;
#36781=AXIS2_PLACEMENT_3D ( 'NONE', #144876, #64067, #143604 ) ;
#36783=CARTESIAN_POINT ( 'NONE',  ( 21.05000000000000071, 76.10000000001218723, -143.0637644362255401 ) ) ;
#36796=CONICAL_SURFACE ( 'NONE', #232415, 4.049999999999998046, 0.7853981633974604915 ) ;
#36798=( NAMED_UNIT ( * ) SI_UNIT ( $, .STERADIAN. ) SOLID_ANGLE_UNIT ( ) );
#36805=DIRECTION ( 'NONE',  ( 0.000000000000000000, -1.000000000000000000, -6.982962677686265922E-15 ) ) ;
#36825=EDGE_CURVE ( 'NONE', #201070, #19723, #7940, .T. ) ;
#36850=CARTESIAN_POINT ( 'NONE',  ( 20.94999999999999929, 64.35000000001195986, -109.8069731475024753 ) ) ;
#36873=CARTESIAN_POINT ( 'NONE',  ( 20.94999999999999929, 74.63912941282003999, -128.4501095574333647 ) ) ;
#36887=CARTESIAN_POINT ( 'NONE',  ( -23.25000000000000000, 87.65000000001192859, -106.1231074845242262 ) ) ;
#36904=AXIS2_PLACEMENT_3D ( 'NONE', #32724, #190498, #131777 ) ;
#36914=CYLINDRICAL_SURFACE ( 'NONE', #83408, 0.09999999999999520384 ) ;
#36938=CARTESIAN_POINT ( 'NONE',  ( 23.14999999999999858, 76.00000000001190870, -103.0231074845243029 ) ) ;
#36980=FACE_OUTER_BOUND ( 'NONE', #97330, .T. ) ;
#36986=DIRECTION ( 'NONE',  ( 0.000000000000000000, 6.938893903907030216E-14, -1.000000000000000000 ) ) ;
#36991=AXIS2_PLACEMENT_3D ( 'NONE', #237612, #58931, #159368 ) ;
#36995=DIRECTION ( 'NONE',  ( 0.000000000000000000, 0.000000000000000000, -1.000000000000000000 ) ) ;
#37014=ADVANCED_FACE ( 'NONE', ( #112185 ), #54747, .T. ) ;
#37028=CARTESIAN_POINT ( 'NONE',  ( 21.05000000000000426, 65.27628289530457550, -128.9286900929112392 ) ) ;
#37032=VECTOR ( 'NONE', #126169, 1000.000000000000000 ) ;
#37039=ORIENTED_EDGE ( 'NONE', *, *, #135755, .T. ) ;
#37048=CARTESIAN_POINT ( 'NONE',  ( 20.94999999999999929, 71.00000000001199396, -115.4283735034374274 ) ) ;
#37055=EDGE_CURVE ( 'NONE', #58001, #151185, #53960, .T. ) ;
#37060=EDGE_CURVE ( 'NONE', #8664, #257983, #199745, .T. ) ;
#37065=TOROIDAL_SURFACE ( 'NONE', #241068, 11.90000000000000391, 0.1000000000000000056 ) ;
#37083=ADVANCED_FACE ( 'NONE', ( #178587 ), #42902, .F. ) ;
#37100=AXIS2_PLACEMENT_3D ( 'NONE', #35241, #95177, #174765 ) ;
#37103=DIRECTION ( 'NONE',  ( 0.000000000000000000, -0.4930308989875575865, -0.8700118002898125091 ) ) ;
#37109=LINE ( 'NONE', #239138, #249626 ) ;
#37147=CARTESIAN_POINT ( 'NONE',  ( 20.94999999999999929, 69.35000000001200249, -115.2731074845243455 ) ) ;
#37160=EDGE_CURVE ( 'NONE', #71963, #24859, #241592, .T. ) ;
#37168=ORIENTED_EDGE ( 'NONE', *, *, #137590, .T. ) ;
#37176=DIRECTION ( 'NONE',  ( 0.000000000000000000, 1.000000000000000000, 6.688090509790097607E-15 ) ) ;
#37226=AXIS2_PLACEMENT_3D ( 'NONE', #53884, #173878, #33081 ) ;
#37236=VECTOR ( 'NONE', #39385, 1000.000000000000000 ) ;
#37299=ADVANCED_FACE ( 'NONE', ( #111864 ), #92281, .F. ) ;
#37312=VERTEX_POINT ( 'NONE', #231819 ) ;
#37321=CARTESIAN_POINT ( 'NONE',  ( -20.94560253601877164, 64.25000000001195133, -110.0130239720089094 ) ) ;
#37350=CARTESIAN_POINT ( 'NONE',  ( -21.44999999999999929, 68.65000000001205649, -124.1731074845243512 ) ) ;
#37379=EDGE_CURVE ( 'NONE', #24249, #139103, #70944, .T. ) ;
#37398=LINE ( 'NONE', #236852, #158373 ) ;
#37403=DIRECTION ( 'NONE',  ( -0.000000000000000000, -0.01283462868040327436, 0.9999176327611370985 ) ) ;
#37438=FACE_OUTER_BOUND ( 'NONE', #118708, .T. ) ;
#37445=ORIENTED_EDGE ( 'NONE', *, *, #166756, .T. ) ;
#37516=DIRECTION ( 'NONE',  ( 0.000000000000000000, -1.000000000000000000, -6.982962677686265922E-15 ) ) ;
#37538=DIRECTION ( 'NONE',  ( 0.000000000000000000, -0.9654727137038715545, -0.2605042016806676242 ) ) ;
#37551=EDGE_LOOP ( 'NONE', ( #115, #244892, #57062, #165619 ) ) ;
#37553=LINE ( 'NONE', #117082, #47855 ) ;
#37560=DIRECTION ( 'NONE',  ( 4.336808689942128965E-15, -0.8660254037844367092, 0.5000000000000037748 ) ) ;
#37576=PLANE ( 'NONE',  #149874 ) ;
#37584=ADVANCED_FACE ( 'NONE', ( #228619 ), #72113, .T. ) ;
#37586=CARTESIAN_POINT ( 'NONE',  ( -20.54999999999999716, 74.00000000001205080, -123.2984855617622060 ) ) ;
#37587=DIRECTION ( 'NONE',  ( 0.000000000000000000, 1.000000000000000000, 6.982962677686266711E-15 ) ) ;
#37605=ORIENTED_EDGE ( 'NONE', *, *, #34578, .T. ) ;
#37625=AXIS2_PLACEMENT_3D ( 'NONE', #17234, #101862, #219257 ) ;
#37652=DIRECTION ( 'NONE',  ( 0.000000000000000000, -0.8660254037844377084, -0.5000000000000016653 ) ) ;
#37662=EDGE_CURVE ( 'NONE', #162824, #87320, #233431, .T. ) ;
#37691=EDGE_LOOP ( 'NONE', ( #136654, #34292, #218971, #158657 ) ) ;
#37701=AXIS2_PLACEMENT_3D ( 'NONE', #60028, #114884, #177458 ) ;
#37713=EDGE_CURVE ( 'NONE', #152046, #194536, #121004, .T. ) ;
#37720=VERTEX_POINT ( 'NONE', #175099 ) ;
#37721=CARTESIAN_POINT ( 'NONE',  ( 18.44208962362753468, 85.55234049691941323, -96.18093442906038604 ) ) ;
#37727=ORIENTED_EDGE ( 'NONE', *, *, #149771, .T. ) ;
#37732=ORIENTED_EDGE ( 'NONE', *, *, #36772, .T. ) ;
#37736=DIRECTION ( 'NONE',  ( -2.940209281316621016E-16, -1.000000000000000000, -9.408669700213187250E-15 ) ) ;
#37764=CYLINDRICAL_SURFACE ( 'NONE', #154405, 0.09999999999999939493 ) ;
#37767=DIRECTION ( 'NONE',  ( 1.000000000000000000, -2.952720810173289112E-16, -2.061873921506763405E-30 ) ) ;
#37785=ADVANCED_FACE ( 'NONE', ( #60220 ), #34287, .F. ) ;
#37803=ORIENTED_EDGE ( 'NONE', *, *, #177821, .T. ) ;
#37812=CARTESIAN_POINT ( 'NONE',  ( 23.24999999999999645, 71.00000000001205080, -124.1178414656112352 ) ) ;
#37823=DIRECTION ( 'NONE',  ( 2.952720810173289605E-16, 1.000000000000000000, 7.086529944415894657E-15 ) ) ;
#37826=SHAPE_DEFINITION_REPRESENTATION ( #232711, #171686 ) ;
#37828=DIRECTION ( 'NONE',  ( 0.000000000000000000, 6.982962677686266711E-15, -1.000000000000000000 ) ) ;
#37831=ORIENTED_EDGE ( 'NONE', *, *, #179036, .F. ) ;
#37839=CIRCLE ( 'NONE', #45996, 0.2000000000000057288 ) ;
#37875=VERTEX_POINT ( 'NONE', #141062 ) ;
#37878=DIRECTION ( 'NONE',  ( 0.000000000000000000, 1.000000000000000000, 0.000000000000000000 ) ) ;
#37881=ADVANCED_FACE ( 'NONE', ( #142326 ), #203594, .T. ) ;
#37903=CARTESIAN_POINT ( 'NONE',  ( 20.94999999999999929, 70.50000000001199396, -115.4283735034374274 ) ) ;
#37925=CARTESIAN_POINT ( 'NONE',  ( 18.49999999999999289, 69.55000000001199112, -115.3731074845243398 ) ) ;
#37943=FACE_BOUND ( 'NONE', #31533, .T. ) ;
#37965=EDGE_CURVE ( 'NONE', #50227, #178804, #54516, .T. ) ;
#37993=DIRECTION ( 'NONE',  ( 0.000000000000000000, -6.982962677686266711E-15, 1.000000000000000000 ) ) ;
#38010=EDGE_CURVE ( 'NONE', #53595, #128962, #253803, .T. ) ;
#38011=VERTEX_POINT ( 'NONE', #30117 ) ;
#38026=CIRCLE ( 'NONE', #75443, 0.5000000000000004441 ) ;
#38066=SURFACE_STYLE_USAGE ( .BOTH. , #27180 ) ;
#38105=CARTESIAN_POINT ( 'NONE',  ( -18.51697539158856998, 65.68434038414356735, -97.48668807260654035 ) ) ;
#38112=DIRECTION ( 'NONE',  ( 0.000000000000000000, 0.1298341882519953583, 0.9915357197604862671 ) ) ;
#38125=CARTESIAN_POINT ( 'NONE',  ( -20.64999999999999858, 68.75000000001199396, -115.2731074845243455 ) ) ;
#38134=AXIS2_PLACEMENT_3D ( 'NONE', #175323, #34519, #218244 ) ;
#38149=DIRECTION ( 'NONE',  ( -0.000000000000000000, -1.000000000000000000, -6.982962677686266711E-15 ) ) ;
#38173=AXIS2_PLACEMENT_3D ( 'NONE', #228992, #109020, #88153 ) ;
#38194=CARTESIAN_POINT ( 'NONE',  ( 21.14999999999999503, 76.10085836911093793, -148.2726746080136877 ) ) ;
#38205=CIRCLE ( 'NONE', #183928, 11.74999999999999645 ) ;
#38214=CARTESIAN_POINT ( 'NONE',  ( 20.99749315643148151, 64.25000000001195133, -110.0379132532841453 ) ) ;
#38221=CARTESIAN_POINT ( 'NONE',  ( 20.94999999999999929, 76.00000000001213607, -136.5231074845242745 ) ) ;
#38238=CARTESIAN_POINT ( 'NONE',  ( -18.59999996769639097, 85.36327376984259274, -129.3416135690586373 ) ) ;
#38267=DIRECTION ( 'NONE',  ( 0.000000000000000000, 0.4999999999999088507, -0.8660254037844913322 ) ) ;
#38272=ORIENTED_EDGE ( 'NONE', *, *, #246090, .F. ) ;
#38277=ADVANCED_FACE ( 'NONE', ( #54323 ), #253808, .T. ) ;
#38308=DIRECTION ( 'NONE',  ( 0.000000000000000000, 0.8777080977375072424, -0.4791956752371691608 ) ) ;
#38319=TOROIDAL_SURFACE ( 'NONE', #25846, 0.2000000000000000111, 0.1000000000000000056 ) ;
#38338=CARTESIAN_POINT ( 'NONE',  ( -22.39999999999999858, 64.35000000001214460, -136.5231074845243597 ) ) ;
#38362=DIRECTION ( 'NONE',  ( -1.000000000000000000, 0.000000000000000000, 0.000000000000000000 ) ) ;
#38383=DIRECTION ( 'NONE',  ( 0.000000000000000000, 6.982962677686266711E-15, -1.000000000000000000 ) ) ;
#38389=AXIS2_PLACEMENT_3D ( 'NONE', #23383, #222818, #1194 ) ;
#38399=CARTESIAN_POINT ( 'NONE',  ( 21.15000000000000213, 76.00000000001217870, -143.0637644362255401 ) ) ;
#38400=DIRECTION ( 'NONE',  ( 1.000000000000000000, -7.304098846218163263E-16, 4.217023435051626718E-16 ) ) ;
#38424=VECTOR ( 'NONE', #71594, 1000.000000000000000 ) ;
#38432=ORIENTED_EDGE ( 'NONE', *, *, #17045, .F. ) ;
#38441=FACE_OUTER_BOUND ( 'NONE', #152842, .T. ) ;
#38451=TOROIDAL_SURFACE ( 'NONE', #134676, 11.89999999999999858, 0.1000000000000000056 ) ;
#38487=CARTESIAN_POINT ( 'NONE',  ( -18.59999999999999787, 77.13501884592203339, -95.30613060109196510 ) ) ;
#38508=FACE_OUTER_BOUND ( 'NONE', #143908, .T. ) ;
#38513=DIRECTION ( 'NONE',  ( 0.000000000000000000, -6.982962677686266711E-15, 1.000000000000000000 ) ) ;
#38548=EDGE_CURVE ( 'NONE', #57850, #174398, #176012, .T. ) ;
#38550=EDGE_LOOP ( 'NONE', ( #144470, #14173, #141872, #108516 ) ) ;
#38552=EDGE_CURVE ( 'NONE', #213781, #230224, #111552, .T. ) ;
#38557=FACE_OUTER_BOUND ( 'NONE', #58917, .T. ) ;
#38592=ORIENTED_EDGE ( 'NONE', *, *, #222303, .T. ) ;
#38604=ORIENTED_EDGE ( 'NONE', *, *, #59909, .F. ) ;
#38640=LINE ( 'NONE', #16524, #96086 ) ;
#38641=ORIENTED_EDGE ( 'NONE', *, *, #36519, .T. ) ;
#38657=AXIS2_PLACEMENT_3D ( 'NONE', #127387, #4836, #187375 ) ;
#38665=DIRECTION ( 'NONE',  ( -4.239556034732056743E-17, -0.1298341882519953583, -0.9915357197604862671 ) ) ;
#38699=ORIENTED_EDGE ( 'NONE', *, *, #174578, .F. ) ;
#38704=ORIENTED_EDGE ( 'NONE', *, *, #52022, .T. ) ;
#38706=VERTEX_POINT ( 'NONE', #162252 ) ;
#38729=AXIS2_PLACEMENT_3D ( 'NONE', #64033, #182717, #198408 ) ;
#38750=EDGE_LOOP ( 'NONE', ( #151249, #652, #129271, #118389 ) ) ;
#38751=DIRECTION ( 'NONE',  ( 0.000000000000000000, 0.000000000000000000, -1.000000000000000000 ) ) ;
#38756=CARTESIAN_POINT ( 'NONE',  ( 21.30000000000002558, 76.00000000001210765, -132.4731074845242915 ) ) ;
#38771=CARTESIAN_POINT ( 'NONE',  ( -21.05000000000000071, 64.25000000001196554, -110.0379132551783243 ) ) ;
#38775=DIRECTION ( 'NONE',  ( 0.7071067811865127117, 0.7071067811865821007, 0.000000000000000000 ) ) ;
#38778=LINE ( 'NONE', #257761, #222317 ) ;
#38859=VECTOR ( 'NONE', #229416, 1000.000000000000000 ) ;
#38923=EDGE_LOOP ( 'NONE', ( #33363, #181667, #21981, #41316 ) ) ;
#38991=FACE_OUTER_BOUND ( 'NONE', #168885, .T. ) ;
#39006=ORIENTED_EDGE ( 'NONE', *, *, #119360, .F. ) ;
#39013=CARTESIAN_POINT ( 'NONE',  ( -21.14999999999999858, 64.35000000001214460, -136.5231074845243597 ) ) ;
#39015=CARTESIAN_POINT ( 'NONE',  ( -20.94999999999999929, 76.25610579210437834, -136.5580039261965908 ) ) ;
#39024=VECTOR ( 'NONE', #195363, 1000.000000000000000 ) ;
#39031=DIRECTION ( 'NONE',  ( -1.000000000000000000, -0.000000000000000000, -0.000000000000000000 ) ) ;
#39044=CARTESIAN_POINT ( 'NONE',  ( 21.04999999999999716, 69.69554417806445201, -136.5020720079842249 ) ) ;
#39045=AXIS2_PLACEMENT_3D ( 'NONE', #95670, #77382, #136061 ) ;
#39063=CARTESIAN_POINT ( 'NONE',  ( -21.07928932188134041, 75.90110485435778287, -142.8516241409176075 ) ) ;
#39064=FACE_OUTER_BOUND ( 'NONE', #49002, .T. ) ;
#39085=ADVANCED_FACE ( 'NONE', ( #58940 ), #153858, .T. ) ;
#39105=CARTESIAN_POINT ( 'NONE',  ( -22.42253884134832020, 75.99806764887692623, -148.1727131818727230 ) ) ;
#39109=ORIENTED_EDGE ( 'NONE', *, *, #202421, .T. ) ;
#39110=DIRECTION ( 'NONE',  ( 0.000000000000000000, 0.000000000000000000, 1.000000000000000000 ) ) ;
#39135=ADVANCED_FACE ( 'NONE', ( #274 ), #249004, .T. ) ;
#39142=EDGE_CURVE ( 'NONE', #7658, #153790, #244018, .T. ) ;
#39149=VERTEX_POINT ( 'NONE', #65391 ) ;
#39163=LINE ( 'NONE', #241207, #90909 ) ;
#39237=AXIS2_PLACEMENT_3D ( 'NONE', #42957, #181200, #2523 ) ;
#39264=ORIENTED_EDGE ( 'NONE', *, *, #244529, .F. ) ;
#39306=EDGE_CURVE ( 'NONE', #53190, #255801, #93939, .T. ) ;
#39309=ORIENTED_EDGE ( 'NONE', *, *, #25797, .T. ) ;
#39317=ADVANCED_FACE ( 'NONE', ( #189202 ), #130551, .T. ) ;
#39318=CARTESIAN_POINT ( 'NONE',  ( -23.25000000000000000, 87.75000000001213607, -136.5231074845242176 ) ) ;
#39327=CARTESIAN_POINT ( 'NONE',  ( -23.25000000000000000, 76.00000000001190870, -103.0231074845243029 ) ) ;
#39362=TOROIDAL_SURFACE ( 'NONE', #5994, 0.2000000000000000111, 0.1000000000000000056 ) ;
#39378=AXIS2_PLACEMENT_3D ( 'NONE', #125135, #185095, #182546 ) ;
#39385=DIRECTION ( 'NONE',  ( 1.000000000000000000, 0.000000000000000000, 0.000000000000000000 ) ) ;
#39415=CIRCLE ( 'NONE', #185133, 0.09999999999999939493 ) ;
#39428=DIRECTION ( 'NONE',  ( 0.000000000000000000, -6.517943393102682774E-15, 1.000000000000000000 ) ) ;
#39441=CARTESIAN_POINT ( 'NONE',  ( -22.00411653889203123, 75.90096189422509099, -143.7765503521646338 ) ) ;
#39448=DIRECTION ( 'NONE',  ( 0.000000000000000000, 6.982962677686266711E-15, -1.000000000000000000 ) ) ;
#39465=DIRECTION ( 'NONE',  ( 0.000000000000000000, -7.034366652768095332E-15, 1.000000000000000000 ) ) ;
#39502=CARTESIAN_POINT ( 'NONE',  ( 23.14999999999999503, 64.35000000001204512, -124.3731074845243825 ) ) ;
#39514=CONICAL_SURFACE ( 'NONE', #185219, 4.299999999999970512, 0.7853981633974466137 ) ;
#39530=EDGE_LOOP ( 'NONE', ( #133654, #138887, #248770, #189325 ) ) ;
#39533=AXIS2_PLACEMENT_3D ( 'NONE', #46798, #126353, #207192 ) ;
#39542=( BOUNDED_CURVE ( )  B_SPLINE_CURVE ( 3, ( #249346, #53693, #133234, #212782 ),
 .UNSPECIFIED., .F., .F. ) 
 B_SPLINE_CURVE_WITH_KNOTS ( ( 4, 4 ),
 ( 0.06456096931748350753, 3.077031684272309775 ),
 .UNSPECIFIED. ) 
 CURVE ( )  GEOMETRIC_REPRESENTATION_ITEM ( )  RATIONAL_B_SPLINE_CURVE ( ( 1.000000000000000000, 0.3763440860215095940, 0.3763440860215095940, 1.000000000000000000 ) ) 
 REPRESENTATION_ITEM ( '' )  );
#39545=AXIS2_PLACEMENT_3D ( 'NONE', #48751, #73492, #192147 ) ;
#39548=CARTESIAN_POINT ( 'NONE',  ( -18.39999999999999858, 85.50000000001209344, -129.4910380878245917 ) ) ;
#39561=VECTOR ( 'NONE', #11281, 1000.000000000000000 ) ;
#39573=EDGE_CURVE ( 'NONE', #232297, #57850, #186330, .T. ) ;
#39586=CARTESIAN_POINT ( 'NONE',  ( 21.09096482362058111, 69.63645563460765686, -136.5625557632984624 ) ) ;
#39652=EDGE_CURVE ( 'NONE', #186897, #111851, #98944, .T. ) ;
#39660=ADVANCED_FACE ( 'NONE', ( #54502 ), #130182, .T. ) ;
#39685=AXIS2_PLACEMENT_3D ( 'NONE', #191089, #12447, #15011 ) ;
#39690=ORIENTED_EDGE ( 'NONE', *, *, #148362, .T. ) ;
#39715=CARTESIAN_POINT ( 'NONE',  ( 23.14999999999999858, 79.90000000001190017, -103.0231074845242745 ) ) ;
#39766=TOROIDAL_SURFACE ( 'NONE', #189590, 11.65000000000000036, 0.1000000000000000056 ) ;
#39780=EDGE_LOOP ( 'NONE', ( #254474, #162230, #22844, #28377 ) ) ;
#39788=EDGE_CURVE ( 'NONE', #4373, #185096, #115528, .T. ) ;
#39807=DIRECTION ( 'NONE',  ( 0.000000000000000000, 0.9654727137038715545, -0.2605042016806676242 ) ) ;
#39814=DIRECTION ( 'NONE',  ( 0.000000000000000000, 1.000000000000000000, 7.272083257015735086E-15 ) ) ;
#39820=CARTESIAN_POINT ( 'NONE',  ( 20.94999999999999929, 69.45000000001205365, -124.3731074845243540 ) ) ;
#39840=ORIENTED_EDGE ( 'NONE', *, *, #26496, .F. ) ;
#39847=CIRCLE ( 'NONE', #35573, 4.000000000000003553 ) ;
#39904=ORIENTED_EDGE ( 'NONE', *, *, #93092, .T. ) ;
#39954=EDGE_CURVE ( 'NONE', #145261, #28934, #86646, .T. ) ;
#40000=ORIENTED_EDGE ( 'NONE', *, *, #248933, .T. ) ;
#40001=EDGE_CURVE ( 'NONE', #136488, #155989, #149150, .T. ) ;
#40017=ORIENTED_EDGE ( 'NONE', *, *, #223409, .F. ) ;
#40067=FACE_OUTER_BOUND ( 'NONE', #112593, .T. ) ;
#40071=DIRECTION ( 'NONE',  ( 1.000000000000000000, 0.000000000000000000, 0.000000000000000000 ) ) ;
#40096=AXIS2_PLACEMENT_3D ( 'NONE', #116631, #38383, #218274 ) ;
#40101=CARTESIAN_POINT ( 'NONE',  ( 20.94999999999999574, 77.83534155023646406, -124.9679561919612922 ) ) ;
#40108=DIRECTION ( 'NONE',  ( -1.000000000000000000, -0.000000000000000000, -0.000000000000000000 ) ) ;
#40139=FACE_OUTER_BOUND ( 'NONE', #66694, .T. ) ;
#40159=FACE_BOUND ( 'NONE', #180530, .T. ) ;
#40177=CARTESIAN_POINT ( 'NONE',  ( -22.48660254037843487, 64.35000000001214460, -136.5731074845243711 ) ) ;
#40195=EDGE_LOOP ( 'NONE', ( #132909, #81155, #98304, #2034 ) ) ;
#40198=VERTEX_POINT ( 'NONE', #18610 ) ;
#40204=EDGE_CURVE ( 'NONE', #95961, #192664, #169939, .T. ) ;
#40281=EDGE_LOOP ( 'NONE', ( #126557, #202385, #197571, #187106 ) ) ;
#40287=EDGE_LOOP ( 'NONE', ( #165941, #40000, #26771, #35341 ) ) ;
#40292=FACE_OUTER_BOUND ( 'NONE', #67350, .T. ) ;
#40314=ORIENTED_EDGE ( 'NONE', *, *, #229771, .T. ) ;
#40335=EDGE_LOOP ( 'NONE', ( #225775, #162497, #133546, #161689 ) ) ;
#40341=EDGE_CURVE ( 'NONE', #234233, #153145, #74249, .T. ) ;
#40342=AXIS2_PLACEMENT_3D ( 'NONE', #85151, #104713, #224687 ) ;
#40350=ORIENTED_EDGE ( 'NONE', *, *, #226869, .F. ) ;
#40385=CARTESIAN_POINT ( 'NONE',  ( 18.49505832270840955, 85.43802806279497020, -129.3246343096303690 ) ) ;
#40404=ORIENTED_EDGE ( 'NONE', *, *, #161052, .F. ) ;
#40413=EDGE_LOOP ( 'NONE', ( #82945, #164081, #27055, #112229, #222948 ) ) ;
#40416=AXIS2_PLACEMENT_3D ( 'NONE', #54458, #151007, #195287 ) ;
#40517=DIRECTION ( 'NONE',  ( 0.000000000000000000, 0.8660254037844424824, 0.4999999999999934497 ) ) ;
#40520=TOROIDAL_SURFACE ( 'NONE', #186225, 2.100000000000002309, 0.1000000000000000056 ) ;
#40576=ORIENTED_EDGE ( 'NONE', *, *, #164466, .F. ) ;
#40581=DIRECTION ( 'NONE',  ( 0.000000000000000000, 1.000000000000000000, 2.775557561562888827E-14 ) ) ;
#40592=CIRCLE ( 'NONE', #127866, 0.9750000000000036415 ) ;
#40618=FACE_OUTER_BOUND ( 'NONE', #211330, .T. ) ;
#40646=ORIENTED_EDGE ( 'NONE', *, *, #69648, .F. ) ;
#40678=LINE ( 'NONE', #223112, #166244 ) ;
#40691=AXIS2_PLACEMENT_3D ( 'NONE', #179728, #55885, #238400 ) ;
#40713=CARTESIAN_POINT ( 'NONE',  ( 20.94999999999999929, 67.07338541492498507, -128.0514244653012383 ) ) ;
#40727=EDGE_CURVE ( 'NONE', #139626, #215553, #69004, .T. ) ;
#40728=CARTESIAN_POINT ( 'NONE',  ( -22.00356870072698712, 76.00000000002593481, -143.7773498462425437 ) ) ;
#40768=LINE ( 'NONE', #195972, #249086 ) ;
#40798=AXIS2_PLACEMENT_3D ( 'NONE', #229802, #245533, #208959 ) ;
#40823=DIRECTION ( 'NONE',  ( -1.000000000000000000, -0.000000000000000000, -0.000000000000000000 ) ) ;
#40826=CARTESIAN_POINT ( 'NONE',  ( -18.43473496883410334, 85.49495241101142540, -129.4772359122960097 ) ) ;
#40835=ORIENTED_EDGE ( 'NONE', *, *, #97709, .T. ) ;
#40840=VERTEX_POINT ( 'NONE', #134073 ) ;
#40846=AXIS2_PLACEMENT_3D ( 'NONE', #133273, #168596, #108572 ) ;
#40873=ORIENTED_EDGE ( 'NONE', *, *, #141451, .T. ) ;
#40886=CARTESIAN_POINT ( 'NONE',  ( 21.05000000000000071, 65.51556651037034840, -129.0663016830324352 ) ) ;
#40893=CARTESIAN_POINT ( 'NONE',  ( -23.15000000000000213, 87.75000000001213607, -136.5231074845242176 ) ) ;
#40915=EDGE_CURVE ( 'NONE', #213961, #191338, #224412, .T. ) ;
#40921=DIRECTION ( 'NONE',  ( 0.000000000000000000, -6.982962677686266711E-15, 1.000000000000000000 ) ) ;
#40943=CARTESIAN_POINT ( 'NONE',  ( 20.94999999999999929, 67.22371710471961137, -127.9644784893834100 ) ) ;
#40952=CARTESIAN_POINT ( 'NONE',  ( 20.85000000000000142, 77.85161776048073534, -91.41991776492061206 ) ) ;
#40969=ORIENTED_EDGE ( 'NONE', *, *, #227253, .F. ) ;
#40996=CARTESIAN_POINT ( 'NONE',  ( 21.05000000000000426, 75.98528214348816334, -142.8678308886149750 ) ) ;
#41006=DIRECTION ( 'NONE',  ( 0.000000000000000000, -0.1568667991644355497, 0.9876197685951332295 ) ) ;
#41036=CARTESIAN_POINT ( 'NONE',  ( -22.50000000000000000, 68.20922040163873135, -136.6231074845243540 ) ) ;
#41047=ADVANCED_FACE ( 'NONE', ( #182207 ), #47797, .T. ) ;
#41089=ORIENTED_EDGE ( 'NONE', *, *, #122902, .T. ) ;
#41113=CARTESIAN_POINT ( 'NONE',  ( 21.05000000000000071, 87.75000000001210765, -133.6231074845242119 ) ) ;
#41220=AXIS2_PLACEMENT_3D ( 'NONE', #223455, #44836, #203903 ) ;
#41239=ORIENTED_EDGE ( 'NONE', *, *, #110067, .T. ) ;
#41245=B_SPLINE_CURVE_WITH_KNOTS ( 'NONE', 3,
 ( #20816, #238551, #23395, #79466, #102871, #182451, #242396 ),
 .UNSPECIFIED., .F., .F.,
 ( 4, 3, 4 ),
 ( 0.000000000000000000, 0.0007844235214594318627, 0.001767853679404347454 ),
 .UNSPECIFIED. ) ;
#41247=ORIENTED_EDGE ( 'NONE', *, *, #184371, .F. ) ;
#41251=CARTESIAN_POINT ( 'NONE',  ( 20.85000000000000142, 77.83585931145546510, -91.51866831572576189 ) ) ;
#41265=DIRECTION ( 'NONE',  ( 1.387778780781405791E-13, 0.9999176327611370985, 0.01283462868040226822 ) ) ;
#41316=ORIENTED_EDGE ( 'NONE', *, *, #70962, .F. ) ;
#41330=CYLINDRICAL_SURFACE ( 'NONE', #208682, 0.09999999999999939493 ) ;
#41335=VECTOR ( 'NONE', #249500, 1000.000000000000000 ) ;
#41345=CARTESIAN_POINT ( 'NONE',  ( -21.64999999999999858, 68.65000000001205649, -124.2731074845243455 ) ) ;
#41346=CARTESIAN_POINT ( 'NONE',  ( 22.50000000000000000, 76.00000000001213607, -136.5231074845242745 ) ) ;
#41364=DIRECTION ( 'NONE',  ( 0.000000000000000000, 1.000000000000000000, 0.000000000000000000 ) ) ;
#41378=DIRECTION ( 'NONE',  ( 0.000000000000000000, 6.982962677686266711E-15, -1.000000000000000000 ) ) ;
#41405=VECTOR ( 'NONE', #247964, 1000.000000000000000 ) ;
#41419=CARTESIAN_POINT ( 'NONE',  ( 23.14999999999999503, 64.25000000001220712, -148.2731074845243882 ) ) ;
#41432=CARTESIAN_POINT ( 'NONE',  ( 18.49999999999999289, 65.75000000001199396, -115.1731074845243796 ) ) ;
#41435=DIRECTION ( 'NONE',  ( 0.000000000000000000, 0.000000000000000000, -1.000000000000000000 ) ) ;
#41451=EDGE_LOOP ( 'NONE', ( #231163, #55202, #109086, #6111, #68097 ) ) ;
#41463=VECTOR ( 'NONE', #214681, 1000.000000000000000 ) ;
#41496=CIRCLE ( 'NONE', #58196, 0.1000000000000028644 ) ;
#41518=VECTOR ( 'NONE', #110231, 1000.000000000000114 ) ;
#41544=DIRECTION ( 'NONE',  ( 1.000000000000000000, 0.000000000000000000, 0.000000000000000000 ) ) ;
#41551=CARTESIAN_POINT ( 'NONE',  ( -21.44999999999999929, 68.75000000001199396, -115.3731074845243540 ) ) ;
#41559=ORIENTED_EDGE ( 'NONE', *, *, #186631, .T. ) ;
#41590=DIRECTION ( 'NONE',  ( 0.000000000000000000, -7.429790795770644761E-15, 1.000000000000000000 ) ) ;
#41618=CARTESIAN_POINT ( 'NONE',  ( 21.05000000000000426, 69.74118280533069480, -136.5567402198579998 ) ) ;
#41619=LINE ( 'NONE', #221491, #172624 ) ;
#41622=AXIS2_PLACEMENT_3D ( 'NONE', #189897, #12565, #8693 ) ;
#41674=DIRECTION ( 'NONE',  ( 0.000000000000000000, 6.982962677686266711E-15, -1.000000000000000000 ) ) ;
#41695=ORIENTED_EDGE ( 'NONE', *, *, #80970, .T. ) ;
#41719=ORIENTED_EDGE ( 'NONE', *, *, #252346, .F. ) ;
#41720=CYLINDRICAL_SURFACE ( 'NONE', #234967, 4.000000000000003553 ) ;
#41723=EDGE_CURVE ( 'NONE', #121092, #133367, #23514, .T. ) ;
#41734=CARTESIAN_POINT ( 'NONE',  ( 20.77526135991770317, 67.06799098339173781, -128.0545389417991089 ) ) ;
#41763=EDGE_CURVE ( 'NONE', #217215, #137344, #20806, .T. ) ;
#41784=CARTESIAN_POINT ( 'NONE',  ( 22.49231231312462853, 64.35001509633487160, -136.5841603721257513 ) ) ;
#41812=DIRECTION ( 'NONE',  ( 1.000000000000000000, 0.000000000000000000, 0.000000000000000000 ) ) ;
#41824=ORIENTED_EDGE ( 'NONE', *, *, #220625, .T. ) ;
#41829=DIRECTION ( 'NONE',  ( -1.000000000000000000, -0.000000000000000000, 0.000000000000000000 ) ) ;
#41848=CARTESIAN_POINT ( 'NONE',  ( -23.15000000000000213, 76.00000000001190870, -103.0231074845243029 ) ) ;
#41864=ORIENTED_EDGE ( 'NONE', *, *, #258052, .T. ) ;
#41868=CARTESIAN_POINT ( 'NONE',  ( -18.59999999999999787, 64.35000000001205933, -124.3731074845243825 ) ) ;
#41914=ORIENTED_EDGE ( 'NONE', *, *, #40727, .F. ) ;
#41925=FACE_OUTER_BOUND ( 'NONE', #98545, .T. ) ;
#41937=DIRECTION ( 'NONE',  ( -1.000000000000000000, 0.000000000000000000, -0.000000000000000000 ) ) ;
#41960=ORIENTED_EDGE ( 'NONE', *, *, #191870, .T. ) ;
#41964=DIRECTION ( 'NONE',  ( -1.000000000000000000, 0.000000000000000000, 0.000000000000000000 ) ) ;
#41969=DIRECTION ( 'NONE',  ( 0.000000000000000000, 6.982962677686266711E-15, -1.000000000000000000 ) ) ;
#41995=EDGE_CURVE ( 'NONE', #207709, #206067, #16701, .T. ) ;
#42027=CARTESIAN_POINT ( 'NONE',  ( 18.60000000000000142, 85.40000000001204228, -129.2258477248609267 ) ) ;
#42033=CARTESIAN_POINT ( 'NONE',  ( 22.47071067811865319, 68.27992525551410097, -136.6221999392269595 ) ) ;
#42057=EDGE_CURVE ( 'NONE', #70458, #57517, #37398, .T. ) ;
#42063=ORIENTED_EDGE ( 'NONE', *, *, #187207, .T. ) ;
#42069=CARTESIAN_POINT ( 'NONE',  ( 20.96077737575347300, 64.37609936600719607, -109.8823155274179584 ) ) ;
#42070=ORIENTED_EDGE ( 'NONE', *, *, #152175, .F. ) ;
#42116=ADVANCED_FACE ( 'NONE', ( #240716 ), #218559, .T. ) ;
#42117=EDGE_LOOP ( 'NONE', ( #163401, #116206, #41719, #111509 ) ) ;
#42131=DIRECTION ( 'NONE',  ( 0.000000000000000000, -0.8660254037844468122, -0.4999999999999859557 ) ) ;
#42147=ORIENTED_EDGE ( 'NONE', *, *, #71789, .T. ) ;
#42151=LINE ( 'NONE', #85072, #156258 ) ;
#42171=AXIS2_PLACEMENT_3D ( 'NONE', #90453, #132164, #170056 ) ;
#42186=CYLINDRICAL_SURFACE ( 'NONE', #148745, 0.09999999999999939493 ) ;
#42208=CARTESIAN_POINT ( 'NONE',  ( -20.64999999999999858, 85.00000000001207923, -126.6291383618717816 ) ) ;
#42209=AXIS2_PLACEMENT_3D ( 'NONE', #76227, #153251, #52813 ) ;
#42225=DIRECTION ( 'NONE',  ( 0.000000000000000000, 1.000000000000000000, 6.982962677686266711E-15 ) ) ;
#42257=LINE ( 'NONE', #243005, #3633 ) ;
#42310=ORIENTED_EDGE ( 'NONE', *, *, #178339, .F. ) ;
#42314=DIRECTION ( 'NONE',  ( 0.000000000000000000, -1.000000000000000000, -6.982962677686265922E-15 ) ) ;
#42331=ORIENTED_EDGE ( 'NONE', *, *, #229821, .F. ) ;
#42332=LINE ( 'NONE', #183138, #123711 ) ;
#42353=CARTESIAN_POINT ( 'NONE',  ( 21.05000000000000071, 76.00000000001190870, -103.0231074845243029 ) ) ;
#42377=AXIS2_PLACEMENT_3D ( 'NONE', #225654, #47027, #126589 ) ;
#42395=CARTESIAN_POINT ( 'NONE',  ( -18.59999999999999787, 66.85000000001200249, -115.3731074845243683 ) ) ;
#42418=EDGE_CURVE ( 'NONE', #186897, #14594, #83985, .T. ) ;
#42451=ORIENTED_EDGE ( 'NONE', *, *, #128832, .T. ) ;
#42452=ORIENTED_EDGE ( 'NONE', *, *, #154702, .F. ) ;
#42483=EDGE_CURVE ( 'NONE', #124002, #139747, #224574, .T. ) ;
#42545=AXIS2_PLACEMENT_3D ( 'NONE', #173377, #153818, #172082 ) ;
#42546=EDGE_CURVE ( 'NONE', #9803, #91270, #199488, .T. ) ;
#42581=DIRECTION ( 'NONE',  ( 1.000000000000000000, 0.000000000000000000, 0.000000000000000000 ) ) ;
#42610=DIRECTION ( 'NONE',  ( 0.000000000000000000, -7.272083257015735086E-15, 1.000000000000000000 ) ) ;
#42611=VECTOR ( 'NONE', #65756, 1000.000000000000000 ) ;
#42621=ADVANCED_FACE ( 'NONE', ( #112162 ), #16500, .F. ) ;
#42625=B_SPLINE_CURVE_WITH_KNOTS ( 'NONE', 3,
 ( #217666, #239835, #40385, #100289, #119912, #233737, #14709, #173810, #80728, #179869 ),
 .UNSPECIFIED., .F., .F.,
 ( 4, 2, 2, 2, 4 ),
 ( 0.000000000000000000, 0.0001584437871624444667, 0.0002376656807436985214, 0.0002772766275343603246, 0.0003168875743250221277 ),
 .UNSPECIFIED. ) ;
#42638=DIRECTION ( 'NONE',  ( 0.000000000000000000, -0.9876197685951263461, 0.1568667991644794590 ) ) ;
#42640=CYLINDRICAL_SURFACE ( 'NONE', #208845, 0.09999999999999939493 ) ;
#42652=CARTESIAN_POINT ( 'NONE',  ( -20.64999999999999858, 73.50000000001205080, -123.2984855617622202 ) ) ;
#42668=ORIENTED_EDGE ( 'NONE', *, *, #188970, .F. ) ;
#42675=CYLINDRICAL_SURFACE ( 'NONE', #47532, 0.1000000000000028644 ) ;
#42700=VECTOR ( 'NONE', #67978, 1000.000000000000000 ) ;
#42704=ORIENTED_EDGE ( 'NONE', *, *, #88066, .F. ) ;
#42709=EDGE_LOOP ( 'NONE', ( #21661, #123575, #188696, #62281 ) ) ;
#42764=EDGE_CURVE ( 'NONE', #208002, #75479, #170664, .T. ) ;
#42782=ORIENTED_EDGE ( 'NONE', *, *, #58949, .F. ) ;
#42786=CARTESIAN_POINT ( 'NONE',  ( -23.15000000000000213, 76.00000000001189449, -101.0231074845243029 ) ) ;
#42810=FACE_OUTER_BOUND ( 'NONE', #8147, .T. ) ;
#42897=CARTESIAN_POINT ( 'NONE',  ( -21.76363531954647357, 75.90099812571274640, -143.5360440323960347 ) ) ;
#42902=PLANE ( 'NONE',  #95650 ) ;
#42906=CARTESIAN_POINT ( 'NONE',  ( 18.59999999999997655, 76.00000000001190870, -103.0231074845243029 ) ) ;
#42943=DIRECTION ( 'NONE',  ( 1.000000000000000000, 0.000000000000000000, 0.000000000000000000 ) ) ;
#42951=AXIS2_PLACEMENT_3D ( 'NONE', #165762, #26244, #129188 ) ;
#42955=ADVANCED_FACE ( 'NONE', ( #72735 ), #152267, .F. ) ;
#42957=CARTESIAN_POINT ( 'NONE',  ( -20.94999999999999929, 77.83534155023646406, -124.9679561919613064 ) ) ;
#42963=DIRECTION ( 'NONE',  ( 1.000000000000000000, 0.000000000000000000, 0.000000000000000000 ) ) ;
#42980=ORIENTED_EDGE ( 'NONE', *, *, #241429, .F. ) ;
#42996=FACE_OUTER_BOUND ( 'NONE', #11292, .T. ) ;
#42998=CARTESIAN_POINT ( 'NONE',  ( 23.14999999999999858, 71.00000000001199396, -115.4283735034374274 ) ) ;
#43005=CARTESIAN_POINT ( 'NONE',  ( 20.12518398540832010, 66.02491127934437998, -128.5264392320576405 ) ) ;
#43035=DIRECTION ( 'NONE',  ( 0.000000000000000000, -1.000000000000000000, -6.982962677686265922E-15 ) ) ;
#43049=VECTOR ( 'NONE', #30863, 1000.000000000000000 ) ;
#43057=DIRECTION ( 'NONE',  ( 0.000000000000000000, 0.000000000000000000, -1.000000000000000000 ) ) ;
#43065=AXIS2_PLACEMENT_3D ( 'NONE', #101161, #2097, #256373 ) ;
#43070=DIRECTION ( 'NONE',  ( 0.000000000000000000, -6.982962677686266711E-15, 1.000000000000000000 ) ) ;
#43077=CARTESIAN_POINT ( 'NONE',  ( -21.52071067811865746, 68.22071067813065781, -115.3731074845243540 ) ) ;
#43121=DIRECTION ( 'NONE',  ( -0.7071067811865475727, 0.7071067811865475727, 4.937700262164531476E-15 ) ) ;
#43124=ORIENTED_EDGE ( 'NONE', *, *, #64661, .T. ) ;
#43153=( GEOMETRIC_REPRESENTATION_CONTEXT ( 3 ) GLOBAL_UNCERTAINTY_ASSIGNED_CONTEXT ( ( #83108 ) ) GLOBAL_UNIT_ASSIGNED_CONTEXT ( ( #7985, #173199, #92315 ) ) REPRESENTATION_CONTEXT ( 'NONE', 'WORKASPACE' ) );
#43182=DIRECTION ( 'NONE',  ( 0.000000000000000000, 0.000000000000000000, 1.000000000000000000 ) ) ;
#43184=CARTESIAN_POINT ( 'NONE',  ( -21.09813707148783735, 75.96864850048277162, -142.9081695902609681 ) ) ;
#43203=ORIENTED_EDGE ( 'NONE', *, *, #189692, .T. ) ;
#43215=EDGE_CURVE ( 'NONE', #143411, #107177, #184634, .T. ) ;
#43218=AXIS2_PLACEMENT_3D ( 'NONE', #136457, #37403, #41265 ) ;
#43250=AXIS2_PLACEMENT_3D ( 'NONE', #138291, #62642, #22242 ) ;
#43257=VECTOR ( 'NONE', #157877, 1000.000000000000114 ) ;
#43259=DIRECTION ( 'NONE',  ( -0.000000000000000000, 1.000000000000000000, 6.982962677686266711E-15 ) ) ;
#43269=CARTESIAN_POINT ( 'NONE',  ( 22.40000000000020819, 76.10085836911189006, -148.2726746080140003 ) ) ;
#43274=FACE_OUTER_BOUND ( 'NONE', #209702, .T. ) ;
#43281=LINE ( 'NONE', #122829, #155864 ) ;
#43317=EDGE_LOOP ( 'NONE', ( #242473, #74468, #85881, #27864 ) ) ;
#43318=SPHERICAL_SURFACE ( 'NONE', #98095, 0.1000000000000000056 ) ;
#43319=ORIENTED_EDGE ( 'NONE', *, *, #36759, .T. ) ;
#43330=ADVANCED_FACE ( 'NONE', ( #188484 ), #11141, .T. ) ;
#43351=AXIS2_PLACEMENT_3D ( 'NONE', #132191, #56483, #34402 ) ;
#43361=DIRECTION ( 'NONE',  ( 0.000000000000000000, -1.000000000000000000, -6.982962677686265922E-15 ) ) ;
#43362=DIRECTION ( 'NONE',  ( 0.000000000000000000, 6.982962677686267499E-15, -1.000000000000000000 ) ) ;
#43365=LINE ( 'NONE', #169763, #170436 ) ;
#43408=CIRCLE ( 'NONE', #176702, 0.09999999999998898659 ) ;
#43417=ORIENTED_EDGE ( 'NONE', *, *, #49468, .F. ) ;
#43436=VERTEX_POINT ( 'NONE', #211921 ) ;
#43444=AXIS2_PLACEMENT_3D ( 'NONE', #231875, #92335, #94893 ) ;
#43456=DIRECTION ( 'NONE',  ( 0.000000000000000000, -0.8700118002898354908, 0.4930308989875170078 ) ) ;
#43518=CIRCLE ( 'NONE', #160245, 0.09999999999999939493 ) ;
#43523=ORIENTED_EDGE ( 'NONE', *, *, #27419, .T. ) ;
#43526=DIRECTION ( 'NONE',  ( -0.000000000000000000, 0.1350103645451859180, 0.9908441862701603542 ) ) ;
#43566=DIRECTION ( 'NONE',  ( -0.000000000000000000, 6.982962677686266711E-15, -1.000000000000000000 ) ) ;
#43620=DIRECTION ( 'NONE',  ( -0.7071067811865474617, 0.7071067811865474617, 4.937700262164531476E-15 ) ) ;
#43621=ORIENTED_EDGE ( 'NONE', *, *, #6965, .F. ) ;
#43627=VECTOR ( 'NONE', #64863, 1000.000000000000000 ) ;
#43639=FACE_OUTER_BOUND ( 'NONE', #257634, .T. ) ;
#43665=FACE_OUTER_BOUND ( 'NONE', #102483, .T. ) ;
#43666=CARTESIAN_POINT ( 'NONE',  ( -18.42554971533677133, 85.49715966944982881, -129.4832805709755803 ) ) ;
#43718=DIRECTION ( 'NONE',  ( 1.000000000000000000, -0.000000000000000000, 0.000000000000000000 ) ) ;
#43737=EDGE_CURVE ( 'NONE', #138262, #194835, #108438, .T. ) ;
#43777=ADVANCED_FACE ( 'NONE', ( #14713 ), #212888, .F. ) ;
#43787=ORIENTED_EDGE ( 'NONE', *, *, #72661, .T. ) ;
#43798=DIRECTION ( 'NONE',  ( 1.000000000000000000, 0.000000000000000000, 0.000000000000000000 ) ) ;
#43841=AXIS2_PLACEMENT_3D ( 'NONE', #184965, #162859, #29781 ) ;
#43863=ORIENTED_EDGE ( 'NONE', *, *, #149847, .F. ) ;
#43879=ORIENTED_EDGE ( 'NONE', *, *, #241293, .F. ) ;
#43894=EDGE_CURVE ( 'NONE', #126916, #133367, #25421, .T. ) ;
#43907=CARTESIAN_POINT ( 'NONE',  ( -21.05000000000000071, 77.16270174995010223, -128.6231074845242972 ) ) ;
#43913=DIRECTION ( 'NONE',  ( -1.000000000000000000, -0.000000000000000000, -0.000000000000000000 ) ) ;
#43926=EDGE_CURVE ( 'NONE', #181257, #228369, #79555, .T. ) ;
#43928=VECTOR ( 'NONE', #231373, 1000.000000000000000 ) ;
#43936=EDGE_CURVE ( 'NONE', #224430, #213545, #171207, .T. ) ;
#43948=AXIS2_PLACEMENT_3D ( 'NONE', #92191, #47926, #147022 ) ;
#43963=LINE ( 'NONE', #41419, #33525 ) ;
#43969=CARTESIAN_POINT ( 'NONE',  ( -23.15000000000000213, 64.25000000001193712, -106.1231074845243825 ) ) ;
#43972=ORIENTED_EDGE ( 'NONE', *, *, #130312, .T. ) ;
#44007=ADVANCED_FACE ( 'NONE', ( #44527 ), #197157, .T. ) ;
#44008=CIRCLE ( 'NONE', #164829, 0.1000000000000028644 ) ;
#44013=DIRECTION ( 'NONE',  ( 0.000000000000000000, 1.000000000000000000, 6.688090509790097607E-15 ) ) ;
#44051=ORIENTED_EDGE ( 'NONE', *, *, #31822, .F. ) ;
#44079=CARTESIAN_POINT ( 'NONE',  ( -22.50000000000094147, 75.89914163091360422, -148.2726746080137161 ) ) ;
#44114=EDGE_CURVE ( 'NONE', #216369, #187259, #167096, .T. ) ;
#44163=ADVANCED_FACE ( 'NONE', ( #40067 ), #79137, .F. ) ;
#44199=AXIS2_PLACEMENT_3D ( 'NONE', #86362, #31595, #168558 ) ;
#44232=AXIS2_PLACEMENT_3D ( 'NONE', #216745, #159367, #23727 ) ;
#44237=ORIENTED_EDGE ( 'NONE', *, *, #160941, .T. ) ;
#44245=EDGE_CURVE ( 'NONE', #87569, #173980, #255166, .T. ) ;
#44271=AXIS2_PLACEMENT_3D ( 'NONE', #242680, #124042, #104434 ) ;
#44298=LINE ( 'NONE', #87241, #227469 ) ;
#44318=CIRCLE ( 'NONE', #27768, 6.258578643762724880 ) ;
#44328=EDGE_LOOP ( 'NONE', ( #183189, #4589, #134813, #48225 ) ) ;
#44337=ORIENTED_EDGE ( 'NONE', *, *, #207459, .T. ) ;
#44389=AXIS2_PLACEMENT_3D ( 'NONE', #144082, #223619, #123259 ) ;
#44407=ORIENTED_EDGE ( 'NONE', *, *, #225083, .T. ) ;
#44426=ORIENTED_EDGE ( 'NONE', *, *, #59909, .T. ) ;
#44462=AXIS2_PLACEMENT_3D ( 'NONE', #61167, #79427, #238518 ) ;
#44465=EDGE_CURVE ( 'NONE', #252068, #81327, #127274, .T. ) ;
#44471=CARTESIAN_POINT ( 'NONE',  ( -18.50000000000000000, 70.05000000001213323, -126.2174051794894893 ) ) ;
#44477=DIRECTION ( 'NONE',  ( 0.000000000000000000, 1.072103779144463779E-14, -1.000000000000000000 ) ) ;
#44495=ORIENTED_EDGE ( 'NONE', *, *, #4526, .F. ) ;
#44504=EDGE_CURVE ( 'NONE', #53190, #163587, #129815, .T. ) ;
#44507=FACE_OUTER_BOUND ( 'NONE', #191956, .T. ) ;
#44523=AXIS2_PLACEMENT_3D ( 'NONE', #238990, #219397, #61626 ) ;
#44527=FACE_OUTER_BOUND ( 'NONE', #109772, .T. ) ;
#44534=DIRECTION ( 'NONE',  ( 0.000000000000000000, 0.000000000000000000, 1.000000000000000000 ) ) ;
#44535=DIRECTION ( 'NONE',  ( 0.000000000000000000, 6.982962677686266711E-15, -1.000000000000000000 ) ) ;
#44546=EDGE_LOOP ( 'NONE', ( #37727, #144223, #117202, #120218 ) ) ;
#44566=CARTESIAN_POINT ( 'NONE',  ( 20.95512820512820085, 65.37615131630018084, -124.3229454650999486 ) ) ;
#44612=LINE ( 'NONE', #162007, #102016 ) ;
#44693=ORIENTED_EDGE ( 'NONE', *, *, #123819, .T. ) ;
#44701=ORIENTED_EDGE ( 'NONE', *, *, #253984, .F. ) ;
#44716=DIRECTION ( 'NONE',  ( 1.000000000000000000, 0.000000000000000000, 0.000000000000000000 ) ) ;
#44717=DIRECTION ( 'NONE',  ( -1.000000000000000000, 0.000000000000000000, -0.000000000000000000 ) ) ;
#44765=AXIS2_PLACEMENT_3D ( 'NONE', #192740, #53219, #49371 ) ;
#44795=CIRCLE ( 'NONE', #94660, 0.1000000000000028644 ) ;
#44827=CARTESIAN_POINT ( 'NONE',  ( 18.59999999999999076, 68.87972903831429505, -99.36354444268502561 ) ) ;
#44831=CIRCLE ( 'NONE', #98966, 0.1000000000000028644 ) ;
#44836=DIRECTION ( 'NONE',  ( 1.000000000000000000, 0.000000000000000000, 0.000000000000000000 ) ) ;
#44855=DIRECTION ( 'NONE',  ( 1.000000000000000000, 0.000000000000000000, 0.000000000000000000 ) ) ;
#44862=AXIS2_PLACEMENT_3D ( 'NONE', #214774, #55664, #34896 ) ;
#44882=VECTOR ( 'NONE', #128787, 1000.000000000000000 ) ;
#44890=CIRCLE ( 'NONE', #153253, 0.09999999999999939493 ) ;
#44909=CARTESIAN_POINT ( 'NONE',  ( 23.15000000000000213, 87.65000000001192859, -106.1231074845242262 ) ) ;
#44953=DIRECTION ( 'NONE',  ( 0.000000000000000000, -6.982962677686266711E-15, 1.000000000000000000 ) ) ;
#44954=DIRECTION ( 'NONE',  ( 0.000000000000000000, 6.982962677686266711E-15, -1.000000000000000000 ) ) ;
#44964=DIRECTION ( 'NONE',  ( 0.000000000000000000, 0.9915357197604804940, -0.1298341882520397950 ) ) ;
#44989=ORIENTED_EDGE ( 'NONE', *, *, #79743, .F. ) ;
#45043=FACE_OUTER_BOUND ( 'NONE', #80271, .T. ) ;
#45060=ORIENTED_EDGE ( 'NONE', *, *, #253950, .F. ) ;
#45072=ORIENTED_EDGE ( 'NONE', *, *, #92427, .F. ) ;
#45078=DIRECTION ( 'NONE',  ( 0.000000000000000000, 6.997203936713175802E-15, -1.000000000000000000 ) ) ;
#45120=CARTESIAN_POINT ( 'NONE',  ( 21.05000000000000071, 76.00000000001193712, -105.9231074845242944 ) ) ;
#45165=CARTESIAN_POINT ( 'NONE',  ( -20.94999999999999929, 87.65000000001192859, -106.1231074845242262 ) ) ;
#45174=DIRECTION ( 'NONE',  ( -1.000000000000000000, 0.000000000000000000, -0.000000000000000000 ) ) ;
#45177=ORIENTED_EDGE ( 'NONE', *, *, #32412, .F. ) ;
#45188=AXIS2_PLACEMENT_3D ( 'NONE', #163800, #142913, #184629 ) ;
#45195=ADVANCED_FACE ( 'NONE', ( #38991 ), #157686, .T. ) ;
#45211=AXIS2_PLACEMENT_3D ( 'NONE', #95463, #56323, #173780 ) ;
#45278=EDGE_CURVE ( 'NONE', #226695, #14872, #17737, .T. ) ;
#45280=AXIS2_PLACEMENT_3D ( 'NONE', #80331, #239450, #242003 ) ;
#45325=ORIENTED_EDGE ( 'NONE', *, *, #127665, .F. ) ;
#45359=CARTESIAN_POINT ( 'NONE',  ( -22.59999970745345976, 76.00935637733975625, -148.2736206921935320 ) ) ;
#45368=CARTESIAN_POINT ( 'NONE',  ( -21.07928932188134041, 69.67148334361344553, -136.6220026301789972 ) ) ;
#45377=DIRECTION ( 'NONE',  ( 1.000000000000000000, -3.265361837132813093E-16, -2.280189983783949500E-30 ) ) ;
#45392=EDGE_LOOP ( 'NONE', ( #9572, #119668, #58802, #180153 ) ) ;
#45410=ORIENTED_EDGE ( 'NONE', *, *, #220105, .F. ) ;
#45412=EDGE_CURVE ( 'NONE', #109129, #88364, #5262, .T. ) ;
#45425=VECTOR ( 'NONE', #22019, 1000.000000000000000 ) ;
#45453=DIRECTION ( 'NONE',  ( -1.000000000000000000, -0.000000000000000000, -0.000000000000000000 ) ) ;
#45523=CARTESIAN_POINT ( 'NONE',  ( 23.14999999999999503, 64.35000000001197407, -115.1731074845243796 ) ) ;
#45526=CIRCLE ( 'NONE', #166358, 0.2000000000000057288 ) ;
#45552=DIRECTION ( 'NONE',  ( -0.000000000000000000, -6.982962677686266711E-15, 1.000000000000000000 ) ) ;
#45556=LINE ( 'NONE', #63839, #107581 ) ;
#45557=DIRECTION ( 'NONE',  ( -1.000000000000000000, 0.000000000000000000, -0.000000000000000000 ) ) ;
#45564=ADVANCED_FACE ( 'NONE', ( #146813 ), #128556, .T. ) ;
#45565=DIRECTION ( 'NONE',  ( 0.000000000000000000, -6.982962677686266711E-15, 1.000000000000000000 ) ) ;
#45572=AXIS2_PLACEMENT_3D ( 'NONE', #211052, #149812, #93662 ) ;
#45622=CIRCLE ( 'NONE', #8030, 11.74999999999999645 ) ;
#45625=ADVANCED_FACE ( 'NONE', ( #8611 ), #28205, .F. ) ;
#45632=EDGE_CURVE ( 'NONE', #216543, #230388, #138703, .T. ) ;
#45647=VERTEX_POINT ( 'NONE', #108975 ) ;
#45688=VERTEX_POINT ( 'NONE', #132408 ) ;
#45778=EDGE_CURVE ( 'NONE', #147787, #187556, #201282, .T. ) ;
#45789=DIRECTION ( 'NONE',  ( 0.000000000000000000, 6.982962677686266711E-15, -1.000000000000000000 ) ) ;
#45817=DIRECTION ( 'NONE',  ( 0.000000000000000000, 0.000000000000000000, 1.000000000000000000 ) ) ;
#45833=CARTESIAN_POINT ( 'NONE',  ( -21.14999999999999858, 64.25000000001209344, -129.7392418215462158 ) ) ;
#45850=DIRECTION ( 'NONE',  ( 0.000000000000000000, 0.000000000000000000, -1.000000000000000000 ) ) ;
#45861=CARTESIAN_POINT ( 'NONE',  ( 21.53551880898957194, 69.21520223859582188, -136.6220772190960133 ) ) ;
#45869=ADVANCED_FACE ( 'NONE', ( #22753 ), #85231, .T. ) ;
#45896=ADVANCED_FACE ( 'NONE', ( #222180 ), #92947, .T. ) ;
#45900=VERTEX_POINT ( 'NONE', #241765 ) ;
#45906=CARTESIAN_POINT ( 'NONE',  ( 21.05000000000000071, 85.50000000001197975, -112.9170766071766820 ) ) ;
#45945=AXIS2_PLACEMENT_3D ( 'NONE', #48094, #208483, #93647 ) ;
#45992=EDGE_LOOP ( 'NONE', ( #17824, #195807, #138526, #51188 ) ) ;
#45996=AXIS2_PLACEMENT_3D ( 'NONE', #23554, #206000, #106885 ) ;
#46039=AXIS2_PLACEMENT_3D ( 'NONE', #126433, #104285, #221665 ) ;
#46056=ADVANCED_FACE ( 'NONE', ( #2517 ), #116076, .F. ) ;
#46084=DIRECTION ( 'NONE',  ( 0.000000000000000000, -7.086529944415894657E-15, 1.000000000000000000 ) ) ;
#46094=CARTESIAN_POINT ( 'NONE',  ( -21.05000000000000071, 87.65000000001212754, -133.5231074845242176 ) ) ;
#46104=AXIS2_PLACEMENT_3D ( 'NONE', #79254, #76700, #117131 ) ;
#46109=CARTESIAN_POINT ( 'NONE',  ( -21.44999999999999929, 68.85000000001200249, -115.2731074845243455 ) ) ;
#46134=DIRECTION ( 'NONE',  ( 0.000000000000000000, 1.000000000000000000, 0.000000000000000000 ) ) ;
#46174=CARTESIAN_POINT ( 'NONE',  ( 21.05000000000000071, 65.27628289530454708, -124.3731074845243825 ) ) ;
#46188=DIRECTION ( 'NONE',  ( 1.000000000000000000, 0.000000000000000000, 0.000000000000000000 ) ) ;
#46271=CARTESIAN_POINT ( 'NONE',  ( -23.15000000000000213, 64.25000000001199396, -115.1731074845243938 ) ) ;
#46273=CARTESIAN_POINT ( 'NONE',  ( 20.95512820512820440, 67.12384868372396340, -127.9644784893834100 ) ) ;
#46281=CIRCLE ( 'NONE', #108830, 0.1000000000000033223 ) ;
#46290=ORIENTED_EDGE ( 'NONE', *, *, #240199, .T. ) ;
#46293=DIRECTION ( 'NONE',  ( 0.000000000000000000, -7.429790795770644761E-15, 1.000000000000000000 ) ) ;
#46312=DIRECTION ( 'NONE',  ( -0.7070776581709311559, 4.937903618720164857E-15, -0.7071359030027479786 ) ) ;
#46334=ORIENTED_EDGE ( 'NONE', *, *, #173248, .F. ) ;
#46343=CARTESIAN_POINT ( 'NONE',  ( 20.94999027547553894, 65.70673848566976005, -97.56382523348287350 ) ) ;
#46350=ORIENTED_EDGE ( 'NONE', *, *, #218127, .T. ) ;
#46359=ORIENTED_EDGE ( 'NONE', *, *, #178390, .T. ) ;
#46379=EDGE_CURVE ( 'NONE', #148174, #180506, #239081, .T. ) ;
#46418=ORIENTED_EDGE ( 'NONE', *, *, #50010, .F. ) ;
#46422=CIRCLE ( 'NONE', #50504, 0.1000000000000028644 ) ;
#46461=EDGE_LOOP ( 'NONE', ( #4906, #7414, #96139, #237203 ) ) ;
#46462=CARTESIAN_POINT ( 'NONE',  ( 18.59999999999999076, 65.79142135624927334, -111.8731074845243683 ) ) ;
#46488=EDGE_CURVE ( 'NONE', #247369, #147468, #172490, .T. ) ;
#46501=EDGE_CURVE ( 'NONE', #53074, #104197, #126641, .T. ) ;
#46526=DIRECTION ( 'NONE',  ( 0.000000000000000000, -0.9908441862701605762, -0.1350103645451835310 ) ) ;
#46535=ORIENTED_EDGE ( 'NONE', *, *, #211589, .T. ) ;
#46665=CARTESIAN_POINT ( 'NONE',  ( -20.64999999999999858, 71.65000000001199965, -115.3731074845243256 ) ) ;
#46677=ORIENTED_EDGE ( 'NONE', *, *, #64609, .T. ) ;
#46678=CARTESIAN_POINT ( 'NONE',  ( -20.64999999999999858, 76.00000000001190870, -103.0231074845243029 ) ) ;
#46696=DIRECTION ( 'NONE',  ( 0.000000000000000000, 0.000000000000000000, 1.000000000000000000 ) ) ;
#46706=ORIENTED_EDGE ( 'NONE', *, *, #96198, .T. ) ;
#46725=CARTESIAN_POINT ( 'NONE',  ( -21.05000000000000071, 74.25000000001205080, -124.8535959266226598 ) ) ;
#46744=ORIENTED_EDGE ( 'NONE', *, *, #10143, .T. ) ;
#46753=CARTESIAN_POINT ( 'NONE',  ( -20.54999999999999716, 85.00000000001207923, -127.1291383618717816 ) ) ;
#46760=LINE ( 'NONE', #126301, #33464 ) ;
#46778=FACE_OUTER_BOUND ( 'NONE', #152929, .T. ) ;
#46798=CARTESIAN_POINT ( 'NONE',  ( -20.94999999999999929, 76.00000000001190870, -103.0231074845243029 ) ) ;
#46819=CARTESIAN_POINT ( 'NONE',  ( -21.05000000000000071, 64.35000000001195986, -110.0379132551783243 ) ) ;
#46845=CARTESIAN_POINT ( 'NONE',  ( 21.08078803292166015, 69.66698703557503336, -136.6022934716821169 ) ) ;
#46876=ORIENTED_EDGE ( 'NONE', *, *, #40341, .T. ) ;
#46880=CIRCLE ( 'NONE', #130083, 0.2000000000000057288 ) ;
#46896=ORIENTED_EDGE ( 'NONE', *, *, #249198, .T. ) ;
#46916=EDGE_LOOP ( 'NONE', ( #97708, #203081, #201652, #42452 ) ) ;
#47012=EDGE_LOOP ( 'NONE', ( #29974, #214878, #230422, #229886 ) ) ;
#47013=TOROIDAL_SURFACE ( 'NONE', #246936, 0.2000000000000000111, 0.1000000000000000056 ) ;
#47015=FACE_OUTER_BOUND ( 'NONE', #209224, .T. ) ;
#47027=DIRECTION ( 'NONE',  ( -1.000000000000000000, -0.000000000000000000, -0.000000000000000000 ) ) ;
#47033=CARTESIAN_POINT ( 'NONE',  ( 22.48660254037844197, 64.35000000001213039, -136.5731074845243995 ) ) ;
#47055=CARTESIAN_POINT ( 'NONE',  ( -20.64999999999999858, 68.85000000001200249, -115.3731074845243540 ) ) ;
#47070=CARTESIAN_POINT ( 'NONE',  ( -21.05000000000000426, 69.74168394268011184, -136.5888090948464821 ) ) ;
#47074=CARTESIAN_POINT ( 'NONE',  ( -18.59999999999999787, 76.00000000001213607, -136.5231074845242745 ) ) ;
#47077=CIRCLE ( 'NONE', #67943, 7.900000000000003908 ) ;
#47126=B_SPLINE_CURVE_WITH_KNOTS ( 'NONE', 3,
 ( #247668, #166887, #31236, #190277, #11646, #32514, #250236, #91160, #71617, #87294 ),
 .UNSPECIFIED., .F., .F.,
 ( 4, 2, 2, 2, 4 ),
 ( 0.000000000000000000, 4.221631689686801018E-05, 8.443263379373602037E-05, 0.0001688652675874720407, 0.0003377305351749303663 ),
 .UNSPECIFIED. ) ;
#47130=DIRECTION ( 'NONE',  ( 1.000000000000000000, 0.000000000000000000, 0.000000000000000000 ) ) ;
#47135=DIRECTION ( 'NONE',  ( 0.000000000000000000, 0.000000000000000000, 1.000000000000000000 ) ) ;
#47142=FACE_BOUND ( 'NONE', #70018, .T. ) ;
#47149=AXIS2_PLACEMENT_3D ( 'NONE', #29492, #149423, #249785 ) ;
#47164=CIRCLE ( 'NONE', #222122, 0.1000000000000033223 ) ;
#47181=VERTEX_POINT ( 'NONE', #156876 ) ;
#47216=AXIS2_PLACEMENT_3D ( 'NONE', #175738, #179580, #38775 ) ;
#47253=EDGE_CURVE ( 'NONE', #31313, #62035, #213928, .T. ) ;
#47262=ADVANCED_FACE ( 'NONE', ( #237668 ), #155600, .T. ) ;
#47280=CARTESIAN_POINT ( 'NONE',  ( 21.14999999999999858, 64.35000000001204512, -124.2731074845243739 ) ) ;
#47292=ORIENTED_EDGE ( 'NONE', *, *, #201184, .F. ) ;
#47332=ADVANCED_FACE ( 'NONE', ( #121602 ), #193094, .T. ) ;
#47336=CARTESIAN_POINT ( 'NONE',  ( 18.52130828395272388, 85.48139550263790909, -129.4986007606406133 ) ) ;
#47338=ORIENTED_EDGE ( 'NONE', *, *, #160611, .F. ) ;
#47356=DIRECTION ( 'NONE',  ( -1.836970198721029934E-16, -1.000000000000000000, -6.982962677686266711E-15 ) ) ;
#47382=CARTESIAN_POINT ( 'NONE',  ( -20.64999999999999858, 71.65000000001199965, -115.2731074845243171 ) ) ;
#47389=AXIS2_PLACEMENT_3D ( 'NONE', #255495, #57323, #116055 ) ;
#47410=EDGE_CURVE ( 'NONE', #211746, #17520, #68010, .T. ) ;
#47423=ORIENTED_EDGE ( 'NONE', *, *, #2216, .F. ) ;
#47446=CARTESIAN_POINT ( 'NONE',  ( 21.10642757222115407, 65.27684371085345560, -124.2824099607391730 ) ) ;
#47451=DIRECTION ( 'NONE',  ( 1.000000000000000000, -0.000000000000000000, 0.000000000000000000 ) ) ;
#47461=AXIS2_PLACEMENT_3D ( 'NONE', #237022, #58348, #254000 ) ;
#47462=EDGE_LOOP ( 'NONE', ( #254454, #195183, #246842, #48833 ) ) ;
#47513=CARTESIAN_POINT ( 'NONE',  ( -22.50000000000000000, 64.35000000001217302, -136.5231074845243597 ) ) ;
#47520=DIRECTION ( 'NONE',  ( 0.000000000000000000, 1.000000000000000000, 6.982962677686266711E-15 ) ) ;
#47529=CARTESIAN_POINT ( 'NONE',  ( 18.49999999999998934, 85.32100840337339775, -129.2871692354463562 ) ) ;
#47532=AXIS2_PLACEMENT_3D ( 'NONE', #160084, #201746, #222574 ) ;
#47533=CARTESIAN_POINT ( 'NONE',  ( 18.59999999999999787, 77.73670573947940454, -91.50568489690056140 ) ) ;
#47539=DIRECTION ( 'NONE',  ( 1.000000000000000000, -0.000000000000000000, 0.000000000000000000 ) ) ;
#47567=ORIENTED_EDGE ( 'NONE', *, *, #166310, .F. ) ;
#47571=VERTEX_POINT ( 'NONE', #157866 ) ;
#47574=CARTESIAN_POINT ( 'NONE',  ( 21.05000000000000071, 76.00000000001213607, -136.5231074845242745 ) ) ;
#47601=VERTEX_POINT ( 'NONE', #73183 ) ;
#47613=DIRECTION ( 'NONE',  ( -1.000000000000000000, 3.265361837132813093E-16, 2.280189983783949500E-30 ) ) ;
#47655=EDGE_CURVE ( 'NONE', #14025, #239754, #122351, .T. ) ;
#47669=CYLINDRICAL_SURFACE ( 'NONE', #174777, 0.09999999999999939493 ) ;
#47670=CARTESIAN_POINT ( 'NONE',  ( -18.50000000000000000, 77.16412189325305349, -95.10825939895268277 ) ) ;
#47705=CARTESIAN_POINT ( 'NONE',  ( -20.64999999999999858, 85.40000000001198543, -112.9170766071766820 ) ) ;
#47714=CARTESIAN_POINT ( 'NONE',  ( 20.94999999999999929, 85.00000000001197975, -112.9170766071766820 ) ) ;
#47737=VECTOR ( 'NONE', #43798, 1000.000000000000000 ) ;
#47760=CARTESIAN_POINT ( 'NONE',  ( 18.47149038651511432, 85.67145715801859751, -96.35032114978582740 ) ) ;
#47788=EDGE_CURVE ( 'NONE', #255696, #88307, #115545, .T. ) ;
#47797=CYLINDRICAL_SURFACE ( 'NONE', #61928, 0.1000000000000028644 ) ;
#47798=EDGE_CURVE ( 'NONE', #206647, #102291, #222269, .T. ) ;
#47812=CARTESIAN_POINT ( 'NONE',  ( -23.15000000000000213, 74.00000000001199396, -116.2477294072864140 ) ) ;
#47855=VECTOR ( 'NONE', #177075, 1000.000000000000000 ) ;
#47866=VERTEX_POINT ( 'NONE', #213284 ) ;
#47884=CARTESIAN_POINT ( 'NONE',  ( -20.54999999999999716, 71.65000000001199965, -115.3731074845243256 ) ) ;
#47922=LINE ( 'NONE', #8816, #150244 ) ;
#47926=DIRECTION ( 'NONE',  ( 1.000000000000000000, 0.000000000000000000, 0.000000000000000000 ) ) ;
#47934=EDGE_LOOP ( 'NONE', ( #41864, #249862, #172130 ) ) ;
#47936=DIRECTION ( 'NONE',  ( 1.000000000000000000, -0.000000000000000000, 0.000000000000000000 ) ) ;
#47984=CARTESIAN_POINT ( 'NONE',  ( 22.49999999999999645, 64.35042919246734527, -136.6231074845243825 ) ) ;
#47986=CIRCLE ( 'NONE', #102122, 0.09999999999999939493 ) ;
#47993=ORIENTED_EDGE ( 'NONE', *, *, #253079, .F. ) ;
#48005=CIRCLE ( 'NONE', #114647, 0.1000000000000028644 ) ;
#48066=ORIENTED_EDGE ( 'NONE', *, *, #161715, .F. ) ;
#48076=CIRCLE ( 'NONE', #252092, 0.09999999999999939493 ) ;
#48091=DIRECTION ( 'NONE',  ( 0.000000000000000000, 0.000000000000000000, -1.000000000000000000 ) ) ;
#48094=CARTESIAN_POINT ( 'NONE',  ( 20.94999999999999929, 76.00000000001190870, -103.0231074845243029 ) ) ;
#48104=ORIENTED_EDGE ( 'NONE', *, *, #161592, .F. ) ;
#48138=LINE ( 'NONE', #125130, #223020 ) ;
#48146=DIRECTION ( 'NONE',  ( 0.000000000000000000, -0.1350103645451974088, 0.9908441862701587999 ) ) ;
#48175=CARTESIAN_POINT ( 'NONE',  ( -21.14999999999999858, 76.10000000001222986, -148.1726782920690937 ) ) ;
#48191=AXIS2_PLACEMENT_3D ( 'NONE', #208929, #48566, #191966 ) ;
#48194=VERTEX_POINT ( 'NONE', #9661 ) ;
#48225=ORIENTED_EDGE ( 'NONE', *, *, #138443, .F. ) ;
#48262=AXIS2_PLACEMENT_3D ( 'NONE', #188902, #204598, #246310 ) ;
#48264=LINE ( 'NONE', #127813, #3160 ) ;
#48275=LINE ( 'NONE', #14320, #84366 ) ;
#48330=EDGE_CURVE ( 'NONE', #105040, #8189, #131086, .T. ) ;
#48339=VECTOR ( 'NONE', #32000, 1000.000000000000000 ) ;
#48343=VECTOR ( 'NONE', #3887, 999.9999999999998863 ) ;
#48355=CARTESIAN_POINT ( 'NONE',  ( -23.25000000000000000, 76.00000000001216449, -140.6731074845242802 ) ) ;
#48357=AXIS2_PLACEMENT_3D ( 'NONE', #20222, #82713, #39807 ) ;
#48371=ORIENTED_EDGE ( 'NONE', *, *, #86219, .T. ) ;
#48378=CARTESIAN_POINT ( 'NONE',  ( 18.50000000000000000, 85.40000000001185754, -96.14106563635155567 ) ) ;
#48406=ADVANCED_FACE ( 'NONE', ( #184132 ), #224546, .T. ) ;
#48431=DIRECTION ( 'NONE',  ( 0.000000000000000000, -7.056502275159890043E-15, 1.000000000000000000 ) ) ;
#48456=FACE_OUTER_BOUND ( 'NONE', #76262, .T. ) ;
#48457=EDGE_LOOP ( 'NONE', ( #15562, #177320, #162561 ) ) ;
#48474=DIRECTION ( 'NONE',  ( -0.000000000000000000, 6.982962677686266711E-15, -1.000000000000000000 ) ) ;
#48477=ORIENTED_EDGE ( 'NONE', *, *, #171094, .F. ) ;
#48511=CARTESIAN_POINT ( 'NONE',  ( 21.05000000000000071, 76.10000000001222986, -148.1726782920690937 ) ) ;
#48518=EDGE_LOOP ( 'NONE', ( #204979, #52670, #193045, #181019, #813 ) ) ;
#48526=CYLINDRICAL_SURFACE ( 'NONE', #59870, 0.09999999999998898659 ) ;
#48529=CYLINDRICAL_SURFACE ( 'NONE', #226969, 0.1000000000000026007 ) ;
#48534=DIRECTION ( 'NONE',  ( 0.000000000000000000, -7.116814260417668513E-15, 1.000000000000000000 ) ) ;
#48536=AXIS2_PLACEMENT_3D ( 'NONE', #243811, #63898, #43057 ) ;
#48552=FACE_OUTER_BOUND ( 'NONE', #42117, .T. ) ;
#48563=ORIENTED_EDGE ( 'NONE', *, *, #31822, .T. ) ;
#48566=DIRECTION ( 'NONE',  ( -0.000000000000000000, -6.982962677686266711E-15, 1.000000000000000000 ) ) ;
#48597=CIRCLE ( 'NONE', #52685, 0.1000000000000070832 ) ;
#48599=DIRECTION ( 'NONE',  ( 0.000000000000000000, 0.1495327102803078179, 0.9887567792719429427 ) ) ;
#48653=CARTESIAN_POINT ( 'NONE',  ( -20.94999999999999929, 87.65000000001212754, -133.6231074845242119 ) ) ;
#48675=CARTESIAN_POINT ( 'NONE',  ( 18.49999999999999645, 74.83729825007408465, -128.4231074845243086 ) ) ;
#48683=LINE ( 'NONE', #108669, #145283 ) ;
#48690=CIRCLE ( 'NONE', #23801, 11.89999999999999325 ) ;
#48693=CARTESIAN_POINT ( 'NONE',  ( -20.94999675878240808, 65.70692517833232671, -97.56446533783034170 ) ) ;
#48711=EDGE_LOOP ( 'NONE', ( #88570, #114411, #201732, #96954 ) ) ;
#48751=CARTESIAN_POINT ( 'NONE',  ( -18.59999999999999787, 64.35000000001205933, -124.3731074845243825 ) ) ;
#48765=DIRECTION ( 'NONE',  ( 0.000000000000000000, 1.000000000000000000, 6.938893903907222067E-15 ) ) ;
#48778=CARTESIAN_POINT ( 'NONE',  ( -22.39999999999999858, 68.20922040163873135, -136.6231074845243540 ) ) ;
#48785=ORIENTED_EDGE ( 'NONE', *, *, #193382, .F. ) ;
#48803=FACE_OUTER_BOUND ( 'NONE', #192019, .T. ) ;
#48804=EDGE_CURVE ( 'NONE', #186173, #197247, #85921, .T. ) ;
#48815=ADVANCED_FACE ( 'NONE', ( #101701 ), #120050, .F. ) ;
#48819=ORIENTED_EDGE ( 'NONE', *, *, #178106, .T. ) ;
#48827=AXIS2_PLACEMENT_3D ( 'NONE', #55243, #244170, #100776 ) ;
#48833=ORIENTED_EDGE ( 'NONE', *, *, #68900, .T. ) ;
#48839=ORIENTED_EDGE ( 'NONE', *, *, #101499, .T. ) ;
#48853=CARTESIAN_POINT ( 'NONE',  ( 20.95083306685154056, 67.08315735812188052, -128.0457826312660075 ) ) ;
#48885=CARTESIAN_POINT ( 'NONE',  ( -23.15000000000000213, 76.00000000001190870, -103.0231074845243029 ) ) ;
#48903=DIRECTION ( 'NONE',  ( -0.000000000000000000, 0.1350103645451945777, -0.9908441862701590219 ) ) ;
#48937=DIRECTION ( 'NONE',  ( 0.000000000000000000, -1.000000000000000000, -6.860497997771531562E-15 ) ) ;
#48938=ORIENTED_EDGE ( 'NONE', *, *, #72207, .F. ) ;
#48997=DIRECTION ( 'NONE',  ( 0.7071067811865474617, -0.7071067811865474617, -4.937700262164531476E-15 ) ) ;
#49002=EDGE_LOOP ( 'NONE', ( #208861, #246537, #88887, #214224 ) ) ;
#49012=CARTESIAN_POINT ( 'NONE',  ( -21.05000000000000071, 69.60000000001207354, -126.5926828544627654 ) ) ;
#49066=ADVANCED_FACE ( 'NONE', ( #225060 ), #85533, .F. ) ;
#49123=EDGE_CURVE ( 'NONE', #127664, #13761, #115350, .T. ) ;
#49130=ORIENTED_EDGE ( 'NONE', *, *, #75866, .F. ) ;
#49134=ORIENTED_EDGE ( 'NONE', *, *, #253984, .T. ) ;
#49135=CARTESIAN_POINT ( 'NONE',  ( -20.94999999999999929, 70.15000000001211333, -126.3906102602463619 ) ) ;
#49168=ORIENTED_EDGE ( 'NONE', *, *, #206645, .T. ) ;
#49197=CIRCLE ( 'NONE', #224168, 0.09999999999998898659 ) ;
#49210=CARTESIAN_POINT ( 'NONE',  ( -23.25000000000000000, 64.35000000001222986, -148.2731074845243882 ) ) ;
#49212=VERTEX_POINT ( 'NONE', #149100 ) ;
#49245=AXIS2_PLACEMENT_3D ( 'NONE', #87790, #112523, #69553 ) ;
#49263=CARTESIAN_POINT ( 'NONE',  ( -18.50000000000000000, 77.13501884592203339, -95.30613060109196510 ) ) ;
#49290=CYLINDRICAL_SURFACE ( 'NONE', #112592, 0.09999999999998898659 ) ;
#49366=EDGE_LOOP ( 'NONE', ( #162713, #122274, #50244, #138814, #41239 ) ) ;
#49371=DIRECTION ( 'NONE',  ( 0.000000000000000000, -6.938893903907222067E-15, 1.000000000000000000 ) ) ;
#49396=ORIENTED_EDGE ( 'NONE', *, *, #246489, .F. ) ;
#49410=FACE_OUTER_BOUND ( 'NONE', #221320, .T. ) ;
#49468=EDGE_CURVE ( 'NONE', #212214, #37875, #166066, .T. ) ;
#49500=AXIS2_PLACEMENT_3D ( 'NONE', #31384, #90018, #169618 ) ;
#49516=ORIENTED_EDGE ( 'NONE', *, *, #10049, .T. ) ;
#49576=CARTESIAN_POINT ( 'NONE',  ( -20.85000000000000142, 68.87972903831429505, -99.36354444268502561 ) ) ;
#49612=DIRECTION ( 'NONE',  ( -1.000000000000000000, 0.000000000000000000, -0.000000000000000000 ) ) ;
#49637=ORIENTED_EDGE ( 'NONE', *, *, #248639, .T. ) ;
#49638=TOROIDAL_SURFACE ( 'NONE', #91351, 0.2000000000000000111, 0.1000000000000000056 ) ;
#49641=DIRECTION ( 'NONE',  ( -0.000000000000000000, -6.982962677686266711E-15, 1.000000000000000000 ) ) ;
#49652=ORIENTED_EDGE ( 'NONE', *, *, #60205, .T. ) ;
#49673=EDGE_CURVE ( 'NONE', #157880, #71756, #224288, .T. ) ;
#49681=CARTESIAN_POINT ( 'NONE',  ( -22.59066674512272144, 64.25000000001213607, -136.5536116081548244 ) ) ;
#49731=CARTESIAN_POINT ( 'NONE',  ( -20.54999999999999716, 87.75000000001199396, -115.3731074845242119 ) ) ;
#49763=CARTESIAN_POINT ( 'NONE',  ( 18.59999999999999076, 64.25000000001220712, -148.2731074845243882 ) ) ;
#49774=CARTESIAN_POINT ( 'NONE',  ( -21.05000000000000071, 70.15000000001211333, -126.3906102602463619 ) ) ;
#49795=EDGE_LOOP ( 'NONE', ( #62641, #62940, #26299, #240070 ) ) ;
#49818=DIRECTION ( 'NONE',  ( 0.000000000000000000, 6.982962677686266711E-15, -1.000000000000000000 ) ) ;
#49822=AXIS2_PLACEMENT_3D ( 'NONE', #152597, #137787, #257690 ) ;
#49832=CARTESIAN_POINT ( 'NONE',  ( 18.56308993302904042, 65.61930884468790737, -111.7838848455857601 ) ) ;
#49839=LINE ( 'NONE', #140252, #148454 ) ;
#49858=CARTESIAN_POINT ( 'NONE',  ( -18.59999999999999787, 85.32100840337338354, -129.2871692354463562 ) ) ;
#49866=AXIS2_PLACEMENT_3D ( 'NONE', #164139, #141984, #162868 ) ;
#49868=AXIS2_PLACEMENT_3D ( 'NONE', #91420, #129258, #187953 ) ;
#49888=DIRECTION ( 'NONE',  ( 0.000000000000000000, 0.000000000000000000, 1.000000000000000000 ) ) ;
#49899=DIRECTION ( 'NONE',  ( -0.000000000000000000, -6.982962677686266711E-15, 1.000000000000000000 ) ) ;
#49913=CARTESIAN_POINT ( 'NONE',  ( -23.15000000000000213, 76.00000000001193712, -107.0231074845243029 ) ) ;
#49920=DIRECTION ( 'NONE',  ( 0.000000000000000000, -7.086529944415894657E-15, 1.000000000000000000 ) ) ;
#49927=ORIENTED_EDGE ( 'NONE', *, *, #95246, .T. ) ;
#49934=ORIENTED_EDGE ( 'NONE', *, *, #63382, .T. ) ;
#49937=ORIENTED_EDGE ( 'NONE', *, *, #147521, .F. ) ;
#49940=DIRECTION ( 'NONE',  ( -1.000000000000000000, 0.000000000000000000, -0.000000000000000000 ) ) ;
#49951=DIRECTION ( 'NONE',  ( 1.000000000000000000, 0.000000000000000000, 0.000000000000000000 ) ) ;
#49956=DIRECTION ( 'NONE',  ( 1.000000000000000000, 0.000000000000000000, 0.000000000000000000 ) ) ;
#49979=AXIS2_PLACEMENT_3D ( 'NONE', #170263, #12443, #125932 ) ;
#49983=EDGE_CURVE ( 'NONE', #185852, #119534, #212021, .T. ) ;
#49986=ORIENTED_EDGE ( 'NONE', *, *, #8735, .T. ) ;
#49989=VERTEX_POINT ( 'NONE', #211016 ) ;
#50007=ORIENTED_EDGE ( 'NONE', *, *, #21284, .T. ) ;
#50010=EDGE_CURVE ( 'NONE', #239754, #52643, #157895, .T. ) ;
#50046=AXIS2_PLACEMENT_3D ( 'NONE', #20866, #196900, #216460 ) ;
#50053=ORIENTED_EDGE ( 'NONE', *, *, #135861, .F. ) ;
#50096=FACE_OUTER_BOUND ( 'NONE', #131603, .T. ) ;
#50115=FACE_OUTER_BOUND ( 'NONE', #191404, .T. ) ;
#50116=AXIS2_PLACEMENT_3D ( 'NONE', #199712, #164421, #142273 ) ;
#50125=CARTESIAN_POINT ( 'NONE',  ( -21.55000000000000426, 68.29142135624930177, -115.3731074845243540 ) ) ;
#50142=DIRECTION ( 'NONE',  ( 1.000000000000000000, 0.000000000000000000, 0.000000000000000000 ) ) ;
#50227=VERTEX_POINT ( 'NONE', #81727 ) ;
#50244=ORIENTED_EDGE ( 'NONE', *, *, #204998, .T. ) ;
#50252=EDGE_CURVE ( 'NONE', #191338, #231430, #99732, .T. ) ;
#50270=EDGE_CURVE ( 'NONE', #54789, #111107, #907, .T. ) ;
#50384=DIRECTION ( 'NONE',  ( 0.000000000000000000, 6.982962677686266711E-15, -1.000000000000000000 ) ) ;
#50406=CARTESIAN_POINT ( 'NONE',  ( -21.52071067811865746, 68.22071067813071465, -124.1731074845243512 ) ) ;
#50427=DIRECTION ( 'NONE',  ( 0.000000000000000000, -6.467318590049456648E-15, 1.000000000000000000 ) ) ;
#50448=DIRECTION ( 'NONE',  ( 1.000000000000000000, 0.000000000000000000, 0.000000000000000000 ) ) ;
#50492=CARTESIAN_POINT ( 'NONE',  ( 23.24999999999999645, 76.00000000001190870, -103.0231074845243029 ) ) ;
#50504=AXIS2_PLACEMENT_3D ( 'NONE', #29552, #9953, #149489 ) ;
#50535=DIRECTION ( 'NONE',  ( -0.000000000000000000, -6.982962677686266711E-15, 1.000000000000000000 ) ) ;
#50570=SPHERICAL_SURFACE ( 'NONE', #83544, 0.1000000000000000056 ) ;
#50572=AXIS2_PLACEMENT_3D ( 'NONE', #42208, #180431, #3052 ) ;
#50594=ORIENTED_EDGE ( 'NONE', *, *, #81127, .F. ) ;
#50600=EDGE_CURVE ( 'NONE', #192664, #140683, #116519, .T. ) ;
#50657=CIRCLE ( 'NONE', #129781, 0.1000000000000028644 ) ;
#50659=CARTESIAN_POINT ( 'NONE',  ( 18.59999999999999076, 65.50857864377465489, -111.7731074845243739 ) ) ;
#50691=ORIENTED_EDGE ( 'NONE', *, *, #189221, .T. ) ;
#50698=CARTESIAN_POINT ( 'NONE',  ( -20.54999999999999716, 85.00000000001197975, -112.9170766071766820 ) ) ;
#50705=CARTESIAN_POINT ( 'NONE',  ( -23.25000000000000000, 74.00000000001199396, -115.6477294072864055 ) ) ;
#50721=FACE_OUTER_BOUND ( 'NONE', #2369, .T. ) ;
#50743=EDGE_CURVE ( 'NONE', #245468, #13286, #36610, .T. ) ;
#50751=DIRECTION ( 'NONE',  ( 0.000000000000000000, 1.000000000000000000, 6.938893903907222067E-15 ) ) ;
#50780=CYLINDRICAL_SURFACE ( 'NONE', #78942, 0.09999999999999939493 ) ;
#50790=EDGE_CURVE ( 'NONE', #88307, #143912, #161978, .T. ) ;
#50795=ORIENTED_EDGE ( 'NONE', *, *, #111492, .T. ) ;
#50796=ORIENTED_EDGE ( 'NONE', *, *, #47253, .T. ) ;
#50830=DIRECTION ( 'NONE',  ( 1.000000000000000000, 0.000000000000000000, 0.000000000000000000 ) ) ;
#50831=LINE ( 'NONE', #149986, #219662 ) ;
#50841=ORIENTED_EDGE ( 'NONE', *, *, #1960, .T. ) ;
#50857=DIRECTION ( 'NONE',  ( 0.000000000000000000, -1.000000000000000000, 2.771150684185008344E-14 ) ) ;
#50861=PLANE ( 'NONE',  #67370 ) ;
#50876=DIRECTION ( 'NONE',  ( 0.000000000000000000, -6.467318590049456648E-15, 1.000000000000000000 ) ) ;
#50883=DIRECTION ( 'NONE',  ( -2.557131231893037478E-16, -0.8660254037844420383, 0.4999999999999941713 ) ) ;
#50890=DIRECTION ( 'NONE',  ( 0.000000000000000000, -6.982962677686266711E-15, 1.000000000000000000 ) ) ;
#50914=ORIENTED_EDGE ( 'NONE', *, *, #42764, .F. ) ;
#50950=FACE_OUTER_BOUND ( 'NONE', #106145, .T. ) ;
#50952=CARTESIAN_POINT ( 'NONE',  ( -2.995603634470891112E-16, 87.75000000001205080, -124.2731074845242176 ) ) ;
#50964=VECTOR ( 'NONE', #101211, 1000.000000000000000 ) ;
#50971=CARTESIAN_POINT ( 'NONE',  ( -23.15000000000000213, 87.65000000001192859, -106.1231074845242262 ) ) ;
#50993=DIRECTION ( 'NONE',  ( -1.000000000000000000, 0.000000000000000000, -0.000000000000000000 ) ) ;
#51008=DIRECTION ( 'NONE',  ( 1.000000000000000000, 0.000000000000000000, -0.000000000000000000 ) ) ;
#51016=CARTESIAN_POINT ( 'NONE',  ( -20.54999999999999716, 66.65000000001205649, -124.2731074845243597 ) ) ;
#51022=ORIENTED_EDGE ( 'NONE', *, *, #204143, .F. ) ;
#51029=AXIS2_PLACEMENT_3D ( 'NONE', #134831, #249680, #54034 ) ;
#51054=ORIENTED_EDGE ( 'NONE', *, *, #67408, .F. ) ;
#51090=CARTESIAN_POINT ( 'NONE',  ( 20.94999999999999929, 76.00000000001190870, -103.0231074845243029 ) ) ;
#51123=CARTESIAN_POINT ( 'NONE',  ( -18.54118089899631272, 85.46353763186019137, -129.4745298866561143 ) ) ;
#51131=CARTESIAN_POINT ( 'NONE',  ( -20.64999999999999858, 68.75000000001199396, -115.3731074845243540 ) ) ;
#51132=CARTESIAN_POINT ( 'NONE',  ( 20.94999999999999929, 71.00000000001205080, -124.1178414656112352 ) ) ;
#51145=DIRECTION ( 'NONE',  ( 0.000000000000000000, -0.008583690987135041833, 0.9999631594459055250 ) ) ;
#51188=ORIENTED_EDGE ( 'NONE', *, *, #12823, .T. ) ;
#51223=DIRECTION ( 'NONE',  ( 1.000000000000000000, -7.304098846218134667E-16, -5.100424963727256530E-30 ) ) ;
#51249=CARTESIAN_POINT ( 'NONE',  ( 22.00356870141344601, 68.74575763752172008, -136.5231074845243597 ) ) ;
#51252=CARTESIAN_POINT ( 'NONE',  ( 23.24999999999999645, 76.00000000001190870, -103.0231074845243029 ) ) ;
#51267=AXIS2_PLACEMENT_3D ( 'NONE', #69457, #104668, #205072 ) ;
#51296=ORIENTED_EDGE ( 'NONE', *, *, #70947, .F. ) ;
#51306=VECTOR ( 'NONE', #33166, 1000.000000000000000 ) ;
#51311=DIRECTION ( 'NONE',  ( 0.000000000000000000, -0.4999999999999608646, 0.8660254037844612451 ) ) ;
#51349=FACE_OUTER_BOUND ( 'NONE', #150009, .T. ) ;
#51388=CARTESIAN_POINT ( 'NONE',  ( -20.94999999999999929, 74.16465844978765176, -124.8679561919613263 ) ) ;
#51401=DIRECTION ( 'NONE',  ( 0.000000000000000000, 7.056502275159890832E-15, -1.000000000000000000 ) ) ;
#51434=DIRECTION ( 'NONE',  ( 0.000000000000000000, -0.9654727137038715545, 0.2605042016806676242 ) ) ;
#51442=ORIENTED_EDGE ( 'NONE', *, *, #92571, .T. ) ;
#51449=AXIS2_PLACEMENT_3D ( 'NONE', #180360, #239045, #1700 ) ;
#51535=AXIS2_PLACEMENT_3D ( 'NONE', #181225, #202056, #23449 ) ;
#51551=FACE_OUTER_BOUND ( 'NONE', #65860, .T. ) ;
#51595=CYLINDRICAL_SURFACE ( 'NONE', #14504, 0.09999999999999939493 ) ;
#51644=ORIENTED_EDGE ( 'NONE', *, *, #194335, .F. ) ;
#51646=CARTESIAN_POINT ( 'NONE',  ( -20.54999999999999716, 68.85000000001203091, -119.7731074845243597 ) ) ;
#51671=CYLINDRICAL_SURFACE ( 'NONE', #89916, 0.1000000000000028644 ) ;
#51699=EDGE_CURVE ( 'NONE', #138262, #197443, #184446, .T. ) ;
#51714=ORIENTED_EDGE ( 'NONE', *, *, #150660, .F. ) ;
#51742=CARTESIAN_POINT ( 'NONE',  ( -23.15000000000000213, 76.00000000001205080, -123.7481074845242972 ) ) ;
#51749=CARTESIAN_POINT ( 'NONE',  ( 20.84999999999998721, 87.75000000001190870, -103.0231074845242176 ) ) ;
#51781=DIRECTION ( 'NONE',  ( -1.000000000000000000, 2.952720810173289112E-16, 2.061873921506763405E-30 ) ) ;
#51816=VERTEX_POINT ( 'NONE', #210457 ) ;
#51848=ORIENTED_EDGE ( 'NONE', *, *, #72051, .T. ) ;
#51864=VERTEX_POINT ( 'NONE', #133473 ) ;
#51894=DIRECTION ( 'NONE',  ( 0.000000000000000000, 0.9908441862701605762, -0.1350103645451835310 ) ) ;
#51911=CARTESIAN_POINT ( 'NONE',  ( -21.05000000000000071, 74.63912941282003999, -128.4501095574333647 ) ) ;
#51916=CARTESIAN_POINT ( 'NONE',  ( -18.59999999999999787, 85.50000000001209344, -128.4231074845242233 ) ) ;
#51929=ORIENTED_EDGE ( 'NONE', *, *, #13770, .T. ) ;
#51957=DIRECTION ( 'NONE',  ( 0.000000000000000000, -1.000000000000000000, -6.982962677686265922E-15 ) ) ;
#51959=DIRECTION ( 'NONE',  ( -0.000000000000000000, 1.000000000000000000, 6.982962677686266711E-15 ) ) ;
#51961=CIRCLE ( 'NONE', #118650, 0.1000000000000028644 ) ;
#51965=ORIENTED_EDGE ( 'NONE', *, *, #23485, .F. ) ;
#51978=AXIS2_PLACEMENT_3D ( 'NONE', #75445, #77962, #17996 ) ;
#51988=EDGE_CURVE ( 'NONE', #130891, #72948, #218120, .T. ) ;
#51997=DIRECTION ( 'NONE',  ( 0.000000000000000000, 0.8700118002898393765, -0.4930308989875104575 ) ) ;
#52007=ORIENTED_EDGE ( 'NONE', *, *, #158792, .T. ) ;
#52022=EDGE_CURVE ( 'NONE', #61549, #108560, #519, .T. ) ;
#52024=ORIENTED_EDGE ( 'NONE', *, *, #122504, .F. ) ;
#52043=ADVANCED_FACE ( 'NONE', ( #198570 ), #83879, .T. ) ;
#52051=ORIENTED_EDGE ( 'NONE', *, *, #106080, .F. ) ;
#52057=CARTESIAN_POINT ( 'NONE',  ( -20.85000000000000142, 87.65000000001191438, -103.0231074845242176 ) ) ;
#52064=DIRECTION ( 'NONE',  ( 1.000000000000000000, 0.000000000000000000, 0.000000000000000000 ) ) ;
#52104=CARTESIAN_POINT ( 'NONE',  ( 18.33996824403519099, 85.56963985944324236, -96.20404184700757355 ) ) ;
#52117=MECHANICAL_DESIGN_GEOMETRIC_PRESENTATION_REPRESENTATION('',(#143711),#89528);
#52128=DIRECTION ( 'NONE',  ( 0.000000000000000000, 1.000000000000000000, 6.982962677686266711E-15 ) ) ;
#52133=EDGE_LOOP ( 'NONE', ( #169984, #19409, #44495, #208889 ) ) ;
#52144=DIRECTION ( 'NONE',  ( 0.000000000000000000, 0.000000000000000000, -1.000000000000000000 ) ) ;
#52175=DIRECTION ( 'NONE',  ( 1.000000000000000000, 0.000000000000000000, 0.000000000000000000 ) ) ;
#52215=FACE_OUTER_BOUND ( 'NONE', #35458, .T. ) ;
#52224=DIRECTION ( 'NONE',  ( 2.840903330521631775E-16, 0.8700118002898354908, -0.4930308989875170078 ) ) ;
#52225=DIRECTION ( 'NONE',  ( -7.304098846218134667E-16, 1.000000000000000000, 6.982962677686267499E-15 ) ) ;
#52231=DIRECTION ( 'NONE',  ( 0.000000000000000000, 0.000000000000000000, -1.000000000000000000 ) ) ;
#52233=VECTOR ( 'NONE', #64485, 1000.000000000000000 ) ;
#52241=CARTESIAN_POINT ( 'NONE',  ( 19.83283456528358712, 64.25000000001196554, -111.6731074851050636 ) ) ;
#52244=EDGE_LOOP ( 'NONE', ( #86133, #174255, #25358 ) ) ;
#52257=ADVANCED_FACE ( 'NONE', ( #157582 ), #175838, .T. ) ;
#52262=ADVANCED_FACE ( 'NONE', ( #97524, #169767 ), #108469, .T. ) ;
#52283=EDGE_LOOP ( 'NONE', ( #126141, #178790, #105584 ) ) ;
#52292=DIRECTION ( 'NONE',  ( 0.000000000000000000, 0.000000000000000000, 1.000000000000000000 ) ) ;
#52299=EDGE_CURVE ( 'NONE', #7536, #172048, #134104, .T. ) ;
#52369=CARTESIAN_POINT ( 'NONE',  ( -23.15000000000000213, 71.75000000001199396, -115.2731074845243171 ) ) ;
#52380=ORIENTED_EDGE ( 'NONE', *, *, #186320, .F. ) ;
#52391=EDGE_LOOP ( 'NONE', ( #147056, #127727, #175168, #225551 ) ) ;
#52409=ADVANCED_FACE ( 'NONE', ( #161404 ), #60991, .F. ) ;
#52415=AXIS2_PLACEMENT_3D ( 'NONE', #154244, #78490, #158096 ) ;
#52425=CARTESIAN_POINT ( 'NONE',  ( 20.95017935633852346, 65.52451072038677182, -128.9456676871338914 ) ) ;
#52433=VECTOR ( 'NONE', #50883, 1000.000000000000000 ) ;
#52436=EDGE_LOOP ( 'NONE', ( #53213, #50007, #150209, #204309, #105295, #157754, #75977 ) ) ;
#52439=CIRCLE ( 'NONE', #48357, 0.09999999999999971412 ) ;
#52450=DIRECTION ( 'NONE',  ( 1.000000000000000000, 0.000000000000000000, 0.000000000000000000 ) ) ;
#52461=CARTESIAN_POINT ( 'NONE',  ( -20.94999999999999929, 77.73625713160946304, -124.9544551555067926 ) ) ;
#52476=CARTESIAN_POINT ( 'NONE',  ( -21.13614978966382196, 69.50089529817834944, -136.5231074845243313 ) ) ;
#52511=DIRECTION ( 'NONE',  ( 0.000000000000000000, 6.982962677686266711E-15, -1.000000000000000000 ) ) ;
#52525=AXIS2_PLACEMENT_3D ( 'NONE', #83002, #43913, #179594 ) ;
#52559=FACE_OUTER_BOUND ( 'NONE', #217431, .T. ) ;
#52566=CARTESIAN_POINT ( 'NONE',  ( -21.14999999999999858, 87.65000000001214175, -136.5231074845242176 ) ) ;
#52568=AXIS2_PLACEMENT_3D ( 'NONE', #3626, #171736, #169167 ) ;
#52598=TOROIDAL_SURFACE ( 'NONE', #231682, 0.2000000000000000111, 0.1000000000000000056 ) ;
#52603=ADVANCED_FACE ( 'NONE', ( #140069 ), #219617, .T. ) ;
#52639=CARTESIAN_POINT ( 'NONE',  ( 20.85000000000000142, 75.83895117929318985, -103.3072973288845162 ) ) ;
#52643=VERTEX_POINT ( 'NONE', #100917 ) ;
#52649=CIRCLE ( 'NONE', #178155, 0.1000000000000028644 ) ;
#52667=CARTESIAN_POINT ( 'NONE',  ( 20.95512840106821528, 65.37615130623873938, -124.3206282637254816 ) ) ;
#52670=ORIENTED_EDGE ( 'NONE', *, *, #245732, .F. ) ;
#52683=AXIS2_PLACEMENT_3D ( 'NONE', #16257, #116611, #37103 ) ;
#52685=AXIS2_PLACEMENT_3D ( 'NONE', #213619, #31184, #254023 ) ;
#52691=CARTESIAN_POINT ( 'NONE',  ( -20.94999999999999929, 64.25000000001210765, -129.5083017138703667 ) ) ;
#52709=LINE ( 'NONE', #132256, #106262 ) ;
#52727=EDGE_CURVE ( 'NONE', #59827, #143912, #96559, .T. ) ;
#52748=DIRECTION ( 'NONE',  ( 1.000000000000000000, 0.000000000000000000, 0.000000000000000000 ) ) ;
#52767=DIRECTION ( 'NONE',  ( 0.000000000000000000, 6.982962677686266711E-15, -1.000000000000000000 ) ) ;
#52774=EDGE_CURVE ( 'NONE', #38011, #122081, #56896, .T. ) ;
#52788=DIRECTION ( 'NONE',  ( -1.000000000000000000, 1.836970198721029934E-16, 1.282749433769087582E-30 ) ) ;
#52813=DIRECTION ( 'NONE',  ( 0.000000000000000000, 0.000000000000000000, 1.000000000000000000 ) ) ;
#52823=CARTESIAN_POINT ( 'NONE',  ( 21.05000000000000071, 76.00000000001213607, -136.5231074845242745 ) ) ;
#52826=ORIENTED_EDGE ( 'NONE', *, *, #167578, .T. ) ;
#52877=FACE_OUTER_BOUND ( 'NONE', #41451, .T. ) ;
#53014=CARTESIAN_POINT ( 'NONE',  ( 21.05000000000000071, 70.50000000001199396, -115.4283735034374274 ) ) ;
#53026=CARTESIAN_POINT ( 'NONE',  ( 22.39999999999999503, 75.90000000001219860, -142.7731074845243029 ) ) ;
#53031=AXIS2_PLACEMENT_3D ( 'NONE', #21686, #123349, #239448 ) ;
#53044=DIRECTION ( 'NONE',  ( 0.000000000000000000, -6.853228547068871147E-15, 1.000000000000000000 ) ) ;
#53054=ORIENTED_EDGE ( 'NONE', *, *, #175708, .F. ) ;
#53074=VERTEX_POINT ( 'NONE', #254776 ) ;
#53120=CIRCLE ( 'NONE', #232220, 0.1000000000000028644 ) ;
#53129=ADVANCED_FACE ( 'NONE', ( #197413 ), #116602, .F. ) ;
#53158=DIRECTION ( 'NONE',  ( 0.000000000000000000, 0.8700118002898356018, -0.4930308989875170078 ) ) ;
#53160=DIRECTION ( 'NONE',  ( 0.000000000000000000, 6.982962677686266711E-15, -1.000000000000000000 ) ) ;
#53173=DIRECTION ( 'NONE',  ( -1.000000000000000000, 0.000000000000000000, -0.000000000000000000 ) ) ;
#53190=VERTEX_POINT ( 'NONE', #236535 ) ;
#53191=DIRECTION ( 'NONE',  ( 1.000000000000000000, 0.000000000000000000, 0.000000000000000000 ) ) ;
#53207=AXIS2_PLACEMENT_3D ( 'NONE', #202784, #222315, #179393 ) ;
#53213=ORIENTED_EDGE ( 'NONE', *, *, #136116, .F. ) ;
#53219=DIRECTION ( 'NONE',  ( -1.000000000000000000, -0.000000000000000000, -0.000000000000000000 ) ) ;
#53252=CIRCLE ( 'NONE', #223917, 2.100000000000004530 ) ;
#53262=CARTESIAN_POINT ( 'NONE',  ( 21.11345278033298456, 67.11787792664036090, -124.2770853137694473 ) ) ;
#53291=ORIENTED_EDGE ( 'NONE', *, *, #59183, .F. ) ;
#53307=CARTESIAN_POINT ( 'NONE',  ( 20.85000000000000142, 68.87972903831429505, -99.36354444268502561 ) ) ;
#53329=DIRECTION ( 'NONE',  ( 0.000000000000000000, 0.9915357197604982575, -0.1298341882519033486 ) ) ;
#53338=DIRECTION ( 'NONE',  ( 0.000000000000000000, -1.000000000000000000, 0.000000000000000000 ) ) ;
#53344=VECTOR ( 'NONE', #27600, 1000.000000000000000 ) ;
#53352=EDGE_CURVE ( 'NONE', #86370, #137392, #133784, .T. ) ;
#53371=DIRECTION ( 'NONE',  ( 1.000000000000000000, 0.000000000000000000, 0.000000000000000000 ) ) ;
#53407=CARTESIAN_POINT ( 'NONE',  ( 18.39999999999999858, 85.50000000001185185, -96.10095763519375112 ) ) ;
#53409=CARTESIAN_POINT ( 'NONE',  ( 23.24999999999999289, 64.35000000001221565, -148.2731074845243882 ) ) ;
#53415=CARTESIAN_POINT ( 'NONE',  ( 18.59999999999999076, 77.25000000001209344, -128.5231074845242745 ) ) ;
#53428=DIRECTION ( 'NONE',  ( 0.000000000000000000, 7.086529944415894657E-15, -1.000000000000000000 ) ) ;
#53454=ORIENTED_EDGE ( 'NONE', *, *, #103943, .T. ) ;
#53464=ORIENTED_EDGE ( 'NONE', *, *, #213875, .F. ) ;
#53510=EDGE_CURVE ( 'NONE', #193905, #102067, #213080, .T. ) ;
#53515=CARTESIAN_POINT ( 'NONE',  ( -18.50000000000000000, 76.00000000001213607, -136.5231074845242745 ) ) ;
#53533=CARTESIAN_POINT ( 'NONE',  ( -20.94999999999999929, 74.26374286841466699, -124.9544551555068068 ) ) ;
#53537=EDGE_CURVE ( 'NONE', #246153, #174077, #172472, .T. ) ;
#53589=CARTESIAN_POINT ( 'NONE',  ( 20.94999999999999929, 65.52661458509918191, -128.9444530202758301 ) ) ;
#53595=VERTEX_POINT ( 'NONE', #121151 ) ;
#53605=VECTOR ( 'NONE', #171928, 1000.000000000000114 ) ;
#53614=AXIS2_PLACEMENT_3D ( 'NONE', #79787, #199787, #220615 ) ;
#53622=EDGE_LOOP ( 'NONE', ( #112919, #18869, #84247, #15302 ) ) ;
#53626=CIRCLE ( 'NONE', #249264, 0.1999999999999987899 ) ;
#53651=CARTESIAN_POINT ( 'NONE',  ( 21.05000000000000071, 76.00000000001188027, -98.92310748452429436 ) ) ;
#53693=CARTESIAN_POINT ( 'NONE',  ( 19.58285714285715073, 65.61500148966067059, -128.8934228171344216 ) ) ;
#53709=AXIS2_PLACEMENT_3D ( 'NONE', #39327, #19757, #120164 ) ;
#53722=CARTESIAN_POINT ( 'NONE',  ( 20.95566103547454517, 65.38175234906502453, -128.8912672915437554 ) ) ;
#53734=CARTESIAN_POINT ( 'NONE',  ( 22.39999999999999503, 76.00000000001222134, -148.1726782920690937 ) ) ;
#53763=AXIS2_PLACEMENT_3D ( 'NONE', #55620, #189716, #30669 ) ;
#53779=CIRCLE ( 'NONE', #241237, 0.1000000000000028644 ) ;
#53787=EDGE_CURVE ( 'NONE', #155470, #13808, #34239, .T. ) ;
#53789=CIRCLE ( 'NONE', #8020, 0.1000000000000028644 ) ;
#53806=ORIENTED_EDGE ( 'NONE', *, *, #70850, .T. ) ;
#53807=CARTESIAN_POINT ( 'NONE',  ( -21.05000000000000071, 74.73821383144705521, -128.4366085209788366 ) ) ;
#53812=CYLINDRICAL_SURFACE ( 'NONE', #206259, 0.09999999999999939493 ) ;
#53836=EDGE_CURVE ( 'NONE', #9803, #226695, #10161, .T. ) ;
#53853=DIRECTION ( 'NONE',  ( -1.000000000000000000, -0.000000000000000000, -0.000000000000000000 ) ) ;
#53858=DIRECTION ( 'NONE',  ( 2.715809747126117987E-16, 1.000000000000000000, 5.431619494252235382E-15 ) ) ;
#53864=AXIS2_PLACEMENT_3D ( 'NONE', #200410, #60885, #41364 ) ;
#53870=ADVANCED_FACE ( 'NONE', ( #152260 ), #175699, .T. ) ;
#53884=CARTESIAN_POINT ( 'NONE',  ( -21.05000000000000071, 76.00000000001213607, -136.5231074845242745 ) ) ;
#53943=ORIENTED_EDGE ( 'NONE', *, *, #88253, .T. ) ;
#53957=ADVANCED_FACE ( 'NONE', ( #37438 ), #158682, .F. ) ;
#53960=CIRCLE ( 'NONE', #49866, 0.1000000000000028644 ) ;
#53985=ORIENTED_EDGE ( 'NONE', *, *, #70947, .T. ) ;
#54007=VERTEX_POINT ( 'NONE', #80361 ) ;
#54008=ADVANCED_FACE ( 'NONE', ( #137782 ), #200989, .T. ) ;
#54011=CIRCLE ( 'NONE', #29119, 0.09999999999998898659 ) ;
#54034=DIRECTION ( 'NONE',  ( 0.000000000000000000, 0.000000000000000000, 1.000000000000000000 ) ) ;
#54151=SPHERICAL_SURFACE ( 'NONE', #67280, 0.1000000000000000056 ) ;
#54159=AXIS2_PLACEMENT_3D ( 'NONE', #200006, #237841, #201276 ) ;
#54188=DIRECTION ( 'NONE',  ( 1.000000000000000000, 0.000000000000000000, 0.000000000000000000 ) ) ;
#54212=CARTESIAN_POINT ( 'NONE',  ( 21.07928932188134397, 75.90110485435778287, -142.8516241409176075 ) ) ;
#54247=VECTOR ( 'NONE', #832, 1000.000000000000000 ) ;
#54263=VERTEX_POINT ( 'NONE', #209315 ) ;
#54276=ORIENTED_EDGE ( 'NONE', *, *, #167696, .F. ) ;
#54308=AXIS2_PLACEMENT_3D ( 'NONE', #247255, #146863, #226398 ) ;
#54323=FACE_OUTER_BOUND ( 'NONE', #156992, .T. ) ;
#54325=DIRECTION ( 'NONE',  ( 0.000000000000000000, 0.000000000000000000, 1.000000000000000000 ) ) ;
#54349=CARTESIAN_POINT ( 'NONE',  ( -23.15000000000000213, 87.65000000001192859, -106.1231074845242262 ) ) ;
#54445=DIRECTION ( 'NONE',  ( 1.000000000000000000, 0.000000000000000000, 0.000000000000000000 ) ) ;
#54458=CARTESIAN_POINT ( 'NONE',  ( 21.14999999999999503, 64.35000000001213039, -136.4231074845243938 ) ) ;
#54502=FACE_OUTER_BOUND ( 'NONE', #245452, .T. ) ;
#54513=DIRECTION ( 'NONE',  ( 0.000000000000000000, 0.8777080977375072424, -0.4791956752371691608 ) ) ;
#54516=CIRCLE ( 'NONE', #221093, 0.09999999999998898659 ) ;
#54530=ORIENTED_EDGE ( 'NONE', *, *, #129486, .F. ) ;
#54548=CARTESIAN_POINT ( 'NONE',  ( 23.15000000000000213, 87.39257802171759693, -106.0970570643561501 ) ) ;
#54581=LINE ( 'NONE', #214944, #157457 ) ;
#54603=FACE_OUTER_BOUND ( 'NONE', #68779, .T. ) ;
#54618=CIRCLE ( 'NONE', #133727, 12.77499999999999503 ) ;
#54644=DIRECTION ( 'NONE',  ( 0.000000000000000000, 6.982962677686266711E-15, -1.000000000000000000 ) ) ;
#54647=ORIENTED_EDGE ( 'NONE', *, *, #156357, .F. ) ;
#54668=ORIENTED_EDGE ( 'NONE', *, *, #94979, .F. ) ;
#54684=CARTESIAN_POINT ( 'NONE',  ( 18.31572054635706692, 85.54847543579089120, -96.17253731977575626 ) ) ;
#54697=EDGE_LOOP ( 'NONE', ( #2441, #51848, #75686 ) ) ;
#54739=FACE_OUTER_BOUND ( 'NONE', #135748, .T. ) ;
#54747=SPHERICAL_SURFACE ( 'NONE', #99731, 0.1000000000000000056 ) ;
#54784=EDGE_LOOP ( 'NONE', ( #53464, #236034, #240046, #237775 ) ) ;
#54789=VERTEX_POINT ( 'NONE', #137181 ) ;
#54812=CARTESIAN_POINT ( 'NONE',  ( 19.94784844284961167, 64.28691006698306865, -111.8209087672259017 ) ) ;
#54826=CARTESIAN_POINT ( 'NONE',  ( 21.05000000000000071, 84.66355140188123585, -126.9990063664569391 ) ) ;
#54844=ORIENTED_EDGE ( 'NONE', *, *, #169067, .T. ) ;
#54854=DIRECTION ( 'NONE',  ( 0.000000000000000000, 0.000000000000000000, 1.000000000000000000 ) ) ;
#54858=ORIENTED_EDGE ( 'NONE', *, *, #250346, .F. ) ;
#54870=AXIS2_PLACEMENT_3D ( 'NONE', #220711, #117753, #98155 ) ;
#54898=CARTESIAN_POINT ( 'NONE',  ( 20.94999999999999929, 85.40000000001198543, -112.9170766071766820 ) ) ;
#54906=ORIENTED_EDGE ( 'NONE', *, *, #180695, .T. ) ;
#54959=EDGE_CURVE ( 'NONE', #252010, #86370, #138762, .T. ) ;
#54983=CARTESIAN_POINT ( 'NONE',  ( 20.95462737510932882, 65.44321804836833678, -128.9531574279620827 ) ) ;
#54998=VERTEX_POINT ( 'NONE', #125334 ) ;
#55024=ORIENTED_EDGE ( 'NONE', *, *, #138206, .F. ) ;
#55074=CIRCLE ( 'NONE', #125819, 0.5000000000000004441 ) ;
#55108=CARTESIAN_POINT ( 'NONE',  ( 23.14999999999999503, 69.45000000001205365, -124.1731074845243370 ) ) ;
#55144=EDGE_CURVE ( 'NONE', #230388, #201537, #214013, .T. ) ;
#55180=LINE ( 'NONE', #192183, #222367 ) ;
#55202=ORIENTED_EDGE ( 'NONE', *, *, #196561, .F. ) ;
#55243=CARTESIAN_POINT ( 'NONE',  ( 20.85000000000000142, 76.00000000001185185, -95.22310748452429152 ) ) ;
#55252=ORIENTED_EDGE ( 'NONE', *, *, #129528, .T. ) ;
#55329=VERTEX_POINT ( 'NONE', #112837 ) ;
#55334=EDGE_LOOP ( 'NONE', ( #1150, #168768, #207649, #246265 ) ) ;
#55340=ORIENTED_EDGE ( 'NONE', *, *, #198327, .T. ) ;
#55414=EDGE_LOOP ( 'NONE', ( #3723, #121756, #20041, #100615, #52051 ) ) ;
#55415=ADVANCED_FACE ( 'NONE', ( #72446 ), #114107, .T. ) ;
#55427=DIRECTION ( 'NONE',  ( 1.000000000000000000, 0.000000000000000000, 0.000000000000000000 ) ) ;
#55437=ORIENTED_EDGE ( 'NONE', *, *, #246905, .T. ) ;
#55513=CARTESIAN_POINT ( 'NONE',  ( 21.05000000000000071, 85.40000000001207070, -126.6291383618717816 ) ) ;
#55524=CIRCLE ( 'NONE', #201879, 0.09999999999999939493 ) ;
#55548=DIRECTION ( 'NONE',  ( 1.000000000000000000, 0.000000000000000000, 0.000000000000000000 ) ) ;
#55552=CARTESIAN_POINT ( 'NONE',  ( 23.15000000000000213, 84.66355140188123585, -126.9990063664569391 ) ) ;
#55556=EDGE_LOOP ( 'NONE', ( #65204, #255478, #182061, #231073 ) ) ;
#55561=ORIENTED_EDGE ( 'NONE', *, *, #47788, .F. ) ;
#55620=CARTESIAN_POINT ( 'NONE',  ( 20.94999999999999929, 76.00000000001190870, -103.0231074845243029 ) ) ;
#55627=DIRECTION ( 'NONE',  ( 0.000000000000000000, 0.000000000000000000, 1.000000000000000000 ) ) ;
#55640=CARTESIAN_POINT ( 'NONE',  ( -23.25000000000000000, 87.75000000001213607, -136.5231074845242176 ) ) ;
#55649=ORIENTED_EDGE ( 'NONE', *, *, #90077, .T. ) ;
#55650=AXIS2_PLACEMENT_3D ( 'NONE', #114237, #212071, #13861 ) ;
#55664=DIRECTION ( 'NONE',  ( -0.000000000000000000, 1.000000000000000000, 6.982962677686266711E-15 ) ) ;
#55718=EDGE_CURVE ( 'NONE', #26810, #240054, #72760, .T. ) ;
#55761=EDGE_LOOP ( 'NONE', ( #189370, #242203, #235291, #215795 ) ) ;
#55779=DIRECTION ( 'NONE',  ( 0.7070776581709139474, 0.7071359030027652981, 2.946958787807621248E-14 ) ) ;
#55781=CARTESIAN_POINT ( 'NONE',  ( 21.13461538461538680, 67.11458296203758778, -124.1731074845243512 ) ) ;
#55798=ORIENTED_EDGE ( 'NONE', *, *, #166904, .F. ) ;
#55808=FACE_OUTER_BOUND ( 'NONE', #13252, .T. ) ;
#55819=DIRECTION ( 'NONE',  ( -1.000000000000000000, -0.000000000000000000, -0.000000000000000000 ) ) ;
#55845=DIRECTION ( 'NONE',  ( -0.000000000000000000, -6.982962677686266711E-15, 1.000000000000000000 ) ) ;
#55849=AXIS2_PLACEMENT_3D ( 'NONE', #210827, #111729, #171735 ) ;
#55885=DIRECTION ( 'NONE',  ( 1.000000000000000000, 0.000000000000000000, 0.000000000000000000 ) ) ;
#55899=CARTESIAN_POINT ( 'NONE',  ( 20.94999999999999929, 85.40000000001207070, -126.6291383618717816 ) ) ;
#55929=ORIENTED_EDGE ( 'NONE', *, *, #132784, .F. ) ;
#55940=CARTESIAN_POINT ( 'NONE',  ( 22.50000000000000000, 68.25000000001213607, -136.6231074845243540 ) ) ;
#55948=CARTESIAN_POINT ( 'NONE',  ( 18.50000000000000355, 85.40000000001185754, -96.14106563635154146 ) ) ;
#55961=ORIENTED_EDGE ( 'NONE', *, *, #218509, .T. ) ;
#55969=DIRECTION ( 'NONE',  ( 0.000000000000000000, 0.000000000000000000, 1.000000000000000000 ) ) ;
#55973=ADVANCED_FACE ( 'NONE', ( #43274 ), #85968, .T. ) ;
#55977=ORIENTED_EDGE ( 'NONE', *, *, #151863, .F. ) ;
#55984=DIRECTION ( 'NONE',  ( 0.000000000000000000, 6.982962677686266711E-15, -1.000000000000000000 ) ) ;
#56000=DIRECTION ( 'NONE',  ( 1.000000000000000000, 0.000000000000000000, 0.000000000000000000 ) ) ;
#56098=CIRCLE ( 'NONE', #160203, 0.09999999999999520384 ) ;
#56138=ADVANCED_FACE ( 'NONE', ( #215179 ), #176084, .F. ) ;
#56140=ORIENTED_EDGE ( 'NONE', *, *, #228080, .T. ) ;
#56175=( BOUNDED_SURFACE ( )  B_SPLINE_SURFACE ( 3, 2, ( 
 ( #242897, #61698, #142500 ),
 ( #65540, #224611, #125523 ),
 ( #141235, #105930, #90223 ),
 ( #49832, #9414, #68120 ),
 ( #169829, #91536, #27745 ),
 ( #129373, #225870, #147653 ) ),
 .UNSPECIFIED., .F., .F., .F. ) 
 B_SPLINE_SURFACE_WITH_KNOTS ( ( 4, 2, 4 ),
 ( 3, 3 ),
 ( 3.141592653589783346, 3.926990816987233845, 4.712388980384684345 ),
 ( 0.000000000000000000, 1.000000000000000000 ),
 .UNSPECIFIED. ) 
 GEOMETRIC_REPRESENTATION_ITEM ( )  RATIONAL_B_SPLINE_SURFACE ( (
 ( 1.000000000000000000, 0.9238795325112774126, 1.000000000000000000),
 ( 1.000000000000000000, 0.9240297172243541191, 1.000000000000000000),
 ( 1.000000000000000000, 0.9038128468039285934, 1.000000000000000000),
 ( 1.000000000000000000, 0.8282379607649370534, 1.000000000000000000),
 ( 1.000000000000000000, 0.7727932973491273838, 1.000000000000000000),
 ( 1.000000000000000000, 0.7071067811865475727, 1.000000000000000000) ) ) 
 REPRESENTATION_ITEM ( '' )  SURFACE ( )  );
#56178=ORIENTED_EDGE ( 'NONE', *, *, #7300, .T. ) ;
#56191=EDGE_LOOP ( 'NONE', ( #153050, #69142, #20040 ) ) ;
#56206=VERTEX_POINT ( 'NONE', #153974 ) ;
#56212=ORIENTED_EDGE ( 'NONE', *, *, #42057, .F. ) ;
#56220=VECTOR ( 'NONE', #62640, 1000.000000000000000 ) ;
#56227=CARTESIAN_POINT ( 'NONE',  ( 20.94999999999999929, 64.35000000001190301, -103.0231074845243882 ) ) ;
#56239=ORIENTED_EDGE ( 'NONE', *, *, #132397, .F. ) ;
#56242=DIRECTION ( 'NONE',  ( 0.000000000000000000, -1.000000000000000000, -6.982962677686265922E-15 ) ) ;
#56263=ORIENTED_EDGE ( 'NONE', *, *, #60846, .T. ) ;
#56278=CARTESIAN_POINT ( 'NONE',  ( -23.15000000000000213, 64.35000000001214460, -136.5231074845243597 ) ) ;
#56284=CARTESIAN_POINT ( 'NONE',  ( 21.05000000000000071, 64.35000000001214460, -136.4231074845243938 ) ) ;
#56302=ORIENTED_EDGE ( 'NONE', *, *, #164322, .T. ) ;
#56314=CARTESIAN_POINT ( 'NONE',  ( 21.14999999999999858, 75.90220970870339556, -142.7809220950004203 ) ) ;
#56323=DIRECTION ( 'NONE',  ( 1.000000000000000000, 0.000000000000000000, 0.000000000000000000 ) ) ;
#56392=ORIENTED_EDGE ( 'NONE', *, *, #119424, .F. ) ;
#56432=ORIENTED_EDGE ( 'NONE', *, *, #105227, .T. ) ;
#56437=ORIENTED_EDGE ( 'NONE', *, *, #207806, .F. ) ;
#56450=DIRECTION ( 'NONE',  ( 0.000000000000000000, -7.116814260417668513E-15, 1.000000000000000000 ) ) ;
#56454=EDGE_CURVE ( 'NONE', #114896, #33295, #2152, .T. ) ;
#56455=FACE_OUTER_BOUND ( 'NONE', #172999, .T. ) ;
#56459=CARTESIAN_POINT ( 'NONE',  ( 23.14999999999999858, 76.00000000001190870, -103.0231074845243029 ) ) ;
#56461=B_SPLINE_CURVE_WITH_KNOTS ( 'NONE', 3,
 ( #181893, #243139, #43666, #85325, #162344, #164897, #61945, #120653, #1942, #141470 ),
 .UNSPECIFIED., .F., .F.,
 ( 4, 2, 2, 2, 4 ),
 ( 0.000000000000000000, 3.990160268013063079E-05, 7.980320536026126157E-05, 0.0001596064107205095669, 0.0003192128214409942514 ),
 .UNSPECIFIED. ) ;
#56483=DIRECTION ( 'NONE',  ( 0.000000000000000000, -1.000000000000000000, -6.982962677686265922E-15 ) ) ;
#56552=CIRCLE ( 'NONE', #69264, 0.1000000000000028644 ) ;
#56557=EDGE_CURVE ( 'NONE', #188914, #238533, #177356, .T. ) ;
#56596=CARTESIAN_POINT ( 'NONE',  ( -18.44232395690051618, 85.55228255706090579, -96.18085549971709725 ) ) ;
#56603=DIRECTION ( 'NONE',  ( 4.408576920032446739E-17, 0.1350103645451945777, -0.9908441862701590219 ) ) ;
#56609=DIRECTION ( 'NONE',  ( -1.836970198721029934E-16, -1.000000000000000000, -6.982962677686266711E-15 ) ) ;
#56619=VERTEX_POINT ( 'NONE', #179114 ) ;
#56636=CARTESIAN_POINT ( 'NONE',  ( 21.04999999999999716, 76.01454569058356014, -143.0201252709570667 ) ) ;
#56639=CARTESIAN_POINT ( 'NONE',  ( 22.50497660315936699, 76.07871793023775808, -148.2729029894197197 ) ) ;
#56659=CARTESIAN_POINT ( 'NONE',  ( -20.54999999999999716, 76.00000000001199396, -115.8981074845243029 ) ) ;
#56691=CIRCLE ( 'NONE', #44271, 4.049999999999998046 ) ;
#56736=CARTESIAN_POINT ( 'NONE',  ( -20.64999999999999858, 68.75000000001205080, -124.1731074845243370 ) ) ;
#56772=LINE ( 'NONE', #193755, #163592 ) ;
#56775=DIRECTION ( 'NONE',  ( 3.265361837132813093E-16, 1.000000000000000000, 6.982962677686266711E-15 ) ) ;
#56777=AXIS2_PLACEMENT_3D ( 'NONE', #195159, #196403, #138968 ) ;
#56781=CARTESIAN_POINT ( 'NONE',  ( -21.05000000000000071, 76.00000000001193712, -107.0231074845243029 ) ) ;
#56789=VERTEX_POINT ( 'NONE', #55899 ) ;
#56872=EDGE_CURVE ( 'NONE', #126698, #93991, #139881, .T. ) ;
#56875=ORIENTED_EDGE ( 'NONE', *, *, #86116, .T. ) ;
#56896=LINE ( 'NONE', #79031, #112951 ) ;
#56897=CARTESIAN_POINT ( 'NONE',  ( -20.94999999999999929, 87.48912529308817909, -133.4231074845242233 ) ) ;
#56906=CARTESIAN_POINT ( 'NONE',  ( -18.50000000000000000, 77.36242903720516040, -95.13422623660308375 ) ) ;
#56922=ORIENTED_EDGE ( 'NONE', *, *, #624, .F. ) ;
#56927=ORIENTED_EDGE ( 'NONE', *, *, #105832, .T. ) ;
#56943=CARTESIAN_POINT ( 'NONE',  ( -22.39999999999999858, 75.90000000001219860, -144.3138870828977076 ) ) ;
#56953=VERTEX_POINT ( 'NONE', #1059 ) ;
#56965=VERTEX_POINT ( 'NONE', #42786 ) ;
#56980=DIRECTION ( 'NONE',  ( 1.000000000000000000, 0.000000000000000000, 0.000000000000000000 ) ) ;
#57002=FACE_OUTER_BOUND ( 'NONE', #118403, .T. ) ;
#57003=AXIS2_PLACEMENT_3D ( 'NONE', #161881, #82284, #103144 ) ;
#57035=EDGE_CURVE ( 'NONE', #207360, #18233, #8796, .T. ) ;
#57059=DIRECTION ( 'NONE',  ( -0.9880948137434723000, -0.1538461538461483591, -1.074301950413233512E-15 ) ) ;
#57062=ORIENTED_EDGE ( 'NONE', *, *, #112133, .F. ) ;
#57094=FACE_BOUND ( 'NONE', #224891, .T. ) ;
#57112=VERTEX_POINT ( 'NONE', #87016 ) ;
#57150=DIRECTION ( 'NONE',  ( -1.000000000000000000, -0.000000000000000000, -0.000000000000000000 ) ) ;
#57180=DIRECTION ( 'NONE',  ( -1.000000000000000000, -0.000000000000000000, -0.000000000000000000 ) ) ;
#57216=DIRECTION ( 'NONE',  ( 1.000000000000000000, 0.000000000000000000, 0.000000000000000000 ) ) ;
#57224=DIRECTION ( 'NONE',  ( 1.000000000000000000, 0.000000000000000000, 0.000000000000000000 ) ) ;
#57230=ORIENTED_EDGE ( 'NONE', *, *, #154202, .F. ) ;
#57235=ORIENTED_EDGE ( 'NONE', *, *, #178725, .F. ) ;
#57237=AXIS2_PLACEMENT_3D ( 'NONE', #46725, #164133, #125007 ) ;
#57242=DIRECTION ( 'NONE',  ( -1.000000000000000000, 0.000000000000000000, -0.000000000000000000 ) ) ;
#57246=CARTESIAN_POINT ( 'NONE',  ( 18.59999999999999787, 76.00000000001213607, -136.5231074845242745 ) ) ;
#57252=DIRECTION ( 'NONE',  ( 0.000000000000000000, 0.9908441862701791170, -0.1350103645450472789 ) ) ;
#57266=DIRECTION ( 'NONE',  ( -1.000000000000000000, -0.000000000000000000, -0.000000000000000000 ) ) ;
#57275=ORIENTED_EDGE ( 'NONE', *, *, #65245, .F. ) ;
#57276=ORIENTED_EDGE ( 'NONE', *, *, #131840, .T. ) ;
#57279=DIRECTION ( 'NONE',  ( 0.000000000000000000, 1.000000000000000000, 0.000000000000000000 ) ) ;
#57286=AXIS2_PLACEMENT_3D ( 'NONE', #197642, #138920, #99802 ) ;
#57323=DIRECTION ( 'NONE',  ( 0.000000000000000000, -1.000000000000000000, -6.982962677686266711E-15 ) ) ;
#57324=FACE_OUTER_BOUND ( 'NONE', #10407, .T. ) ;
#57325=CARTESIAN_POINT ( 'NONE',  ( 20.94999999999999929, 65.27628289530447603, -115.2731074845243739 ) ) ;
#57355=EDGE_CURVE ( 'NONE', #152046, #107540, #219182, .T. ) ;
#57358=DIRECTION ( 'NONE',  ( 1.000000000000000000, 0.000000000000000000, 0.000000000000000000 ) ) ;
#57368=DIRECTION ( 'NONE',  ( 0.000000000000000000, -0.9908441862701610203, 0.1350103645451807555 ) ) ;
#57396=DIRECTION ( 'NONE',  ( 1.000000000000000000, -2.952720810173289112E-16, -2.061873921506763405E-30 ) ) ;
#57423=EDGE_CURVE ( 'NONE', #155438, #161400, #102637, .T. ) ;
#57424=DIRECTION ( 'NONE',  ( 0.000000000000000000, -7.056502275159890832E-15, 1.000000000000000000 ) ) ;
#57432=VECTOR ( 'NONE', #4723, 1000.000000000000000 ) ;
#57446=LINE ( 'NONE', #99134, #144566 ) ;
#57485=AXIS2_PLACEMENT_3D ( 'NONE', #256204, #75108, #154643 ) ;
#57486=ORIENTED_EDGE ( 'NONE', *, *, #222303, .F. ) ;
#57494=ORIENTED_EDGE ( 'NONE', *, *, #34455, .F. ) ;
#57506=CYLINDRICAL_SURFACE ( 'NONE', #172192, 0.09999999999999939493 ) ;
#57517=VERTEX_POINT ( 'NONE', #7180 ) ;
#57526=VECTOR ( 'NONE', #8111, 1000.000000000000000 ) ;
#57527=AXIS2_PLACEMENT_3D ( 'NONE', #142631, #107369, #145207 ) ;
#57545=ADVANCED_FACE ( 'NONE', ( #29376 ), #52598, .F. ) ;
#57557=ORIENTED_EDGE ( 'NONE', *, *, #178552, .F. ) ;
#57558=CIRCLE ( 'NONE', #236629, 0.1000000000000043771 ) ;
#57569=CARTESIAN_POINT ( 'NONE',  ( 22.41477678272288188, 75.99917613424928220, -148.1726927690397133 ) ) ;
#57606=CARTESIAN_POINT ( 'NONE',  ( 20.94999999999999574, 77.83534155023646406, -124.8679561919613121 ) ) ;
#57608=EDGE_CURVE ( 'NONE', #146363, #118755, #165992, .T. ) ;
#57630=DIRECTION ( 'NONE',  ( 0.000000000000000000, 1.000000000000000000, 7.272083257015735086E-15 ) ) ;
#57631=VERTEX_POINT ( 'NONE', #31928 ) ;
#57639=DIRECTION ( 'NONE',  ( 1.000000000000000000, 0.000000000000000000, 0.000000000000000000 ) ) ;
#57688=CYLINDRICAL_SURFACE ( 'NONE', #165853, 12.87499999999999822 ) ;
#57689=CARTESIAN_POINT ( 'NONE',  ( -18.39999999999999858, 85.68240343348826116, -96.36626410711143365 ) ) ;
#57706=DIRECTION ( 'NONE',  ( -1.000000000000000000, 0.000000000000000000, 0.000000000000000000 ) ) ;
#57730=CARTESIAN_POINT ( 'NONE',  ( 18.59999999999999076, 69.35000000001200249, -115.3731074845243398 ) ) ;
#57744=CARTESIAN_POINT ( 'NONE',  ( 20.94999999999999929, 64.36312671090750825, -109.8448666978492270 ) ) ;
#57773=CARTESIAN_POINT ( 'NONE',  ( -18.58693740092131108, 85.40643215026497614, -129.3982910280227543 ) ) ;
#57808=CARTESIAN_POINT ( 'NONE',  ( 18.40000000000000213, 85.51932773110452501, -129.5501311079648872 ) ) ;
#57850=VERTEX_POINT ( 'NONE', #203809 ) ;
#57856=CIRCLE ( 'NONE', #149675, 0.09999999999999939493 ) ;
#57886=EDGE_CURVE ( 'NONE', #182465, #242065, #185538, .T. ) ;
#57896=DIRECTION ( 'NONE',  ( -0.000000000000000000, 6.982962677686266711E-15, -1.000000000000000000 ) ) ;
#57944=ADVANCED_FACE ( 'NONE', ( #171159 ), #32929, .F. ) ;
#57965=AXIS2_PLACEMENT_3D ( 'NONE', #152868, #232390, #133268 ) ;
#57979=DIRECTION ( 'NONE',  ( 0.000000000000000000, 1.000000000000000000, 6.982962677686266711E-15 ) ) ;
#57995=AXIS2_PLACEMENT_3D ( 'NONE', #75898, #251958, #96706 ) ;
#57996=ORIENTED_EDGE ( 'NONE', *, *, #85520, .T. ) ;
#58001=VERTEX_POINT ( 'NONE', #73329 ) ;
#58028=CIRCLE ( 'NONE', #124701, 0.09999999999999938105 ) ;
#58033=DIRECTION ( 'NONE',  ( 0.000000000000000000, 0.000000000000000000, 1.000000000000000000 ) ) ;
#58057=LINE ( 'NONE', #41113, #94807 ) ;
#58084=ORIENTED_EDGE ( 'NONE', *, *, #81939, .T. ) ;
#58095=EDGE_CURVE ( 'NONE', #173897, #172048, #218989, .T. ) ;
#58109=ORIENTED_EDGE ( 'NONE', *, *, #176439, .T. ) ;
#58122=TOROIDAL_SURFACE ( 'NONE', #133177, 11.65000000000000036, 0.1000000000000000056 ) ;
#58142=VECTOR ( 'NONE', #120608, 1000.000000000000114 ) ;
#58169=VECTOR ( 'NONE', #187859, 1000.000000000000000 ) ;
#58171=ORIENTED_EDGE ( 'NONE', *, *, #24580, .F. ) ;
#58192=CARTESIAN_POINT ( 'NONE',  ( 22.39999999999999503, 75.90000000001219860, -144.3138870828976792 ) ) ;
#58196=AXIS2_PLACEMENT_3D ( 'NONE', #112462, #32953, #210275 ) ;
#58206=LINE ( 'NONE', #21679, #206092 ) ;
#58209=VERTEX_POINT ( 'NONE', #176274 ) ;
#58241=AXIS2_PLACEMENT_3D ( 'NONE', #216701, #95467, #156761 ) ;
#58260=ORIENTED_EDGE ( 'NONE', *, *, #208727, .F. ) ;
#58265=ORIENTED_EDGE ( 'NONE', *, *, #63923, .T. ) ;
#58287=CARTESIAN_POINT ( 'NONE',  ( 21.08489247129321242, 67.12232480914198618, -124.1731074845243654 ) ) ;
#58348=DIRECTION ( 'NONE',  ( 0.000000000000000000, -6.982962677686266711E-15, 1.000000000000000000 ) ) ;
#58356=CARTESIAN_POINT ( 'NONE',  ( 21.04105312098505109, 67.12466737696844632, -124.1946007373119585 ) ) ;
#58366=ORIENTED_EDGE ( 'NONE', *, *, #54959, .F. ) ;
#58380=DIRECTION ( 'NONE',  ( 0.000000000000000000, 0.000000000000000000, -1.000000000000000000 ) ) ;
#58386=AXIS2_PLACEMENT_3D ( 'NONE', #181214, #126354, #186344 ) ;
#58387=ORIENTED_EDGE ( 'NONE', *, *, #71789, .F. ) ;
#58401=DIRECTION ( 'NONE',  ( -1.000000000000000000, 0.000000000000000000, 0.000000000000000000 ) ) ;
#58404=CARTESIAN_POINT ( 'NONE',  ( -20.94999999999999929, 76.00000000001190870, -103.0231074845243029 ) ) ;
#58426=EDGE_CURVE ( 'NONE', #231702, #47601, #235573, .T. ) ;
#58447=EDGE_CURVE ( 'NONE', #24249, #39149, #85874, .T. ) ;
#58453=DIRECTION ( 'NONE',  ( 1.000000000000000000, 0.000000000000000000, 0.000000000000000000 ) ) ;
#58468=DIRECTION ( 'NONE',  ( 0.000000000000000000, 6.982962677686266711E-15, -1.000000000000000000 ) ) ;
#58476=DIRECTION ( 'NONE',  ( 1.000000000000000000, 0.000000000000000000, 0.000000000000000000 ) ) ;
#58542=CIRCLE ( 'NONE', #8495, 11.80000000000000426 ) ;
#58549=ORIENTED_EDGE ( 'NONE', *, *, #119360, .T. ) ;
#58550=ORIENTED_EDGE ( 'NONE', *, *, #14435, .T. ) ;
#58556=AXIS2_PLACEMENT_3D ( 'NONE', #93279, #252345, #75044 ) ;
#58600=ORIENTED_EDGE ( 'NONE', *, *, #243122, .F. ) ;
#58606=CARTESIAN_POINT ( 'NONE',  ( -20.94999999999999929, 77.16412189325305349, -95.10825939895268277 ) ) ;
#58624=CARTESIAN_POINT ( 'NONE',  ( -22.48479450179659977, 75.95300841882533405, -148.1731059307759324 ) ) ;
#58671=DIRECTION ( 'NONE',  ( 0.000000000000000000, 0.000000000000000000, 1.000000000000000000 ) ) ;
#58678=DIRECTION ( 'NONE',  ( -1.000000000000000000, 0.000000000000000000, -0.000000000000000000 ) ) ;
#58698=DIRECTION ( 'NONE',  ( 1.000000000000000000, 0.000000000000000000, 0.000000000000000000 ) ) ;
#58710=ORIENTED_EDGE ( 'NONE', *, *, #249108, .F. ) ;
#58716=DIRECTION ( 'NONE',  ( -1.000000000000000000, -0.000000000000000000, -0.000000000000000000 ) ) ;
#58736=DIRECTION ( 'NONE',  ( 0.000000000000000000, 0.000000000000000000, 1.000000000000000000 ) ) ;
#58802=ORIENTED_EDGE ( 'NONE', *, *, #34323, .F. ) ;
#58813=AXIS2_PLACEMENT_3D ( 'NONE', #216249, #155039, #78026 ) ;
#58859=CARTESIAN_POINT ( 'NONE',  ( 20.94999999999999574, 77.16270174995010223, -128.4231074845242802 ) ) ;
#58882=AXIS2_PLACEMENT_3D ( 'NONE', #29330, #205333, #230059 ) ;
#58884=AXIS2_PLACEMENT_3D ( 'NONE', #203012, #24408, #103894 ) ;
#58906=DIRECTION ( 'NONE',  ( 0.000000000000000000, -6.982962677686266711E-15, 1.000000000000000000 ) ) ;
#58917=EDGE_LOOP ( 'NONE', ( #157509, #252853, #16875, #13193 ) ) ;
#58931=DIRECTION ( 'NONE',  ( 1.000000000000000000, 0.000000000000000000, 0.000000000000000000 ) ) ;
#58940=FACE_OUTER_BOUND ( 'NONE', #207884, .T. ) ;
#58945=DIRECTION ( 'NONE',  ( 0.000000000000000000, 0.9999631594459055250, 0.008583690987131395445 ) ) ;
#58949=EDGE_CURVE ( 'NONE', #224430, #70177, #5624, .T. ) ;
#58953=CARTESIAN_POINT ( 'NONE',  ( -18.50000000000000000, 65.70729864261004138, -97.56574559737242680 ) ) ;
#58957=CARTESIAN_POINT ( 'NONE',  ( -18.54270223418607699, 85.62410550289477840, -96.28217243411681636 ) ) ;
#58976=DIRECTION ( 'NONE',  ( 1.000000000000000000, 0.000000000000000000, 0.000000000000000000 ) ) ;
#58993=LINE ( 'NONE', #81138, #129950 ) ;
#58994=DIRECTION ( 'NONE',  ( 1.000000000000000000, 0.000000000000000000, 0.000000000000000000 ) ) ;
#58998=DIRECTION ( 'NONE',  ( 1.000000000000000000, -2.952720810173289112E-16, -2.061873921506763405E-30 ) ) ;
#59028=ADVANCED_FACE ( 'NONE', ( #26520 ), #65619, .T. ) ;
#59038=EDGE_CURVE ( 'NONE', #23492, #94251, #98501, .T. ) ;
#59061=ORIENTED_EDGE ( 'NONE', *, *, #52727, .T. ) ;
#59064=VERTEX_POINT ( 'NONE', #49913 ) ;
#59103=ORIENTED_EDGE ( 'NONE', *, *, #154802, .T. ) ;
#59129=CARTESIAN_POINT ( 'NONE',  ( -23.15000000000000213, 73.40000000001222702, -148.2731074845243313 ) ) ;
#59152=ORIENTED_EDGE ( 'NONE', *, *, #43926, .T. ) ;
#59156=CARTESIAN_POINT ( 'NONE',  ( -20.94999999999999574, 64.37928932189329601, -109.8915241368653284 ) ) ;
#59159=CARTESIAN_POINT ( 'NONE',  ( -18.50000000000000000, 85.42129027953527043, -96.19922530549789030 ) ) ;
#59183=EDGE_CURVE ( 'NONE', #8870, #229103, #179282, .T. ) ;
#59197=CARTESIAN_POINT ( 'NONE',  ( -23.15000000000000213, 87.48912529308798014, -106.1231074845242262 ) ) ;
#59198=CARTESIAN_POINT ( 'NONE',  ( 21.05000000000000071, 76.02138556595014052, -142.8280685972092954 ) ) ;
#59250=B_SPLINE_CURVE_WITH_KNOTS ( 'NONE', 3,
 ( #201958, #162845, #64998, #39044, #41618, #24629 ),
 .UNSPECIFIED., .F., .F.,
 ( 4, 2, 4 ),
 ( 0.000000000000000000, 0.0001895189928937444739, 0.0003790379857874889478 ),
 .UNSPECIFIED. ) ;
#59372=EDGE_LOOP ( 'NONE', ( #196440, #78440, #74436, #43124 ) ) ;
#59374=CARTESIAN_POINT ( 'NONE',  ( 20.04142135623730070, 64.25000000001196554, -111.8731074845243825 ) ) ;
#59385=CARTESIAN_POINT ( 'NONE',  ( 23.25000000000000000, 87.48912529308798014, -106.1231074845242262 ) ) ;
#59412=ORIENTED_EDGE ( 'NONE', *, *, #236828, .F. ) ;
#59427=FACE_OUTER_BOUND ( 'NONE', #132002, .T. ) ;
#59439=VERTEX_POINT ( 'NONE', #211265 ) ;
#59538=ORIENTED_EDGE ( 'NONE', *, *, #33799, .T. ) ;
#59543=CARTESIAN_POINT ( 'NONE',  ( -20.94999999999999929, 76.00000000001190870, -103.0231074845243029 ) ) ;
#59578=DIRECTION ( 'NONE',  ( 1.000000000000000000, 0.000000000000000000, 0.000000000000000000 ) ) ;
#59632=TOROIDAL_SURFACE ( 'NONE', #130583, 0.6000000000000013101, 0.1000000000000000056 ) ;
#59638=EDGE_CURVE ( 'NONE', #216543, #201537, #16957, .T. ) ;
#59671=EDGE_LOOP ( 'NONE', ( #87670, #237479, #233538, #236491 ) ) ;
#59678=CARTESIAN_POINT ( 'NONE',  ( -22.50000000000000000, 64.35023708198022518, -136.6119174609113145 ) ) ;
#59731=ORIENTED_EDGE ( 'NONE', *, *, #242689, .F. ) ;
#59769=DIRECTION ( 'NONE',  ( 1.000000000000000000, 0.000000000000000000, 0.000000000000000000 ) ) ;
#59789=CARTESIAN_POINT ( 'NONE',  ( 23.25000000000000000, 87.65000000001214175, -136.5231074845242176 ) ) ;
#59817=DIRECTION ( 'NONE',  ( 2.827886303505249259E-16, 0.8660254037844377084, 0.5000000000000016653 ) ) ;
#59827=VERTEX_POINT ( 'NONE', #89707 ) ;
#59833=ADVANCED_FACE ( 'NONE', ( #191426 ), #50570, .T. ) ;
#59843=AXIS2_PLACEMENT_3D ( 'NONE', #88938, #87656, #244162 ) ;
#59847=CARTESIAN_POINT ( 'NONE',  ( 18.50000000000000000, 85.50000000001209344, -129.4910380878245633 ) ) ;
#59859=CARTESIAN_POINT ( 'NONE',  ( -22.42357213249529480, 75.90091303601063544, -144.1960398708842206 ) ) ;
#59870=AXIS2_PLACEMENT_3D ( 'NONE', #151511, #228471, #88923 ) ;
#59881=DIRECTION ( 'NONE',  ( 0.000000000000000000, -1.000000000000000000, -6.352154140967427193E-15 ) ) ;
#59909=EDGE_CURVE ( 'NONE', #119976, #21421, #239140, .T. ) ;
#59916=EDGE_CURVE ( 'NONE', #8334, #163587, #183538, .T. ) ;
#59919=LINE ( 'NONE', #161638, #15380 ) ;
#59947=EDGE_LOOP ( 'NONE', ( #89236, #140196, #161879 ) ) ;
#59952=AXIS2_PLACEMENT_3D ( 'NONE', #139273, #3624, #200554 ) ;
#59958=CARTESIAN_POINT ( 'NONE',  ( -23.25000000000000000, 76.00000000001216449, -140.5731074845242858 ) ) ;
#59967=CARTESIAN_POINT ( 'NONE',  ( 20.44999100639871514, 65.56028929680029194, -128.7640317585553476 ) ) ;
#59980=TOROIDAL_SURFACE ( 'NONE', #122361, 0.2000000000000000111, 0.1000000000000000056 ) ;
#60014=VERTEX_POINT ( 'NONE', #227477 ) ;
#60028=CARTESIAN_POINT ( 'NONE',  ( -18.59999999999999787, 77.83585931145546510, -91.51866831572576189 ) ) ;
#60103=ORIENTED_EDGE ( 'NONE', *, *, #79951, .F. ) ;
#60112=ORIENTED_EDGE ( 'NONE', *, *, #105378, .F. ) ;
#60146=ORIENTED_EDGE ( 'NONE', *, *, #21652, .T. ) ;
#60158=FILL_AREA_STYLE ('',( #120191 ) ) ;
#60205=EDGE_CURVE ( 'NONE', #105079, #131402, #96214, .T. ) ;
#60212=CARTESIAN_POINT ( 'NONE',  ( -18.59999999999999787, 64.35000000001222986, -148.2731074845243882 ) ) ;
#60219=EDGE_CURVE ( 'NONE', #62401, #235424, #158797, .T. ) ;
#60220=FACE_OUTER_BOUND ( 'NONE', #53622, .T. ) ;
#60245=CARTESIAN_POINT ( 'NONE',  ( -22.49999999999999645, 64.25043287652275126, -136.6239658536231332 ) ) ;
#60257=EDGE_CURVE ( 'NONE', #162766, #238178, #142015, .T. ) ;
#60268=ORIENTED_EDGE ( 'NONE', *, *, #73518, .T. ) ;
#60293=CIRCLE ( 'NONE', #164556, 0.5000000000000004441 ) ;
#60315=CARTESIAN_POINT ( 'NONE',  ( 21.05315837517336419, 64.24999999299804188, -109.8647514757571315 ) ) ;
#60345=DIRECTION ( 'NONE',  ( 1.000000000000000000, 0.000000000000000000, 0.000000000000000000 ) ) ;
#60377=ORIENTED_EDGE ( 'NONE', *, *, #177386, .T. ) ;
#60382=ORIENTED_EDGE ( 'NONE', *, *, #200956, .T. ) ;
#60396=DIRECTION ( 'NONE',  ( 0.000000000000000000, 6.982962677686266711E-15, -1.000000000000000000 ) ) ;
#60406=DIRECTION ( 'NONE',  ( -1.000000000000000000, 2.952720810173289112E-16, 2.061873921506763405E-30 ) ) ;
#60426=CIRCLE ( 'NONE', #135439, 0.09999999999999939493 ) ;
#60435=ADVANCED_FACE ( 'NONE', ( #243404 ), #42640, .T. ) ;
#60455=DIRECTION ( 'NONE',  ( 1.000000000000000000, 0.000000000000000000, 0.000000000000000000 ) ) ;
#60461=TOROIDAL_SURFACE ( 'NONE', #110548, 12.97499999999999609, 0.1000000000000000056 ) ;
#60468=CARTESIAN_POINT ( 'NONE',  ( -18.48179518609121885, 85.51832530050704406, -96.13340190776337124 ) ) ;
#60487=EDGE_LOOP ( 'NONE', ( #28412, #108540, #137071, #160553 ) ) ;
#60489=DIRECTION ( 'NONE',  ( 0.000000000000000000, 0.000000000000000000, -1.000000000000000000 ) ) ;
#60506=CARTESIAN_POINT ( 'NONE',  ( 21.11825140030062897, 75.99279637937912923, -142.9685150499435338 ) ) ;
#60533=ADVANCED_FACE ( 'NONE', ( #90738 ), #249835, .T. ) ;
#60543=CARTESIAN_POINT ( 'NONE',  ( -21.45000000000000284, 68.29142135624930177, -115.2731074845243455 ) ) ;
#60588=ORIENTED_EDGE ( 'NONE', *, *, #156013, .F. ) ;
#60607=AXIS2_PLACEMENT_3D ( 'NONE', #91444, #246646, #68021 ) ;
#60626=DIRECTION ( 'NONE',  ( 0.000000000000000000, 0.000000000000000000, 1.000000000000000000 ) ) ;
#60637=VERTEX_POINT ( 'NONE', #137564 ) ;
#60670=VERTEX_POINT ( 'NONE', #98411 ) ;
#60684=VERTEX_POINT ( 'NONE', #20220 ) ;
#60720=ADVANCED_FACE ( 'NONE', ( #138828 ), #237959, .T. ) ;
#60749=CARTESIAN_POINT ( 'NONE',  ( -20.94999999999999929, 76.00000000001188027, -98.92310748452429436 ) ) ;
#60841=CARTESIAN_POINT ( 'NONE',  ( -23.15000000000000213, 84.66355140188123585, -126.9990063664569391 ) ) ;
#60846=EDGE_CURVE ( 'NONE', #16570, #14025, #134176, .T. ) ;
#60872=FACE_OUTER_BOUND ( 'NONE', #89268, .T. ) ;
#60885=DIRECTION ( 'NONE',  ( -1.000000000000000000, 2.952720810173289112E-16, 2.061873921506763405E-30 ) ) ;
#60902=CARTESIAN_POINT ( 'NONE',  ( 23.14999999999999503, 64.35000000001195986, -110.0379132551783243 ) ) ;
#60927=EDGE_CURVE ( 'NONE', #107540, #74720, #129591, .T. ) ;
#60934=AXIS2_PLACEMENT_3D ( 'NONE', #64243, #216882, #117792 ) ;
#60939=DIRECTION ( 'NONE',  ( 0.000000000000000000, 0.000000000000000000, 1.000000000000000000 ) ) ;
#60941=DIRECTION ( 'NONE',  ( -3.265361837132813093E-16, -1.000000000000000000, 7.445645354460596589E-46 ) ) ;
#60944=PRODUCT_DEFINITION_CONTEXT ( 'detailed design', #197444, 'design' ) ;
#60960=ORIENTED_EDGE ( 'NONE', *, *, #233606, .F. ) ;
#60962=DIRECTION ( 'NONE',  ( -3.265361837132813093E-16, -1.000000000000000000, -6.982962677686266711E-15 ) ) ;
#60977=VERTEX_POINT ( 'NONE', #214262 ) ;
#60981=EDGE_CURVE ( 'NONE', #38706, #193905, #175910, .T. ) ;
#60990=ORIENTED_EDGE ( 'NONE', *, *, #10143, .F. ) ;
#60991=SPHERICAL_SURFACE ( 'NONE', #196528, 0.1000000000000000056 ) ;
#60995=VECTOR ( 'NONE', #106372, 1000.000000000000000 ) ;
#61013=VERTEX_POINT ( 'NONE', #93021 ) ;
#61045=VERTEX_POINT ( 'NONE', #13499 ) ;
#61062=AXIS2_PLACEMENT_3D ( 'NONE', #228764, #47520, #189632 ) ;
#61096=DIRECTION ( 'NONE',  ( 0.000000000000000000, 1.000000000000000000, 0.000000000000000000 ) ) ;
#61097=DIRECTION ( 'NONE',  ( 0.000000000000000000, -0.1575844902526687130, -0.9875055080513762684 ) ) ;
#61123=VECTOR ( 'NONE', #68405, 1000.000000000000114 ) ;
#61144=LINE ( 'NONE', #140679, #249624 ) ;
#61165=ORIENTED_EDGE ( 'NONE', *, *, #208727, .T. ) ;
#61166=DIRECTION ( 'NONE',  ( 0.000000000000000000, -7.086529944415894657E-15, 1.000000000000000000 ) ) ;
#61167=CARTESIAN_POINT ( 'NONE',  ( -20.00857864376270001, 66.85000000001200249, -115.2731074845243597 ) ) ;
#61172=FACE_OUTER_BOUND ( 'NONE', #100247, .T. ) ;
#61173=CARTESIAN_POINT ( 'NONE',  ( -20.94999999999999929, 61.95000000001210338, -131.0094124137634140 ) ) ;
#61179=AXIS2_PLACEMENT_3D ( 'NONE', #230647, #71586, #76348 ) ;
#61194=DIRECTION ( 'NONE',  ( 0.000000000000000000, 0.000000000000000000, -1.000000000000000000 ) ) ;
#61201=CARTESIAN_POINT ( 'NONE',  ( 21.05000000000000071, 87.39257802171759693, -106.0970570643561501 ) ) ;
#61241=EDGE_CURVE ( 'NONE', #21421, #5563, #71857, .T. ) ;
#61277=CARTESIAN_POINT ( 'NONE',  ( 20.84451136049623798, 65.37985808520379294, -129.0291829250029707 ) ) ;
#61305=CARTESIAN_POINT ( 'NONE',  ( 23.15000000000000213, 87.65000000001192859, -106.1231074845242262 ) ) ;
#61308=CARTESIAN_POINT ( 'NONE',  ( -20.94999999999999929, 76.00000000001193712, -107.0231074845243029 ) ) ;
#61324=VERTEX_POINT ( 'NONE', #170696 ) ;
#61326=CARTESIAN_POINT ( 'NONE',  ( -18.59999999999999787, 64.25000000001222134, -148.2731074845243882 ) ) ;
#61361=ORIENTED_EDGE ( 'NONE', *, *, #49123, .F. ) ;
#61367=EDGE_LOOP ( 'NONE', ( #151846, #142222, #196846, #44701 ) ) ;
#61375=ORIENTED_EDGE ( 'NONE', *, *, #23048, .F. ) ;
#61423=TOROIDAL_SURFACE ( 'NONE', #77975, 0.6000000000000017542, 0.1000000000000000056 ) ;
#61475=CARTESIAN_POINT ( 'NONE',  ( 20.04142135623730070, 64.25000000001220712, -148.2731074845243882 ) ) ;
#61481=CYLINDRICAL_SURFACE ( 'NONE', #75711, 0.1000000000000028644 ) ;
#61484=DIRECTION ( 'NONE',  ( 0.7071067811865127117, 0.7071067811865821007, 0.000000000000000000 ) ) ;
#61512=CARTESIAN_POINT ( 'NONE',  ( -18.59117750673696889, 65.66751761918668251, -97.42826094061121012 ) ) ;
#61518=DIRECTION ( 'NONE',  ( 1.000000000000000000, 0.000000000000000000, 0.000000000000000000 ) ) ;
#61526=CYLINDRICAL_SURFACE ( 'NONE', #98123, 0.09999999999999939493 ) ;
#61548=CARTESIAN_POINT ( 'NONE',  ( 22.50000000000000000, 75.95437663941591211, -148.1736118230718944 ) ) ;
#61549=VERTEX_POINT ( 'NONE', #81771 ) ;
#61564=FACE_OUTER_BOUND ( 'NONE', #71979, .T. ) ;
#61574=VECTOR ( 'NONE', #108250, 1000.000000000000000 ) ;
#61589=ORIENTED_EDGE ( 'NONE', *, *, #96563, .T. ) ;
#61626=DIRECTION ( 'NONE',  ( -1.000000000000000000, 0.000000000000000000, 0.000000000000000000 ) ) ;
#61648=ORIENTED_EDGE ( 'NONE', *, *, #140716, .T. ) ;
#61680=ORIENTED_EDGE ( 'NONE', *, *, #127346, .T. ) ;
#61687=AXIS2_PLACEMENT_3D ( 'NONE', #88297, #223979, #67479 ) ;
#61698=CARTESIAN_POINT ( 'NONE',  ( 18.49999999999999289, 65.75000000001195133, -111.8731074845243825 ) ) ;
#61699=VECTOR ( 'NONE', #122540, 1000.000000000000000 ) ;
#61705=CARTESIAN_POINT ( 'NONE',  ( 23.14999999999999503, 64.35000000001197407, -115.1731074845243796 ) ) ;
#61728=CARTESIAN_POINT ( 'NONE',  ( 20.94999999999999929, 71.18691588786253988, -124.5815897280005089 ) ) ;
#61730=EDGE_CURVE ( 'NONE', #17884, #33201, #109420, .T. ) ;
#61780=DIRECTION ( 'NONE',  ( 1.000000000000000000, 0.000000000000000000, 0.000000000000000000 ) ) ;
#61804=DIRECTION ( 'NONE',  ( -1.000000000000000000, 0.000000000000000000, 0.000000000000000000 ) ) ;
#61860=EDGE_CURVE ( 'NONE', #229115, #231485, #15118, .T. ) ;
#61910=DIRECTION ( 'NONE',  ( 1.000000000000000000, 0.000000000000000000, 0.000000000000000000 ) ) ;
#61917=AXIS2_PLACEMENT_3D ( 'NONE', #198746, #538, #179219 ) ;
#61918=DIRECTION ( 'NONE',  ( 0.000000000000000000, -0.9915357197604982575, 0.1298341882519033486 ) ) ;
#61928=AXIS2_PLACEMENT_3D ( 'NONE', #43969, #205594, #206897 ) ;
#61945=CARTESIAN_POINT ( 'NONE',  ( -18.47653818581420637, 85.46528038777508129, -129.3971466683843801 ) ) ;
#61960=DIRECTION ( 'NONE',  ( -1.000000000000000000, 0.000000000000000000, -0.000000000000000000 ) ) ;
#61990=AXIS2_PLACEMENT_3D ( 'NONE', #24743, #104224, #245039 ) ;
#62015=ADVANCED_FACE ( 'NONE', ( #5793 ), #13945, .T. ) ;
#62018=VECTOR ( 'NONE', #254715, 1000.000000000000000 ) ;
#62022=EDGE_LOOP ( 'NONE', ( #235621, #229857, #181496, #125256 ) ) ;
#62035=VERTEX_POINT ( 'NONE', #180607 ) ;
#62036=CARTESIAN_POINT ( 'NONE',  ( 18.59999999999999787, 77.83534155023646406, -124.9679561919613064 ) ) ;
#62057=DIRECTION ( 'NONE',  ( -1.000000000000000000, 0.000000000000000000, -0.000000000000000000 ) ) ;
#62076=CARTESIAN_POINT ( 'NONE',  ( 20.85882249326303040, 65.66751761918668251, -97.42826094061121012 ) ) ;
#62084=DIRECTION ( 'NONE',  ( -2.952720810173289112E-16, -1.000000000000000000, -6.982962677686266711E-15 ) ) ;
#62085=CARTESIAN_POINT ( 'NONE',  ( 21.97500000000000497, 66.25000000001207923, -124.2731074845243597 ) ) ;
#62141=EDGE_CURVE ( 'NONE', #45900, #64483, #230613, .T. ) ;
#62155=CARTESIAN_POINT ( 'NONE',  ( -23.15000000000000213, 87.39257802171759693, -106.0970570643561501 ) ) ;
#62163=CIRCLE ( 'NONE', #37226, 11.64999999999999325 ) ;
#62171=AXIS2_PLACEMENT_3D ( 'NONE', #158063, #175061, #137163 ) ;
#62180=DIRECTION ( 'NONE',  ( -1.836970198721029934E-16, -1.000000000000000000, -6.982962677686266711E-15 ) ) ;
#62183=TOROIDAL_SURFACE ( 'NONE', #141281, 4.099999999999999645, 0.1000000000000000056 ) ;
#62204=LINE ( 'NONE', #100005, #104819 ) ;
#62215=AXIS2_PLACEMENT_3D ( 'NONE', #188137, #234647, #246810 ) ;
#62216=DIRECTION ( 'NONE',  ( -1.000000000000000000, 1.836970198721029934E-16, 1.601412966608202925E-30 ) ) ;
#62240=ADVANCED_FACE ( 'NONE', ( #115196 ), #176474, .T. ) ;
#62257=DIRECTION ( 'NONE',  ( 1.000000000000000000, 0.000000000000000000, 0.000000000000000000 ) ) ;
#62259=EDGE_CURVE ( 'NONE', #231766, #24249, #55180, .T. ) ;
#62268=ORIENTED_EDGE ( 'NONE', *, *, #106080, .T. ) ;
#62272=ORIENTED_EDGE ( 'NONE', *, *, #226404, .T. ) ;
#62280=DIRECTION ( 'NONE',  ( 0.000000000000000000, -6.982962677686266711E-15, 1.000000000000000000 ) ) ;
#62281=ORIENTED_EDGE ( 'NONE', *, *, #201541, .F. ) ;
#62288=LINE ( 'NONE', #20617, #69949 ) ;
#62298=ADVANCED_FACE ( 'NONE', ( #17383 ), #254661, .F. ) ;
#62306=CARTESIAN_POINT ( 'NONE',  ( 20.85000000000000142, 77.26327546522911405, -95.12124281777788326 ) ) ;
#62370=DIRECTION ( 'NONE',  ( 0.000000000000000000, -1.000000000000000000, -8.609265936414504429E-15 ) ) ;
#62374=EDGE_LOOP ( 'NONE', ( #255997, #35912, #255613, #84098 ) ) ;
#62401=VERTEX_POINT ( 'NONE', #199887 ) ;
#62404=AXIS2_PLACEMENT_3D ( 'NONE', #178588, #1182, #80716 ) ;
#62438=CARTESIAN_POINT ( 'NONE',  ( -21.05000000000000071, 76.00000000001190870, -103.0231074845243029 ) ) ;
#62463=CARTESIAN_POINT ( 'NONE',  ( -22.37643362114956602, 75.90091862633082087, -144.1488974784826951 ) ) ;
#62484=DIRECTION ( 'NONE',  ( 0.000000000000000000, 1.000000000000000000, 7.272083257015735086E-15 ) ) ;
#62495=DIRECTION ( 'NONE',  ( 0.000000000000000000, 6.982962677686266711E-15, -1.000000000000000000 ) ) ;
#62517=CARTESIAN_POINT ( 'NONE',  ( 18.49999999999999289, 69.35000000001200249, -115.1731074845243512 ) ) ;
#62534=AXIS2_PLACEMENT_3D ( 'NONE', #154246, #172533, #252006 ) ;
#62538=EDGE_CURVE ( 'NONE', #199002, #125361, #206291, .T. ) ;
#62554=DIRECTION ( 'NONE',  ( 0.000000000000000000, -6.938893903907222067E-15, 1.000000000000000000 ) ) ;
#62566=CARTESIAN_POINT ( 'NONE',  ( 20.22894356738409627, 66.72150177717436748, -128.2545845782748586 ) ) ;
#62618=ORIENTED_EDGE ( 'NONE', *, *, #231316, .T. ) ;
#62640=DIRECTION ( 'NONE',  ( 0.000000000000000000, -6.982962677686266711E-15, 1.000000000000000000 ) ) ;
#62641=ORIENTED_EDGE ( 'NONE', *, *, #69806, .T. ) ;
#62642=DIRECTION ( 'NONE',  ( -1.836970198721029934E-16, -1.000000000000000000, -6.982962677686266711E-15 ) ) ;
#62652=DIRECTION ( 'NONE',  ( 0.000000000000000000, 1.000000000000000000, 6.982962677686266711E-15 ) ) ;
#62705=VERTEX_POINT ( 'NONE', #54898 ) ;
#62731=EDGE_CURVE ( 'NONE', #14025, #13648, #157920, .T. ) ;
#62743=CYLINDRICAL_SURFACE ( 'NONE', #232696, 0.1000000000000028644 ) ;
#62768=DIRECTION ( 'NONE',  ( 0.000000000000000000, 0.000000000000000000, 1.000000000000000000 ) ) ;
#62802=DIRECTION ( 'NONE',  ( 0.000000000000000000, 0.000000000000000000, 1.000000000000000000 ) ) ;
#62803=CARTESIAN_POINT ( 'NONE',  ( 21.04999999999999716, 67.10527618163435193, -128.0360231613754536 ) ) ;
#62809=FACE_OUTER_BOUND ( 'NONE', #106199, .T. ) ;
#62813=CARTESIAN_POINT ( 'NONE',  ( -21.64999999999999858, 68.65000000001199965, -115.3731074845243540 ) ) ;
#62824=CARTESIAN_POINT ( 'NONE',  ( 22.40000000000010516, 76.00000000001317346, -148.1726782920694063 ) ) ;
#62827=EDGE_CURVE ( 'NONE', #57112, #188655, #226094, .T. ) ;
#62842=EDGE_LOOP ( 'NONE', ( #19199, #89262, #19745, #130028 ) ) ;
#62862=PLANE ( 'NONE',  #187256 ) ;
#62864=AXIS2_PLACEMENT_3D ( 'NONE', #96260, #62280, #58401 ) ;
#62884=ORIENTED_EDGE ( 'NONE', *, *, #198327, .F. ) ;
#62936=ORIENTED_EDGE ( 'NONE', *, *, #156937, .F. ) ;
#62940=ORIENTED_EDGE ( 'NONE', *, *, #209202, .F. ) ;
#63010=CARTESIAN_POINT ( 'NONE',  ( -22.39999999999999858, 76.00000000001213607, -136.6231074845242972 ) ) ;
#63067=VECTOR ( 'NONE', #90166, 1000.000000000000000 ) ;
#63081=FACE_OUTER_BOUND ( 'NONE', #39530, .T. ) ;
#63096=DIRECTION ( 'NONE',  ( 1.000000000000000000, 0.000000000000000000, 0.000000000000000000 ) ) ;
#63106=CARTESIAN_POINT ( 'NONE',  ( -20.54999999999999716, 76.00000000001189449, -101.1231074845242972 ) ) ;
#63175=AXIS2_PLACEMENT_3D ( 'NONE', #107325, #167335, #106019 ) ;
#63179=ORIENTED_EDGE ( 'NONE', *, *, #179880, .F. ) ;
#63207=DIRECTION ( 'NONE',  ( 0.7071067811865474617, -0.7071067811865474617, -4.937700262164531476E-15 ) ) ;
#63211=VECTOR ( 'NONE', #163210, 1000.000000000000000 ) ;
#63221=EDGE_CURVE ( 'NONE', #64056, #29923, #180647, .T. ) ;
#63223=ORIENTED_EDGE ( 'NONE', *, *, #43737, .T. ) ;
#63258=VERTEX_POINT ( 'NONE', #247019 ) ;
#63268=CARTESIAN_POINT ( 'NONE',  ( 18.59999999999999076, 69.55000000001207638, -126.5060803140843291 ) ) ;
#63337=CARTESIAN_POINT ( 'NONE',  ( -23.25000000000000000, 64.25000000001215028, -136.5231074845243597 ) ) ;
#63358=ORIENTED_EDGE ( 'NONE', *, *, #123819, .F. ) ;
#63376=ORIENTED_EDGE ( 'NONE', *, *, #37713, .F. ) ;
#63382=EDGE_CURVE ( 'NONE', #62705, #213961, #234689, .T. ) ;
#63384=FACE_OUTER_BOUND ( 'NONE', #12416, .T. ) ;
#63394=ORIENTED_EDGE ( 'NONE', *, *, #166153, .T. ) ;
#63407=ORIENTED_EDGE ( 'NONE', *, *, #68793, .T. ) ;
#63411=DIRECTION ( 'NONE',  ( 1.000000000000000000, 0.000000000000000000, 0.000000000000000000 ) ) ;
#63474=CARTESIAN_POINT ( 'NONE',  ( -18.59999999999999787, 77.86671491006937629, -124.7704322382422788 ) ) ;
#63535=EDGE_CURVE ( 'NONE', #203841, #119361, #168273, .T. ) ;
#63573=CARTESIAN_POINT ( 'NONE',  ( 21.53699400384966367, 76.00000000001219291, -143.3108192777618797 ) ) ;
#63607=ADVANCED_FACE ( 'NONE', ( #246720 ), #48526, .T. ) ;
#63636=ORIENTED_EDGE ( 'NONE', *, *, #207459, .F. ) ;
#63644=CARTESIAN_POINT ( 'NONE',  ( -21.04999999999999716, 69.70076908991985931, -136.6215449845246610 ) ) ;
#63685=FACE_OUTER_BOUND ( 'NONE', #235443, .T. ) ;
#63714=ORIENTED_EDGE ( 'NONE', *, *, #246706, .T. ) ;
#63715=DIRECTION ( 'NONE',  ( 1.000000000000000000, 0.000000000000000000, 0.000000000000000000 ) ) ;
#63724=EDGE_CURVE ( 'NONE', #89014, #231809, #109954, .T. ) ;
#63725=VERTEX_POINT ( 'NONE', #11997 ) ;
#63741=EDGE_CURVE ( 'NONE', #60637, #65006, #9395, .T. ) ;
#63742=AXIS2_PLACEMENT_3D ( 'NONE', #164812, #21464, #124406 ) ;
#63750=DIRECTION ( 'NONE',  ( -0.000000000000000000, -1.000000000000000000, -6.982962677686266711E-15 ) ) ;
#63767=EDGE_LOOP ( 'NONE', ( #167910, #174269, #80428, #74046 ) ) ;
#63779=AXIS2_PLACEMENT_3D ( 'NONE', #16171, #132239, #192229 ) ;
#63804=CARTESIAN_POINT ( 'NONE',  ( 20.94999999999999574, 65.57661458509917907, -129.0310555606542664 ) ) ;
#63838=CARTESIAN_POINT ( 'NONE',  ( -20.85000000000000142, 68.97833521811179480, -99.28954208262706516 ) ) ;
#63839=CARTESIAN_POINT ( 'NONE',  ( -23.25000000000000000, 69.06610602788553877, -99.23746165015076315 ) ) ;
#63863=CARTESIAN_POINT ( 'NONE',  ( 21.08134388332231879, 69.66531941949419604, -136.5989264020313669 ) ) ;
#63883=AXIS2_PLACEMENT_3D ( 'NONE', #135004, #38513, #196287 ) ;
#63898=DIRECTION ( 'NONE',  ( 0.000000000000000000, -1.000000000000000000, -6.982962677686266711E-15 ) ) ;
#63915=EDGE_LOOP ( 'NONE', ( #66149, #74598, #249389, #203759 ) ) ;
#63917=ORIENTED_EDGE ( 'NONE', *, *, #63741, .T. ) ;
#63923=EDGE_CURVE ( 'NONE', #149131, #61324, #26783, .T. ) ;
#63925=CIRCLE ( 'NONE', #176367, 11.74999999999999645 ) ;
#63936=ORIENTED_EDGE ( 'NONE', *, *, #179991, .F. ) ;
#63955=CIRCLE ( 'NONE', #30654, 0.1000000000000028644 ) ;
#63959=PLANE ( 'NONE',  #172966 ) ;
#63984=ORIENTED_EDGE ( 'NONE', *, *, #134902, .F. ) ;
#63990=VECTOR ( 'NONE', #123295, 1000.000000000000000 ) ;
#64009=CARTESIAN_POINT ( 'NONE',  ( -23.15000000000000213, 76.00000000001190870, -103.0231074845243029 ) ) ;
#64024=DIRECTION ( 'NONE',  ( 0.000000000000000000, -0.7397360091702802620, 0.6728971962616779878 ) ) ;
#64026=CARTESIAN_POINT ( 'NONE',  ( -18.50000000000000000, 76.00000000001190870, -103.0231074845243029 ) ) ;
#64033=CARTESIAN_POINT ( 'NONE',  ( -18.59999999999999787, 77.83585931145546510, -91.51866831572576189 ) ) ;
#64056=VERTEX_POINT ( 'NONE', #23269 ) ;
#64067=DIRECTION ( 'NONE',  ( 0.000000000000000000, 1.000000000000000000, 6.982962677686266711E-15 ) ) ;
#64068=CARTESIAN_POINT ( 'NONE',  ( -18.55807992284872299, 65.67101464000501210, -97.44043916224792667 ) ) ;
#64149=CARTESIAN_POINT ( 'NONE',  ( 21.07928932188134397, 69.67148334361883144, -136.6220026301787414 ) ) ;
#64212=CARTESIAN_POINT ( 'NONE',  ( -23.15000000000000213, 76.00000000001213607, -136.5231074845242745 ) ) ;
#64222=EDGE_CURVE ( 'NONE', #2636, #239290, #43518, .T. ) ;
#64240=ORIENTED_EDGE ( 'NONE', *, *, #110067, .F. ) ;
#64243=CARTESIAN_POINT ( 'NONE',  ( 21.14999999999999858, 87.65000000001214175, -136.5231074845242176 ) ) ;
#64246=ORIENTED_EDGE ( 'NONE', *, *, #252959, .T. ) ;
#64256=AXIS2_PLACEMENT_3D ( 'NONE', #53026, #34790, #12648 ) ;
#64258=ORIENTED_EDGE ( 'NONE', *, *, #15983, .F. ) ;
#64387=DIRECTION ( 'NONE',  ( 0.000000000000000000, 0.8660254037844281605, -0.5000000000000185407 ) ) ;
#64409=VERTEX_POINT ( 'NONE', #5908 ) ;
#64415=CIRCLE ( 'NONE', #80960, 0.09999999999998898659 ) ;
#64435=DIRECTION ( 'NONE',  ( -1.000000000000000000, -0.000000000000000000, -0.000000000000000000 ) ) ;
#64483=VERTEX_POINT ( 'NONE', #60749 ) ;
#64485=DIRECTION ( 'NONE',  ( -1.000000000000000000, -7.304098846218135653E-16, -5.100424963727256530E-30 ) ) ;
#64491=ORIENTED_EDGE ( 'NONE', *, *, #19494, .T. ) ;
#64512=PLANE ( 'NONE',  #23986 ) ;
#64533=VERTEX_POINT ( 'NONE', #125861 ) ;
#64565=DIRECTION ( 'NONE',  ( 0.000000000000000000, -7.304098846218139203E-15, 1.000000000000000000 ) ) ;
#64574=DIRECTION ( 'NONE',  ( 0.000000000000000000, 7.086529944415894657E-15, -1.000000000000000000 ) ) ;
#64596=DIRECTION ( 'NONE',  ( 0.000000000000000000, -1.000000000000000000, -7.272083257015735086E-15 ) ) ;
#64609=EDGE_CURVE ( 'NONE', #213669, #18414, #65282, .T. ) ;
#64611=EDGE_CURVE ( 'NONE', #72948, #5563, #60426, .T. ) ;
#64615=ADVANCED_FACE ( 'NONE', ( #14624 ), #227030, .F. ) ;
#64625=AXIS2_PLACEMENT_3D ( 'NONE', #82511, #103367, #180368 ) ;
#64639=TOROIDAL_SURFACE ( 'NONE', #27271, 0.2000000000000000111, 0.1000000000000000056 ) ;
#64661=EDGE_CURVE ( 'NONE', #69624, #193905, #85344, .T. ) ;
#64677=FACE_OUTER_BOUND ( 'NONE', #125934, .T. ) ;
#64718=AXIS2_PLACEMENT_3D ( 'NONE', #205253, #46188, #203979 ) ;
#64728=DIRECTION ( 'NONE',  ( 1.000000000000000000, -1.836970198721029934E-16, -1.282749433769087582E-30 ) ) ;
#64818=CARTESIAN_POINT ( 'NONE',  ( -21.05000000000000071, 77.83534155023646406, -124.9679561919613064 ) ) ;
#64830=DIRECTION ( 'NONE',  ( 1.000000000000000000, 0.000000000000000000, 0.000000000000000000 ) ) ;
#64832=EDGE_CURVE ( 'NONE', #224952, #186279, #108274, .T. ) ;
#64863=DIRECTION ( 'NONE',  ( 1.000000000000000000, -1.836970198721029934E-16, -1.601412966608202925E-30 ) ) ;
#64892=CIRCLE ( 'NONE', #144172, 4.149999999999987033 ) ;
#64922=CARTESIAN_POINT ( 'NONE',  ( -21.05000000000000071, 69.50298221358116280, -136.5085617939581653 ) ) ;
#64928=AXIS2_PLACEMENT_3D ( 'NONE', #37048, #35761, #177840 ) ;
#64934=ORIENTED_EDGE ( 'NONE', *, *, #166153, .F. ) ;
#64950=CIRCLE ( 'NONE', #214800, 12.87499999999999822 ) ;
#64969=DIRECTION ( 'NONE',  ( 0.000000000000000000, -6.547589603894034005E-15, 1.000000000000000000 ) ) ;
#64996=ORIENTED_EDGE ( 'NONE', *, *, #39788, .T. ) ;
#64998=CARTESIAN_POINT ( 'NONE',  ( 21.05000000000000426, 69.58617371119916584, -136.4373665474909956 ) ) ;
#65005=EDGE_LOOP ( 'NONE', ( #185890, #41960, #220709, #138819 ) ) ;
#65006=VERTEX_POINT ( 'NONE', #239770 ) ;
#65015=CARTESIAN_POINT ( 'NONE',  ( 21.97500000000000497, 66.25000000001206502, -124.1731074845243654 ) ) ;
#65019=ADVANCED_FACE ( 'NONE', ( #177257 ), #27354, .F. ) ;
#65034=CYLINDRICAL_SURFACE ( 'NONE', #252131, 0.1000000000000028644 ) ;
#65090=DIRECTION ( 'NONE',  ( 0.000000000000000000, -6.608470384673536824E-15, 1.000000000000000000 ) ) ;
#65092=CARTESIAN_POINT ( 'NONE',  ( 23.14999999999999503, 64.35000000001195986, -110.0379132551783243 ) ) ;
#65167=AXIS2_PLACEMENT_3D ( 'NONE', #134757, #171386, #31860 ) ;
#65176=CIRCLE ( 'NONE', #69479, 0.1000000000000072220 ) ;
#65202=CARTESIAN_POINT ( 'NONE',  ( 18.49999999999998934, 69.45000000001199680, -115.2731074845243455 ) ) ;
#65204=ORIENTED_EDGE ( 'NONE', *, *, #19334, .T. ) ;
#65232=ADVANCED_FACE ( 'NONE', ( #23313 ), #27541, .F. ) ;
#65245=EDGE_CURVE ( 'NONE', #161343, #57517, #210646, .T. ) ;
#65266=AXIS2_PLACEMENT_3D ( 'NONE', #82318, #238860, #41964 ) ;
#65282=B_SPLINE_CURVE_WITH_KNOTS ( 'NONE', 3,
 ( #191982, #52425, #35483, #73326, #251923, #72020, #31629, #173730, #32926, #112431, #54983, #111133, #133267, #190702, #13325, #92842, #185846, #152867, #53722, #212813, #34198, #75858 ),
 .UNSPECIFIED., .F., .F.,
 ( 4, 3, 3, 3, 3, 3, 3, 4 ),
 ( 0.000000000000000000, 7.307836821087015899E-06, 4.161455748548358328E-05, 7.576591810648404394E-05, 0.0001098090429817646371, 0.0001438003617351047325, 0.0001777914035423768749, 0.0002117966137402968007 ),
 .UNSPECIFIED. ) ;
#65293=ORIENTED_EDGE ( 'NONE', *, *, #243383, .T. ) ;
#65308=CARTESIAN_POINT ( 'NONE',  ( 21.14999999999999858, 76.10000000001218723, -143.0637644362255401 ) ) ;
#65338=EDGE_CURVE ( 'NONE', #57631, #162828, #93519, .T. ) ;
#65367=CARTESIAN_POINT ( 'NONE',  ( 20.95512820512820440, 67.12384868372396340, -127.9644784893834100 ) ) ;
#65379=CARTESIAN_POINT ( 'NONE',  ( 21.14999999999999858, 65.28660755661216797, -124.2731074845243739 ) ) ;
#65391=CARTESIAN_POINT ( 'NONE',  ( -18.59999999999999787, 77.16270174995010223, -128.5231074845242745 ) ) ;
#65397=DIRECTION ( 'NONE',  ( -1.000000000000000000, 0.000000000000000000, -0.000000000000000000 ) ) ;
#65405=ORIENTED_EDGE ( 'NONE', *, *, #236265, .T. ) ;
#65420=DIRECTION ( 'NONE',  ( 1.000000000000000000, 0.000000000000000000, 0.000000000000000000 ) ) ;
#65431=DIRECTION ( 'NONE',  ( 1.000000000000000000, 0.000000000000000000, 0.000000000000000000 ) ) ;
#65441=ORIENTED_EDGE ( 'NONE', *, *, #238598, .F. ) ;
#65466=CARTESIAN_POINT ( 'NONE',  ( -20.85000000000000142, 77.85161776048073534, -91.41991776492061206 ) ) ;
#65472=VECTOR ( 'NONE', #142743, 1000.000000000000000 ) ;
#65511=ORIENTED_EDGE ( 'NONE', *, *, #52727, .F. ) ;
#65536=AXIS2_PLACEMENT_3D ( 'NONE', #145995, #67753, #228122 ) ;
#65540=CARTESIAN_POINT ( 'NONE',  ( 18.52928932304161336, 65.72071067697032731, -111.8468540517208112 ) ) ;
#65555=ORIENTED_EDGE ( 'NONE', *, *, #176326, .T. ) ;
#65600=DIRECTION ( 'NONE',  ( 1.000000000000000000, 0.000000000000000000, 0.000000000000000000 ) ) ;
#65602=AXIS2_PLACEMENT_3D ( 'NONE', #193712, #254895, #257466 ) ;
#65619=CYLINDRICAL_SURFACE ( 'NONE', #127794, 0.1000000000000028644 ) ;
#65659=CARTESIAN_POINT ( 'NONE',  ( 21.13461538461538325, 67.11458296203758778, -124.1731074845243512 ) ) ;
#65669=EDGE_CURVE ( 'NONE', #28671, #165453, #210594, .T. ) ;
#65677=FACE_OUTER_BOUND ( 'NONE', #22405, .T. ) ;
#65679=VECTOR ( 'NONE', #17581, 1000.000000000000000 ) ;
#65695=FACE_OUTER_BOUND ( 'NONE', #161176, .T. ) ;
#65699=DIRECTION ( 'NONE',  ( 0.000000000000000000, 0.000000000000000000, 1.000000000000000000 ) ) ;
#65712=ORIENTED_EDGE ( 'NONE', *, *, #5662, .F. ) ;
#65748=DIRECTION ( 'NONE',  ( -0.000000000000000000, -0.8660254037844377084, -0.5000000000000016653 ) ) ;
#65756=DIRECTION ( 'NONE',  ( -0.000000000000000000, 6.982962677686266711E-15, -1.000000000000000000 ) ) ;
#65763=CARTESIAN_POINT ( 'NONE',  ( -18.59999999999999787, 64.35000000001205933, -124.3731074845243825 ) ) ;
#65764=CARTESIAN_POINT ( 'NONE',  ( -21.05000000000000071, 77.85102823015292017, -124.8691942151017855 ) ) ;
#65773=EDGE_CURVE ( 'NONE', #186173, #38706, #89346, .T. ) ;
#65779=EDGE_LOOP ( 'NONE', ( #34469, #45060, #38272, #219170, #138057 ) ) ;
#65798=CARTESIAN_POINT ( 'NONE',  ( 21.14999999999999503, 87.65000000001212754, -133.6231074845242119 ) ) ;
#65818=DIRECTION ( 'NONE',  ( 0.000000000000000000, 6.982962677686266711E-15, -1.000000000000000000 ) ) ;
#65834=DIRECTION ( 'NONE',  ( 2.710505431213777355E-16, 1.000000000000000000, 6.982962677686266711E-15 ) ) ;
#65842=ORIENTED_EDGE ( 'NONE', *, *, #36759, .F. ) ;
#65846=CARTESIAN_POINT ( 'NONE',  ( 21.05000000000000071, 70.10000000001197407, -113.2422072491807086 ) ) ;
#65856=ADVANCED_FACE ( 'NONE', ( #76204 ), #214435, .T. ) ;
#65860=EDGE_LOOP ( 'NONE', ( #214864, #134469, #24484, #152821 ) ) ;
#65879=ORIENTED_EDGE ( 'NONE', *, *, #37060, .T. ) ;
#65902=CIRCLE ( 'NONE', #3530, 0.1000000000000028644 ) ;
#65907=ADVANCED_FACE ( 'NONE', ( #81318 ), #181982, .T. ) ;
#65913=DIRECTION ( 'NONE',  ( 0.000000000000000000, 6.982962677686266711E-15, -1.000000000000000000 ) ) ;
#65930=DIRECTION ( 'NONE',  ( 0.000000000000000000, -6.982962677686266711E-15, 1.000000000000000000 ) ) ;
#65931=DIRECTION ( 'NONE',  ( 1.000000000000000000, 0.000000000000000000, 0.000000000000000000 ) ) ;
#65961=ORIENTED_EDGE ( 'NONE', *, *, #231552, .T. ) ;
#65969=CYLINDRICAL_SURFACE ( 'NONE', #246853, 11.74999999999999645 ) ;
#65973=DIRECTION ( 'NONE',  ( 0.000000000000000000, 2.775557561562812086E-13, -1.000000000000000000 ) ) ;
#66007=ORIENTED_EDGE ( 'NONE', *, *, #254488, .T. ) ;
#66035=TOROIDAL_SURFACE ( 'NONE', #11908, 3.899999999999999467, 0.1000000000000000056 ) ;
#66054=AXIS2_PLACEMENT_3D ( 'NONE', #88556, #112008, #109408 ) ;
#66072=CARTESIAN_POINT ( 'NONE',  ( -21.05000000000000071, 87.65000000001212754, -133.6231074845242119 ) ) ;
#66098=CARTESIAN_POINT ( 'NONE',  ( -21.14999999999999858, 64.35000000001214460, -136.4231074845243938 ) ) ;
#66149=ORIENTED_EDGE ( 'NONE', *, *, #37379, .T. ) ;
#66221=ORIENTED_EDGE ( 'NONE', *, *, #50790, .F. ) ;
#66222=CARTESIAN_POINT ( 'NONE',  ( -21.07954640115405454, 69.67071230398723003, -136.5891151916643480 ) ) ;
#66327=CARTESIAN_POINT ( 'NONE',  ( -22.00411653962151348, 68.74655713164203519, -136.6221455902930018 ) ) ;
#66332=FACE_OUTER_BOUND ( 'NONE', #180077, .T. ) ;
#66338=DIRECTION ( 'NONE',  ( 0.000000000000000000, 1.000000000000000000, 6.982962677686267499E-15 ) ) ;
#66340=ADVANCED_FACE ( 'NONE', ( #84531 ), #144541, .F. ) ;
#66345=EDGE_LOOP ( 'NONE', ( #119964, #50841, #71297, #235242 ) ) ;
#66354=ORIENTED_EDGE ( 'NONE', *, *, #53787, .T. ) ;
#66372=AXIS2_PLACEMENT_3D ( 'NONE', #80665, #22015, #257989 ) ;
#66400=VERTEX_POINT ( 'NONE', #68891 ) ;
#66427=AXIS2_PLACEMENT_3D ( 'NONE', #75889, #234971, #173761 ) ;
#66433=CARTESIAN_POINT ( 'NONE',  ( 21.08884785362045378, 69.64280663258689685, -136.5728905795911885 ) ) ;
#66461=DIRECTION ( 'NONE',  ( 0.000000000000000000, 0.000000000000000000, 1.000000000000000000 ) ) ;
#66502=ORIENTED_EDGE ( 'NONE', *, *, #17045, .T. ) ;
#66518=EDGE_CURVE ( 'NONE', #219486, #99212, #44795, .T. ) ;
#66529=ORIENTED_EDGE ( 'NONE', *, *, #117503, .F. ) ;
#66561=CIRCLE ( 'NONE', #212317, 0.1000000000000028644 ) ;
#66582=PLANE ( 'NONE',  #191411 ) ;
#66586=CARTESIAN_POINT ( 'NONE',  ( 18.59999999999999076, 64.35000000001190301, -103.0231074845243882 ) ) ;
#66590=EDGE_CURVE ( 'NONE', #191338, #170720, #219931, .T. ) ;
#66650=VERTEX_POINT ( 'NONE', #855 ) ;
#66666=CARTESIAN_POINT ( 'NONE',  ( -23.15000000000000213, 71.75000000001205080, -124.1731074845243228 ) ) ;
#66675=CARTESIAN_POINT ( 'NONE',  ( 18.50000000000000711, 85.41907808086139653, -96.19318213431596121 ) ) ;
#66685=CARTESIAN_POINT ( 'NONE',  ( -20.85000000000000142, 76.00000000001190870, -103.0231074845243029 ) ) ;
#66694=EDGE_LOOP ( 'NONE', ( #135717, #215756, #160862, #8342, #176848 ) ) ;
#66724=VECTOR ( 'NONE', #135171, 1000.000000000000114 ) ;
#66741=DIRECTION ( 'NONE',  ( -1.000000000000000000, -0.000000000000000000, -0.000000000000000000 ) ) ;
#66798=DIRECTION ( 'NONE',  ( -1.000000000000000000, 0.000000000000000000, -0.000000000000000000 ) ) ;
#66845=ORIENTED_EDGE ( 'NONE', *, *, #252306, .F. ) ;
#66856=ORIENTED_EDGE ( 'NONE', *, *, #1149, .T. ) ;
#66863=CARTESIAN_POINT ( 'NONE',  ( -18.43569575749026512, 85.51932773110456765, -129.5501311079648872 ) ) ;
#66870=FACE_OUTER_BOUND ( 'NONE', #30586, .T. ) ;
#66873=CARTESIAN_POINT ( 'NONE',  ( -18.50000000000000000, 102.4393534156129562, -118.3815988770166427 ) ) ;
#66886=DIRECTION ( 'NONE',  ( 1.296989514748957922E-15, 0.9887567792719351711, -0.1495327102803594987 ) ) ;
#66908=CARTESIAN_POINT ( 'NONE',  ( -18.50000000000000000, 64.35000000001214460, -136.4231074845243938 ) ) ;
#66914=EDGE_CURVE ( 'NONE', #213545, #70203, #197478, .T. ) ;
#66922=DIRECTION ( 'NONE',  ( -1.000000000000000000, 0.000000000000000000, -0.000000000000000000 ) ) ;
#66962=DIRECTION ( 'NONE',  ( 1.000000000000000000, 0.000000000000000000, 0.000000000000000000 ) ) ;
#66967=DIRECTION ( 'NONE',  ( 0.000000000000000000, -6.982962677686266711E-15, 1.000000000000000000 ) ) ;
#66980=DIRECTION ( 'NONE',  ( 1.000000000000000000, 7.304098846218134667E-16, 4.639676173203993355E-30 ) ) ;
#66987=CIRCLE ( 'NONE', #221091, 11.74999999999999645 ) ;
#67006=EDGE_LOOP ( 'NONE', ( #109774, #69796 ) ) ;
#67025=CARTESIAN_POINT ( 'NONE',  ( 23.14999999999999858, 64.35000000001195986, -110.0379132551783243 ) ) ;
#67034=CARTESIAN_POINT ( 'NONE',  ( 21.09696443733127325, 65.27599011609358115, -124.2883299574761509 ) ) ;
#67060=DIRECTION ( 'NONE',  ( 0.000000000000000000, 0.8660254037844377084, 0.5000000000000016653 ) ) ;
#67099=AXIS2_PLACEMENT_3D ( 'NONE', #153614, #131426, #113151 ) ;
#67101=VERTEX_POINT ( 'NONE', #167382 ) ;
#67104=EDGE_CURVE ( 'NONE', #149131, #59064, #174195, .T. ) ;
#67107=ADVANCED_FACE ( 'NONE', ( #12156 ), #189493, .T. ) ;
#67116=LINE ( 'NONE', #146629, #61123 ) ;
#67122=EDGE_CURVE ( 'NONE', #149997, #20295, #215279, .T. ) ;
#67126=FACE_OUTER_BOUND ( 'NONE', #239553, .T. ) ;
#67136=CARTESIAN_POINT ( 'NONE',  ( 23.25000000000000000, 69.45000000001205365, -124.1731074845243370 ) ) ;
#67138=AXIS2_PLACEMENT_3D ( 'NONE', #55513, #65818, #125786 ) ;
#67171=VECTOR ( 'NONE', #103603, 1000.000000000000000 ) ;
#67235=EDGE_LOOP ( 'NONE', ( #244541, #72219, #6862, #8807 ) ) ;
#67280=AXIS2_PLACEMENT_3D ( 'NONE', #149437, #111576, #34623 ) ;
#67298=EDGE_LOOP ( 'NONE', ( #107831, #98259, #150703, #49637 ) ) ;
#67315=EDGE_CURVE ( 'NONE', #162858, #105040, #240795, .T. ) ;
#67350=EDGE_LOOP ( 'NONE', ( #41695, #108699, #17114, #228481, #238696, #172425, #73908, #240533, #58109, #225674, #81774, #41824, #49396, #239966, #118504, #129645, #174359, #19523, #119017, #37039, #139352, #69878, #246895, #51022, #154642 ) ) ;
#67351=AXIS2_PLACEMENT_3D ( 'NONE', #86838, #242073, #26919 ) ;
#67367=ORIENTED_EDGE ( 'NONE', *, *, #74544, .T. ) ;
#67370=AXIS2_PLACEMENT_3D ( 'NONE', #129151, #245250, #226960 ) ;
#67390=CARTESIAN_POINT ( 'NONE',  ( 22.50000000000000000, 76.00000000001213607, -136.5231074845242745 ) ) ;
#67396=DIRECTION ( 'NONE',  ( 0.000000000000000000, 6.982962677686267499E-15, -1.000000000000000000 ) ) ;
#67404=DIRECTION ( 'NONE',  ( 1.000000000000000000, 0.000000000000000000, 0.000000000000000000 ) ) ;
#67408=EDGE_CURVE ( 'NONE', #80343, #88161, #124083, .T. ) ;
#67436=ORIENTED_EDGE ( 'NONE', *, *, #77598, .F. ) ;
#67443=ORIENTED_EDGE ( 'NONE', *, *, #166425, .T. ) ;
#67479=DIRECTION ( 'NONE',  ( 1.000000000000000000, 0.000000000000000000, 0.000000000000000000 ) ) ;
#67489=EDGE_CURVE ( 'NONE', #99499, #147639, #42332, .T. ) ;
#67493=CARTESIAN_POINT ( 'NONE',  ( -21.05000000000000071, 69.74218538953063273, -136.6208977758335550 ) ) ;
#67608=CARTESIAN_POINT ( 'NONE',  ( -18.59999999999999787, 68.97833521811179480, -99.38954208262707368 ) ) ;
#67615=ORIENTED_EDGE ( 'NONE', *, *, #176326, .F. ) ;
#67640=DIRECTION ( 'NONE',  ( 0.000000000000000000, -7.026728003956683390E-15, 1.000000000000000000 ) ) ;
#67646=CARTESIAN_POINT ( 'NONE',  ( 21.14999999999999858, 64.25000000001205080, -124.3731074845243825 ) ) ;
#67663=EDGE_CURVE ( 'NONE', #139774, #135040, #224803, .T. ) ;
#67694=VERTEX_POINT ( 'NONE', #30492 ) ;
#67753=DIRECTION ( 'NONE',  ( 1.000000000000000000, 0.000000000000000000, 0.000000000000000000 ) ) ;
#67757=ORIENTED_EDGE ( 'NONE', *, *, #85294, .F. ) ;
#67776=ORIENTED_EDGE ( 'NONE', *, *, #169783, .T. ) ;
#67810=ORIENTED_EDGE ( 'NONE', *, *, #80854, .F. ) ;
#67814=ORIENTED_EDGE ( 'NONE', *, *, #251391, .T. ) ;
#67830=AXIS2_PLACEMENT_3D ( 'NONE', #77970, #55819, #97512 ) ;
#67850=DIRECTION ( 'NONE',  ( 0.000000000000000000, 0.4999999999999943379, 0.8660254037844420383 ) ) ;
#67882=CIRCLE ( 'NONE', #38657, 0.09999999999999939493 ) ;
#67887=CARTESIAN_POINT ( 'NONE',  ( -20.64999999999999858, 68.75000000001205080, -124.2731074845243455 ) ) ;
#67927=VERTEX_POINT ( 'NONE', #120325 ) ;
#67936=FACE_OUTER_BOUND ( 'NONE', #47462, .T. ) ;
#67943=AXIS2_PLACEMENT_3D ( 'NONE', #201401, #47451, #85284 ) ;
#67957=AXIS2_PLACEMENT_3D ( 'NONE', #69029, #148556, #251486 ) ;
#67978=DIRECTION ( 'NONE',  ( -1.000000000000000000, 0.000000000000000000, -0.000000000000000000 ) ) ;
#67988=CARTESIAN_POINT ( 'NONE',  ( -23.15000000000000213, 76.00000000001199396, -114.8231074845243000 ) ) ;
#68002=DIRECTION ( 'NONE',  ( 1.000000000000000000, -0.000000000000000000, 0.000000000000000000 ) ) ;
#68010=LINE ( 'NONE', #49731, #188995 ) ;
#68021=DIRECTION ( 'NONE',  ( 0.000000000000000000, 1.000000000000000000, 0.000000000000000000 ) ) ;
#68022=AXIS2_PLACEMENT_3D ( 'NONE', #47714, #91985, #127271 ) ;
#68052=ORIENTED_EDGE ( 'NONE', *, *, #187082, .F. ) ;
#68069=DIRECTION ( 'NONE',  ( -1.000000000000000000, -0.000000000000000000, -0.000000000000000000 ) ) ;
#68097=ORIENTED_EDGE ( 'NONE', *, *, #79443, .F. ) ;
#68109=EDGE_CURVE ( 'NONE', #29923, #255801, #178067, .T. ) ;
#68120=CARTESIAN_POINT ( 'NONE',  ( 18.49999999999999289, 65.65621891165885415, -111.6946622066469530 ) ) ;
#68191=AXIS2_PLACEMENT_3D ( 'NONE', #166367, #148056, #8544 ) ;
#68193=CARTESIAN_POINT ( 'NONE',  ( -20.85000000000000142, 65.66751761918668251, -97.42826094061121012 ) ) ;
#68196=DIRECTION ( 'NONE',  ( -1.000000000000000000, -0.000000000000000000, -0.000000000000000000 ) ) ;
#68237=ORIENTED_EDGE ( 'NONE', *, *, #37055, .F. ) ;
#68255=DIRECTION ( 'NONE',  ( 0.000000000000000000, 6.982962677686266711E-15, -1.000000000000000000 ) ) ;
#68356=ORIENTED_EDGE ( 'NONE', *, *, #154802, .F. ) ;
#68372=DIRECTION ( 'NONE',  ( 1.000000000000000000, 0.000000000000000000, 0.000000000000000000 ) ) ;
#68405=DIRECTION ( 'NONE',  ( 0.000000000000000000, -0.1350103645451945777, 0.9908441862701590219 ) ) ;
#68407=ORIENTED_EDGE ( 'NONE', *, *, #186631, .F. ) ;
#68428=DIRECTION ( 'NONE',  ( 0.000000000000000000, -0.9908441862701791170, 0.1350103645450472789 ) ) ;
#68438=ADVANCED_FACE ( 'NONE', ( #165534 ), #247622, .F. ) ;
#68444=DIRECTION ( 'NONE',  ( -1.000000000000000000, 2.952720810173289112E-16, 2.061873921506763405E-30 ) ) ;
#68456=VERTEX_POINT ( 'NONE', #162972 ) ;
#68473=PLANE ( 'NONE',  #164143 ) ;
#68535=ORIENTED_EDGE ( 'NONE', *, *, #245769, .T. ) ;
#68558=VECTOR ( 'NONE', #254004, 1000.000000000000000 ) ;
#68604=EDGE_LOOP ( 'NONE', ( #117406, #61165, #254037, #24476, #37803, #235583, #50914, #146982, #145084, #202953, #11796, #115958, #58084, #171733, #183002, #103668, #88669, #96146 ) ) ;
#68688=CARTESIAN_POINT ( 'NONE',  ( 22.39999999999999503, 76.00000000001219291, -144.2731074845243313 ) ) ;
#68727=LINE ( 'NONE', #166569, #43627 ) ;
#68756=DIRECTION ( 'NONE',  ( -1.000000000000000000, -0.000000000000000000, -0.000000000000000000 ) ) ;
#68779=EDGE_LOOP ( 'NONE', ( #31613, #191894, #54276, #176329 ) ) ;
#68793=EDGE_CURVE ( 'NONE', #239007, #12375, #139198, .T. ) ;
#68801=ADVANCED_FACE ( 'NONE', ( #161372, #57094, #40159 ), #37576, .F. ) ;
#68806=EDGE_CURVE ( 'NONE', #237888, #48194, #253883, .T. ) ;
#68827=ADVANCED_FACE ( 'NONE', ( #4818 ), #83164, .F. ) ;
#68846=DIRECTION ( 'NONE',  ( 1.000000000000000000, -3.265361837132813093E-16, -2.280189983783949500E-30 ) ) ;
#68850=CARTESIAN_POINT ( 'NONE',  ( -23.15000000000000213, 74.00000000001199396, -115.7477294072863998 ) ) ;
#68859=ORIENTED_EDGE ( 'NONE', *, *, #109447, .F. ) ;
#68876=CARTESIAN_POINT ( 'NONE',  ( 20.93284271247462414, 64.25000000001195133, -110.0379132551783243 ) ) ;
#68891=CARTESIAN_POINT ( 'NONE',  ( -20.54999999999999716, 84.73084112150731073, -112.6211822035085675 ) ) ;
#68900=EDGE_CURVE ( 'NONE', #61013, #15448, #241439, .T. ) ;
#68969=DIRECTION ( 'NONE',  ( 0.000000000000000000, 0.000000000000000000, 1.000000000000000000 ) ) ;
#69004=LINE ( 'NONE', #144650, #236888 ) ;
#69029=CARTESIAN_POINT ( 'NONE',  ( 20.94999999999999929, 77.16270174995010223, -128.6231074845242972 ) ) ;
#69043=DIRECTION ( 'NONE',  ( 0.000000000000000000, 0.000000000000000000, -1.000000000000000000 ) ) ;
#69079=CYLINDRICAL_SURFACE ( 'NONE', #243921, 0.1000000000000028644 ) ;
#69085=FACE_OUTER_BOUND ( 'NONE', #17653, .T. ) ;
#69086=VERTEX_POINT ( 'NONE', #95923 ) ;
#69132=EDGE_LOOP ( 'NONE', ( #39109, #11097, #136182, #121847 ) ) ;
#69142=ORIENTED_EDGE ( 'NONE', *, *, #144515, .T. ) ;
#69145=EDGE_CURVE ( 'NONE', #21653, #55329, #76357, .T. ) ;
#69150=DIRECTION ( 'NONE',  ( 0.000000000000000000, -0.1350103645451835865, -0.9908441862701605762 ) ) ;
#69153=EDGE_CURVE ( 'NONE', #176995, #132343, #143221, .T. ) ;
#69181=( BOUNDED_SURFACE ( )  B_SPLINE_SURFACE ( 3, 2, ( 
 ( #38399, #94507, #134897 ),
 ( #98323, #56636, #177923 ),
 ( #60506, #175371, #257378 ),
 ( #78782, #40996, #59198 ),
 ( #138736, #218289, #219586 ),
 ( #119230, #194924, #214452 ) ),
 .UNSPECIFIED., .F., .F., .F. ) 
 B_SPLINE_SURFACE_WITH_KNOTS ( ( 4, 2, 4 ),
 ( 3, 3 ),
 ( 0.0001300404313046574028, 0.0003183318589266556425, 0.0005066232865486539364 ),
 ( 0.000000000000000000, 1.000000000000000000 ),
 .UNSPECIFIED. ) 
 GEOMETRIC_REPRESENTATION_ITEM ( )  RATIONAL_B_SPLINE_SURFACE ( (
 ( 1.000000000000000000, 0.7071067811865352493, 1.000000000000000000),
 ( 1.000000000000000000, 0.7625113560535959900, 1.000000000000000000),
 ( 1.000000000000000000, 0.8126073484694479321, 1.000000000000000000),
 ( 1.000000000000000000, 0.8923049332726290528, 1.000000000000000000),
 ( 1.000000000000000000, 0.9231914937774552410, 1.000000000000000000),
 ( 1.000000000000000000, 0.9238795325112713064, 1.000000000000000000) ) ) 
 REPRESENTATION_ITEM ( '' )  SURFACE ( )  );
#69183=EDGE_CURVE ( 'NONE', #157880, #68456, #218218, .T. ) ;
#69188=CARTESIAN_POINT ( 'NONE',  ( 23.14999999999999503, 64.35000000001197407, -115.1731074845243796 ) ) ;
#69223=AXIS2_PLACEMENT_3D ( 'NONE', #250498, #71890, #125438 ) ;
#69264=AXIS2_PLACEMENT_3D ( 'NONE', #51742, #131301, #32232 ) ;
#69275=CARTESIAN_POINT ( 'NONE',  ( 19.97071067695833690, 64.27928932305363219, -111.8468540517207117 ) ) ;
#69277=DIRECTION ( 'NONE',  ( 0.000000000000000000, 6.982962677686266711E-15, -1.000000000000000000 ) ) ;
#69279=EDGE_CURVE ( 'NONE', #235424, #164288, #70652, .T. ) ;
#69315=CARTESIAN_POINT ( 'NONE',  ( 20.95595624212458219, 65.37610879691791865, -128.8934745703975580 ) ) ;
#69338=AXIS2_PLACEMENT_3D ( 'NONE', #157384, #3058, #236876 ) ;
#69350=DIRECTION ( 'NONE',  ( 1.000000000000000000, -3.265361837132813093E-16, -2.280189983783949500E-30 ) ) ;
#69362=AXIS2_PLACEMENT_3D ( 'NONE', #192381, #57979, #187595 ) ;
#69373=AXIS2_PLACEMENT_3D ( 'NONE', #84109, #46312, #164988 ) ;
#69409=CIRCLE ( 'NONE', #98561, 0.2000000000000057288 ) ;
#69417=DIRECTION ( 'NONE',  ( 1.000000000000000000, 0.000000000000000000, 0.000000000000000000 ) ) ;
#69457=CARTESIAN_POINT ( 'NONE',  ( -20.94999999999999929, 74.83729825007408465, -128.4231074845243086 ) ) ;
#69465=DIRECTION ( 'NONE',  ( 0.000000000000000000, 0.4930308989875575865, 0.8700118002898125091 ) ) ;
#69477=CARTESIAN_POINT ( 'NONE',  ( -23.25000000000000000, 85.00000000001197975, -112.9170766071766820 ) ) ;
#69479=AXIS2_PLACEMENT_3D ( 'NONE', #238010, #120668, #1957 ) ;
#69481=CARTESIAN_POINT ( 'NONE',  ( -18.39999999999999858, 85.60000000001187459, -96.42291809330220076 ) ) ;
#69514=CARTESIAN_POINT ( 'NONE',  ( 18.60000000000000142, 85.32100840337338354, -129.2871692354463278 ) ) ;
#69515=CARTESIAN_POINT ( 'NONE',  ( -21.14999999999999858, 69.45934304831089889, -136.5231074845243313 ) ) ;
#69536=DIRECTION ( 'NONE',  ( 0.000000000000000000, 0.000000000000000000, 1.000000000000000000 ) ) ;
#69550=EDGE_LOOP ( 'NONE', ( #11944, #114245, #199166, #119790, #5291 ) ) ;
#69553=DIRECTION ( 'NONE',  ( 0.000000000000000000, 0.000000000000000000, -1.000000000000000000 ) ) ;
#69589=VECTOR ( 'NONE', #197170, 1000.000000000000000 ) ;
#69622=AXIS2_PLACEMENT_3D ( 'NONE', #45165, #64728, #184669 ) ;
#69624=VERTEX_POINT ( 'NONE', #140871 ) ;
#69628=CARTESIAN_POINT ( 'NONE',  ( 18.59999999999999076, 69.45000000001199680, -115.2731074845243455 ) ) ;
#69635=CARTESIAN_POINT ( 'NONE',  ( -20.94999999999999929, 87.75000000001212186, -133.6231074845242119 ) ) ;
#69645=ORIENTED_EDGE ( 'NONE', *, *, #16092, .T. ) ;
#69648=EDGE_CURVE ( 'NONE', #189431, #231942, #230929, .T. ) ;
#69715=LINE ( 'NONE', #128391, #146958 ) ;
#69717=CARTESIAN_POINT ( 'NONE',  ( 21.05000000000000071, 64.35000000001195986, -110.0379132551783243 ) ) ;
#69757=DIRECTION ( 'NONE',  ( 5.421010862427554711E-16, 1.000000000000000000, 1.023556919514279895E-14 ) ) ;
#69787=LINE ( 'NONE', #174048, #182962 ) ;
#69789=ORIENTED_EDGE ( 'NONE', *, *, #209202, .T. ) ;
#69796=ORIENTED_EDGE ( 'NONE', *, *, #237778, .T. ) ;
#69806=EDGE_CURVE ( 'NONE', #30941, #154018, #243545, .T. ) ;
#69839=AXIS2_PLACEMENT_3D ( 'NONE', #206358, #167254, #222028 ) ;
#69863=ORIENTED_EDGE ( 'NONE', *, *, #149257, .F. ) ;
#69878=ORIENTED_EDGE ( 'NONE', *, *, #207870, .F. ) ;
#69891=CYLINDRICAL_SURFACE ( 'NONE', #69622, 0.1000000000000028644 ) ;
#69896=CARTESIAN_POINT ( 'NONE',  ( -20.64999999999999858, 85.00000000001197975, -112.9170766071766820 ) ) ;
#69902=EDGE_CURVE ( 'NONE', #133238, #252010, #164457, .T. ) ;
#69905=ORIENTED_EDGE ( 'NONE', *, *, #179880, .T. ) ;
#69920=DIRECTION ( 'NONE',  ( 1.000000000000000000, 0.000000000000000000, 0.000000000000000000 ) ) ;
#69949=VECTOR ( 'NONE', #77988, 1000.000000000000114 ) ;
#70006=DIRECTION ( 'NONE',  ( 1.000000000000000000, 0.000000000000000000, 0.000000000000000000 ) ) ;
#70016=FACE_OUTER_BOUND ( 'NONE', #131672, .T. ) ;
#70018=EDGE_LOOP ( 'NONE', ( #175966, #246224 ) ) ;
#70035=VERTEX_POINT ( 'NONE', #106531 ) ;
#70074=DIRECTION ( 'NONE',  ( 1.000000000000000000, 0.000000000000000000, 0.000000000000000000 ) ) ;
#70112=DIRECTION ( 'NONE',  ( 0.000000000000000000, 0.000000000000000000, -1.000000000000000000 ) ) ;
#70150=DIRECTION ( 'NONE',  ( 2.952720810173289112E-16, 1.000000000000000000, 6.982962677686266711E-15 ) ) ;
#70165=EDGE_LOOP ( 'NONE', ( #35517, #172010, #135972, #207198 ) ) ;
#70169=CARTESIAN_POINT ( 'NONE',  ( 20.85000000000000142, 64.25000000001195133, -109.8069731475024753 ) ) ;
#70177=VERTEX_POINT ( 'NONE', #131248 ) ;
#70203=VERTEX_POINT ( 'NONE', #50406 ) ;
#70282=ORIENTED_EDGE ( 'NONE', *, *, #1968, .T. ) ;
#70312=ADVANCED_FACE ( 'NONE', ( #176815 ), #39766, .T. ) ;
#70346=CARTESIAN_POINT ( 'NONE',  ( 22.60000000000000142, 64.25043287652275126, -136.6239658536230763 ) ) ;
#70375=DIRECTION ( 'NONE',  ( 0.000000000000000000, 0.9908441862701791170, -0.1350103645450472789 ) ) ;
#70416=ORIENTED_EDGE ( 'NONE', *, *, #2874, .T. ) ;
#70458=VERTEX_POINT ( 'NONE', #47533 ) ;
#70472=AXIS2_PLACEMENT_3D ( 'NONE', #17421, #136059, #233903 ) ;
#70484=DIRECTION ( 'NONE',  ( 1.000000000000000000, 0.000000000000000000, 0.000000000000000000 ) ) ;
#70554=CARTESIAN_POINT ( 'NONE',  ( 18.41416235934318379, 85.50000000001188027, -96.42291809330222918 ) ) ;
#70563=DIRECTION ( 'NONE',  ( 0.000000000000000000, -6.467318590049456648E-15, 1.000000000000000000 ) ) ;
#70590=ADVANCED_FACE ( 'NONE', ( #50115 ), #85656, .F. ) ;
#70639=CIRCLE ( 'NONE', #53864, 0.6000000000000033085 ) ;
#70652=LINE ( 'NONE', #51016, #80853 ) ;
#70660=DIRECTION ( 'NONE',  ( -0.000000000000000000, 6.982962677686266711E-15, -1.000000000000000000 ) ) ;
#70688=ORIENTED_EDGE ( 'NONE', *, *, #105881, .F. ) ;
#70735=ORIENTED_EDGE ( 'NONE', *, *, #13130, .F. ) ;
#70744=ORIENTED_EDGE ( 'NONE', *, *, #29106, .T. ) ;
#70769=ORIENTED_EDGE ( 'NONE', *, *, #20263, .T. ) ;
#70788=CARTESIAN_POINT ( 'NONE',  ( -20.54999999999999716, 68.75000000001205080, -124.2731074845243455 ) ) ;
#70820=EDGE_CURVE ( 'NONE', #208002, #224260, #127399, .T. ) ;
#70832=ORIENTED_EDGE ( 'NONE', *, *, #82070, .T. ) ;
#70850=EDGE_CURVE ( 'NONE', #201537, #119534, #29023, .T. ) ;
#70852=DIRECTION ( 'NONE',  ( 7.304098846218134667E-16, 1.000000000000000000, 6.982962677686266711E-15 ) ) ;
#70887=VECTOR ( 'NONE', #48997, 1000.000000000000114 ) ;
#70918=DIRECTION ( 'NONE',  ( -1.000000000000000000, -0.000000000000000000, -0.000000000000000000 ) ) ;
#70924=DIRECTION ( 'NONE',  ( 2.952720810173289112E-16, 1.000000000000000000, 6.530723674265620862E-15 ) ) ;
#70940=FACE_OUTER_BOUND ( 'NONE', #225279, .T. ) ;
#70944=CIRCLE ( 'NONE', #224834, 0.1000000000000033362 ) ;
#70947=EDGE_CURVE ( 'NONE', #185852, #247118, #224154, .T. ) ;
#70962=EDGE_CURVE ( 'NONE', #228369, #181257, #164987, .T. ) ;
#70983=AXIS2_PLACEMENT_3D ( 'NONE', #46271, #163675, #107535 ) ;
#70998=ORIENTED_EDGE ( 'NONE', *, *, #109099, .F. ) ;
#71004=CIRCLE ( 'NONE', #216715, 0.1000000000000045158 ) ;
#71008=DIRECTION ( 'NONE',  ( -3.265361837132813093E-16, -1.000000000000000000, -7.086529944415894657E-15 ) ) ;
#71046=DIRECTION ( 'NONE',  ( 0.000000000000000000, -6.938893903907222067E-15, 1.000000000000000000 ) ) ;
#71054=DIRECTION ( 'NONE',  ( 0.000000000000000000, -8.326672684688666480E-14, 1.000000000000000000 ) ) ;
#71059=ORIENTED_EDGE ( 'NONE', *, *, #1968, .F. ) ;
#71098=ADVANCED_FACE ( 'NONE', ( #203325 ), #127640, .T. ) ;
#71107=AXIS2_PLACEMENT_3D ( 'NONE', #237594, #155520, #159353 ) ;
#71112=EDGE_CURVE ( 'NONE', #56965, #181257, #189939, .T. ) ;
#71117=ORIENTED_EDGE ( 'NONE', *, *, #188842, .T. ) ;
#71145=ORIENTED_EDGE ( 'NONE', *, *, #139454, .T. ) ;
#71152=ORIENTED_EDGE ( 'NONE', *, *, #49673, .F. ) ;
#71172=CARTESIAN_POINT ( 'NONE',  ( 23.14999999999999503, 61.95000000001194707, -108.5368025552853197 ) ) ;
#71177=LINE ( 'NONE', #30772, #100454 ) ;
#71189=DIRECTION ( 'NONE',  ( -0.000000000000000000, 1.000000000000000000, 6.352154140967427193E-15 ) ) ;
#71215=CARTESIAN_POINT ( 'NONE',  ( 18.59999999999999076, 69.55000000001207638, -126.5060803140843291 ) ) ;
#71225=ORIENTED_EDGE ( 'NONE', *, *, #96418, .T. ) ;
#71257=LINE ( 'NONE', #171656, #65472 ) ;
#71264=ORIENTED_EDGE ( 'NONE', *, *, #181323, .T. ) ;
#71279=CIRCLE ( 'NONE', #204530, 12.87499999999999822 ) ;
#71295=CARTESIAN_POINT ( 'NONE',  ( 20.95512820512820440, 67.12384868372396340, -127.9644784893834100 ) ) ;
#71297=ORIENTED_EDGE ( 'NONE', *, *, #241672, .T. ) ;
#71299=ORIENTED_EDGE ( 'NONE', *, *, #42546, .T. ) ;
#71332=EDGE_LOOP ( 'NONE', ( #203692, #90786, #127964, #113936 ) ) ;
#71345=CARTESIAN_POINT ( 'NONE',  ( 21.05000000000000071, 85.00000000001207923, -126.6291383618717816 ) ) ;
#71349=ORIENTED_EDGE ( 'NONE', *, *, #92732, .F. ) ;
#71401=CIRCLE ( 'NONE', #75500, 0.1000000000000028644 ) ;
#71429=CARTESIAN_POINT ( 'NONE',  ( 22.57320508075688537, 64.25000000001213607, -136.5231074845243882 ) ) ;
#71524=FACE_OUTER_BOUND ( 'NONE', #164254, .T. ) ;
#71532=CARTESIAN_POINT ( 'NONE',  ( 18.59999999999999076, 65.75000000001196554, -111.7731074845243739 ) ) ;
#71542=ADVANCED_FACE ( 'NONE', ( #3286 ), #145379, .F. ) ;
#71550=CARTESIAN_POINT ( 'NONE',  ( 21.76363531954645936, 68.98706345214041846, -136.6221093588237920 ) ) ;
#71586=DIRECTION ( 'NONE',  ( 1.000000000000000000, 0.000000000000000000, 0.000000000000000000 ) ) ;
#71591=EDGE_LOOP ( 'NONE', ( #59152, #172160 ) ) ;
#71594=DIRECTION ( 'NONE',  ( -1.000000000000000000, 0.000000000000000000, 0.000000000000000000 ) ) ;
#71603=AXIS2_PLACEMENT_3D ( 'NONE', #111589, #189840, #149450 ) ;
#71617=CARTESIAN_POINT ( 'NONE',  ( -18.50000000000000000, 85.41908450282512888, -96.19319967749882494 ) ) ;
#71624=ORIENTED_EDGE ( 'NONE', *, *, #133439, .T. ) ;
#71642=EDGE_CURVE ( 'NONE', #186173, #183267, #19446, .T. ) ;
#71676=LINE ( 'NONE', #12993, #174898 ) ;
#71684=DIRECTION ( 'NONE',  ( -6.938893903907222856E-15, -1.000000000000000000, -6.982962677686266711E-15 ) ) ;
#71701=DIRECTION ( 'NONE',  ( -7.304098846218134667E-16, 1.000000000000000000, 6.982962677686267499E-15 ) ) ;
#71708=CARTESIAN_POINT ( 'NONE',  ( 18.41832399655378083, 85.68240326668595230, -96.36626386449687232 ) ) ;
#71720=DIRECTION ( 'NONE',  ( -1.000000000000000000, 7.304098846218163263E-16, -4.217023435051627211E-16 ) ) ;
#71723=DIRECTION ( 'NONE',  ( 0.000000000000000000, -6.938893903907222067E-15, 1.000000000000000000 ) ) ;
#71726=CARTESIAN_POINT ( 'NONE',  ( -18.59999999999999787, 77.16270174995010223, -128.4231074845242802 ) ) ;
#71756=VERTEX_POINT ( 'NONE', #237769 ) ;
#71786=ORIENTED_EDGE ( 'NONE', *, *, #106408, .F. ) ;
#71789=EDGE_CURVE ( 'NONE', #243260, #194615, #82127, .T. ) ;
#71790=EDGE_CURVE ( 'NONE', #8771, #12190, #82513, .T. ) ;
#71808=CARTESIAN_POINT ( 'NONE',  ( -21.05000000000000071, 69.66772772607649244, -136.4855714212387170 ) ) ;
#71826=LINE ( 'NONE', #230906, #257536 ) ;
#71837=EDGE_LOOP ( 'NONE', ( #117808, #235938, #198686, #84985 ) ) ;
#71843=VECTOR ( 'NONE', #256134, 1000.000000000000000 ) ;
#71857=CIRCLE ( 'NONE', #26063, 0.1000000000000060701 ) ;
#71871=ORIENTED_EDGE ( 'NONE', *, *, #92766, .F. ) ;
#71875=VERTEX_POINT ( 'NONE', #143792 ) ;
#71890=DIRECTION ( 'NONE',  ( 1.000000000000000000, 0.000000000000000000, 0.000000000000000000 ) ) ;
#71897=CARTESIAN_POINT ( 'NONE',  ( 18.49999999999999289, 65.70729864261004138, -97.56574559737244101 ) ) ;
#71909=ORIENTED_EDGE ( 'NONE', *, *, #87523, .T. ) ;
#71963=VERTEX_POINT ( 'NONE', #32889 ) ;
#71965=DIRECTION ( 'NONE',  ( -0.000000000000000000, 1.000000000000000000, 6.982962677686266711E-15 ) ) ;
#71979=EDGE_LOOP ( 'NONE', ( #76953, #126470, #140526, #144481 ) ) ;
#72013=CARTESIAN_POINT ( 'NONE',  ( 23.14999999999999858, 76.00000000001190870, -103.0231074845243029 ) ) ;
#72020=CARTESIAN_POINT ( 'NONE',  ( 20.95203847575071521, 65.49893946073807172, -128.9560361359008027 ) ) ;
#72022=DIRECTION ( 'NONE',  ( 1.000000000000000000, 0.000000000000000000, 0.000000000000000000 ) ) ;
#72041=DIRECTION ( 'NONE',  ( 2.952720810173289112E-16, 1.000000000000000000, 6.530723674265620862E-15 ) ) ;
#72051=EDGE_CURVE ( 'NONE', #111107, #143411, #127576, .T. ) ;
#72056=VECTOR ( 'NONE', #80134, 1000.000000000000000 ) ;
#72065=DIRECTION ( 'NONE',  ( 1.000000000000000000, 0.000000000000000000, 0.000000000000000000 ) ) ;
#72078=ORIENTED_EDGE ( 'NONE', *, *, #253030, .F. ) ;
#72087=EDGE_CURVE ( 'NONE', #220201, #54789, #256970, .T. ) ;
#72098=FACE_OUTER_BOUND ( 'NONE', #142215, .T. ) ;
#72113=SPHERICAL_SURFACE ( 'NONE', #100094, 0.1000000000000000056 ) ;
#72125=AXIS2_PLACEMENT_3D ( 'NONE', #7715, #31156, #225439 ) ;
#72165=CARTESIAN_POINT ( 'NONE',  ( 21.05000000000000071, 70.15000000001198543, -113.1556047088022581 ) ) ;
#72173=VECTOR ( 'NONE', #244471, 1000.000000000000000 ) ;
#72207=EDGE_CURVE ( 'NONE', #245468, #23492, #119197, .T. ) ;
#72210=CARTESIAN_POINT ( 'NONE',  ( -20.54999999999999716, 76.00000000001190870, -103.0231074845243029 ) ) ;
#72219=ORIENTED_EDGE ( 'NONE', *, *, #209227, .F. ) ;
#72238=VECTOR ( 'NONE', #23791, 1000.000000000000000 ) ;
#72257=CARTESIAN_POINT ( 'NONE',  ( 21.53752568622128294, 75.90102553874136504, -143.3099153590727610 ) ) ;
#72265=ORIENTED_EDGE ( 'NONE', *, *, #69279, .T. ) ;
#72282=CARTESIAN_POINT ( 'NONE',  ( -21.14999999999999503, 64.25000000001209344, -129.6039602385655769 ) ) ;
#72291=AXIS2_PLACEMENT_3D ( 'NONE', #35650, #175172, #254630 ) ;
#72302=ORIENTED_EDGE ( 'NONE', *, *, #110941, .T. ) ;
#72344=CYLINDRICAL_SURFACE ( 'NONE', #31888, 0.1000000000000070832 ) ;
#72366=CARTESIAN_POINT ( 'NONE',  ( -21.07933241753356413, 75.90662040959291801, -142.8517534329040473 ) ) ;
#72381=ADVANCED_FACE ( 'NONE', ( #153497 ), #73613, .T. ) ;
#72393=ORIENTED_EDGE ( 'NONE', *, *, #106949, .T. ) ;
#72446=FACE_OUTER_BOUND ( 'NONE', #32612, .T. ) ;
#72455=ORIENTED_EDGE ( 'NONE', *, *, #248985, .T. ) ;
#72463=TOROIDAL_SURFACE ( 'NONE', #30778, 11.90000000000000213, 0.1000000000000000056 ) ;
#72601=CARTESIAN_POINT ( 'NONE',  ( -21.05315837517722244, 64.24999999299802766, -109.8647514757331294 ) ) ;
#72618=DIRECTION ( 'NONE',  ( 0.000000000000000000, -6.982962677686266711E-15, 1.000000000000000000 ) ) ;
#72658=ORIENTED_EDGE ( 'NONE', *, *, #159760, .F. ) ;
#72661=EDGE_CURVE ( 'NONE', #154428, #241341, #119378, .T. ) ;
#72708=EDGE_CURVE ( 'NONE', #215387, #105012, #173599, .T. ) ;
#72717=AXIS2_PLACEMENT_3D ( 'NONE', #52639, #115195, #132190 ) ;
#72722=AXIS2_PLACEMENT_3D ( 'NONE', #151800, #253430, #16145 ) ;
#72735=FACE_OUTER_BOUND ( 'NONE', #81372, .T. ) ;
#72754=EDGE_CURVE ( 'NONE', #231809, #112979, #19614, .T. ) ;
#72760=CIRCLE ( 'NONE', #93567, 0.1000000000000028644 ) ;
#72777=CARTESIAN_POINT ( 'NONE',  ( -2.995603634470891112E-16, 87.75000000001199396, -115.2731074845242176 ) ) ;
#72813=DIRECTION ( 'NONE',  ( 0.000000000000000000, 0.000000000000000000, 1.000000000000000000 ) ) ;
#72825=VECTOR ( 'NONE', #9329, 1000.000000000000000 ) ;
#72831=DIRECTION ( 'NONE',  ( -0.000000000000000000, 0.4791956752371485107, 0.8777080977375185666 ) ) ;
#72852=CARTESIAN_POINT ( 'NONE',  ( 20.95512828230159030, 67.12384868768677393, -124.3206772190210074 ) ) ;
#72912=ORIENTED_EDGE ( 'NONE', *, *, #151544, .F. ) ;
#72946=CARTESIAN_POINT ( 'NONE',  ( -23.25000000000000000, 68.97833521811179480, -99.18954208262705663 ) ) ;
#72948=VERTEX_POINT ( 'NONE', #38338 ) ;
#72988=VECTOR ( 'NONE', #218495, 1000.000000000000000 ) ;
#72994=ORIENTED_EDGE ( 'NONE', *, *, #40001, .F. ) ;
#73007=CARTESIAN_POINT ( 'NONE',  ( 18.48197441911431937, 85.51795479471547878, -96.13289584231789320 ) ) ;
#73011=TOROIDAL_SURFACE ( 'NONE', #102155, 4.099999999999999645, 0.1000000000000000056 ) ;
#73028=EDGE_LOOP ( 'NONE', ( #197897, #72302, #163091, #19728 ) ) ;
#73033=DIRECTION ( 'NONE',  ( -0.000000000000000000, 0.4791956752371484551, 0.8777080977375184556 ) ) ;
#73038=EDGE_CURVE ( 'NONE', #213344, #64533, #163417, .T. ) ;
#73052=CIRCLE ( 'NONE', #97913, 2.000000000000001776 ) ;
#73065=ORIENTED_EDGE ( 'NONE', *, *, #103265, .T. ) ;
#73086=ORIENTED_EDGE ( 'NONE', *, *, #131137, .T. ) ;
#73129=CARTESIAN_POINT ( 'NONE',  ( -22.39999999999999858, 64.25000000001215028, -136.6231074845243825 ) ) ;
#73146=PLANE ( 'NONE',  #241032 ) ;
#73151=LINE ( 'NONE', #246610, #42700 ) ;
#73178=VERTEX_POINT ( 'NONE', #56284 ) ;
#73183=CARTESIAN_POINT ( 'NONE',  ( -23.15000000000000213, 76.00000000001192291, -105.0231074845243029 ) ) ;
#73184=CARTESIAN_POINT ( 'NONE',  ( 20.95262331984766746, 65.49584273722216210, -128.9622191549310912 ) ) ;
#73188=ORIENTED_EDGE ( 'NONE', *, *, #103117, .T. ) ;
#73218=AXIS2_PLACEMENT_3D ( 'NONE', #226792, #87269, #127712 ) ;
#73232=CIRCLE ( 'NONE', #77277, 0.09999999999998898659 ) ;
#73258=ORIENTED_EDGE ( 'NONE', *, *, #177290, .F. ) ;
#73271=ORIENTED_EDGE ( 'NONE', *, *, #122973, .T. ) ;
#73280=CARTESIAN_POINT ( 'NONE',  ( 18.52928932188133970, 65.72071067813062939, -111.7731074845243739 ) ) ;
#73309=CYLINDRICAL_SURFACE ( 'NONE', #33908, 0.1000000000000070832 ) ;
#73312=AXIS2_PLACEMENT_3D ( 'NONE', #171519, #166388, #189766 ) ;
#73326=CARTESIAN_POINT ( 'NONE',  ( 20.95052659398289308, 65.52017563223218133, -128.9478687286587615 ) ) ;
#73329=CARTESIAN_POINT ( 'NONE',  ( 21.87500000000000355, 66.25000000001199396, -115.3731074845243683 ) ) ;
#73333=CARTESIAN_POINT ( 'NONE',  ( 22.50000000000000000, 75.90000000001222702, -148.1726782920690937 ) ) ;
#73341=EDGE_LOOP ( 'NONE', ( #250607, #153516, #243227, #123490 ) ) ;
#73357=CARTESIAN_POINT ( 'NONE',  ( 22.39999999999999858, 75.90000000001219860, -144.3138870828976792 ) ) ;
#73435=EDGE_LOOP ( 'NONE', ( #200285, #64246, #218878, #187830, #70416, #221343 ) ) ;
#73441=LINE ( 'NONE', #152987, #8660 ) ;
#73471=FACE_OUTER_BOUND ( 'NONE', #37551, .T. ) ;
#73477=LINE ( 'NONE', #12211, #248667 ) ;
#73492=DIRECTION ( 'NONE',  ( 0.000000000000000000, -1.000000000000000000, -6.982962677686266711E-15 ) ) ;
#73518=EDGE_CURVE ( 'NONE', #101582, #112033, #11420, .T. ) ;
#73526=DIRECTION ( 'NONE',  ( -1.000000000000000000, -0.000000000000000000, -0.000000000000000000 ) ) ;
#73559=ORIENTED_EDGE ( 'NONE', *, *, #248933, .F. ) ;
#73573=ORIENTED_EDGE ( 'NONE', *, *, #53537, .F. ) ;
#73592=CARTESIAN_POINT ( 'NONE',  ( -22.57320508075687115, 64.25000000001215028, -136.5231074845243597 ) ) ;
#73596=EDGE_LOOP ( 'NONE', ( #35722, #113133, #107363, #191507 ) ) ;
#73611=EDGE_LOOP ( 'NONE', ( #132670, #153250, #42070, #57557 ) ) ;
#73613=TOROIDAL_SURFACE ( 'NONE', #219317, 0.2000000000000000111, 0.1000000000000000056 ) ;
#73627=DIRECTION ( 'NONE',  ( 0.000000000000000000, -6.652207440891554563E-15, 1.000000000000000000 ) ) ;
#73634=DIRECTION ( 'NONE',  ( -1.000000000000000000, -0.000000000000000000, -0.000000000000000000 ) ) ;
#73669=LINE ( 'NONE', #235268, #91266 ) ;
#73678=DIRECTION ( 'NONE',  ( 0.000000000000000000, 0.000000000000000000, -1.000000000000000000 ) ) ;
#73683=VERTEX_POINT ( 'NONE', #101492 ) ;
#73695=CARTESIAN_POINT ( 'NONE',  ( 23.14999999999999858, 71.00000000001199396, -114.9283735034374274 ) ) ;
#73718=ORIENTED_EDGE ( 'NONE', *, *, #205689, .T. ) ;
#73735=DIRECTION ( 'NONE',  ( 0.000000000000000000, -6.938893903907222067E-15, 1.000000000000000000 ) ) ;
#73739=EDGE_CURVE ( 'NONE', #81327, #54263, #158979, .T. ) ;
#73777=VERTEX_POINT ( 'NONE', #49263 ) ;
#73784=ORIENTED_EDGE ( 'NONE', *, *, #2855, .F. ) ;
#73799=CARTESIAN_POINT ( 'NONE',  ( -22.39999999999999858, 76.10085836911093793, -148.2726746080136877 ) ) ;
#73853=VERTEX_POINT ( 'NONE', #68850 ) ;
#73885=EDGE_LOOP ( 'NONE', ( #218824, #149737, #92237, #63376 ) ) ;
#73897=CARTESIAN_POINT ( 'NONE',  ( -21.05000000000000071, 64.40000000001194280, -109.9513107147998880 ) ) ;
#73908=ORIENTED_EDGE ( 'NONE', *, *, #151545, .T. ) ;
#73915=VECTOR ( 'NONE', #127982, 1000.000000000000000 ) ;
#73999=ORIENTED_EDGE ( 'NONE', *, *, #178725, .T. ) ;
#74000=DIRECTION ( 'NONE',  ( -0.000000000000000000, 1.000000000000000000, 6.982962677686266711E-15 ) ) ;
#74046=ORIENTED_EDGE ( 'NONE', *, *, #177386, .F. ) ;
#74066=CARTESIAN_POINT ( 'NONE',  ( 22.39999999999999503, 64.25000000001213607, -136.6231074845243825 ) ) ;
#74074=EDGE_LOOP ( 'NONE', ( #66529, #228058, #21417, #113350 ) ) ;
#74097=EDGE_CURVE ( 'NONE', #57112, #170896, #27827, .T. ) ;
#74149=CARTESIAN_POINT ( 'NONE',  ( 18.59999999999999432, 77.26178616857710324, -128.4366085209788366 ) ) ;
#74205=CARTESIAN_POINT ( 'NONE',  ( -22.59999999999999787, 75.90000000001222702, -148.1726782920690937 ) ) ;
#74209=DIRECTION ( 'NONE',  ( 0.000000000000000000, 0.000000000000000000, -1.000000000000000000 ) ) ;
#74216=ORIENTED_EDGE ( 'NONE', *, *, #86219, .F. ) ;
#74221=CARTESIAN_POINT ( 'NONE',  ( 20.94999999999999929, 61.95000000001194707, -108.5368025552853197 ) ) ;
#74226=ORIENTED_EDGE ( 'NONE', *, *, #219922, .T. ) ;
#74237=ORIENTED_EDGE ( 'NONE', *, *, #91438, .T. ) ;
#74241=CARTESIAN_POINT ( 'NONE',  ( 21.05000000000000071, 69.65000000001205649, -126.6792853948412159 ) ) ;
#74249=CIRCLE ( 'NONE', #7771, 0.2000000000000057288 ) ;
#74257=EDGE_LOOP ( 'NONE', ( #256941, #105502, #107981, #208555 ) ) ;
#74267=ORIENTED_EDGE ( 'NONE', *, *, #160748, .F. ) ;
#74273=ORIENTED_EDGE ( 'NONE', *, *, #169067, .F. ) ;
#74289=CARTESIAN_POINT ( 'NONE',  ( 18.59999996954842771, 85.52320413787082032, -96.14006577260795439 ) ) ;
#74295=CIRCLE ( 'NONE', #95106, 0.1000000000000028644 ) ;
#74328=CARTESIAN_POINT ( 'NONE',  ( -21.05000000000000071, 76.00000000001190870, -103.0231074845243029 ) ) ;
#74333=PLANE ( 'NONE',  #241076 ) ;
#74373=ADVANCED_FACE ( 'NONE', ( #54603 ), #173331, .T. ) ;
#74378=AXIS2_PLACEMENT_3D ( 'NONE', #244470, #170127, #71008 ) ;
#74390=CARTESIAN_POINT ( 'NONE',  ( -22.47071067811865319, 75.90090754530959316, -144.2431822290223522 ) ) ;
#74433=CARTESIAN_POINT ( 'NONE',  ( 20.04142135623731136, 64.25000000001196554, -111.8731074845243825 ) ) ;
#74436=ORIENTED_EDGE ( 'NONE', *, *, #179866, .F. ) ;
#74468=ORIENTED_EDGE ( 'NONE', *, *, #36730, .F. ) ;
#74493=EDGE_CURVE ( 'NONE', #240054, #79346, #253541, .T. ) ;
#74500=AXIS2_PLACEMENT_3D ( 'NONE', #151046, #170653, #111929 ) ;
#74510=ORIENTED_EDGE ( 'NONE', *, *, #113080, .F. ) ;
#74544=EDGE_CURVE ( 'NONE', #231430, #234281, #247948, .T. ) ;
#74545=ORIENTED_EDGE ( 'NONE', *, *, #145090, .T. ) ;
#74598=ORIENTED_EDGE ( 'NONE', *, *, #19975, .F. ) ;
#74622=LINE ( 'NONE', #78420, #120475 ) ;
#74644=( LENGTH_UNIT ( ) NAMED_UNIT ( * ) SI_UNIT ( .MILLI., .METRE. ) );
#74650=EDGE_LOOP ( 'NONE', ( #129590, #165452, #87926, #176343 ) ) ;
#74653=SPHERICAL_SURFACE ( 'NONE', #168044, 0.1000000000000000056 ) ;
#74696=CARTESIAN_POINT ( 'NONE',  ( 20.94999999999999929, 71.00000000001199396, -115.4283735034374274 ) ) ;
#74720=VERTEX_POINT ( 'NONE', #229685 ) ;
#74726=CARTESIAN_POINT ( 'NONE',  ( 23.14999999999998437, 76.00000000001210765, -132.4731074845242915 ) ) ;
#74732=CARTESIAN_POINT ( 'NONE',  ( -23.15000000000000213, 87.48912529308798014, -106.1231074845242262 ) ) ;
#74736=EDGE_LOOP ( 'NONE', ( #213957, #174284, #121007, #37445 ) ) ;
#74750=CYLINDRICAL_SURFACE ( 'NONE', #105536, 0.09999999999999939493 ) ;
#74752=VERTEX_POINT ( 'NONE', #134401 ) ;
#74757=B_SPLINE_CURVE_WITH_KNOTS ( 'NONE', 3,
 ( #46174, #103563, #26644, #243094, #205239, #142698, #86563, #83971, #245670, #67034, #47446, #127005, #206542, #27941, #107439, #8355 ),
 .UNSPECIFIED., .F., .F.,
 ( 4, 3, 3, 3, 3, 4 ),
 ( 0.000000000000000000, 3.357088238233600668E-05, 6.714213034886770139E-05, 0.0001007408646120938085, 0.0001343627955914254344, 0.0001573956632896058639 ),
 .UNSPECIFIED. ) ;
#74803=ORIENTED_EDGE ( 'NONE', *, *, #85253, .T. ) ;
#74814=VERTEX_POINT ( 'NONE', #120033 ) ;
#74818=EDGE_LOOP ( 'NONE', ( #90806, #252641, #197297, #87940 ) ) ;
#74842=AXIS2_PLACEMENT_3D ( 'NONE', #144949, #224500, #127981 ) ;
#74883=DIRECTION ( 'NONE',  ( 0.000000000000000000, -6.467318590049456648E-15, 1.000000000000000000 ) ) ;
#74925=FACE_OUTER_BOUND ( 'NONE', #110020, .T. ) ;
#74930=CIRCLE ( 'NONE', #16663, 6.258578643762696458 ) ;
#74943=CARTESIAN_POINT ( 'NONE',  ( -18.59999994787167310, 85.52363768977360792, -96.14065794975194024 ) ) ;
#74978=CARTESIAN_POINT ( 'NONE',  ( -23.25000000000000000, 76.00000000001210765, -132.3731074845242972 ) ) ;
#74985=DIRECTION ( 'NONE',  ( -1.000000000000000000, 0.000000000000000000, -0.000000000000000000 ) ) ;
#75009=DIRECTION ( 'NONE',  ( 0.000000000000000000, 0.1350103645451807832, 0.9908441862701610203 ) ) ;
#75026=CARTESIAN_POINT ( 'NONE',  ( -23.15000000000000213, 76.00000000001190870, -103.0231074845243029 ) ) ;
#75044=DIRECTION ( 'NONE',  ( 0.000000000000000000, 0.000000000000000000, 1.000000000000000000 ) ) ;
#75057=CARTESIAN_POINT ( 'NONE',  ( 18.49999999999999289, 65.79142135624930177, -115.1731074845243796 ) ) ;
#75062=ORIENTED_EDGE ( 'NONE', *, *, #3406, .T. ) ;
#75079=AXIS2_PLACEMENT_3D ( 'NONE', #157945, #41829, #237436 ) ;
#75108=DIRECTION ( 'NONE',  ( 1.875376730785737719E-16, 1.000000000000000000, 6.982962677686266711E-15 ) ) ;
#75132=EDGE_CURVE ( 'NONE', #30882, #100578, #18015, .T. ) ;
#75217=CARTESIAN_POINT ( 'NONE',  ( 20.94999999999999929, 65.27628289530457550, -128.8581939154367717 ) ) ;
#75253=CIRCLE ( 'NONE', #108548, 0.09999999999998898659 ) ;
#75305=CARTESIAN_POINT ( 'NONE',  ( 23.14999999999999503, 61.90000000001194280, -108.6234050956637560 ) ) ;
#75307=DIRECTION ( 'NONE',  ( 0.000000000000000000, -7.086529944415894657E-15, 1.000000000000000000 ) ) ;
#75313=ORIENTED_EDGE ( 'NONE', *, *, #155034, .T. ) ;
#75318=DIRECTION ( 'NONE',  ( -1.000000000000000000, 2.952720810173289112E-16, 2.061873921506763405E-30 ) ) ;
#75337=CARTESIAN_POINT ( 'NONE',  ( 18.59999999999999432, 77.86671491006937629, -124.7704322382422788 ) ) ;
#75351=EDGE_CURVE ( 'NONE', #255544, #170158, #54011, .T. ) ;
#75354=ORIENTED_EDGE ( 'NONE', *, *, #79129, .F. ) ;
#75364=TOROIDAL_SURFACE ( 'NONE', #309, 0.2000000000000000111, 0.1000000000000000056 ) ;
#75368=CIRCLE ( 'NONE', #104525, 0.1000000000000045158 ) ;
#75384=DIRECTION ( 'NONE',  ( 1.000000000000000000, -2.952720810173289112E-16, -2.061873921506763405E-30 ) ) ;
#75415=ORIENTED_EDGE ( 'NONE', *, *, #157341, .T. ) ;
#75417=CARTESIAN_POINT ( 'NONE',  ( 21.08804582317324261, 67.12183383292016003, -124.1731076551190114 ) ) ;
#75443=AXIS2_PLACEMENT_3D ( 'NONE', #165271, #244799, #201832 ) ;
#75445=CARTESIAN_POINT ( 'NONE',  ( 21.14999999999999858, 76.10000000001214460, -136.5231074845242745 ) ) ;
#75479=VERTEX_POINT ( 'NONE', #142463 ) ;
#75500=AXIS2_PLACEMENT_3D ( 'NONE', #69717, #30596, #125810 ) ;
#75502=ORIENTED_EDGE ( 'NONE', *, *, #177803, .T. ) ;
#75527=FACE_OUTER_BOUND ( 'NONE', #158268, .T. ) ;
#75530=CARTESIAN_POINT ( 'NONE',  ( -20.64999999999999858, 85.00000000001197975, -112.9170766071766820 ) ) ;
#75552=VECTOR ( 'NONE', #183722, 1000.000000000000000 ) ;
#75611=DIRECTION ( 'NONE',  ( -1.000000000000000000, 0.000000000000000000, 0.000000000000000000 ) ) ;
#75686=ORIENTED_EDGE ( 'NONE', *, *, #136196, .F. ) ;
#75711=AXIS2_PLACEMENT_3D ( 'NONE', #101861, #242673, #241411 ) ;
#75740=EDGE_LOOP ( 'NONE', ( #71225, #158898, #241448 ) ) ;
#75759=CARTESIAN_POINT ( 'NONE',  ( 22.49806830649814060, 64.35011034517307849, -136.6005718008498775 ) ) ;
#75800=EDGE_CURVE ( 'NONE', #126029, #192766, #79121, .T. ) ;
#75842=VERTEX_POINT ( 'NONE', #212738 ) ;
#75856=CARTESIAN_POINT ( 'NONE',  ( -18.50000000000000711, 64.35000000001208775, -129.5083017138703667 ) ) ;
#75858=CARTESIAN_POINT ( 'NONE',  ( 20.95512820512820440, 65.37615131630019505, -128.8581939154367717 ) ) ;
#75866=EDGE_CURVE ( 'NONE', #102067, #60014, #75253, .T. ) ;
#75889=CARTESIAN_POINT ( 'NONE',  ( -23.15000000000000213, 76.00000000001192291, -105.1231074845242972 ) ) ;
#75898=CARTESIAN_POINT ( 'NONE',  ( 23.24999999999999289, 69.35000000001205933, -124.1731074845243370 ) ) ;
#75899=DIRECTION ( 'NONE',  ( 0.000000000000000000, -0.9998779222360097974, 0.01562500000000363945 ) ) ;
#75909=AXIS2_PLACEMENT_3D ( 'NONE', #199760, #197154, #18534 ) ;
#75950=ORIENTED_EDGE ( 'NONE', *, *, #218090, .T. ) ;
#75966=CARTESIAN_POINT ( 'NONE',  ( 20.85000000000000142, 77.83585931145546510, -91.51866831572576189 ) ) ;
#75977=ORIENTED_EDGE ( 'NONE', *, *, #210232, .T. ) ;
#75983=CARTESIAN_POINT ( 'NONE',  ( 21.53699400380725137, 69.21228820682151195, -136.5231074845243597 ) ) ;
#75987=DIRECTION ( 'NONE',  ( 1.000000000000000000, -2.952720810173289112E-16, -2.061873921506763405E-30 ) ) ;
#75990=CARTESIAN_POINT ( 'NONE',  ( -18.59999999999999787, 74.83729825007408465, -128.4231074845243086 ) ) ;
#76036=CARTESIAN_POINT ( 'NONE',  ( 20.94999999999999929, 64.25000000001195133, -109.8069731475024753 ) ) ;
#76039=EDGE_CURVE ( 'NONE', #202540, #217215, #37839, .T. ) ;
#76049=ORIENTED_EDGE ( 'NONE', *, *, #181014, .F. ) ;
#76054=DIRECTION ( 'NONE',  ( 1.441126678808781001E-14, -0.9876197685951241256, -0.1568667991644932258 ) ) ;
#76064=DIRECTION ( 'NONE',  ( 0.000000000000000000, 1.000000000000000000, 6.982962677686266711E-15 ) ) ;
#76069=DIRECTION ( 'NONE',  ( 1.000000000000000000, 0.000000000000000000, 0.000000000000000000 ) ) ;
#76088=CARTESIAN_POINT ( 'NONE',  ( -20.85000000000000142, 77.16412189325305349, -95.10825939895268277 ) ) ;
#76132=ORIENTED_EDGE ( 'NONE', *, *, #209439, .F. ) ;
#76136=VERTEX_POINT ( 'NONE', #213693 ) ;
#76141=CIRCLE ( 'NONE', #242734, 0.09999999999999939493 ) ;
#76173=ORIENTED_EDGE ( 'NONE', *, *, #40204, .T. ) ;
#76181=CARTESIAN_POINT ( 'NONE',  ( -18.33682934331560688, 85.51118559110531692, -96.11745271585121486 ) ) ;
#76202=ORIENTED_EDGE ( 'NONE', *, *, #123122, .T. ) ;
#76204=FACE_OUTER_BOUND ( 'NONE', #114760, .T. ) ;
#76227=CARTESIAN_POINT ( 'NONE',  ( 20.94999999999999574, 87.65000000001211333, -133.4231074845242233 ) ) ;
#76235=EDGE_CURVE ( 'NONE', #79346, #215387, #142038, .T. ) ;
#76241=CARTESIAN_POINT ( 'NONE',  ( 18.59999999999999076, 76.00000000001190870, -103.0231074845243029 ) ) ;
#76262=EDGE_LOOP ( 'NONE', ( #131250, #199929, #145514, #71117, #164598, #214831 ) ) ;
#76270=VERTEX_POINT ( 'NONE', #139265 ) ;
#76303=ORIENTED_EDGE ( 'NONE', *, *, #201594, .F. ) ;
#76348=DIRECTION ( 'NONE',  ( 0.000000000000000000, -6.938893903907222067E-15, 1.000000000000000000 ) ) ;
#76357=LINE ( 'NONE', #155943, #201478 ) ;
#76365=VECTOR ( 'NONE', #35299, 1000.000000000000000 ) ;
#76377=ORIENTED_EDGE ( 'NONE', *, *, #33799, .F. ) ;
#76410=EDGE_CURVE ( 'NONE', #18420, #2705, #38026, .T. ) ;
#76416=CARTESIAN_POINT ( 'NONE',  ( -20.96428641294177808, 64.25000000001195133, -109.8482143065830456 ) ) ;
#76418=EDGE_CURVE ( 'NONE', #25096, #106161, #183747, .T. ) ;
#76427=FACE_OUTER_BOUND ( 'NONE', #170666, .T. ) ;
#76462=CARTESIAN_POINT ( 'NONE',  ( -21.51976009735018991, 69.08954155835293420, -136.5231074845243313 ) ) ;
#76474=B_SPLINE_CURVE_WITH_KNOTS ( 'NONE', 3,
 ( #102107, #157331, #164685, #244196 ),
 .UNSPECIFIED., .F., .F.,
 ( 4, 4 ),
 ( 0.000000000000000000, 0.001767853679387121216 ),
 .UNSPECIFIED. ) ;
#76493=DIRECTION ( 'NONE',  ( 9.044546369203337730E-15, 0.7397360091702647189, 0.6728971962616949742 ) ) ;
#76504=VECTOR ( 'NONE', #206601, 1000.000000000000000 ) ;
#76539=FACE_OUTER_BOUND ( 'NONE', #84793, .T. ) ;
#76568=EDGE_CURVE ( 'NONE', #229103, #164631, #30933, .T. ) ;
#76585=DIRECTION ( 'NONE',  ( -4.801466763864314121E-15, 0.2605042016806606298, 0.9654727137038736640 ) ) ;
#76684=ORIENTED_EDGE ( 'NONE', *, *, #12823, .F. ) ;
#76700=DIRECTION ( 'NONE',  ( -0.000000000000000000, -6.982962677686266711E-15, 1.000000000000000000 ) ) ;
#76701=DIRECTION ( 'NONE',  ( 0.000000000000000000, -6.982962677686266711E-15, 1.000000000000000000 ) ) ;
#76731=CARTESIAN_POINT ( 'NONE',  ( -23.15000000000000213, 74.00000000001199396, -116.2477294072864140 ) ) ;
#76738=EDGE_CURVE ( 'NONE', #126698, #127664, #38205, .T. ) ;
#76815=CARTESIAN_POINT ( 'NONE',  ( -21.05000000000000071, 76.10000000001218723, -143.0637644362255401 ) ) ;
#76825=VERTEX_POINT ( 'NONE', #120733 ) ;
#76895=EDGE_CURVE ( 'NONE', #146024, #70177, #113008, .T. ) ;
#76910=CARTESIAN_POINT ( 'NONE',  ( -18.39999999999999858, 85.68240343348826116, -96.36626410711143365 ) ) ;
#76926=VERTEX_POINT ( 'NONE', #13608 ) ;
#76951=DIRECTION ( 'NONE',  ( 0.000000000000000000, 0.000000000000000000, -1.000000000000000000 ) ) ;
#76953=ORIENTED_EDGE ( 'NONE', *, *, #125698, .F. ) ;
#76954=VERTEX_POINT ( 'NONE', #247056 ) ;
#77035=DIRECTION ( 'NONE',  ( 0.000000000000000000, -6.982962677686266711E-15, 1.000000000000000000 ) ) ;
#77096=ORIENTED_EDGE ( 'NONE', *, *, #221011, .T. ) ;
#77105=DIRECTION ( 'NONE',  ( -0.000000000000000000, 1.000000000000000000, 6.982962677686266711E-15 ) ) ;
#77124=ADVANCED_FACE ( 'NONE', ( #246449 ), #86053, .T. ) ;
#77136=DIRECTION ( 'NONE',  ( -1.000000000000000000, -0.000000000000000000, -0.000000000000000000 ) ) ;
#77144=CARTESIAN_POINT ( 'NONE',  ( 22.45301702632625762, 75.98478912030203958, -148.1728997087846835 ) ) ;
#77173=FACE_OUTER_BOUND ( 'NONE', #79835, .T. ) ;
#77217=CARTESIAN_POINT ( 'NONE',  ( -22.39999999999999858, 75.90000000001214175, -136.5231074845242745 ) ) ;
#77230=FACE_OUTER_BOUND ( 'NONE', #152213, .T. ) ;
#77244=DIRECTION ( 'NONE',  ( -1.000000000000000000, 2.952720810173289112E-16, 2.061873921506763405E-30 ) ) ;
#77250=ORIENTED_EDGE ( 'NONE', *, *, #108656, .F. ) ;
#77256=CARTESIAN_POINT ( 'NONE',  ( -18.58735405345342429, 85.56647862034844820, -96.20039283825825294 ) ) ;
#77270=DIRECTION ( 'NONE',  ( 0.000000000000000000, -6.982962677686266711E-15, 1.000000000000000000 ) ) ;
#77277=AXIS2_PLACEMENT_3D ( 'NONE', #171135, #208928, #10736 ) ;
#77337=CARTESIAN_POINT ( 'NONE',  ( -18.42609945526433535, 85.49999971050304737, -129.5237449942748640 ) ) ;
#77354=ADVANCED_FACE ( 'NONE', ( #229459 ), #152516, .F. ) ;
#77372=CARTESIAN_POINT ( 'NONE',  ( 18.39999999999999858, 85.50000000001209344, -129.4910380878245633 ) ) ;
#77382=DIRECTION ( 'NONE',  ( -0.000000000000000000, 1.000000000000000000, 6.982962677686266711E-15 ) ) ;
#77441=DIRECTION ( 'NONE',  ( 0.000000000000000000, 0.000000000000000000, 1.000000000000000000 ) ) ;
#77468=ORIENTED_EDGE ( 'NONE', *, *, #63535, .F. ) ;
#77470=EDGE_CURVE ( 'NONE', #170896, #207616, #171121, .T. ) ;
#77479=AXIS2_PLACEMENT_3D ( 'NONE', #153114, #93084, #115223 ) ;
#77545=DIRECTION ( 'NONE',  ( 0.000000000000000000, -0.4999999999999689138, -0.8660254037844565822 ) ) ;
#77547=ADVANCED_FACE ( 'NONE', ( #201876 ), #172858, .T. ) ;
#77550=DIRECTION ( 'NONE',  ( -1.000000000000000000, 0.000000000000000000, 0.000000000000000000 ) ) ;
#77560=CARTESIAN_POINT ( 'NONE',  ( -20.64999999999999858, 76.00000000001190870, -103.0231074845243029 ) ) ;
#77598=EDGE_CURVE ( 'NONE', #181206, #102067, #47922, .T. ) ;
#77613=DIRECTION ( 'NONE',  ( 2.952720810173289112E-16, 1.000000000000000000, 6.982962677686266711E-15 ) ) ;
#77616=VECTOR ( 'NONE', #48903, 1000.000000000000114 ) ;
#77624=ORIENTED_EDGE ( 'NONE', *, *, #198474, .T. ) ;
#77632=CARTESIAN_POINT ( 'NONE',  ( -21.05000000000000071, 87.29603075034741266, -133.4752083248603469 ) ) ;
#77633=TOROIDAL_SURFACE ( 'NONE', #144263, 0.9750000000000019762, 0.1000000000000000056 ) ;
#77635=AXIS2_PLACEMENT_3D ( 'NONE', #80429, #122177, #184697 ) ;
#77637=CARTESIAN_POINT ( 'NONE',  ( -18.50000000000000000, 77.16412189325305349, -95.30825939895268561 ) ) ;
#77652=DIRECTION ( 'NONE',  ( -0.000000000000000000, 1.000000000000000000, 6.982962677686266711E-15 ) ) ;
#77773=EDGE_CURVE ( 'NONE', #8640, #147707, #760, .T. ) ;
#77786=ORIENTED_EDGE ( 'NONE', *, *, #171438, .T. ) ;
#77815=DIRECTION ( 'NONE',  ( 0.000000000000000000, 0.1350103645451945777, -0.9908441862701591329 ) ) ;
#77865=CARTESIAN_POINT ( 'NONE',  ( 21.05281448260627641, 67.22398984147443457, -124.3495495727129310 ) ) ;
#77896=ORIENTED_EDGE ( 'NONE', *, *, #206162, .T. ) ;
#77917=ORIENTED_EDGE ( 'NONE', *, *, #21529, .F. ) ;
#77928=DIRECTION ( 'NONE',  ( 0.000000000000000000, -6.517943393102682774E-15, 1.000000000000000000 ) ) ;
#77962=DIRECTION ( 'NONE',  ( 0.000000000000000000, -6.982962677686266711E-15, 1.000000000000000000 ) ) ;
#77968=AXIS2_PLACEMENT_3D ( 'NONE', #255094, #154799, #55627 ) ;
#77969=ORIENTED_EDGE ( 'NONE', *, *, #74544, .F. ) ;
#77970=CARTESIAN_POINT ( 'NONE',  ( -20.54999999999999716, 74.00000000001199396, -116.2477294072864140 ) ) ;
#77975=AXIS2_PLACEMENT_3D ( 'NONE', #246151, #162777, #226559 ) ;
#77983=ORIENTED_EDGE ( 'NONE', *, *, #39573, .F. ) ;
#77988=DIRECTION ( 'NONE',  ( -2.840903330521632269E-16, -0.8700118002898356018, 0.4930308989875170078 ) ) ;
#78011=EDGE_CURVE ( 'NONE', #229125, #124002, #992, .T. ) ;
#78026=DIRECTION ( 'NONE',  ( 0.000000000000000000, 7.116814260417668513E-15, -1.000000000000000000 ) ) ;
#78048=DIRECTION ( 'NONE',  ( 1.000000000000000000, 0.000000000000000000, 0.000000000000000000 ) ) ;
#78052=SPHERICAL_SURFACE ( 'NONE', #61687, 0.1000000000000000056 ) ;
#78079=EDGE_LOOP ( 'NONE', ( #4174, #197991, #162462, #77468 ) ) ;
#78091=CARTESIAN_POINT ( 'NONE',  ( -20.94999999999999929, 88.41227409416161720, -106.0231074845242176 ) ) ;
#78094=CIRCLE ( 'NONE', #19674, 0.6000000000000033085 ) ;
#78100=ORIENTED_EDGE ( 'NONE', *, *, #173248, .T. ) ;
#78136=LINE ( 'NONE', #175998, #199895 ) ;
#78172=CARTESIAN_POINT ( 'NONE',  ( 20.94999999999999574, 70.10000000001213039, -126.3040077198679398 ) ) ;
#78177=DIRECTION ( 'NONE',  ( 0.000000000000000000, 6.982962677686266711E-15, -1.000000000000000000 ) ) ;
#78202=AXIS2_PLACEMENT_3D ( 'NONE', #39015, #95121, #57252 ) ;
#78205=ADVANCED_FACE ( 'NONE', ( #4341 ), #120487, .T. ) ;
#78218=DIRECTION ( 'NONE',  ( 0.000000000000000000, 6.982962677686266711E-15, -1.000000000000000000 ) ) ;
#78226=DIRECTION ( 'NONE',  ( 0.000000000000000000, -7.272083257015735086E-15, 1.000000000000000000 ) ) ;
#78277=VECTOR ( 'NONE', #119251, 1000.000000000000000 ) ;
#78291=CARTESIAN_POINT ( 'NONE',  ( -23.15000000000000213, 76.00000000001190870, -103.0231074845243029 ) ) ;
#78339=AXIS2_PLACEMENT_3D ( 'NONE', #161889, #160612, #100568 ) ;
#78341=AXIS2_PLACEMENT_3D ( 'NONE', #31832, #111342, #250830 ) ;
#78367=DIRECTION ( 'NONE',  ( 0.000000000000000000, -6.982962677686266711E-15, 1.000000000000000000 ) ) ;
#78406=ORIENTED_EDGE ( 'NONE', *, *, #12626, .T. ) ;
#78411=DIRECTION ( 'NONE',  ( 0.000000000000000000, 0.1455152366551500653, 0.9893560106964507384 ) ) ;
#78420=CARTESIAN_POINT ( 'NONE',  ( -22.39999999999999858, 76.00000000001217870, -142.7731074845243029 ) ) ;
#78426=CARTESIAN_POINT ( 'NONE',  ( 22.40736611211992368, 76.00000000001222134, -148.1726782920690937 ) ) ;
#78438=FACE_OUTER_BOUND ( 'NONE', #144674, .T. ) ;
#78440=ORIENTED_EDGE ( 'NONE', *, *, #75866, .T. ) ;
#78462=ADVANCED_FACE ( 'NONE', ( #193281 ), #74653, .F. ) ;
#78482=CARTESIAN_POINT ( 'NONE',  ( -18.58222699835055280, 65.66799936921530900, -97.42993998886007034 ) ) ;
#78490=DIRECTION ( 'NONE',  ( -7.304098846218134667E-16, -1.000000000000000000, -6.982962677686267499E-15 ) ) ;
#78528=FACE_OUTER_BOUND ( 'NONE', #244075, .T. ) ;
#78542=ORIENTED_EDGE ( 'NONE', *, *, #176439, .F. ) ;
#78547=EDGE_CURVE ( 'NONE', #17884, #64483, #159812, .T. ) ;
#78574=DIRECTION ( 'NONE',  ( -1.000000000000000000, 0.000000000000000000, -0.000000000000000000 ) ) ;
#78634=CIRCLE ( 'NONE', #187020, 0.09999999999999939493 ) ;
#78668=EDGE_LOOP ( 'NONE', ( #232420, #141154, #146718 ) ) ;
#78679=CIRCLE ( 'NONE', #249401, 7.800000000000001599 ) ;
#78693=EDGE_LOOP ( 'NONE', ( #148559, #40314, #147828, #218413 ) ) ;
#78750=CARTESIAN_POINT ( 'NONE',  ( -20.54999999999999716, 73.60000000001197407, -112.9170766071767531 ) ) ;
#78766=ORIENTED_EDGE ( 'NONE', *, *, #62827, .F. ) ;
#78782=CARTESIAN_POINT ( 'NONE',  ( 21.09107601085585770, 75.96069283529517691, -142.8869854598850111 ) ) ;
#78794=EDGE_CURVE ( 'NONE', #73683, #35302, #22266, .T. ) ;
#78856=CARTESIAN_POINT ( 'NONE',  ( -18.59999999999999787, 64.35000000001222986, -148.2731074845243882 ) ) ;
#78864=LINE ( 'NONE', #119307, #58142 ) ;
#78890=CIRCLE ( 'NONE', #212216, 0.1000000000000028644 ) ;
#78926=VERTEX_POINT ( 'NONE', #5974 ) ;
#78942=AXIS2_PLACEMENT_3D ( 'NONE', #191640, #54644, #36406 ) ;
#78958=DIRECTION ( 'NONE',  ( -1.000000000000000000, 0.000000000000000000, 0.000000000000000000 ) ) ;
#78965=ORIENTED_EDGE ( 'NONE', *, *, #179148, .F. ) ;
#78986=AXIS2_PLACEMENT_3D ( 'NONE', #217080, #219659, #98392 ) ;
#78995=ADVANCED_FACE ( 'NONE', ( #64677 ), #24296, .F. ) ;
#79005=CARTESIAN_POINT ( 'NONE',  ( -21.05000000000000071, 75.96824164695662773, -142.7819546076043764 ) ) ;
#79026=ORIENTED_EDGE ( 'NONE', *, *, #23764, .T. ) ;
#79031=CARTESIAN_POINT ( 'NONE',  ( 23.24999999999999289, 69.55000000001223270, -148.2731074845243597 ) ) ;
#79044=CARTESIAN_POINT ( 'NONE',  ( 23.15000000000000213, 85.00000000001197975, -112.4170766071766678 ) ) ;
#79105=EDGE_CURVE ( 'NONE', #51816, #60637, #181621, .T. ) ;
#79107=ORIENTED_EDGE ( 'NONE', *, *, #257661, .T. ) ;
#79121=CIRCLE ( 'NONE', #175057, 0.1000000000000028644 ) ;
#79129=EDGE_CURVE ( 'NONE', #230388, #236302, #245897, .T. ) ;
#79137=CYLINDRICAL_SURFACE ( 'NONE', #158890, 0.1000000000000028644 ) ;
#79152=ORIENTED_EDGE ( 'NONE', *, *, #30098, .F. ) ;
#79245=CYLINDRICAL_SURFACE ( 'NONE', #35079, 0.5000000000000004441 ) ;
#79254=CARTESIAN_POINT ( 'NONE',  ( -23.15000000000000213, 73.40000000001201386, -116.2477294072864140 ) ) ;
#79265=DIRECTION ( 'NONE',  ( 1.000000000000000000, 0.000000000000000000, 0.000000000000000000 ) ) ;
#79290=ORIENTED_EDGE ( 'NONE', *, *, #231786, .F. ) ;
#79305=DIRECTION ( 'NONE',  ( 0.000000000000000000, 0.1298341882519953583, 0.9915357197604862671 ) ) ;
#79329=CARTESIAN_POINT ( 'NONE',  ( -23.25000000000000000, 70.05000000001197691, -113.3288097895591591 ) ) ;
#79330=CARTESIAN_POINT ( 'NONE',  ( 18.59999999999999787, 77.83585931145546510, -91.51866831572576189 ) ) ;
#79334=VERTEX_POINT ( 'NONE', #222132 ) ;
#79346=VERTEX_POINT ( 'NONE', #183055 ) ;
#79404=AXIS2_PLACEMENT_3D ( 'NONE', #159692, #20183, #218345 ) ;
#79421=CARTESIAN_POINT ( 'NONE',  ( -18.59999999999999787, 77.16412189325305349, -95.10825939895268277 ) ) ;
#79427=DIRECTION ( 'NONE',  ( 0.000000000000000000, 6.982962677686266711E-15, -1.000000000000000000 ) ) ;
#79439=EDGE_CURVE ( 'NONE', #157942, #73178, #109906, .T. ) ;
#79443=EDGE_CURVE ( 'NONE', #202540, #158504, #98349, .T. ) ;
#79462=CARTESIAN_POINT ( 'NONE',  ( 20.94999999999999929, 88.41227409416161720, -106.0231074845242176 ) ) ;
#79466=CARTESIAN_POINT ( 'NONE',  ( 21.70464131381650219, 68.90464198104429272, -136.5231074845243313 ) ) ;
#79532=CARTESIAN_POINT ( 'NONE',  ( 20.19326291201646129, 65.84393901210815159, -128.7612456769174685 ) ) ;
#79555=CIRCLE ( 'NONE', #150325, 2.100000000000004530 ) ;
#79591=DIRECTION ( 'NONE',  ( 1.000000000000000000, 0.000000000000000000, 0.000000000000000000 ) ) ;
#79613=EDGE_CURVE ( 'NONE', #24834, #105325, #193321, .T. ) ;
#79644=CARTESIAN_POINT ( 'NONE',  ( 23.15000000000000213, 85.00000000001197975, -112.9170766071766820 ) ) ;
#79671=EDGE_CURVE ( 'NONE', #153892, #156274, #190184, .T. ) ;
#79707=DIRECTION ( 'NONE',  ( -0.000000000000000000, 0.1298341882520054891, 0.9915357197604850459 ) ) ;
#79731=DIRECTION ( 'NONE',  ( -0.000000000000000000, 1.000000000000000000, 6.982962677686266711E-15 ) ) ;
#79743=EDGE_CURVE ( 'NONE', #246153, #242065, #105441, .T. ) ;
#79753=DIRECTION ( 'NONE',  ( -0.000000000000000000, 1.000000000000000000, 6.982962677686267499E-15 ) ) ;
#79754=CARTESIAN_POINT ( 'NONE',  ( -18.50000324121759121, 65.70692517833234092, -97.56446533783034170 ) ) ;
#79758=FACE_OUTER_BOUND ( 'NONE', #200587, .T. ) ;
#79782=EDGE_CURVE ( 'NONE', #139626, #250872, #2896, .T. ) ;
#79787=CARTESIAN_POINT ( 'NONE',  ( 23.15000000000000213, 85.60000000001208775, -126.6291383618717816 ) ) ;
#79794=AXIS2_PLACEMENT_3D ( 'NONE', #24473, #4844, #85657 ) ;
#79835=EDGE_LOOP ( 'NONE', ( #77786, #58265 ) ) ;
#79876=EDGE_CURVE ( 'NONE', #221149, #18233, #190375, .T. ) ;
#79882=DIRECTION ( 'NONE',  ( -1.000000000000000000, -7.304098846218135653E-16, -4.639676173203994055E-30 ) ) ;
#79884=CARTESIAN_POINT ( 'NONE',  ( -18.41799967126736348, 85.50000000001209344, -129.4910376712676907 ) ) ;
#79887=AXIS2_PLACEMENT_3D ( 'NONE', #108061, #183744, #67640 ) ;
#79951=EDGE_CURVE ( 'NONE', #135981, #155470, #193019, .T. ) ;
#79969=CIRCLE ( 'NONE', #217533, 0.1000000000000028644 ) ;
#79972=CIRCLE ( 'NONE', #67351, 12.77499999999999503 ) ;
#80025=CARTESIAN_POINT ( 'NONE',  ( 21.05000000000000071, 67.12338541492499644, -128.1380270056797031 ) ) ;
#80026=VERTEX_POINT ( 'NONE', #61201 ) ;
#80030=EDGE_CURVE ( 'NONE', #191527, #111919, #78094, .T. ) ;
#80061=DIRECTION ( 'NONE',  ( 0.000000000000000000, 0.9908441862701791170, -0.1350103645450472789 ) ) ;
#80093=ADVANCED_FACE ( 'NONE', ( #220293 ), #99010, .F. ) ;
#80134=DIRECTION ( 'NONE',  ( -2.952720810173289112E-16, -1.000000000000000000, -6.982962677686266711E-15 ) ) ;
#80135=AXIS2_PLACEMENT_3D ( 'NONE', #175657, #118239, #255124 ) ;
#80142=FACE_OUTER_BOUND ( 'NONE', #55414, .T. ) ;
#80157=CARTESIAN_POINT ( 'NONE',  ( -23.15000000000000213, 85.00000000001207923, -126.6291383618717816 ) ) ;
#80162=B_SPLINE_CURVE_WITH_KNOTS ( 'NONE', 3,
 ( #255164, #178286, #236945, #199104, #58287, #218650 ),
 .UNSPECIFIED., .F., .F.,
 ( 4, 2, 4 ),
 ( 0.000000000000000000, 0.0001496588209255877576, 0.0002993176418511755152 ),
 .UNSPECIFIED. ) ;
#80163=CIRCLE ( 'NONE', #159338, 2.000000000000001776 ) ;
#80171=DIRECTION ( 'NONE',  ( -1.000000000000000000, -0.000000000000000000, -0.000000000000000000 ) ) ;
#80198=LINE ( 'NONE', #243159, #256117 ) ;
#80213=ORIENTED_EDGE ( 'NONE', *, *, #224498, .F. ) ;
#80221=DIRECTION ( 'NONE',  ( -1.000000000000000000, 0.000000000000000000, -0.000000000000000000 ) ) ;
#80242=DIRECTION ( 'NONE',  ( 0.000000000000000000, -0.1495327102803078179, 0.9887567792719429427 ) ) ;
#80262=AXIS2_PLACEMENT_3D ( 'NONE', #210656, #167708, #90697 ) ;
#80263=ORIENTED_EDGE ( 'NONE', *, *, #43894, .F. ) ;
#80271=EDGE_LOOP ( 'NONE', ( #191659, #205241, #112938, #109140 ) ) ;
#80275=ORIENTED_EDGE ( 'NONE', *, *, #240199, .F. ) ;
#80283=CARTESIAN_POINT ( 'NONE',  ( -21.05000000000000071, 75.98514436511875658, -142.8674665265674264 ) ) ;
#80294=CARTESIAN_POINT ( 'NONE',  ( -20.94999999999999929, 64.40000000001195701, -109.9513107147998880 ) ) ;
#80318=ORIENTED_EDGE ( 'NONE', *, *, #179148, .T. ) ;
#80331=CARTESIAN_POINT ( 'NONE',  ( -20.64999999999999858, 71.65000000001199965, -115.3731074845243256 ) ) ;
#80341=DIRECTION ( 'NONE',  ( 0.000000000000000000, 0.000000000000000000, -1.000000000000000000 ) ) ;
#80343=VERTEX_POINT ( 'NONE', #250110 ) ;
#80361=CARTESIAN_POINT ( 'NONE',  ( 20.85000000000000142, 69.06610602788553877, -99.23746165015076315 ) ) ;
#80363=DIRECTION ( 'NONE',  ( 0.000000000000000000, 1.000000000000000000, 6.982962677686266711E-15 ) ) ;
#80376=DIRECTION ( 'NONE',  ( 1.000000000000000000, 0.000000000000000000, 0.000000000000000000 ) ) ;
#80389=CARTESIAN_POINT ( 'NONE',  ( -23.25000000000000000, 71.75000000001199396, -115.3731074845243256 ) ) ;
#80396=CARTESIAN_POINT ( 'NONE',  ( 23.15000000000000213, 84.59626168225496201, -112.4732350016745244 ) ) ;
#80416=CARTESIAN_POINT ( 'NONE',  ( -18.59999999999999787, 68.92903212821303782, -99.27654326265604823 ) ) ;
#80428=ORIENTED_EDGE ( 'NONE', *, *, #163894, .F. ) ;
#80429=CARTESIAN_POINT ( 'NONE',  ( 20.94999999999999929, 76.00000000001190870, -103.0231074845243029 ) ) ;
#80431=ORIENTED_EDGE ( 'NONE', *, *, #62141, .T. ) ;
#80444=LINE ( 'NONE', #6068, #112267 ) ;
#80478=EDGE_CURVE ( 'NONE', #228703, #8664, #105109, .T. ) ;
#80512=ORIENTED_EDGE ( 'NONE', *, *, #105881, .T. ) ;
#80566=AXIS2_PLACEMENT_3D ( 'NONE', #25068, #66741, #141145 ) ;
#80581=EDGE_CURVE ( 'NONE', #229103, #164288, #186449, .T. ) ;
#80606=AXIS2_PLACEMENT_3D ( 'NONE', #32981, #92893, #214142 ) ;
#80624=AXIS2_PLACEMENT_3D ( 'NONE', #224513, #23787, #142409 ) ;
#80630=LINE ( 'NONE', #118522, #186341 ) ;
#80631=EDGE_LOOP ( 'NONE', ( #21142, #31841, #236669, #197323 ) ) ;
#80648=ORIENTED_EDGE ( 'NONE', *, *, #200566, .F. ) ;
#80660=DIRECTION ( 'NONE',  ( 0.000000000000000000, 0.000000000000000000, 1.000000000000000000 ) ) ;
#80665=CARTESIAN_POINT ( 'NONE',  ( 18.49999999999999289, 68.97833521811179480, -99.18954208262705663 ) ) ;
#80693=ORIENTED_EDGE ( 'NONE', *, *, #242464, .F. ) ;
#80715=DIRECTION ( 'NONE',  ( 0.000000000000000000, -7.172728831056617961E-15, 1.000000000000000000 ) ) ;
#80716=DIRECTION ( 'NONE',  ( 0.000000000000000000, 3.208737065390626061E-15, 1.000000000000000000 ) ) ;
#80728=CARTESIAN_POINT ( 'NONE',  ( 18.41356215285961540, 85.50000000001209344, -129.4910380878245917 ) ) ;
#80782=ADVANCED_FACE ( 'NONE', ( #203628 ), #178972, .F. ) ;
#80807=AXIS2_PLACEMENT_3D ( 'NONE', #247601, #45552, #245035 ) ;
#80815=CARTESIAN_POINT ( 'NONE',  ( 20.54374330479327426, 65.49498968578909341, -128.7974238496362602 ) ) ;
#80837=CARTESIAN_POINT ( 'NONE',  ( 21.07933241753356768, 69.67135405163237749, -136.6164870749436488 ) ) ;
#80853=VECTOR ( 'NONE', #25410, 1000.000000000000000 ) ;
#80854=EDGE_CURVE ( 'NONE', #45647, #1820, #242740, .T. ) ;
#80891=CARTESIAN_POINT ( 'NONE',  ( -21.45000000000000284, 68.29142135624930177, -115.2731074845243455 ) ) ;
#80898=CIRCLE ( 'NONE', #122638, 11.65000000000000746 ) ;
#80904=AXIS2_PLACEMENT_3D ( 'NONE', #92988, #207841, #29218 ) ;
#80914=DIRECTION ( 'NONE',  ( 2.952720810173289112E-16, 1.000000000000000000, 6.308085367188367561E-15 ) ) ;
#80920=AXIS2_PLACEMENT_3D ( 'NONE', #257011, #156713, #78411 ) ;
#80937=ORIENTED_EDGE ( 'NONE', *, *, #134080, .F. ) ;
#80960=AXIS2_PLACEMENT_3D ( 'NONE', #211130, #207299, #147301 ) ;
#80970=EDGE_CURVE ( 'NONE', #153127, #16840, #229618, .T. ) ;
#81007=CARTESIAN_POINT ( 'NONE',  ( -21.05000000000000071, 76.00000000001188027, -98.92310748452429436 ) ) ;
#81080=CARTESIAN_POINT ( 'NONE',  ( -21.53699400384082807, 75.99999999999387512, -143.3108192777702072 ) ) ;
#81127=EDGE_CURVE ( 'NONE', #17682, #8134, #216457, .T. ) ;
#81132=DIRECTION ( 'NONE',  ( 1.000000000000000000, 0.000000000000000000, 0.000000000000000000 ) ) ;
#81134=CIRCLE ( 'NONE', #143686, 0.09999999999998898659 ) ;
#81138=CARTESIAN_POINT ( 'NONE',  ( -21.55000000000000426, 68.29142135624930177, -115.2731074845243455 ) ) ;
#81155=ORIENTED_EDGE ( 'NONE', *, *, #141451, .F. ) ;
#81183=EDGE_LOOP ( 'NONE', ( #144456, #152037, #57275, #74273 ) ) ;
#81212=CARTESIAN_POINT ( 'NONE',  ( -23.15000000000000213, 76.00000000001213607, -136.5231074845242745 ) ) ;
#81239=SPHERICAL_SURFACE ( 'NONE', #28349, 0.1000000000000000056 ) ;
#81256=ORIENTED_EDGE ( 'NONE', *, *, #136335, .T. ) ;
#81263=DIRECTION ( 'NONE',  ( 1.000000000000000000, 0.000000000000000000, 0.000000000000000000 ) ) ;
#81296=DIRECTION ( 'NONE',  ( -1.000000000000000000, -0.000000000000000000, -0.000000000000000000 ) ) ;
#81318=FACE_OUTER_BOUND ( 'NONE', #40281, .T. ) ;
#81327=VERTEX_POINT ( 'NONE', #128930 ) ;
#81355=AXIS2_PLACEMENT_3D ( 'NONE', #154418, #136067, #235201 ) ;
#81357=DIRECTION ( 'NONE',  ( -1.000000000000000000, 0.000000000000000000, -0.000000000000000000 ) ) ;
#81372=EDGE_LOOP ( 'NONE', ( #3015, #179836, #254780, #31985 ) ) ;
#81388=DIRECTION ( 'NONE',  ( 0.000000000000000000, 0.000000000000000000, 1.000000000000000000 ) ) ;
#81441=ORIENTED_EDGE ( 'NONE', *, *, #203677, .T. ) ;
#81466=DIRECTION ( 'NONE',  ( 1.000000000000000000, -2.952720810173289112E-16, -2.061873921506763405E-30 ) ) ;
#81474=DIRECTION ( 'NONE',  ( -0.000000000000000000, 1.000000000000000000, 6.982962677686266711E-15 ) ) ;
#81548=LINE ( 'NONE', #217218, #72988 ) ;
#81552=CARTESIAN_POINT ( 'NONE',  ( -20.94999999999999929, 68.96868720525668550, -99.41395654629704381 ) ) ;
#81563=AXIS2_PLACEMENT_3D ( 'NONE', #208892, #231051, #48534 ) ;
#81595=CARTESIAN_POINT ( 'NONE',  ( 20.94999999999999929, 65.70711192142366031, -97.56510546851220056 ) ) ;
#81706=AXIS2_PLACEMENT_3D ( 'NONE', #161375, #203045, #217462 ) ;
#81718=DIRECTION ( 'NONE',  ( -1.000000000000000000, -4.163336342344362270E-13, 0.000000000000000000 ) ) ;
#81727=CARTESIAN_POINT ( 'NONE',  ( -18.59999999999999787, 64.25000000001210765, -129.5083017138703667 ) ) ;
#81729=DIRECTION ( 'NONE',  ( -2.602085213965226419E-14, 6.982962677686266711E-15, -1.000000000000000000 ) ) ;
#81752=AXIS2_PLACEMENT_3D ( 'NONE', #100237, #39031, #136821 ) ;
#81757=FACE_OUTER_BOUND ( 'NONE', #9045, .T. ) ;
#81768=B_SPLINE_CURVE_WITH_KNOTS ( 'NONE', 3,
 ( #114378, #213472, #193930, #174408 ),
 .UNSPECIFIED., .F., .F.,
 ( 4, 4 ),
 ( 0.000000000000000000, 0.0002118541922231925311 ),
 .UNSPECIFIED. ) ;
#81771=CARTESIAN_POINT ( 'NONE',  ( 23.14999999999998437, 80.05000000001213323, -136.5231074845242460 ) ) ;
#81774=ORIENTED_EDGE ( 'NONE', *, *, #11028, .T. ) ;
#81785=FACE_OUTER_BOUND ( 'NONE', #98932, .T. ) ;
#81891=AXIS2_PLACEMENT_3D ( 'NONE', #30656, #151892, #52748 ) ;
#81900=ORIENTED_EDGE ( 'NONE', *, *, #113708, .F. ) ;
#81909=DIRECTION ( 'NONE',  ( 1.000000000000000000, -7.304098846218134667E-16, -5.100424963727256530E-30 ) ) ;
#81910=CARTESIAN_POINT ( 'NONE',  ( -18.59999999999999787, 85.40000000001187175, -96.14106563635156988 ) ) ;
#81928=DIRECTION ( 'NONE',  ( 0.000000000000000000, -6.938893903907222067E-15, 1.000000000000000000 ) ) ;
#81939=EDGE_CURVE ( 'NONE', #22794, #147164, #78864, .T. ) ;
#81944=EDGE_LOOP ( 'NONE', ( #50053, #13292, #107213 ) ) ;
#81972=ORIENTED_EDGE ( 'NONE', *, *, #205128, .F. ) ;
#81982=DIRECTION ( 'NONE',  ( -0.000000000000000000, 1.000000000000000000, 6.982962677686266711E-15 ) ) ;
#81998=CARTESIAN_POINT ( 'NONE',  ( 23.14999999999998437, 76.00000000001213607, -136.5231074845242745 ) ) ;
#82006=AXIS2_PLACEMENT_3D ( 'NONE', #26915, #2165, #102529 ) ;
#82032=EDGE_LOOP ( 'NONE', ( #39309, #96760, #121314, #109501 ) ) ;
#82051=CARTESIAN_POINT ( 'NONE',  ( 20.94999999999999929, 76.00000000001190870, -103.0231074845243029 ) ) ;
#82054=CARTESIAN_POINT ( 'NONE',  ( -18.50000000000000000, 69.15387683765929694, -99.28538121767448388 ) ) ;
#82070=EDGE_CURVE ( 'NONE', #28671, #162629, #66561, .T. ) ;
#82074=EDGE_CURVE ( 'NONE', #156363, #213344, #163571, .T. ) ;
#82091=CARTESIAN_POINT ( 'NONE',  ( 20.22516295850462598, 66.10063570456183868, -128.6130417724335473 ) ) ;
#82110=AXIS2_PLACEMENT_3D ( 'NONE', #92861, #195852, #211541 ) ;
#82127=CIRCLE ( 'NONE', #48827, 0.1000000000000028644 ) ;
#82189=VERTEX_POINT ( 'NONE', #243096 ) ;
#82200=EDGE_CURVE ( 'NONE', #78926, #144360, #220953, .T. ) ;
#82220=ADVANCED_FACE ( 'NONE', ( #123161 ), #103564, .T. ) ;
#82249=CARTESIAN_POINT ( 'NONE',  ( 21.05000000000000426, 76.03753606329787829, -142.8553797584599749 ) ) ;
#82252=TOROIDAL_SURFACE ( 'NONE', #244585, 7.800000000000000711, 0.1000000000000000056 ) ;
#82253=ORIENTED_EDGE ( 'NONE', *, *, #61241, .F. ) ;
#82273=DIRECTION ( 'NONE',  ( -1.000000000000000000, 0.000000000000000000, -0.000000000000000000 ) ) ;
#82274=CARTESIAN_POINT ( 'NONE',  ( 21.05000000000000071, 74.16465844978765176, -124.9679561919613207 ) ) ;
#82284=DIRECTION ( 'NONE',  ( 1.000000000000000000, 0.000000000000000000, 0.000000000000000000 ) ) ;
#82295=CYLINDRICAL_SURFACE ( 'NONE', #78339, 12.87499999999999822 ) ;
#82296=CARTESIAN_POINT ( 'NONE',  ( -21.44999999999999929, 68.85000000001205933, -124.1731074845243370 ) ) ;
#82309=AXIS2_PLACEMENT_3D ( 'NONE', #31703, #192051, #251996 ) ;
#82318=CARTESIAN_POINT ( 'NONE',  ( 23.14999999999999503, 64.35000000001195986, -110.0379132551783243 ) ) ;
#82327=ORIENTED_EDGE ( 'NONE', *, *, #46379, .F. ) ;
#82332=DIRECTION ( 'NONE',  ( 1.000000000000000000, 0.000000000000000000, 0.000000000000000000 ) ) ;
#82380=EDGE_CURVE ( 'NONE', #235551, #69086, #220683, .T. ) ;
#82423=CIRCLE ( 'NONE', #40798, 11.80000000000000426 ) ;
#82427=CARTESIAN_POINT ( 'NONE',  ( -23.15000000000000213, 64.35000000001205933, -124.3731074845243825 ) ) ;
#82430=DIRECTION ( 'NONE',  ( -1.000000000000000000, -0.000000000000000000, -0.000000000000000000 ) ) ;
#82476=EDGE_LOOP ( 'NONE', ( #18576, #119474, #161014, #243803 ) ) ;
#82490=CIRCLE ( 'NONE', #36781, 0.1000000000000028644 ) ;
#82494=CARTESIAN_POINT ( 'NONE',  ( 21.04999999999999716, 69.70076908992525944, -136.6215449845243768 ) ) ;
#82511=CARTESIAN_POINT ( 'NONE',  ( -21.05000000000000071, 77.16270174995010223, -128.4231074845242802 ) ) ;
#82513=LINE ( 'NONE', #102082, #23922 ) ;
#82555=VECTOR ( 'NONE', #94775, 1000.000000000000000 ) ;
#82579=CARTESIAN_POINT ( 'NONE',  ( -18.40000000000000213, 85.68240343348826116, -96.36626410711144786 ) ) ;
#82597=VERTEX_POINT ( 'NONE', #150140 ) ;
#82643=CARTESIAN_POINT ( 'NONE',  ( -20.64999999999999858, 85.00000000001207923, -126.6291383618717816 ) ) ;
#82651=ADVANCED_FACE ( 'NONE', ( #127996 ), #181211, .F. ) ;
#82664=LINE ( 'NONE', #145228, #525 ) ;
#82680=VERTEX_POINT ( 'NONE', #117412 ) ;
#82698=VERTEX_POINT ( 'NONE', #236069 ) ;
#82710=DIRECTION ( 'NONE',  ( 0.000000000000000000, 0.000000000000000000, 1.000000000000000000 ) ) ;
#82713=DIRECTION ( 'NONE',  ( 0.000000000000000000, -0.2605042016806647931, -0.9654727137038724427 ) ) ;
#82748=PLANE ( 'NONE',  #165222 ) ;
#82751=ORIENTED_EDGE ( 'NONE', *, *, #72708, .T. ) ;
#82754=CIRCLE ( 'NONE', #20461, 0.09999999999998898659 ) ;
#82760=EDGE_LOOP ( 'NONE', ( #151858, #104299, #215966, #224445 ) ) ;
#82828=ORIENTED_EDGE ( 'NONE', *, *, #51699, .F. ) ;
#82847=FACE_OUTER_BOUND ( 'NONE', #209829, .T. ) ;
#82866=ORIENTED_EDGE ( 'NONE', *, *, #63535, .T. ) ;
#82877=CARTESIAN_POINT ( 'NONE',  ( 20.94788355080264353, 65.69792220476320210, -97.53355541284612684 ) ) ;
#82924=CARTESIAN_POINT ( 'NONE',  ( 21.05000000000000071, 87.48912529308798014, -105.9231074845242091 ) ) ;
#82929=DIRECTION ( 'NONE',  ( 0.000000000000000000, -7.086529944415894657E-15, 1.000000000000000000 ) ) ;
#82945=ORIENTED_EDGE ( 'NONE', *, *, #34455, .T. ) ;
#82954=DIRECTION ( 'NONE',  ( -1.000000000000000000, 0.000000000000000000, 0.000000000000000000 ) ) ;
#82956=DIRECTION ( 'NONE',  ( -0.000000000000000000, 1.000000000000000000, 6.352154140967427193E-15 ) ) ;
#82957=CARTESIAN_POINT ( 'NONE',  ( -21.64999999999999858, 68.75000000001206502, -124.2731074845243455 ) ) ;
#83002=CARTESIAN_POINT ( 'NONE',  ( -23.15000000000000213, 76.00000000001190870, -103.0231074845243029 ) ) ;
#83051=ORIENTED_EDGE ( 'NONE', *, *, #207818, .F. ) ;
#83069=CIRCLE ( 'NONE', #66372, 0.2000000000000057288 ) ;
#83094=CARTESIAN_POINT ( 'NONE',  ( 22.50000000000000000, 75.90000000001219860, -144.3138870828976792 ) ) ;
#83108=UNCERTAINTY_MEASURE_WITH_UNIT (LENGTH_MEASURE( 1.000000000000000082E-05 ), #7985, 'distance_accuracy_value', 'NONE');
#83111=ORIENTED_EDGE ( 'NONE', *, *, #238546, .F. ) ;
#83154=FACE_OUTER_BOUND ( 'NONE', #78668, .T. ) ;
#83157=SPHERICAL_SURFACE ( 'NONE', #197239, 0.1000000000000000056 ) ;
#83164=TOROIDAL_SURFACE ( 'NONE', #141458, 12.97499999999999787, 0.1000000000000000056 ) ;
#83185=CARTESIAN_POINT ( 'NONE',  ( 18.59999999999998366, 76.00000000001190870, -103.0231074845243029 ) ) ;
#83211=CIRCLE ( 'NONE', #62404, 12.97499999999999964 ) ;
#83223=DIRECTION ( 'NONE',  ( -0.000000000000000000, -1.000000000000000000, -7.272083257015735086E-15 ) ) ;
#83239=DIRECTION ( 'NONE',  ( 0.000000000000000000, 6.938893903907222067E-15, -1.000000000000000000 ) ) ;
#83262=ORIENTED_EDGE ( 'NONE', *, *, #75351, .T. ) ;
#83269=CARTESIAN_POINT ( 'NONE',  ( -22.32929514600008503, 75.90092432189828742, -144.1017550499008166 ) ) ;
#83278=AXIS2_PLACEMENT_3D ( 'NONE', #257640, #76493, #217274 ) ;
#83287=EDGE_LOOP ( 'NONE', ( #173423, #117499, #81900, #4206 ) ) ;
#83318=ORIENTED_EDGE ( 'NONE', *, *, #208019, .F. ) ;
#83373=LINE ( 'NONE', #164242, #123560 ) ;
#83386=DIRECTION ( 'NONE',  ( 1.000000000000000000, 0.000000000000000000, 0.000000000000000000 ) ) ;
#83392=CARTESIAN_POINT ( 'NONE',  ( 21.14999999999999858, 69.45934304831089889, -136.5231074845243313 ) ) ;
#83408=AXIS2_PLACEMENT_3D ( 'NONE', #72165, #173871, #111283 ) ;
#83416=CARTESIAN_POINT ( 'NONE',  ( -23.25000000000000000, 85.60000000001197407, -112.9170766071766820 ) ) ;
#83433=CARTESIAN_POINT ( 'NONE',  ( -23.25000000000000000, 77.73670573947940454, -91.50568489690056140 ) ) ;
#83475=DIRECTION ( 'NONE',  ( 1.000000000000000000, 0.000000000000000000, 0.000000000000000000 ) ) ;
#83482=CARTESIAN_POINT ( 'NONE',  ( -21.05000000000000071, 61.95000000001210338, -131.0094124137634140 ) ) ;
#83484=AXIS2_PLACEMENT_3D ( 'NONE', #4737, #62180, #20497 ) ;
#83485=ORIENTED_EDGE ( 'NONE', *, *, #203602, .T. ) ;
#83533=CARTESIAN_POINT ( 'NONE',  ( 20.94999999999999929, 70.50000000001199396, -115.4283735034374274 ) ) ;
#83536=CARTESIAN_POINT ( 'NONE',  ( 20.84999999999998721, 64.25000000001190870, -103.0231074845243882 ) ) ;
#83544=AXIS2_PLACEMENT_3D ( 'NONE', #131408, #251352, #88411 ) ;
#83596=CARTESIAN_POINT ( 'NONE',  ( -18.59999999999999787, 65.66751761918668251, -97.42826094061121012 ) ) ;
#83600=ORIENTED_EDGE ( 'NONE', *, *, #50600, .T. ) ;
#83607=DIRECTION ( 'NONE',  ( 1.000000000000000000, 0.000000000000000000, 0.000000000000000000 ) ) ;
#83635=CIRCLE ( 'NONE', #237800, 4.299999999999970512 ) ;
#83642=CARTESIAN_POINT ( 'NONE',  ( -18.59999999999999787, 70.10000000001213039, -126.3040077198679398 ) ) ;
#83644=LINE ( 'NONE', #242744, #170724 ) ;
#83675=CARTESIAN_POINT ( 'NONE',  ( 20.94999999999999929, 77.83534155023646406, -124.9679561919612922 ) ) ;
#83688=LINE ( 'NONE', #201115, #151616 ) ;
#83693=EDGE_CURVE ( 'NONE', #213545, #132227, #154615, .T. ) ;
#83735=ORIENTED_EDGE ( 'NONE', *, *, #169783, .F. ) ;
#83759=CARTESIAN_POINT ( 'NONE',  ( 23.14999999999999503, 69.35000000001205933, -124.3731074845243540 ) ) ;
#83780=CARTESIAN_POINT ( 'NONE',  ( 20.94999999999999929, 85.40000000001198543, -112.9170766071766820 ) ) ;
#83784=CARTESIAN_POINT ( 'NONE',  ( 18.59999999999999432, 74.83729825007408465, -128.5231074845243029 ) ) ;
#83786=ADVANCED_FACE ( 'NONE', ( #228428 ), #250069, .T. ) ;
#83804=CIRCLE ( 'NONE', #58884, 0.1000000000000064587 ) ;
#83815=CARTESIAN_POINT ( 'NONE',  ( 20.85000000000000142, 64.35000000001190301, -103.0231074845243882 ) ) ;
#83847=CARTESIAN_POINT ( 'NONE',  ( -20.54999999999999716, 85.50000000001197975, -112.9170766071766820 ) ) ;
#83854=CARTESIAN_POINT ( 'NONE',  ( 21.05000000000000071, 76.00000000001190870, -103.0231074845243029 ) ) ;
#83873=AXIS2_PLACEMENT_3D ( 'NONE', #69896, #252344, #227651 ) ;
#83875=EDGE_CURVE ( 'NONE', #37720, #197779, #137606, .T. ) ;
#83876=DIRECTION ( 'NONE',  ( -1.000000000000000000, 0.000000000000000000, -0.000000000000000000 ) ) ;
#83879=TOROIDAL_SURFACE ( 'NONE', #163062, 11.65000000000000036, 0.1000000000000000056 ) ;
#83896=CARTESIAN_POINT ( 'NONE',  ( -22.50000000000000000, 75.90000000001214175, -136.5231074845242745 ) ) ;
#83913=ORIENTED_EDGE ( 'NONE', *, *, #145410, .F. ) ;
#83923=AXIS2_PLACEMENT_3D ( 'NONE', #239160, #98318, #141341 ) ;
#83930=EDGE_CURVE ( 'NONE', #64533, #172048, #241357, .T. ) ;
#83968=ORIENTED_EDGE ( 'NONE', *, *, #109677, .F. ) ;
#83971=CARTESIAN_POINT ( 'NONE',  ( 21.07888907270776002, 65.27493078649683866, -124.3019138976911790 ) ) ;
#83978=ADVANCED_FACE ( 'NONE', ( #182581 ), #161741, .T. ) ;
#83985=B_SPLINE_CURVE_WITH_KNOTS ( 'NONE', 3,
 ( #112759, #72366, #115314, #133594, #151909, #198398, #103130, #246506, #147412, #144827, #245239, #43184, #101833, #105685, #24920, #161865, #23650, #182705, #183970 ),
 .UNSPECIFIED., .F., .F.,
 ( 4, 3, 3, 3, 3, 3, 4 ),
 ( 0.000000000000000000, 1.655171619026472483E-05, 2.773500582848447571E-05, 5.941817267378177332E-05, 0.0001114174635873370778, 0.0001914169455916087017, 0.0002627181070750251170 ),
 .UNSPECIFIED. ) ;
#84000=ORIENTED_EDGE ( 'NONE', *, *, #14494, .T. ) ;
#84098=ORIENTED_EDGE ( 'NONE', *, *, #176789, .F. ) ;
#84100=EDGE_CURVE ( 'NONE', #125361, #170795, #99997, .T. ) ;
#84101=TOROIDAL_SURFACE ( 'NONE', #34131, 0.2000000000000000111, 0.1000000000000000056 ) ;
#84109=CARTESIAN_POINT ( 'NONE',  ( -22.39999999999999858, 75.90000000001219860, -144.3138870828977076 ) ) ;
#84122=EDGE_CURVE ( 'NONE', #2981, #88364, #47126, .T. ) ;
#84173=VECTOR ( 'NONE', #195823, 999.9999999999998863 ) ;
#84194=AXIS2_PLACEMENT_3D ( 'NONE', #2466, #81982, #102838 ) ;
#84238=CARTESIAN_POINT ( 'NONE',  ( 18.59999999999999432, 74.83729825007408465, -128.4231074845243086 ) ) ;
#84247=ORIENTED_EDGE ( 'NONE', *, *, #35369, .F. ) ;
#84326=CARTESIAN_POINT ( 'NONE',  ( 21.05000000000000071, 76.00000000001190870, -103.0231074845243029 ) ) ;
#84328=DIRECTION ( 'NONE',  ( -0.000000000000000000, 0.1298341882519668811, 0.9915357197604899309 ) ) ;
#84351=ORIENTED_EDGE ( 'NONE', *, *, #3406, .F. ) ;
#84366=VECTOR ( 'NONE', #234618, 1000.000000000000000 ) ;
#84371=CARTESIAN_POINT ( 'NONE',  ( 22.47007471830798053, 76.00000000001219291, -144.2438181364507841 ) ) ;
#84411=CIRCLE ( 'NONE', #155247, 0.1000000000000028644 ) ;
#84421=ORIENTED_EDGE ( 'NONE', *, *, #89125, .F. ) ;
#84429=TOROIDAL_SURFACE ( 'NONE', #92853, 0.2000000000000000111, 0.1000000000000000056 ) ;
#84444=CARTESIAN_POINT ( 'NONE',  ( -21.05000000000000071, 69.45934304831089889, -136.4231074845243654 ) ) ;
#84464=PLANE ( 'NONE',  #218973 ) ;
#84489=CARTESIAN_POINT ( 'NONE',  ( -21.14999999999999858, 76.00000000001213607, -136.5231074845242745 ) ) ;
#84500=ORIENTED_EDGE ( 'NONE', *, *, #59638, .F. ) ;
#84531=FACE_OUTER_BOUND ( 'NONE', #202693, .T. ) ;
#84533=DIRECTION ( 'NONE',  ( 0.000000000000000000, 0.000000000000000000, -1.000000000000000000 ) ) ;
#84571=CARTESIAN_POINT ( 'NONE',  ( -22.50000000000000000, 75.90736249940275115, -148.1728046915650339 ) ) ;
#84591=DIRECTION ( 'NONE',  ( -1.000000000000000000, 0.000000000000000000, -0.000000000000000000 ) ) ;
#84648=CYLINDRICAL_SURFACE ( 'NONE', #210924, 0.1000000000000028644 ) ;
#84659=FACE_OUTER_BOUND ( 'NONE', #249990, .T. ) ;
#84669=VECTOR ( 'NONE', #29293, 1000.000000000000000 ) ;
#84672=EDGE_LOOP ( 'NONE', ( #63223, #33842, #103251, #82828 ) ) ;
#84685=AXIS2_PLACEMENT_3D ( 'NONE', #80157, #200152, #159741 ) ;
#84759=EDGE_LOOP ( 'NONE', ( #113435, #132841, #119657 ) ) ;
#84787=DIRECTION ( 'NONE',  ( 1.000000000000000000, -0.000000000000000000, 0.000000000000000000 ) ) ;
#84791=ADVANCED_FACE ( 'NONE', ( #182917 ), #25133, .F. ) ;
#84793=EDGE_LOOP ( 'NONE', ( #106611, #29136, #66502, #151142 ) ) ;
#84796=AXIS2_PLACEMENT_3D ( 'NONE', #113983, #111431, #233940 ) ;
#84846=CARTESIAN_POINT ( 'NONE',  ( -22.59999999999999787, 76.00000000001213607, -136.5231074845242745 ) ) ;
#84866=ADVANCED_FACE ( 'NONE', ( #32858 ), #232324, .T. ) ;
#84874=AXIS2_PLACEMENT_3D ( 'NONE', #141798, #237064, #216197 ) ;
#84878=ORIENTED_EDGE ( 'NONE', *, *, #160038, .F. ) ;
#84923=CARTESIAN_POINT ( 'NONE',  ( -20.95613430942437105, 64.25000000001207923, -129.6659448363049023 ) ) ;
#84938=CARTESIAN_POINT ( 'NONE',  ( 18.49999999999998934, 69.35000000001205933, -124.1731074845243370 ) ) ;
#84985=ORIENTED_EDGE ( 'NONE', *, *, #108147, .T. ) ;
#85002=ADVANCED_FACE ( 'NONE', ( #109315 ), #246287, .T. ) ;
#85025=ORIENTED_EDGE ( 'NONE', *, *, #18856, .T. ) ;
#85039=CIRCLE ( 'NONE', #47461, 0.09999999999999939493 ) ;
#85057=CARTESIAN_POINT ( 'NONE',  ( 21.13422380239043719, 69.50667348520650535, -136.5231074845243313 ) ) ;
#85072=CARTESIAN_POINT ( 'NONE',  ( -23.15000000000000213, 87.41227409416161720, -106.0231074845242176 ) ) ;
#85101=LINE ( 'NONE', #162134, #95894 ) ;
#85143=ORIENTED_EDGE ( 'NONE', *, *, #145216, .F. ) ;
#85151=CARTESIAN_POINT ( 'NONE',  ( -23.15000000000000213, 76.00000000001216449, -140.6731074845242802 ) ) ;
#85182=CARTESIAN_POINT ( 'NONE',  ( -20.94999999999999929, 76.00000000001190870, -103.0231074845243029 ) ) ;
#85213=DIRECTION ( 'NONE',  ( 0.000000000000000000, -6.982962677686266711E-15, 1.000000000000000000 ) ) ;
#85223=CARTESIAN_POINT ( 'NONE',  ( -20.85000000000000142, 65.66751761918668251, -97.42826094061121012 ) ) ;
#85231=CYLINDRICAL_SURFACE ( 'NONE', #205366, 0.1000000000000028644 ) ;
#85238=LINE ( 'NONE', #126972, #198950 ) ;
#85253=EDGE_CURVE ( 'NONE', #38706, #89168, #229759, .T. ) ;
#85255=DIRECTION ( 'NONE',  ( 0.000000000000000000, 0.9876197685951241256, 0.1568667991644932258 ) ) ;
#85275=ADVANCED_FACE ( 'NONE', ( #902 ), #161316, .T. ) ;
#85276=ORIENTED_EDGE ( 'NONE', *, *, #94094, .F. ) ;
#85284=DIRECTION ( 'NONE',  ( 0.000000000000000000, 7.026728003956683390E-15, -1.000000000000000000 ) ) ;
#85294=EDGE_CURVE ( 'NONE', #153656, #229115, #62204, .T. ) ;
#85318=ORIENTED_EDGE ( 'NONE', *, *, #75132, .F. ) ;
#85325=CARTESIAN_POINT ( 'NONE',  ( -18.44362607810620602, 85.49049615809693137, -129.4651536176771174 ) ) ;
#85327=CARTESIAN_POINT ( 'NONE',  ( -22.50000000000000000, 76.00000000001213607, -136.5231074845242745 ) ) ;
#85344=CIRCLE ( 'NONE', #193721, 0.2000000000000057288 ) ;
#85444=CARTESIAN_POINT ( 'NONE',  ( 20.92356734117541706, 65.68026841930900162, -97.47257401318893244 ) ) ;
#85454=CARTESIAN_POINT ( 'NONE',  ( -20.54999999999999716, 76.00000000001190870, -103.0231074845243029 ) ) ;
#85470=ORIENTED_EDGE ( 'NONE', *, *, #189221, .F. ) ;
#85508=CARTESIAN_POINT ( 'NONE',  ( -23.25000000000000000, 73.40000000001205649, -123.2984855617622202 ) ) ;
#85520=EDGE_CURVE ( 'NONE', #18414, #51864, #142456, .T. ) ;
#85524=DIRECTION ( 'NONE',  ( -1.000000000000000000, -0.000000000000000000, -0.000000000000000000 ) ) ;
#85533=CYLINDRICAL_SURFACE ( 'NONE', #82006, 0.09999999999999867328 ) ;
#85568=DIRECTION ( 'NONE',  ( 0.000000000000000000, -0.9274965247785323941, -0.3738317757009769760 ) ) ;
#85587=EDGE_CURVE ( 'NONE', #134440, #161509, #143174, .T. ) ;
#85598=VERTEX_POINT ( 'NONE', #51749 ) ;
#85604=FACE_OUTER_BOUND ( 'NONE', #14992, .T. ) ;
#85618=DIRECTION ( 'NONE',  ( 0.000000000000000000, -6.652207440891584540E-15, 1.000000000000000000 ) ) ;
#85620=ORIENTED_EDGE ( 'NONE', *, *, #180761, .F. ) ;
#85628=CARTESIAN_POINT ( 'NONE',  ( 18.59999999999999432, 77.83585931145546510, -91.51866831572576189 ) ) ;
#85632=DIRECTION ( 'NONE',  ( 1.000000000000000000, 0.000000000000000000, 0.000000000000000000 ) ) ;
#85651=CARTESIAN_POINT ( 'NONE',  ( -20.00857864376270001, 66.65000000001205649, -124.2731074845243597 ) ) ;
#85656=TOROIDAL_SURFACE ( 'NONE', #98139, 7.791421356237316687, 0.1000000000000000056 ) ;
#85657=DIRECTION ( 'NONE',  ( -6.938893903907222067E-15, -1.000000000000000000, -6.982962677686266711E-15 ) ) ;
#85664=LINE ( 'NONE', #32179, #147009 ) ;
#85678=CARTESIAN_POINT ( 'NONE',  ( -20.94999999999999929, 77.83534155023646406, -124.9679561919612922 ) ) ;
#85736=ORIENTED_EDGE ( 'NONE', *, *, #110845, .F. ) ;
#85790=CIRCLE ( 'NONE', #144067, 1.899999999999999023 ) ;
#85796=CARTESIAN_POINT ( 'NONE',  ( 22.49544290803779489, 64.25012976215485594, -136.5884194437818735 ) ) ;
#85808=CIRCLE ( 'NONE', #81706, 0.09999999999998898659 ) ;
#85827=EDGE_LOOP ( 'NONE', ( #28973, #49168, #70735, #239612 ) ) ;
#85845=CARTESIAN_POINT ( 'NONE',  ( -22.47007471830799474, 68.27928934808565486, -136.5231074845243597 ) ) ;
#85872=( BOUNDED_CURVE ( )  B_SPLINE_CURVE ( 3, ( #110002, #14795, #10924, #232556 ),
 .UNSPECIFIED., .F., .F. ) 
 B_SPLINE_CURVE_WITH_KNOTS ( ( 4, 4 ),
 ( 4.712388980384689674, 6.231880751915386263 ),
 .UNSPECIFIED. ) 
 CURVE ( )  GEOMETRIC_REPRESENTATION_ITEM ( )  RATIONAL_B_SPLINE_CURVE ( ( 1.000000000000000000, 0.8166740347213228279, 0.8166740347213228279, 1.000000000000000000 ) ) 
 REPRESENTATION_ITEM ( '' )  );
#85874=CIRCLE ( 'NONE', #194269, 0.09999999999998898659 ) ;
#85881=ORIENTED_EDGE ( 'NONE', *, *, #46501, .F. ) ;
#85910=EDGE_CURVE ( 'NONE', #143912, #48194, #225994, .T. ) ;
#85921=CIRCLE ( 'NONE', #206752, 0.2000000000000057288 ) ;
#85930=DIRECTION ( 'NONE',  ( 1.000000000000000000, 0.000000000000000000, 0.000000000000000000 ) ) ;
#85939=EDGE_CURVE ( 'NONE', #224224, #163243, #13643, .T. ) ;
#85966=VERTEX_POINT ( 'NONE', #149312 ) ;
#85968=( BOUNDED_SURFACE ( )  B_SPLINE_SURFACE ( 3, 2, ( 
 ( #181515, #22445, #45833 ),
 ( #142359, #5392, #25015 ),
 ( #221876, #125381, #163228 ),
 ( #21171, #84923, #160681 ),
 ( #164515, #244024, #242737 ),
 ( #121557, #204892, #23739 ) ),
 .UNSPECIFIED., .F., .F., .F. ) 
 B_SPLINE_SURFACE_WITH_KNOTS ( ( 4, 2, 4 ),
 ( 3, 3 ),
 ( 1.570796326794895448, 2.356194490192343505, 3.141592653589791784 ),
 ( 0.000000000000000000, 1.000000000000000000 ),
 .UNSPECIFIED. ) 
 GEOMETRIC_REPRESENTATION_ITEM ( )  RATIONAL_B_SPLINE_SURFACE ( (
 ( 1.000000000000000000, 0.7071067811865475727, 1.000000000000000000),
 ( 1.000000000000000000, 0.6611148371778297061, 1.000000000000000000),
 ( 1.000000000000000000, 0.6092287576697440477, 1.000000000000000000),
 ( 1.000000000000000000, 0.5278258667056308084, 1.000000000000000000),
 ( 1.000000000000000000, 0.4993418825335151356, 1.000000000000000000),
 ( 1.000000000000000000, 0.5000000000000456302, 1.000000000000000000) ) ) 
 REPRESENTATION_ITEM ( '' )  SURFACE ( )  );
#85993=ORIENTED_EDGE ( 'NONE', *, *, #190725, .F. ) ;
#85995=CIRCLE ( 'NONE', #119341, 0.3999999999999975797 ) ;
#86009=ORIENTED_EDGE ( 'NONE', *, *, #43936, .F. ) ;
#86019=DIRECTION ( 'NONE',  ( 0.000000000000000000, -6.982962677686266711E-15, 1.000000000000000000 ) ) ;
#86040=FACE_OUTER_BOUND ( 'NONE', #189872, .T. ) ;
#86053=CYLINDRICAL_SURFACE ( 'NONE', #100122, 11.74999999999999645 ) ;
#86116=EDGE_CURVE ( 'NONE', #246341, #13368, #196125, .T. ) ;
#86133=ORIENTED_EDGE ( 'NONE', *, *, #123858, .T. ) ;
#86148=AXIS2_PLACEMENT_3D ( 'NONE', #63804, #243723, #248525 ) ;
#86150=LINE ( 'NONE', #189137, #166198 ) ;
#86165=B_SPLINE_CURVE_WITH_KNOTS ( 'NONE', 3,
 ( #252884, #95102, #114666, #212498, #215049, #76815 ),
 .UNSPECIFIED., .F., .F.,
 ( 4, 2, 4 ),
 ( 0.000000000000000000, 0.0001891491689349454879, 0.0003782983378698909758 ),
 .UNSPECIFIED. ) ;
#86179=DIRECTION ( 'NONE',  ( 0.000000000000000000, 0.000000000000000000, 1.000000000000000000 ) ) ;
#86212=LINE ( 'NONE', #122821, #186382 ) ;
#86219=EDGE_CURVE ( 'NONE', #17520, #207643, #201086, .T. ) ;
#86241=CARTESIAN_POINT ( 'NONE',  ( 22.39999999999999503, 68.20922040163875977, -136.5231074845243313 ) ) ;
#86251=DIRECTION ( 'NONE',  ( 0.000000000000000000, 6.982962677686266711E-15, -1.000000000000000000 ) ) ;
#86270=EDGE_LOOP ( 'NONE', ( #57276, #161262, #240633, #213475 ) ) ;
#86316=AXIS2_PLACEMENT_3D ( 'NONE', #255169, #12798, #16637 ) ;
#86362=CARTESIAN_POINT ( 'NONE',  ( 18.59999999999999076, 64.35000000001197407, -111.6731074845243796 ) ) ;
#86368=AXIS2_PLACEMENT_3D ( 'NONE', #36887, #139778, #155547 ) ;
#86370=VERTEX_POINT ( 'NONE', #215054 ) ;
#86385=CIRCLE ( 'NONE', #149369, 4.000000000000003553 ) ;
#86388=AXIS2_PLACEMENT_3D ( 'NONE', #34498, #93151, #71054 ) ;
#86452=AXIS2_PLACEMENT_3D ( 'NONE', #213515, #131414, #54445 ) ;
#86455=DIRECTION ( 'NONE',  ( 0.000000000000000000, 0.000000000000000000, -1.000000000000000000 ) ) ;
#86467=VECTOR ( 'NONE', #247576, 1000.000000000000000 ) ;
#86489=CIRCLE ( 'NONE', #153193, 4.300000000000025580 ) ;
#86528=LINE ( 'NONE', #186975, #174057 ) ;
#86563=CARTESIAN_POINT ( 'NONE',  ( 21.07189867249812210, 65.27501972991890966, -124.3106560422476434 ) ) ;
#86579=ORIENTED_EDGE ( 'NONE', *, *, #217372, .F. ) ;
#86584=DIRECTION ( 'NONE',  ( 1.000000000000000000, -2.952720810173289112E-16, -2.061873921506763405E-30 ) ) ;
#86599=CARTESIAN_POINT ( 'NONE',  ( 23.14999999999999858, 76.00000000001190870, -103.0231074845243029 ) ) ;
#86620=DIRECTION ( 'NONE',  ( 0.000000000000000000, 0.000000000000000000, -1.000000000000000000 ) ) ;
#86623=CARTESIAN_POINT ( 'NONE',  ( 23.24999999999997513, 64.25000000001195133, -110.0379132551783243 ) ) ;
#86635=ORIENTED_EDGE ( 'NONE', *, *, #240182, .F. ) ;
#86646=CIRCLE ( 'NONE', #165824, 0.1000000000000028644 ) ;
#86656=DIRECTION ( 'NONE',  ( 0.000000000000000000, 0.9999176327611370985, -0.01283462868041289687 ) ) ;
#86660=CARTESIAN_POINT ( 'NONE',  ( -18.50000000000000000, 64.35000000001198828, -115.1731074845243796 ) ) ;
#86683=CARTESIAN_POINT ( 'NONE',  ( 23.14999999999999858, 76.00000000001213607, -136.5231074845242745 ) ) ;
#86725=DIRECTION ( 'NONE',  ( 1.000000000000000000, 0.000000000000000000, 0.000000000000000000 ) ) ;
#86731=CARTESIAN_POINT ( 'NONE',  ( 18.59999999999999076, 64.25000000001196554, -111.6731074845243796 ) ) ;
#86734=ORIENTED_EDGE ( 'NONE', *, *, #241913, .F. ) ;
#86736=VERTEX_POINT ( 'NONE', #116931 ) ;
#86741=CARTESIAN_POINT ( 'NONE',  ( 18.59999999999999076, 74.16465844978765176, -124.9679561919613207 ) ) ;
#86746=CARTESIAN_POINT ( 'NONE',  ( 20.94983749550516450, 65.70233904877009934, -97.54874109119680270 ) ) ;
#86750=DIRECTION ( 'NONE',  ( -1.000000000000000000, 0.000000000000000000, -0.000000000000000000 ) ) ;
#86751=FACE_OUTER_BOUND ( 'NONE', #207645, .T. ) ;
#86778=AXIS2_PLACEMENT_3D ( 'NONE', #47055, #164463, #142311 ) ;
#86780=ORIENTED_EDGE ( 'NONE', *, *, #190359, .T. ) ;
#86803=EDGE_CURVE ( 'NONE', #442, #88307, #226364, .T. ) ;
#86824=DIRECTION ( 'NONE',  ( 0.000000000000000000, -7.056502275159890832E-15, 1.000000000000000000 ) ) ;
#86838=CARTESIAN_POINT ( 'NONE',  ( -23.25000000000000000, 76.00000000001213607, -136.5231074845242745 ) ) ;
#86856=LINE ( 'NONE', #184686, #5850 ) ;
#86880=CIRCLE ( 'NONE', #57286, 0.09999999999999939493 ) ;
#86882=CIRCLE ( 'NONE', #16203, 0.09999999999999939493 ) ;
#86883=CARTESIAN_POINT ( 'NONE',  ( 18.60000000000000497, 85.52394631232958488, -96.14107948918599789 ) ) ;
#86933=VERTEX_POINT ( 'NONE', #3379 ) ;
#86943=CARTESIAN_POINT ( 'NONE',  ( -23.25000000000000000, 77.16412189325305349, -95.10825939895268277 ) ) ;
#86967=FACE_OUTER_BOUND ( 'NONE', #257352, .T. ) ;
#86995=DIRECTION ( 'NONE',  ( 0.000000000000000000, 0.000000000000000000, 1.000000000000000000 ) ) ;
#86998=ORIENTED_EDGE ( 'NONE', *, *, #47788, .T. ) ;
#87000=AXIS2_PLACEMENT_3D ( 'NONE', #69188, #187845, #148711 ) ;
#87016=CARTESIAN_POINT ( 'NONE',  ( 21.14999999999999858, 76.00000000001222134, -148.1726782920690937 ) ) ;
#87035=CARTESIAN_POINT ( 'NONE',  ( -21.05000000000000071, 69.58633726514295859, -136.4375146211624497 ) ) ;
#87102=AXIS2_PLACEMENT_3D ( 'NONE', #78091, #157692, #237189 ) ;
#87120=EDGE_LOOP ( 'NONE', ( #119304, #127208, #57486, #179450 ) ) ;
#87129=CARTESIAN_POINT ( 'NONE',  ( -23.25000000000000000, 71.85000000001198828, -115.2731074845243171 ) ) ;
#87171=DIRECTION ( 'NONE',  ( -3.265361837132813093E-16, -1.000000000000000000, 7.445645354460596589E-46 ) ) ;
#87228=CARTESIAN_POINT ( 'NONE',  ( -20.64999999999999858, 76.00000000001189449, -101.0231074845243029 ) ) ;
#87232=DIRECTION ( 'NONE',  ( 1.000000000000000000, 0.000000000000000000, 0.000000000000000000 ) ) ;
#87240=ORIENTED_EDGE ( 'NONE', *, *, #38010, .T. ) ;
#87241=CARTESIAN_POINT ( 'NONE',  ( -23.15000000000000213, 64.25000000001222134, -148.2731074845243882 ) ) ;
#87245=CARTESIAN_POINT ( 'NONE',  ( -18.39999999999999858, 85.40000000001222702, -148.2731074845242460 ) ) ;
#87267=FACE_OUTER_BOUND ( 'NONE', #146055, .T. ) ;
#87269=DIRECTION ( 'NONE',  ( 0.000000000000000000, -1.000000000000000000, -6.982962677686265922E-15 ) ) ;
#87294=CARTESIAN_POINT ( 'NONE',  ( -18.50000000000000000, 85.40000000001187175, -96.14106563635156988 ) ) ;
#87303=VERTEX_POINT ( 'NONE', #80025 ) ;
#87306=EDGE_LOOP ( 'NONE', ( #71871, #142509, #224844, #196759 ) ) ;
#87320=VERTEX_POINT ( 'NONE', #159611 ) ;
#87322=AXIS2_PLACEMENT_3D ( 'NONE', #258043, #95167, #255471 ) ;
#87325=SPHERICAL_SURFACE ( 'NONE', #249836, 0.1000000000000000056 ) ;
#87341=AXIS2_PLACEMENT_3D ( 'NONE', #219531, #123025, #121753 ) ;
#87358=CARTESIAN_POINT ( 'NONE',  ( 23.14999999999999503, 64.35000000001197407, -115.2731074845243739 ) ) ;
#87470=CARTESIAN_POINT ( 'NONE',  ( -18.50000000000000000, 65.70729864261004138, -97.56574559737242680 ) ) ;
#87479=DIRECTION ( 'NONE',  ( 0.000000000000000000, 0.000000000000000000, 1.000000000000000000 ) ) ;
#87485=DIRECTION ( 'NONE',  ( 0.000000000000000000, -6.982962677686266711E-15, 1.000000000000000000 ) ) ;
#87487=CARTESIAN_POINT ( 'NONE',  ( 20.94999999999999929, 69.15387683765929694, -99.28538121767448388 ) ) ;
#87523=EDGE_CURVE ( 'NONE', #128325, #161509, #155004, .T. ) ;
#87541=DIRECTION ( 'NONE',  ( 1.734723475976817507E-14, -6.982962677686266711E-15, 1.000000000000000000 ) ) ;
#87557=CARTESIAN_POINT ( 'NONE',  ( 21.05000000000000071, 65.51540711881749246, -129.0663939139408285 ) ) ;
#87562=CYLINDRICAL_SURFACE ( 'NONE', #69223, 0.1000000000000028644 ) ;
#87569=VERTEX_POINT ( 'NONE', #150329 ) ;
#87656=DIRECTION ( 'NONE',  ( 0.000000000000000000, 6.982962677686267499E-15, -1.000000000000000000 ) ) ;
#87661=CARTESIAN_POINT ( 'NONE',  ( -23.25000000000000000, 74.00000000001205080, -123.2984855617622060 ) ) ;
#87669=FACE_OUTER_BOUND ( 'NONE', #148703, .T. ) ;
#87670=ORIENTED_EDGE ( 'NONE', *, *, #251975, .T. ) ;
#87702=CARTESIAN_POINT ( 'NONE',  ( -20.85000000000000142, 69.15387683765929694, -99.28538121767448388 ) ) ;
#87725=ORIENTED_EDGE ( 'NONE', *, *, #251258, .F. ) ;
#87749=CARTESIAN_POINT ( 'NONE',  ( 23.24999999999999645, 70.40000000001207070, -124.1178414656112352 ) ) ;
#87762=ORIENTED_EDGE ( 'NONE', *, *, #70850, .F. ) ;
#87785=CIRCLE ( 'NONE', #46104, 0.09999999999999939493 ) ;
#87790=CARTESIAN_POINT ( 'NONE',  ( -23.15000000000000213, 76.00000000001193712, -106.9231074845242944 ) ) ;
#87811=EDGE_CURVE ( 'NONE', #88928, #13286, #56691, .T. ) ;
#87839=AXIS2_PLACEMENT_3D ( 'NONE', #181049, #59769, #239729 ) ;
#87851=CARTESIAN_POINT ( 'NONE',  ( -20.94999999999999929, 87.65000000001212754, -133.5231074845242176 ) ) ;
#87865=ADVANCED_FACE ( 'NONE', ( #232133 ), #102478, .F. ) ;
#87877=CIRCLE ( 'NONE', #242022, 0.1000000000000028644 ) ;
#87903=ADVANCED_FACE ( 'NONE', ( #93884 ), #160812, .F. ) ;
#87912=LINE ( 'NONE', #47513, #18853 ) ;
#87919=EDGE_CURVE ( 'NONE', #152168, #153892, #213835, .T. ) ;
#87926=ORIENTED_EDGE ( 'NONE', *, *, #163894, .T. ) ;
#87927=CARTESIAN_POINT ( 'NONE',  ( 21.06280952165553444, 65.37286769941074738, -124.3190535977457500 ) ) ;
#87930=AXIS2_PLACEMENT_3D ( 'NONE', #112225, #42943, #39110 ) ;
#87940=ORIENTED_EDGE ( 'NONE', *, *, #124699, .F. ) ;
#87941=VERTEX_POINT ( 'NONE', #3427 ) ;
#87964=DIRECTION ( 'NONE',  ( 0.000000000000000000, -6.608470384673558123E-15, 1.000000000000000000 ) ) ;
#87994=DIRECTION ( 'NONE',  ( 0.000000000000000000, -7.272083257015735086E-15, 1.000000000000000000 ) ) ;
#88026=LINE ( 'NONE', #7221, #187367 ) ;
#88039=DIRECTION ( 'NONE',  ( 0.000000000000000000, 6.467318590049456648E-15, -1.000000000000000000 ) ) ;
#88047=ORIENTED_EDGE ( 'NONE', *, *, #222637, .F. ) ;
#88061=CARTESIAN_POINT ( 'NONE',  ( 20.95512820512820440, 65.37615131630019505, -128.8581939154367717 ) ) ;
#88066=EDGE_CURVE ( 'NONE', #211628, #200753, #167678, .T. ) ;
#88080=AXIS2_PLACEMENT_3D ( 'NONE', #60902, #37516, #238258 ) ;
#88087=ORIENTED_EDGE ( 'NONE', *, *, #172754, .F. ) ;
#88153=DIRECTION ( 'NONE',  ( 0.000000000000000000, 1.000000000000000000, 0.000000000000000000 ) ) ;
#88161=VERTEX_POINT ( 'NONE', #33319 ) ;
#88188=ADVANCED_FACE ( 'NONE', ( #151969 ), #6842, .T. ) ;
#88196=VERTEX_POINT ( 'NONE', #252305 ) ;
#88197=ORIENTED_EDGE ( 'NONE', *, *, #174089, .T. ) ;
#88231=DIRECTION ( 'NONE',  ( -1.000000000000000000, 0.000000000000000000, 0.000000000000000000 ) ) ;
#88253=EDGE_CURVE ( 'NONE', #236445, #140955, #94316, .T. ) ;
#88278=EDGE_CURVE ( 'NONE', #57631, #14587, #119283, .T. ) ;
#88283=ADVANCED_FACE ( 'NONE', ( #218305 ), #117940, .T. ) ;
#88297=CARTESIAN_POINT ( 'NONE',  ( -20.64999999999999858, 68.85000000001205933, -124.1731074845243370 ) ) ;
#88301=TOROIDAL_SURFACE ( 'NONE', #9784, 11.90000000000000213, 0.1000000000000000056 ) ;
#88307=VERTEX_POINT ( 'NONE', #179232 ) ;
#88312=DIRECTION ( 'NONE',  ( 1.000000000000000000, 0.000000000000000000, 0.000000000000000000 ) ) ;
#88364=VERTEX_POINT ( 'NONE', #120542 ) ;
#88367=CARTESIAN_POINT ( 'NONE',  ( 18.50000000000000000, 85.50000000001185185, -96.42291809330220076 ) ) ;
#88411=DIRECTION ( 'NONE',  ( 1.000000000000000000, 0.000000000000000000, 0.000000000000000000 ) ) ;
#88443=ORIENTED_EDGE ( 'NONE', *, *, #142114, .T. ) ;
#88514=CARTESIAN_POINT ( 'NONE',  ( 20.97250901189795513, 65.37543196631021658, -128.8585617675573758 ) ) ;
#88515=ORIENTED_EDGE ( 'NONE', *, *, #141510, .F. ) ;
#88534=CARTESIAN_POINT ( 'NONE',  ( 23.15000000000000213, 87.65000000001192859, -106.0231074845242176 ) ) ;
#88556=CARTESIAN_POINT ( 'NONE',  ( -20.94999999999999929, 76.00000000001190870, -103.0231074845243029 ) ) ;
#88570=ORIENTED_EDGE ( 'NONE', *, *, #114393, .T. ) ;
#88588=ORIENTED_EDGE ( 'NONE', *, *, #229983, .T. ) ;
#88627=ORIENTED_EDGE ( 'NONE', *, *, #11629, .T. ) ;
#88638=ORIENTED_EDGE ( 'NONE', *, *, #230374, .T. ) ;
#88646=ORIENTED_EDGE ( 'NONE', *, *, #104890, .F. ) ;
#88649=LINE ( 'NONE', #28758, #61574 ) ;
#88651=ORIENTED_EDGE ( 'NONE', *, *, #157153, .F. ) ;
#88656=AXIS2_PLACEMENT_3D ( 'NONE', #164064, #182350, #241038 ) ;
#88658=CARTESIAN_POINT ( 'NONE',  ( 21.05000000000000071, 85.00000000001197975, -112.4170766071766678 ) ) ;
#88667=FACE_OUTER_BOUND ( 'NONE', #92127, .T. ) ;
#88669=ORIENTED_EDGE ( 'NONE', *, *, #246642, .T. ) ;
#88737=CARTESIAN_POINT ( 'NONE',  ( -18.59999999999999787, 77.83585931145546510, -91.51866831572576189 ) ) ;
#88743=EDGE_CURVE ( 'NONE', #25751, #228703, #216737, .T. ) ;
#88753=CARTESIAN_POINT ( 'NONE',  ( -20.54999999999999716, 84.73084112150739600, -126.9250327655398962 ) ) ;
#88773=CARTESIAN_POINT ( 'NONE',  ( 21.08804281139605408, 65.37816569817088919, -124.1731075171459082 ) ) ;
#88778=SPHERICAL_SURFACE ( 'NONE', #190825, 0.1000000000000000056 ) ;
#88794=CARTESIAN_POINT ( 'NONE',  ( 19.90621891164687440, 64.25000000001196554, -111.6946622066469672 ) ) ;
#88803=AXIS2_PLACEMENT_3D ( 'NONE', #211667, #92977, #253332 ) ;
#88807=AXIS2_PLACEMENT_3D ( 'NONE', #209464, #32143, #46526 ) ;
#88839=VECTOR ( 'NONE', #164509, 1000.000000000000000 ) ;
#88849=ORIENTED_EDGE ( 'NONE', *, *, #126438, .T. ) ;
#88850=CARTESIAN_POINT ( 'NONE',  ( 18.50000324121758055, 65.70692517833211355, -97.56446533783039854 ) ) ;
#88887=ORIENTED_EDGE ( 'NONE', *, *, #20427, .T. ) ;
#88888=AXIS2_PLACEMENT_3D ( 'NONE', #184190, #104627, #246732 ) ;
#88901=ADVANCED_FACE ( 'NONE', ( #3652 ), #83157, .T. ) ;
#88915=ORIENTED_EDGE ( 'NONE', *, *, #150753, .T. ) ;
#88923=DIRECTION ( 'NONE',  ( 0.000000000000000000, 0.000000000000000000, 1.000000000000000000 ) ) ;
#88928=VERTEX_POINT ( 'NONE', #21958 ) ;
#88938=CARTESIAN_POINT ( 'NONE',  ( -21.44999999999999929, 68.65000000001199965, -115.2731074845243455 ) ) ;
#88955=TOROIDAL_SURFACE ( 'NONE', #155650, 0.9750000000000019762, 0.1000000000000000056 ) ;
#88983=DIRECTION ( 'NONE',  ( 1.734723475976817507E-14, -6.982962677686266711E-15, 1.000000000000000000 ) ) ;
#89000=CARTESIAN_POINT ( 'NONE',  ( -23.15000000000000213, 74.08971962618021223, -115.6544753397232626 ) ) ;
#89014=VERTEX_POINT ( 'NONE', #79329 ) ;
#89030=VECTOR ( 'NONE', #159142, 1000.000000000000000 ) ;
#89060=PLANE ( 'NONE',  #82309 ) ;
#89125=EDGE_CURVE ( 'NONE', #192475, #224260, #151667, .T. ) ;
#89168=VERTEX_POINT ( 'NONE', #91064 ) ;
#89175=ORIENTED_EDGE ( 'NONE', *, *, #41995, .T. ) ;
#89201=CIRCLE ( 'NONE', #5989, 0.2000000000000057288 ) ;
#89211=DIRECTION ( 'NONE',  ( 0.000000000000000000, -0.1298341882519953583, -0.9915357197604861561 ) ) ;
#89236=ORIENTED_EDGE ( 'NONE', *, *, #30374, .F. ) ;
#89242=VERTEX_POINT ( 'NONE', #67646 ) ;
#89247=LINE ( 'NONE', #125807, #172163 ) ;
#89257=CARTESIAN_POINT ( 'NONE',  ( 20.95289811251229750, 67.10683199555347755, -128.0212979906058308 ) ) ;
#89260=ORIENTED_EDGE ( 'NONE', *, *, #233497, .T. ) ;
#89262=ORIENTED_EDGE ( 'NONE', *, *, #223657, .T. ) ;
#89263=CARTESIAN_POINT ( 'NONE',  ( -18.59999999999999787, 77.25000000001185185, -95.22262673010921219 ) ) ;
#89268=EDGE_LOOP ( 'NONE', ( #110127, #29828, #83111 ) ) ;
#89277=CIRCLE ( 'NONE', #235046, 2.000000000000001776 ) ;
#89333=LINE ( 'NONE', #204146, #253388 ) ;
#89339=AXIS2_PLACEMENT_3D ( 'NONE', #149706, #227935, #10178 ) ;
#89346=LINE ( 'NONE', #112785, #235957 ) ;
#89362=ADVANCED_FACE ( 'NONE', ( #175758 ), #255215, .T. ) ;
#89409=EDGE_CURVE ( 'NONE', #145844, #127497, #134843, .T. ) ;
#89412=CARTESIAN_POINT ( 'NONE',  ( -20.85000000000000142, 77.14957036958755054, -95.20719500002232394 ) ) ;
#89424=DIRECTION ( 'NONE',  ( 1.000000000000000000, 7.304098846218133681E-16, 5.311601492717083645E-30 ) ) ;
#89447=EDGE_LOOP ( 'NONE', ( #168504, #246441, #120601, #90241 ) ) ;
#89460=FACE_OUTER_BOUND ( 'NONE', #133787, .T. ) ;
#89509=DIRECTION ( 'NONE',  ( 0.000000000000000000, 0.000000000000000000, 1.000000000000000000 ) ) ;
#89525=CIRCLE ( 'NONE', #222805, 0.8750000000000007772 ) ;
#89528=( GEOMETRIC_REPRESENTATION_CONTEXT ( 3 ) GLOBAL_UNCERTAINTY_ASSIGNED_CONTEXT ( ( #230290 ) ) GLOBAL_UNIT_ASSIGNED_CONTEXT ( ( #198401, #219236, #176293 ) ) REPRESENTATION_CONTEXT ( 'NONE', 'WORKASPACE' ) );
#89542=DIRECTION ( 'NONE',  ( 2.952720810173289112E-16, 1.000000000000000000, 6.982962677686266711E-15 ) ) ;
#89640=EDGE_LOOP ( 'NONE', ( #65511, #18303, #71059 ) ) ;
#89649=AXIS2_PLACEMENT_3D ( 'NONE', #5758, #61910, #180575 ) ;
#89669=CYLINDRICAL_SURFACE ( 'NONE', #191801, 0.1000000000000028644 ) ;
#89680=ORIENTED_EDGE ( 'NONE', *, *, #102924, .F. ) ;
#89707=CARTESIAN_POINT ( 'NONE',  ( 22.39999999999999503, 76.00000000001219291, -144.3138870828976792 ) ) ;
#89747=AXIS2_PLACEMENT_3D ( 'NONE', #117418, #58698, #157872 ) ;
#89749=CIRCLE ( 'NONE', #102194, 7.900000000000003908 ) ;
#89781=FACE_OUTER_BOUND ( 'NONE', #130266, .T. ) ;
#89783=DIRECTION ( 'NONE',  ( -1.000000000000000000, 0.000000000000000000, -0.000000000000000000 ) ) ;
#89800=AXIS2_PLACEMENT_3D ( 'NONE', #47670, #106357, #65973 ) ;
#89842=DIRECTION ( 'NONE',  ( -1.000000000000000000, -0.000000000000000000, -0.000000000000000000 ) ) ;
#89848=DIRECTION ( 'NONE',  ( 0.000000000000000000, 6.982962677686266711E-15, -1.000000000000000000 ) ) ;
#89862=DIRECTION ( 'NONE',  ( -1.000000000000000000, -0.000000000000000000, -0.000000000000000000 ) ) ;
#89913=CARTESIAN_POINT ( 'NONE',  ( -20.64999999999999858, 74.00000000001199396, -116.2477294072864140 ) ) ;
#89916=AXIS2_PLACEMENT_3D ( 'NONE', #86943, #70006, #149545 ) ;
#89919=CARTESIAN_POINT ( 'NONE',  ( -21.59142135623730852, 68.15000000001199965, -115.2731074845243455 ) ) ;
#89949=AXIS2_PLACEMENT_3D ( 'NONE', #186346, #89783, #147203 ) ;
#89963=CARTESIAN_POINT ( 'NONE',  ( 23.14999999999999858, 87.75000000001222134, -148.2731074845242176 ) ) ;
#89966=CARTESIAN_POINT ( 'NONE',  ( -20.00857864376270001, 66.75000000001199396, -115.3731074845243683 ) ) ;
#89982=ORIENTED_EDGE ( 'NONE', *, *, #95562, .T. ) ;
#90001=CARTESIAN_POINT ( 'NONE',  ( 22.39999999999999858, 68.20922040163875977, -136.6231074845243540 ) ) ;
#90018=DIRECTION ( 'NONE',  ( 3.616040088954490704E-32, 7.105427357601001859E-15, -1.000000000000000000 ) ) ;
#90033=EDGE_CURVE ( 'NONE', #215553, #177416, #22842, .T. ) ;
#90034=AXIS2_PLACEMENT_3D ( 'NONE', #212568, #14381, #247827 ) ;
#90049=CARTESIAN_POINT ( 'NONE',  ( -20.64999999999999858, 74.00000000001199396, -116.2477294072864140 ) ) ;
#90058=DIRECTION ( 'NONE',  ( 0.000000000000000000, 7.056502275159890832E-15, -1.000000000000000000 ) ) ;
#90077=EDGE_CURVE ( 'NONE', #247118, #67101, #55524, .T. ) ;
#90124=ORIENTED_EDGE ( 'NONE', *, *, #20822, .F. ) ;
#90146=AXIS2_PLACEMENT_3D ( 'NONE', #83759, #396, #218152 ) ;
#90160=CARTESIAN_POINT ( 'NONE',  ( -20.85000000000000142, 76.00000000001190870, -103.0231074845243029 ) ) ;
#90166=DIRECTION ( 'NONE',  ( 0.000000000000000000, -0.8660254037844377084, -0.5000000000000016653 ) ) ;
#90176=EDGE_LOOP ( 'NONE', ( #127966, #108543, #110917, #213287 ) ) ;
#90223=CARTESIAN_POINT ( 'NONE',  ( 18.49999999999999289, 65.76093837589047553, -111.7687100499271651 ) ) ;
#90241=ORIENTED_EDGE ( 'NONE', *, *, #193121, .F. ) ;
#90260=ORIENTED_EDGE ( 'NONE', *, *, #251581, .T. ) ;
#90272=CIRCLE ( 'NONE', #115234, 0.1000000000000064587 ) ;
#90319=CARTESIAN_POINT ( 'NONE',  ( 18.59999999999997655, 64.25000000001190870, -103.0231074845243882 ) ) ;
#90339=ADVANCED_FACE ( 'NONE', ( #128955 ), #169401, .F. ) ;
#90371=CARTESIAN_POINT ( 'NONE',  ( 23.24999999999999289, 64.25000000001220712, -148.2731074845243882 ) ) ;
#90381=LINE ( 'NONE', #252029, #170 ) ;
#90390=CARTESIAN_POINT ( 'NONE',  ( -20.88420186297724257, 65.66974365629666011, -97.43601455626048846 ) ) ;
#90424=TOROIDAL_SURFACE ( 'NONE', #123768, 4.149999999999999467, 0.1000000000000000056 ) ;
#90438=CIRCLE ( 'NONE', #207167, 11.64999999999999325 ) ;
#90453=CARTESIAN_POINT ( 'NONE',  ( 21.05000000000000071, 87.75000000001190870, -105.9231074845242091 ) ) ;
#90456=CYLINDRICAL_SURFACE ( 'NONE', #221464, 0.1000000000000106914 ) ;
#90457=EDGE_CURVE ( 'NONE', #147707, #10477, #176574, .T. ) ;
#90496=EDGE_CURVE ( 'NONE', #13684, #60684, #234449, .T. ) ;
#90535=AXIS2_PLACEMENT_3D ( 'NONE', #253968, #128912, #72813 ) ;
#90585=ORIENTED_EDGE ( 'NONE', *, *, #209757, .F. ) ;
#90596=EDGE_LOOP ( 'NONE', ( #161556, #83262, #35798, #50796 ) ) ;
#90606=AXIS2_PLACEMENT_3D ( 'NONE', #131117, #112847, #93274 ) ;
#90618=ADVANCED_FACE ( 'NONE', ( #220034 ), #158805, .T. ) ;
#90638=EDGE_LOOP ( 'NONE', ( #246712, #33401, #46290 ) ) ;
#90666=ADVANCED_FACE ( 'NONE', ( #221292 ), #42675, .T. ) ;
#90669=CIRCLE ( 'NONE', #211310, 0.2000000000000057288 ) ;
#90672=AXIS2_PLACEMENT_3D ( 'NONE', #204930, #121654, #36986 ) ;
#90694=ORIENTED_EDGE ( 'NONE', *, *, #199429, .T. ) ;
#90697=DIRECTION ( 'NONE',  ( 0.000000000000000000, 0.000000000000000000, 1.000000000000000000 ) ) ;
#90708=CYLINDRICAL_SURFACE ( 'NONE', #229680, 0.1000000000000028644 ) ;
#90738=FACE_OUTER_BOUND ( 'NONE', #126247, .T. ) ;
#90769=DIRECTION ( 'NONE',  ( 0.000000000000000000, -1.000000000000000000, -6.982962677686266711E-15 ) ) ;
#90786=ORIENTED_EDGE ( 'NONE', *, *, #211589, .F. ) ;
#90792=CARTESIAN_POINT ( 'NONE',  ( 18.59999999999999076, 69.35000000001200249, -115.3731074845243398 ) ) ;
#90796=CARTESIAN_POINT ( 'NONE',  ( -21.98333005346336577, 76.00000000001219291, -143.8971828135809972 ) ) ;
#90806=ORIENTED_EDGE ( 'NONE', *, *, #76418, .T. ) ;
#90815=ORIENTED_EDGE ( 'NONE', *, *, #76895, .F. ) ;
#90838=CIRCLE ( 'NONE', #144824, 0.1999999999999918510 ) ;
#90849=ADVANCED_FACE ( 'NONE', ( #115480 ), #254934, .F. ) ;
#90886=ORIENTED_EDGE ( 'NONE', *, *, #93092, .F. ) ;
#90909=VECTOR ( 'NONE', #196921, 1000.000000000000000 ) ;
#90912=DIRECTION ( 'NONE',  ( 1.000000000000000000, -0.000000000000000000, -0.000000000000000000 ) ) ;
#90922=ORIENTED_EDGE ( 'NONE', *, *, #240187, .T. ) ;
#90966=CARTESIAN_POINT ( 'NONE',  ( 22.59999999999999432, 64.25043287652275126, -136.6239658536231047 ) ) ;
#90983=DIRECTION ( 'NONE',  ( 0.000000000000000000, 0.000000000000000000, 1.000000000000000000 ) ) ;
#90992=ORIENTED_EDGE ( 'NONE', *, *, #249540, .T. ) ;
#90998=DIRECTION ( 'NONE',  ( -1.000000000000000000, -0.000000000000000000, -0.000000000000000000 ) ) ;
#91016=CARTESIAN_POINT ( 'NONE',  ( -22.00356870141341759, 68.74575763752174851, -136.5231074845243882 ) ) ;
#91018=PLANE ( 'NONE',  #14010 ) ;
#91038=ORIENTED_EDGE ( 'NONE', *, *, #47253, .F. ) ;
#91064=CARTESIAN_POINT ( 'NONE',  ( 20.94999999999999574, 77.85102823015292017, -124.8691942151017855 ) ) ;
#91069=ADVANCED_FACE ( 'NONE', ( #43665 ), #202728, .F. ) ;
#91070=CIRCLE ( 'NONE', #174322, 0.1000000000000028644 ) ;
#91095=EDGE_CURVE ( 'NONE', #241360, #59439, #126853, .T. ) ;
#91155=ORIENTED_EDGE ( 'NONE', *, *, #247066, .T. ) ;
#91160=CARTESIAN_POINT ( 'NONE',  ( -18.49513951962167724, 85.43772502668957713, -96.24503490949508944 ) ) ;
#91184=CIRCLE ( 'NONE', #187063, 0.09999999999998898659 ) ;
#91214=AXIS2_PLACEMENT_3D ( 'NONE', #98755, #221289, #158802 ) ;
#91265=ADVANCED_FACE ( 'NONE', ( #173935 ), #31836, .T. ) ;
#91266=VECTOR ( 'NONE', #56603, 1000.000000000000114 ) ;
#91270=VERTEX_POINT ( 'NONE', #230000 ) ;
#91280=DIRECTION ( 'NONE',  ( 6.938893903907222067E-15, 1.000000000000000000, 6.982962677686266711E-15 ) ) ;
#91306=AXIS2_PLACEMENT_3D ( 'NONE', #136632, #949, #137913 ) ;
#91321=EDGE_CURVE ( 'NONE', #119361, #177518, #189399, .T. ) ;
#91351=AXIS2_PLACEMENT_3D ( 'NONE', #193285, #94160, #173769 ) ;
#91377=CARTESIAN_POINT ( 'NONE',  ( 18.44444291854882323, 85.49010118095512212, -96.39420351963327960 ) ) ;
#91380=LINE ( 'NONE', #134329, #3529 ) ;
#91387=DIRECTION ( 'NONE',  ( -1.000000000000000000, 0.000000000000000000, -0.000000000000000000 ) ) ;
#91396=CARTESIAN_POINT ( 'NONE',  ( 20.04142135391667168, 64.25000000001196554, -111.8206006188945025 ) ) ;
#91401=AXIS2_PLACEMENT_3D ( 'NONE', #3768, #161583, #221509 ) ;
#91420=CARTESIAN_POINT ( 'NONE',  ( 20.94999999999999929, 76.00000000001190870, -103.0231074845243029 ) ) ;
#91424=ORIENTED_EDGE ( 'NONE', *, *, #186537, .T. ) ;
#91429=DIRECTION ( 'NONE',  ( 0.000000000000000000, 0.000000000000000000, 1.000000000000000000 ) ) ;
#91438=EDGE_CURVE ( 'NONE', #219596, #28335, #251934, .T. ) ;
#91444=CARTESIAN_POINT ( 'NONE',  ( 23.14999999999999503, 69.35000000001200249, -115.3731074845243398 ) ) ;
#91459=ADVANCED_FACE ( 'NONE', ( #5486 ), #203721, .T. ) ;
#91515=DIRECTION ( 'NONE',  ( -0.000000000000000000, 6.982962677686266711E-15, -1.000000000000000000 ) ) ;
#91536=CARTESIAN_POINT ( 'NONE',  ( 18.49999999999999289, 65.55993210786772352, -111.7559897356389911 ) ) ;
#91544=DIRECTION ( 'NONE',  ( 1.000000000000000000, 0.000000000000000000, 0.000000000000000000 ) ) ;
#91549=ORIENTED_EDGE ( 'NONE', *, *, #239549, .T. ) ;
#91581=ORIENTED_EDGE ( 'NONE', *, *, #153874, .F. ) ;
#91585=CIRCLE ( 'NONE', #249806, 0.1000000000000009492 ) ;
#91589=ORIENTED_EDGE ( 'NONE', *, *, #42483, .F. ) ;
#91610=CARTESIAN_POINT ( 'NONE',  ( 23.15000000000000213, 85.00000000001197975, -112.9170766071766820 ) ) ;
#91660=DIRECTION ( 'NONE',  ( 0.000000000000000000, 0.000000000000000000, -1.000000000000000000 ) ) ;
#91665=DIRECTION ( 'NONE',  ( 0.000000000000000000, -1.000000000000000000, 0.000000000000000000 ) ) ;
#91671=DIRECTION ( 'NONE',  ( -1.000000000000000000, -0.000000000000000000, -0.000000000000000000 ) ) ;
#91686=CARTESIAN_POINT ( 'NONE',  ( -18.59999999999999787, 77.25000000001209344, -128.5231074845242745 ) ) ;
#91693=CARTESIAN_POINT ( 'NONE',  ( 21.93340585972002543, 68.67585297715832837, -136.5231074845243597 ) ) ;
#91734=DIRECTION ( 'NONE',  ( 0.000000000000000000, 0.000000000000000000, 1.000000000000000000 ) ) ;
#91755=ORIENTED_EDGE ( 'NONE', *, *, #39142, .F. ) ;
#91784=CARTESIAN_POINT ( 'NONE',  ( -21.07928932188134041, 69.67148334361884565, -136.6220026301787414 ) ) ;
#91790=ADVANCED_FACE ( 'NONE', ( #24472 ), #987, .T. ) ;
#91796=DIRECTION ( 'NONE',  ( 1.000000000000000000, -0.000000000000000000, 0.000000000000000000 ) ) ;
#91801=DIRECTION ( 'NONE',  ( 0.000000000000000000, 0.000000000000000000, 1.000000000000000000 ) ) ;
#91810=CARTESIAN_POINT ( 'NONE',  ( 22.00356870072048920, 76.00000000002594902, -143.7773498462486259 ) ) ;
#91827=EDGE_CURVE ( 'NONE', #159137, #197206, #18209, .T. ) ;
#91844=ORIENTED_EDGE ( 'NONE', *, *, #206678, .T. ) ;
#91851=DIRECTION ( 'NONE',  ( 2.694716079187273439E-16, 1.000000000000000000, 6.467318590049456648E-15 ) ) ;
#91853=DIRECTION ( 'NONE',  ( 1.000000000000000000, 0.000000000000000000, 0.000000000000000000 ) ) ;
#91863=EDGE_CURVE ( 'NONE', #13761, #185096, #44008, .T. ) ;
#91977=ORIENTED_EDGE ( 'NONE', *, *, #194600, .T. ) ;
#91985=DIRECTION ( 'NONE',  ( 1.000000000000000000, 0.000000000000000000, 0.000000000000000000 ) ) ;
#92017=CARTESIAN_POINT ( 'NONE',  ( -21.05000000000000071, 70.10000000001197407, -113.2422072491807086 ) ) ;
#92036=CARTESIAN_POINT ( 'NONE',  ( -20.64999999999999858, 71.65000000001207070, -124.2731074845243313 ) ) ;
#92047=LINE ( 'NONE', #172923, #226405 ) ;
#92056=ORIENTED_EDGE ( 'NONE', *, *, #135755, .F. ) ;
#92078=EDGE_LOOP ( 'NONE', ( #195817, #151855, #154691, #167944 ) ) ;
#92127=EDGE_LOOP ( 'NONE', ( #256093, #229934, #47993, #179668 ) ) ;
#92130=ORIENTED_EDGE ( 'NONE', *, *, #195787, .F. ) ;
#92140=CARTESIAN_POINT ( 'NONE',  ( -21.02374657821566828, 64.39999999919209017, -109.9513107143265387 ) ) ;
#92163=ORIENTED_EDGE ( 'NONE', *, *, #187841, .T. ) ;
#92191=CARTESIAN_POINT ( 'NONE',  ( -18.59999999999999787, 64.35000000001198828, -115.1731074845243796 ) ) ;
#92220=DIRECTION ( 'NONE',  ( 1.000000000000000000, -0.000000000000000000, 0.000000000000000000 ) ) ;
#92233=EDGE_CURVE ( 'NONE', #154466, #126916, #160756, .T. ) ;
#92237=ORIENTED_EDGE ( 'NONE', *, *, #227436, .T. ) ;
#92276=DIRECTION ( 'NONE',  ( 0.000000000000000000, -0.4930308989875170078, -0.8700118002898356018 ) ) ;
#92281=CYLINDRICAL_SURFACE ( 'NONE', #12481, 0.09999999999999939493 ) ;
#92285=CARTESIAN_POINT ( 'NONE',  ( 20.84999999999998721, 65.66751761918668251, -97.42826094061121012 ) ) ;
#92293=FACE_OUTER_BOUND ( 'NONE', #153220, .T. ) ;
#92296=DIRECTION ( 'NONE',  ( 0.000000000000000000, -1.000000000000000000, -6.982962677686267499E-15 ) ) ;
#92315=( NAMED_UNIT ( * ) SI_UNIT ( $, .STERADIAN. ) SOLID_ANGLE_UNIT ( ) );
#92322=DIRECTION ( 'NONE',  ( 0.000000000000000000, -0.1350103645451557199, -0.9908441862701644620 ) ) ;
#92328=VECTOR ( 'NONE', #65930, 1000.000000000000000 ) ;
#92329=ADVANCED_FACE ( 'NONE', ( #96905 ), #10894, .T. ) ;
#92332=VERTEX_POINT ( 'NONE', #155672 ) ;
#92335=DIRECTION ( 'NONE',  ( -1.000000000000000000, -0.000000000000000000, -0.000000000000000000 ) ) ;
#92368=ORIENTED_EDGE ( 'NONE', *, *, #2874, .F. ) ;
#92369=CARTESIAN_POINT ( 'NONE',  ( 20.94999999999999929, 87.48912529308798014, -106.0231074845242176 ) ) ;
#92414=ORIENTED_EDGE ( 'NONE', *, *, #165874, .T. ) ;
#92427=EDGE_CURVE ( 'NONE', #190621, #154962, #231647, .T. ) ;
#92462=EDGE_CURVE ( 'NONE', #135981, #63725, #244273, .T. ) ;
#92473=EDGE_CURVE ( 'NONE', #87303, #221570, #31933, .T. ) ;
#92489=FACE_OUTER_BOUND ( 'NONE', #26186, .T. ) ;
#92520=CARTESIAN_POINT ( 'NONE',  ( 18.47135592147649774, 85.47108861327761531, -96.33951254468077252 ) ) ;
#92571=EDGE_CURVE ( 'NONE', #236445, #156311, #127593, .T. ) ;
#92666=FACE_OUTER_BOUND ( 'NONE', #171876, .T. ) ;
#92692=CARTESIAN_POINT ( 'NONE',  ( -20.85000000000000142, 77.83585931145546510, -91.41866831572575336 ) ) ;
#92702=EDGE_LOOP ( 'NONE', ( #74803, #24628, #140882, #6234 ) ) ;
#92708=EDGE_LOOP ( 'NONE', ( #216522, #71145, #56302, #227456 ) ) ;
#92710=DIRECTION ( 'NONE',  ( 0.000000000000000000, 1.000000000000000000, 6.982962677686266711E-15 ) ) ;
#92724=LINE ( 'NONE', #109717, #97212 ) ;
#92732=EDGE_CURVE ( 'NONE', #106161, #155283, #144299, .T. ) ;
#92745=CARTESIAN_POINT ( 'NONE',  ( 23.14999999999999858, 76.00000000001192291, -105.0231074845243029 ) ) ;
#92766=EDGE_CURVE ( 'NONE', #102756, #195402, #152745, .T. ) ;
#92807=CARTESIAN_POINT ( 'NONE',  ( -22.45354308602430748, 75.99999978013465807, -148.2735403749860836 ) ) ;
#92809=LINE ( 'NONE', #32894, #152574 ) ;
#92832=AXIS2_PLACEMENT_3D ( 'NONE', #171253, #68255, #66962 ) ;
#92842=CARTESIAN_POINT ( 'NONE',  ( 20.95568717954149562, 65.39800594612027851, -128.9205991162557154 ) ) ;
#92853=AXIS2_PLACEMENT_3D ( 'NONE', #112027, #96276, #74209 ) ;
#92861=CARTESIAN_POINT ( 'NONE',  ( -21.44999999999999929, 68.65000000001199965, -115.2731074845243455 ) ) ;
#92864=DIRECTION ( 'NONE',  ( 0.000000000000000000, 0.000000000000000000, -1.000000000000000000 ) ) ;
#92874=AXIS2_PLACEMENT_3D ( 'NONE', #9626, #212969, #70924 ) ;
#92893=DIRECTION ( 'NONE',  ( -0.7071067811865475727, 0.7071067811865475727, 4.937700262164531476E-15 ) ) ;
#92923=DIRECTION ( 'NONE',  ( 1.000000000000000000, 0.000000000000000000, 0.000000000000000000 ) ) ;
#92939=CARTESIAN_POINT ( 'NONE',  ( 23.14999999999999858, 78.10000000001190301, -103.0231074845242887 ) ) ;
#92946=CIRCLE ( 'NONE', #72125, 7.900000000000003908 ) ;
#92947=TOROIDAL_SURFACE ( 'NONE', #63742, 3.899999999999999467, 0.1000000000000000056 ) ;
#92960=ORIENTED_EDGE ( 'NONE', *, *, #31554, .F. ) ;
#92977=DIRECTION ( 'NONE',  ( 0.000000000000000000, -0.4930308989875170078, -0.8700118002898356018 ) ) ;
#92988=CARTESIAN_POINT ( 'NONE',  ( 20.85000000000000142, 76.32388570108224712, -103.0655178952103199 ) ) ;
#93015=VERTEX_POINT ( 'NONE', #234326 ) ;
#93021=CARTESIAN_POINT ( 'NONE',  ( 22.50000000000000000, 68.20922040163875977, -136.6231074845243540 ) ) ;
#93033=CARTESIAN_POINT ( 'NONE',  ( 21.05000000000000071, 87.65000000001212754, -133.6231074845242119 ) ) ;
#93037=DIRECTION ( 'NONE',  ( 0.000000000000000000, 6.938893903907222067E-15, -1.000000000000000000 ) ) ;
#93084=DIRECTION ( 'NONE',  ( 1.000000000000000000, 0.000000000000000000, 0.000000000000000000 ) ) ;
#93092=EDGE_CURVE ( 'NONE', #196564, #7658, #33621, .T. ) ;
#93104=CARTESIAN_POINT ( 'NONE',  ( -23.25000000000000000, 74.00000000001199396, -116.2477294072864140 ) ) ;
#93151=DIRECTION ( 'NONE',  ( -1.000000000000000000, -0.000000000000000000, -0.000000000000000000 ) ) ;
#93216=AXIS2_PLACEMENT_3D ( 'NONE', #48885, #206682, #71046 ) ;
#93219=DIRECTION ( 'NONE',  ( 0.000000000000000000, -6.982962677686266711E-15, 1.000000000000000000 ) ) ;
#93232=ORIENTED_EDGE ( 'NONE', *, *, #2031, .F. ) ;
#93237=ORIENTED_EDGE ( 'NONE', *, *, #140649, .T. ) ;
#93259=CARTESIAN_POINT ( 'NONE',  ( 21.05000000000000071, 70.60000000001205933, -124.1178414656112352 ) ) ;
#93274=DIRECTION ( 'NONE',  ( 1.000000000000000000, 0.000000000000000000, 0.000000000000000000 ) ) ;
#93279=CARTESIAN_POINT ( 'NONE',  ( 18.39999999999999858, 85.60000000001186038, -96.42291809330220076 ) ) ;
#93297=CIRCLE ( 'NONE', #14226, 0.1000000000000072220 ) ;
#93354=AXIS2_PLACEMENT_3D ( 'NONE', #235699, #15396, #191481 ) ;
#93362=ORIENTED_EDGE ( 'NONE', *, *, #33124, .T. ) ;
#93379=ORIENTED_EDGE ( 'NONE', *, *, #126277, .T. ) ;
#93422=DIRECTION ( 'NONE',  ( -1.000000000000000000, 0.000000000000000000, 0.000000000000000000 ) ) ;
#93475=DIRECTION ( 'NONE',  ( -1.000000000000000000, 2.952720810173289112E-16, 2.061873921506763405E-30 ) ) ;
#93479=ORIENTED_EDGE ( 'NONE', *, *, #20822, .T. ) ;
#93487=CARTESIAN_POINT ( 'NONE',  ( 20.94999999999999929, 76.00000000001190870, -103.0231074845243029 ) ) ;
#93489=DIRECTION ( 'NONE',  ( 0.000000000000000000, 1.000000000000000000, 6.608470384673536824E-15 ) ) ;
#93503=DIRECTION ( 'NONE',  ( 0.000000000000000000, -0.01562499999999307672, 0.9998779222360100194 ) ) ;
#93519=LINE ( 'NONE', #148369, #256372 ) ;
#93530=ORIENTED_EDGE ( 'NONE', *, *, #94608, .T. ) ;
#93532=PLANE ( 'NONE',  #250213 ) ;
#93534=VECTOR ( 'NONE', #140336, 1000.000000000000000 ) ;
#93566=FACE_OUTER_BOUND ( 'NONE', #22967, .T. ) ;
#93567=AXIS2_PLACEMENT_3D ( 'NONE', #21462, #100922, #180523 ) ;
#93615=ORIENTED_EDGE ( 'NONE', *, *, #145586, .T. ) ;
#93635=FACE_OUTER_BOUND ( 'NONE', #108467, .T. ) ;
#93647=DIRECTION ( 'NONE',  ( 0.000000000000000000, -7.116814260417668513E-15, 1.000000000000000000 ) ) ;
#93660=CARTESIAN_POINT ( 'NONE',  ( 18.52928932188133970, 65.72071067813062939, -111.8731074845243683 ) ) ;
#93662=DIRECTION ( 'NONE',  ( 0.000000000000000000, -1.000000000000000000, -7.272083257015735086E-15 ) ) ;
#93663=CARTESIAN_POINT ( 'NONE',  ( 21.09787244211741708, 67.22462929267473442, -124.2838541002068240 ) ) ;
#93678=DIRECTION ( 'NONE',  ( -1.000000000000000000, -0.000000000000000000, -0.000000000000000000 ) ) ;
#93718=ADVANCED_FACE ( 'NONE', ( #63081 ), #236456, .T. ) ;
#93724=TOROIDAL_SURFACE ( 'NONE', #122953, 11.65000000000000036, 0.1000000000000000056 ) ;
#93761=VERTEX_POINT ( 'NONE', #224716 ) ;
#93788=ORIENTED_EDGE ( 'NONE', *, *, #150414, .F. ) ;
#93827=VERTEX_POINT ( 'NONE', #33005 ) ;
#93832=DIRECTION ( 'NONE',  ( -1.000000000000000000, 0.000000000000000000, -0.000000000000000000 ) ) ;
#93836=ADVANCED_FACE ( 'NONE', ( #212882 ), #89060, .F. ) ;
#93840=AXIS2_PLACEMENT_3D ( 'NONE', #202194, #1405, #143492 ) ;
#93884=FACE_OUTER_BOUND ( 'NONE', #136415, .T. ) ;
#93886=ORIENTED_EDGE ( 'NONE', *, *, #92233, .F. ) ;
#93933=DIRECTION ( 'NONE',  ( 0.000000000000000000, -1.000000000000000000, -6.982962677686265922E-15 ) ) ;
#93939=LINE ( 'NONE', #169678, #76365 ) ;
#93942=ORIENTED_EDGE ( 'NONE', *, *, #79782, .F. ) ;
#93947=ORIENTED_EDGE ( 'NONE', *, *, #108553, .F. ) ;
#93950=EDGE_CURVE ( 'NONE', #245468, #18434, #49197, .T. ) ;
#93957=CARTESIAN_POINT ( 'NONE',  ( 20.85000000000000142, 77.83585931145546510, -91.51866831572576189 ) ) ;
#93969=CARTESIAN_POINT ( 'NONE',  ( -23.15000000000000213, 76.00000000001216449, -140.5731074845242858 ) ) ;
#93987=CARTESIAN_POINT ( 'NONE',  ( 20.94999999999999574, 76.00000000001213607, -136.5231074845242745 ) ) ;
#93991=VERTEX_POINT ( 'NONE', #134595 ) ;
#93992=CIRCLE ( 'NONE', #10627, 0.1000000000000028644 ) ;
#93994=TOROIDAL_SURFACE ( 'NONE', #27409, 4.149999999999999467, 0.1000000000000000056 ) ;
#93997=CARTESIAN_POINT ( 'NONE',  ( 18.51697539158856642, 65.68434038414355314, -97.48668807260654035 ) ) ;
#94010=CARTESIAN_POINT ( 'NONE',  ( 23.14999999999999503, 69.35000000001200249, -115.2731074845243455 ) ) ;
#94076=EDGE_CURVE ( 'NONE', #217215, #162824, #82490, .T. ) ;
#94094=EDGE_CURVE ( 'NONE', #211746, #228703, #215782, .T. ) ;
#94102=ORIENTED_EDGE ( 'NONE', *, *, #231951, .F. ) ;
#94103=ADVANCED_FACE ( 'NONE', ( #199756 ), #124059, .T. ) ;
#94112=CARTESIAN_POINT ( 'NONE',  ( 21.00000000000000000, 66.25000000001199396, -115.2731074845243597 ) ) ;
#94158=CARTESIAN_POINT ( 'NONE',  ( -23.25000000000000000, 65.66751761918668251, -97.42826094061121012 ) ) ;
#94160=DIRECTION ( 'NONE',  ( 1.000000000000000000, 0.000000000000000000, 0.000000000000000000 ) ) ;
#94161=CARTESIAN_POINT ( 'NONE',  ( 20.95512820512820440, 67.12384868372393498, -124.3731074845243683 ) ) ;
#94203=FACE_OUTER_BOUND ( 'NONE', #82032, .T. ) ;
#94210=FACE_OUTER_BOUND ( 'NONE', #229189, .T. ) ;
#94222=VECTOR ( 'NONE', #11119, 1000.000000000000000 ) ;
#94251=VERTEX_POINT ( 'NONE', #48355 ) ;
#94295=DIRECTION ( 'NONE',  ( 0.000000000000000000, 1.000000000000000000, 6.938893903907222067E-15 ) ) ;
#94316=CIRCLE ( 'NONE', #198382, 11.64999999999999325 ) ;
#94317=CIRCLE ( 'NONE', #235969, 7.900000000000003908 ) ;
#94326=DIRECTION ( 'NONE',  ( 0.000000000000000000, -5.551115123125777653E-14, 1.000000000000000000 ) ) ;
#94335=CARTESIAN_POINT ( 'NONE',  ( -22.47071067811865319, 68.27992525551407255, -136.6221999392269595 ) ) ;
#94342=LINE ( 'NONE', #13547, #84669 ) ;
#94365=DIRECTION ( 'NONE',  ( 1.000000000000000000, 0.000000000000000000, 0.000000000000000000 ) ) ;
#94379=ADVANCED_FACE ( 'NONE', ( #57324 ), #97723, .F. ) ;
#94387=ADVANCED_FACE ( 'NONE', ( #117324 ), #156487, .F. ) ;
#94391=FACE_OUTER_BOUND ( 'NONE', #176538, .T. ) ;
#94399=ORIENTED_EDGE ( 'NONE', *, *, #32412, .T. ) ;
#94437=CIRCLE ( 'NONE', #69338, 4.000000000000003553 ) ;
#94457=VERTEX_POINT ( 'NONE', #89412 ) ;
#94464=CARTESIAN_POINT ( 'NONE',  ( -18.40904629823847216, 85.50000000001186606, -96.42291792204295575 ) ) ;
#94483=ORIENTED_EDGE ( 'NONE', *, *, #112133, .T. ) ;
#94500=LINE ( 'NONE', #115353, #11981 ) ;
#94501=CIRCLE ( 'NONE', #240278, 4.049999999999998046 ) ;
#94506=CARTESIAN_POINT ( 'NONE',  ( 19.75857864376268935, 64.25000000001196554, -111.6731074845243796 ) ) ;
#94507=CARTESIAN_POINT ( 'NONE',  ( 21.05000000000000071, 76.00000000001217870, -143.0637644362255401 ) ) ;
#94516=CARTESIAN_POINT ( 'NONE',  ( 18.59999999999999076, 77.14957036958755054, -95.20719500002232394 ) ) ;
#94525=CYLINDRICAL_SURFACE ( 'NONE', #178188, 0.1000000000000033362 ) ;
#94558=CARTESIAN_POINT ( 'NONE',  ( 21.87500000000000355, 66.25000000001199396, -115.2731074845243597 ) ) ;
#94570=AXIS2_PLACEMENT_3D ( 'NONE', #86599, #189595, #226108 ) ;
#94598=VECTOR ( 'NONE', #223366, 1000.000000000000000 ) ;
#94604=CARTESIAN_POINT ( 'NONE',  ( -22.59999999999999787, 75.89914163091351895, -148.2726746080136877 ) ) ;
#94608=EDGE_CURVE ( 'NONE', #59064, #88196, #86385, .T. ) ;
#94647=DIRECTION ( 'NONE',  ( 0.000000000000000000, 0.9908441862701605762, 0.1350103645451835310 ) ) ;
#94651=CARTESIAN_POINT ( 'NONE',  ( -23.25000000000000000, 85.00000000001197975, -112.9170766071766820 ) ) ;
#94660=AXIS2_PLACEMENT_3D ( 'NONE', #208405, #29784, #190111 ) ;
#94668=EDGE_LOOP ( 'NONE', ( #131928, #140639, #19559, #103270 ) ) ;
#94687=ORIENTED_EDGE ( 'NONE', *, *, #21363, .T. ) ;
#94701=AXIS2_PLACEMENT_3D ( 'NONE', #69481, #193269, #92864 ) ;
#94733=CIRCLE ( 'NONE', #240491, 11.80000000000000426 ) ;
#94759=EDGE_CURVE ( 'NONE', #116058, #23751, #132396, .T. ) ;
#94767=AXIS2_PLACEMENT_3D ( 'NONE', #208094, #242055, #243339 ) ;
#94773=ORIENTED_EDGE ( 'NONE', *, *, #18221, .F. ) ;
#94775=DIRECTION ( 'NONE',  ( 1.000000000000000000, -0.000000000000000000, 0.000000000000000000 ) ) ;
#94798=ORIENTED_EDGE ( 'NONE', *, *, #164141, .T. ) ;
#94807=VECTOR ( 'NONE', #256205, 1000.000000000000000 ) ;
#94821=DIRECTION ( 'NONE',  ( -0.000000000000000000, 1.000000000000000000, 6.982962677686266711E-15 ) ) ;
#94838=EDGE_LOOP ( 'NONE', ( #212837, #138, #257970, #144992, #185778, #181367, #168227, #58549, #61680, #62268, #88638 ) ) ;
#94856=DIRECTION ( 'NONE',  ( 0.000000000000000000, -0.9876197685951263461, 0.1568667991644794590 ) ) ;
#94867=CARTESIAN_POINT ( 'NONE',  ( 21.06600267594171783, 67.22483393081216718, -124.3188447021496188 ) ) ;
#94893=DIRECTION ( 'NONE',  ( 0.000000000000000000, -1.186135710069611419E-15, 1.000000000000000000 ) ) ;
#94897=CARTESIAN_POINT ( 'NONE',  ( -18.50000000000000000, 64.35000000001191722, -103.0231074845243882 ) ) ;
#94924=AXIS2_PLACEMENT_3D ( 'NONE', #209095, #111289, #145575 ) ;
#94928=VECTOR ( 'NONE', #79265, 1000.000000000000000 ) ;
#94930=CARTESIAN_POINT ( 'NONE',  ( 18.52928932188134326, 65.72071067813062939, -111.8145288407616960 ) ) ;
#94966=FACE_OUTER_BOUND ( 'NONE', #44546, .T. ) ;
#94975=CARTESIAN_POINT ( 'NONE',  ( -20.64999999999999858, 76.00000000001190870, -103.0231074845243029 ) ) ;
#94979=EDGE_CURVE ( 'NONE', #221570, #213669, #207815, .T. ) ;
#94988=DIRECTION ( 'NONE',  ( 0.000000000000000000, -0.8700118002898357128, 0.4930308989875171188 ) ) ;
#95047=CARTESIAN_POINT ( 'NONE',  ( 20.94999999999999929, 71.14953271029243353, -124.4888400755226598 ) ) ;
#95069=( BOUNDED_CURVE ( )  B_SPLINE_CURVE ( 3, ( #7630, #208419, #6328, #183705 ),
 .UNSPECIFIED., .F., .F. ) 
 B_SPLINE_CURVE_WITH_KNOTS ( ( 4, 4 ),
 ( 0.000000000000000000, 1.570796326794908992 ),
 .UNSPECIFIED. ) 
 CURVE ( )  GEOMETRIC_REPRESENTATION_ITEM ( )  RATIONAL_B_SPLINE_CURVE ( ( 1.000000000000000000, 0.8047378541243619399, 0.8047378541243619399, 1.000000000000000000 ) ) 
 REPRESENTATION_ITEM ( '' )  );
#95102=CARTESIAN_POINT ( 'NONE',  ( -21.05000000000000071, 75.96636726467852441, -142.7819246792058152 ) ) ;
#95106=AXIS2_PLACEMENT_3D ( 'NONE', #5325, #79731, #142292 ) ;
#95121=DIRECTION ( 'NONE',  ( 0.000000000000000000, -0.1350103645451807555, -0.9908441862701609093 ) ) ;
#95130=EDGE_LOOP ( 'NONE', ( #135751, #153072, #58171, #191968 ) ) ;
#95131=EDGE_LOOP ( 'NONE', ( #177907, #186179, #247453, #145048 ) ) ;
#95167=DIRECTION ( 'NONE',  ( 2.840903330521633255E-16, 0.8700118002898357128, -0.4930308989875171188 ) ) ;
#95177=DIRECTION ( 'NONE',  ( 0.000000000000000000, 1.000000000000000000, 6.982962677686266711E-15 ) ) ;
#95180=EDGE_CURVE ( 'NONE', #188655, #140955, #170050, .T. ) ;
#95206=PRODUCT_CONTEXT ( 'NONE', #243908, 'mechanical' ) ;
#95243=DIRECTION ( 'NONE',  ( 0.000000000000000000, 0.000000000000000000, 1.000000000000000000 ) ) ;
#95246=EDGE_CURVE ( 'NONE', #145844, #186227, #174134, .T. ) ;
#95257=DIRECTION ( 'NONE',  ( 1.000000000000000000, 0.000000000000000000, 0.000000000000000000 ) ) ;
#95275=CARTESIAN_POINT ( 'NONE',  ( -18.59999999999999787, 74.16465844978765176, -124.9679561919613207 ) ) ;
#95378=CARTESIAN_POINT ( 'NONE',  ( 20.94999999999999929, 87.65000000001190017, -103.0231074845242176 ) ) ;
#95411=CARTESIAN_POINT ( 'NONE',  ( -18.59999999999999787, 76.00000000001213607, -136.5231074845242745 ) ) ;
#95417=EDGE_LOOP ( 'NONE', ( #98083, #73065, #79290, #170062, #223448, #134111, #56178, #251590, #65961, #73271 ) ) ;
#95447=ORIENTED_EDGE ( 'NONE', *, *, #87919, .T. ) ;
#95463=CARTESIAN_POINT ( 'NONE',  ( -23.25000000000000000, 77.83585931145546510, -91.51866831572576189 ) ) ;
#95467=DIRECTION ( 'NONE',  ( -1.000000000000000000, 0.000000000000000000, -0.000000000000000000 ) ) ;
#95503=ORIENTED_EDGE ( 'NONE', *, *, #76418, .F. ) ;
#95519=CARTESIAN_POINT ( 'NONE',  ( -21.05000000000000071, 76.00000000001216449, -140.8231074845242574 ) ) ;
#95562=EDGE_CURVE ( 'NONE', #64056, #194835, #28584, .T. ) ;
#95569=EDGE_CURVE ( 'NONE', #28934, #153892, #91070, .T. ) ;
#95588=CARTESIAN_POINT ( 'NONE',  ( 20.12481660106788439, 66.47365600773714789, -128.2969658154281660 ) ) ;
#95607=AXIS2_PLACEMENT_3D ( 'NONE', #122131, #221207, #158717 ) ;
#95621=DIRECTION ( 'NONE',  ( 0.000000000000000000, 7.056502275159890832E-15, -1.000000000000000000 ) ) ;
#95639=AXIS2_PLACEMENT_3D ( 'NONE', #186679, #86251, #6739 ) ;
#95650=AXIS2_PLACEMENT_3D ( 'NONE', #243660, #181139, #80715 ) ;
#95670=CARTESIAN_POINT ( 'NONE',  ( 21.05000000000000071, 76.00000000001205080, -123.5481074845242802 ) ) ;
#95717=CARTESIAN_POINT ( 'NONE',  ( -21.05000000000000071, 87.75000000001192291, -106.0231074845242176 ) ) ;
#95718=DIRECTION ( 'NONE',  ( -1.000000000000000000, -0.000000000000000000, -0.000000000000000000 ) ) ;
#95738=CARTESIAN_POINT ( 'NONE',  ( -18.31572283045166216, 85.54843783089741294, -96.17248183346565327 ) ) ;
#95740=FACE_OUTER_BOUND ( 'NONE', #146631, .T. ) ;
#95750=AXIS2_PLACEMENT_3D ( 'NONE', #163752, #86750, #45078 ) ;
#95784=ORIENTED_EDGE ( 'NONE', *, *, #6965, .T. ) ;
#95785=CARTESIAN_POINT ( 'NONE',  ( 22.57856590037848576, 76.00412833007658264, -148.2731659471997148 ) ) ;
#95789=DIRECTION ( 'NONE',  ( 2.259780016855445309E-14, -0.9875055080513764905, 0.1575844902526679359 ) ) ;
#95795=ORIENTED_EDGE ( 'NONE', *, *, #154765, .T. ) ;
#95870=B_SPLINE_CURVE_WITH_KNOTS ( 'NONE', 3,
 ( #239968, #195724, #75759, #179997, #41784, #200836, #121335 ),
 .UNSPECIFIED., .F., .F.,
 ( 4, 3, 4 ),
 ( 0.000000000000000000, 3.357501770814687536E-05, 5.199112466349470742E-05 ),
 .UNSPECIFIED. ) ;
#95883=ORIENTED_EDGE ( 'NONE', *, *, #240182, .T. ) ;
#95890=DIRECTION ( 'NONE',  ( -0.000000000000000000, -6.982962677686266711E-15, 1.000000000000000000 ) ) ;
#95894=VECTOR ( 'NONE', #17765, 1000.000000000000000 ) ;
#95922=ORIENTED_EDGE ( 'NONE', *, *, #220141, .F. ) ;
#95923=CARTESIAN_POINT ( 'NONE',  ( 23.14999999999999858, 71.18691588786246882, -114.9646252410481537 ) ) ;
#95961=VERTEX_POINT ( 'NONE', #123471 ) ;
#95984=CIRCLE ( 'NONE', #145878, 0.09999999999998898659 ) ;
#95986=ORIENTED_EDGE ( 'NONE', *, *, #148288, .F. ) ;
#96021=CARTESIAN_POINT ( 'NONE',  ( -22.16821283564876666, 68.44102665923136897, -136.5231074845243313 ) ) ;
#96023=VECTOR ( 'NONE', #102517, 1000.000000000000000 ) ;
#96039=ORIENTED_EDGE ( 'NONE', *, *, #209227, .T. ) ;
#96066=ORIENTED_EDGE ( 'NONE', *, *, #43936, .T. ) ;
#96086=VECTOR ( 'NONE', #176889, 1000.000000000000000 ) ;
#96114=CARTESIAN_POINT ( 'NONE',  ( -18.50000000000000000, 68.97833521811179480, -99.38954208262707368 ) ) ;
#96139=ORIENTED_EDGE ( 'NONE', *, *, #251975, .F. ) ;
#96140=EDGE_CURVE ( 'NONE', #241350, #12190, #109128, .T. ) ;
#96142=CARTESIAN_POINT ( 'NONE',  ( 21.07964655665547582, 67.22511038503350278, -124.3011909015603038 ) ) ;
#96146=ORIENTED_EDGE ( 'NONE', *, *, #38010, .F. ) ;
#96185=DIRECTION ( 'NONE',  ( -0.000000000000000000, 0.1298341882519735979, 0.9915357197604890427 ) ) ;
#96198=EDGE_CURVE ( 'NONE', #146024, #152762, #19915, .T. ) ;
#96214=CIRCLE ( 'NONE', #137899, 0.5000000000000004441 ) ;
#96250=ORIENTED_EDGE ( 'NONE', *, *, #203219, .F. ) ;
#96260=CARTESIAN_POINT ( 'NONE',  ( 23.14999999999999858, 70.40000000001199965, -115.4283735034374274 ) ) ;
#96276=DIRECTION ( 'NONE',  ( -1.000000000000000000, 0.000000000000000000, -0.000000000000000000 ) ) ;
#96297=TOROIDAL_SURFACE ( 'NONE', #183807, 7.800000000000000711, 0.1000000000000000056 ) ;
#96311=EDGE_CURVE ( 'NONE', #53074, #91270, #169907, .T. ) ;
#96388=EDGE_CURVE ( 'NONE', #29926, #151185, #28948, .T. ) ;
#96409=ORIENTED_EDGE ( 'NONE', *, *, #245732, .T. ) ;
#96418=EDGE_CURVE ( 'NONE', #225759, #53074, #224692, .T. ) ;
#96454=CARTESIAN_POINT ( 'NONE',  ( -23.15000000000000213, 87.65000000001192859, -106.1231074845242262 ) ) ;
#96495=CARTESIAN_POINT ( 'NONE',  ( 21.05000000000000071, 71.14953271029243353, -124.4888400755226598 ) ) ;
#96499=EDGE_CURVE ( 'NONE', #144360, #16182, #183204, .T. ) ;
#96505=ORIENTED_EDGE ( 'NONE', *, *, #240187, .F. ) ;
#96506=EDGE_CURVE ( 'NONE', #87569, #154428, #242559, .T. ) ;
#96523=AXIS2_PLACEMENT_3D ( 'NONE', #129648, #231338, #111372 ) ;
#96529=CARTESIAN_POINT ( 'NONE',  ( 21.05000000000000071, 71.00000000001205080, -124.1178414656112352 ) ) ;
#96544=AXIS2_PLACEMENT_3D ( 'NONE', #128213, #223438, #69536 ) ;
#96559=CIRCLE ( 'NONE', #229862, 0.09999999999999230338 ) ;
#96563=EDGE_CURVE ( 'NONE', #215553, #27724, #19685, .T. ) ;
#96587=CARTESIAN_POINT ( 'NONE',  ( 18.59999999999998366, 68.97833521811179480, -99.18954208262705663 ) ) ;
#96593=CARTESIAN_POINT ( 'NONE',  ( 18.39999999999999858, 85.50000000001185185, -96.42291809330220076 ) ) ;
#96606=ORIENTED_EDGE ( 'NONE', *, *, #104249, .F. ) ;
#96613=ORIENTED_EDGE ( 'NONE', *, *, #247190, .F. ) ;
#96657=FACE_OUTER_BOUND ( 'NONE', #55556, .T. ) ;
#96668=ADVANCED_FACE ( 'NONE', ( #69085 ), #87325, .F. ) ;
#96677=EDGE_CURVE ( 'NONE', #22494, #126916, #148617, .T. ) ;
#96706=DIRECTION ( 'NONE',  ( 0.000000000000000000, 1.000000000000000000, 0.000000000000000000 ) ) ;
#96719=TOROIDAL_SURFACE ( 'NONE', #146796, 0.2000000000000000111, 0.1000000000000000056 ) ;
#96722=CARTESIAN_POINT ( 'NONE',  ( -20.64999999999999858, 73.60000000001204512, -123.2984855617622202 ) ) ;
#96760=ORIENTED_EDGE ( 'NONE', *, *, #142242, .T. ) ;
#96773=DIRECTION ( 'NONE',  ( 0.000000000000000000, -0.9908441862701420355, -0.1350103645453197554 ) ) ;
#96777=CARTESIAN_POINT ( 'NONE',  ( -21.53752568622143571, 75.90102553874154978, -143.3099153590729031 ) ) ;
#96786=CARTESIAN_POINT ( 'NONE',  ( 23.14999999999999858, 71.00000000001199396, -115.4283735034374274 ) ) ;
#96798=CARTESIAN_POINT ( 'NONE',  ( -20.07928932188135107, 66.77928932189333011, -115.2731074845243597 ) ) ;
#96854=DIRECTION ( 'NONE',  ( 0.000000000000000000, 1.000000000000000000, 6.938893903907222067E-15 ) ) ;
#96873=CARTESIAN_POINT ( 'NONE',  ( -18.49346865148325492, 85.44307379853697171, -129.3379112292089417 ) ) ;
#96874=CARTESIAN_POINT ( 'NONE',  ( -21.59780538579341069, 69.15290947006889155, -136.6220861541223428 ) ) ;
#96877=CIRCLE ( 'NONE', #205226, 0.1000000000000028644 ) ;
#96905=FACE_OUTER_BOUND ( 'NONE', #38923, .T. ) ;
#96935=CARTESIAN_POINT ( 'NONE',  ( 21.05000000000000071, 65.57661458509917907, -129.0310555606542664 ) ) ;
#96940=ORIENTED_EDGE ( 'NONE', *, *, #125030, .F. ) ;
#96954=ORIENTED_EDGE ( 'NONE', *, *, #58426, .F. ) ;
#96957=AXIS2_PLACEMENT_3D ( 'NONE', #163540, #27915, #1867 ) ;
#97000=CARTESIAN_POINT ( 'NONE',  ( -18.49372193242234275, 85.44248452336996991, -96.25832622448969289 ) ) ;
#97212=VECTOR ( 'NONE', #51008, 1000.000000000000000 ) ;
#97216=EDGE_CURVE ( 'NONE', #138262, #1820, #121699, .T. ) ;
#97240=DIRECTION ( 'NONE',  ( 0.000000000000000000, -6.454785026890489601E-15, 1.000000000000000000 ) ) ;
#97265=ORIENTED_EDGE ( 'NONE', *, *, #77470, .T. ) ;
#97270=CARTESIAN_POINT ( 'NONE',  ( -20.54999999999999716, 74.07476635515219243, -115.7533510176504450 ) ) ;
#97274=AXIS2_PLACEMENT_3D ( 'NONE', #12266, #10964, #150483 ) ;
#97306=CARTESIAN_POINT ( 'NONE',  ( -20.94999999999999929, 65.70729864261004138, -97.56574559737244101 ) ) ;
#97330=EDGE_LOOP ( 'NONE', ( #73258, #39264, #186103, #180573 ) ) ;
#97350=CARTESIAN_POINT ( 'NONE',  ( 19.97071067811864609, 64.27928932189330169, -111.8731074845243825 ) ) ;
#97384=AXIS2_PLACEMENT_3D ( 'NONE', #151158, #129025, #149883 ) ;
#97400=DIRECTION ( 'NONE',  ( 0.000000000000000000, 0.000000000000000000, 1.000000000000000000 ) ) ;
#97451=CIRCLE ( 'NONE', #101731, 12.87499999999999822 ) ;
#97512=DIRECTION ( 'NONE',  ( 0.000000000000000000, 0.000000000000000000, 1.000000000000000000 ) ) ;
#97516=CARTESIAN_POINT ( 'NONE',  ( -18.59999999999999787, 64.25000000001206502, -124.3731074845243825 ) ) ;
#97520=CARTESIAN_POINT ( 'NONE',  ( -23.24999999999999645, 85.60000000001186038, -96.32291809330219223 ) ) ;
#97524=FACE_BOUND ( 'NONE', #190784, .T. ) ;
#97527=CARTESIAN_POINT ( 'NONE',  ( -22.50000000000000000, 75.90000000001222702, -148.1726782920690937 ) ) ;
#97535=CARTESIAN_POINT ( 'NONE',  ( -20.94999999999999929, 77.84915357198788399, -91.41714086472724432 ) ) ;
#97551=DIRECTION ( 'NONE',  ( 0.000000000000000000, 0.1455152366551500653, 0.9893560106964507384 ) ) ;
#97607=DIRECTION ( 'NONE',  ( 0.000000000000000000, -7.116814260417668513E-15, 1.000000000000000000 ) ) ;
#97658=DIRECTION ( 'NONE',  ( 1.000000000000000000, 0.000000000000000000, 0.000000000000000000 ) ) ;
#97668=ORIENTED_EDGE ( 'NONE', *, *, #76235, .T. ) ;
#97702=DIRECTION ( 'NONE',  ( -1.000000000000000000, 0.000000000000000000, 0.000000000000000000 ) ) ;
#97708=ORIENTED_EDGE ( 'NONE', *, *, #17494, .T. ) ;
#97709=EDGE_CURVE ( 'NONE', #49212, #122858, #221788, .T. ) ;
#97723=PLANE ( 'NONE',  #236812 ) ;
#97759=CARTESIAN_POINT ( 'NONE',  ( -21.14999999999999858, 76.10000000001218723, -142.7731074845243029 ) ) ;
#97795=CARTESIAN_POINT ( 'NONE',  ( 22.47071067811865319, 75.90090754530959316, -144.2431822290223522 ) ) ;
#97816=AXIS2_PLACEMENT_3D ( 'NONE', #35303, #57368, #254285 ) ;
#97913=AXIS2_PLACEMENT_3D ( 'NONE', #175178, #58998, #94295 ) ;
#97977=CIRCLE ( 'NONE', #118871, 11.74999999999999645 ) ;
#98030=CYLINDRICAL_SURFACE ( 'NONE', #75909, 0.1000000000000028644 ) ;
#98080=FACE_OUTER_BOUND ( 'NONE', #226691, .T. ) ;
#98083=ORIENTED_EDGE ( 'NONE', *, *, #119574, .F. ) ;
#98095=AXIS2_PLACEMENT_3D ( 'NONE', #83675, #1601, #81132 ) ;
#98105=CARTESIAN_POINT ( 'NONE',  ( 18.49999999999999645, 77.83585931145546510, -91.51866831572576189 ) ) ;
#98108=CARTESIAN_POINT ( 'NONE',  ( 21.05000000000000071, 84.73084112150729652, -112.6211822035085675 ) ) ;
#98120=AXIS2_PLACEMENT_3D ( 'NONE', #35310, #194372, #76951 ) ;
#98123=AXIS2_PLACEMENT_3D ( 'NONE', #240167, #44535, #82332 ) ;
#98139=AXIS2_PLACEMENT_3D ( 'NONE', #128386, #171402, #33174 ) ;
#98149=CARTESIAN_POINT ( 'NONE',  ( -20.94999999999999929, 74.16465844978765176, -124.9679561919613207 ) ) ;
#98155=DIRECTION ( 'NONE',  ( 0.000000000000000000, -1.000000000000000000, 0.000000000000000000 ) ) ;
#98164=AXIS2_PLACEMENT_3D ( 'NONE', #255167, #76585, #178289 ) ;
#98195=CARTESIAN_POINT ( 'NONE',  ( -23.15000000000000213, 71.65000000001199965, -115.1731074845243370 ) ) ;
#98218=CARTESIAN_POINT ( 'NONE',  ( -23.15000000000000213, 76.00000000001213607, -136.5231074845242745 ) ) ;
#98250=DIRECTION ( 'NONE',  ( -1.000000000000000000, -0.000000000000000000, -0.000000000000000000 ) ) ;
#98259=ORIENTED_EDGE ( 'NONE', *, *, #50790, .T. ) ;
#98273=CARTESIAN_POINT ( 'NONE',  ( -21.05000000000000071, 74.83729825007408465, -128.4231074845243086 ) ) ;
#98274=ORIENTED_EDGE ( 'NONE', *, *, #154702, .T. ) ;
#98286=CARTESIAN_POINT ( 'NONE',  ( -18.58744394320951798, 85.56638515456029381, -96.20025943064806029 ) ) ;
#98290=LINE ( 'NONE', #78750, #231779 ) ;
#98301=ORIENTED_EDGE ( 'NONE', *, *, #184371, .T. ) ;
#98304=ORIENTED_EDGE ( 'NONE', *, *, #236265, .F. ) ;
#98318=DIRECTION ( 'NONE',  ( 1.000000000000000000, 0.000000000000000000, 0.000000000000000000 ) ) ;
#98323=CARTESIAN_POINT ( 'NONE',  ( 21.13435531349785634, 76.00000000001217870, -143.0168285481170471 ) ) ;
#98349=CIRCLE ( 'NONE', #106769, 7.800000000000001599 ) ;
#98392=DIRECTION ( 'NONE',  ( 1.040834085586054469E-13, -1.000000000000000000, 0.000000000000000000 ) ) ;
#98411=CARTESIAN_POINT ( 'NONE',  ( 21.14999999999999858, 69.45934304831089889, -136.5231074845243313 ) ) ;
#98441=DIRECTION ( 'NONE',  ( -0.000000000000000000, 1.000000000000000000, 6.352154140967427193E-15 ) ) ;
#98442=AXIS2_PLACEMENT_3D ( 'NONE', #124504, #89211, #44964 ) ;
#98478=ADVANCED_FACE ( 'NONE', ( #122044 ), #3352, .T. ) ;
#98481=CARTESIAN_POINT ( 'NONE',  ( 20.85000000000000142, 77.16412189325305349, -95.10825939895268277 ) ) ;
#98482=EDGE_LOOP ( 'NONE', ( #155420, #217639, #8586, #167993 ) ) ;
#98501=CIRCLE ( 'NONE', #40342, 0.09999999999998898659 ) ;
#98511=EDGE_LOOP ( 'NONE', ( #40646, #74226, #227013 ) ) ;
#98545=EDGE_LOOP ( 'NONE', ( #86780, #179330, #172460, #96613 ) ) ;
#98561=AXIS2_PLACEMENT_3D ( 'NONE', #208510, #126381, #109368 ) ;
#98585=DIRECTION ( 'NONE',  ( -0.000000000000000000, 6.982962677686266711E-15, -1.000000000000000000 ) ) ;
#98595=CIRCLE ( 'NONE', #86148, 0.1000000000000072220 ) ;
#98643=VERTEX_POINT ( 'NONE', #165016 ) ;
#98677=DIRECTION ( 'NONE',  ( -1.000000000000000000, -0.000000000000000000, -0.000000000000000000 ) ) ;
#98693=CARTESIAN_POINT ( 'NONE',  ( 22.39999999999999503, 64.25000000001213607, -136.4231074845243938 ) ) ;
#98695=EDGE_CURVE ( 'NONE', #230368, #78926, #87877, .T. ) ;
#98714=DIRECTION ( 'NONE',  ( 0.000000000000000000, 0.1568667991644355497, 0.9876197685951332295 ) ) ;
#98755=CARTESIAN_POINT ( 'NONE',  ( -23.25000000000000000, 76.00000000001190870, -103.0231074845243029 ) ) ;
#98794=PRODUCT_DEFINITION_FORMATION_WITH_SPECIFIED_SOURCE ( 'ANY', '', #32833, .NOT_KNOWN. ) ;
#98816=DIRECTION ( 'NONE',  ( 0.000000000000000000, 0.000000000000000000, 1.000000000000000000 ) ) ;
#98847=DIRECTION ( 'NONE',  ( 0.000000000000000000, 1.000000000000000000, 6.982962677686266711E-15 ) ) ;
#98851=PLANE ( 'NONE',  #223254 ) ;
#98868=AXIS2_PLACEMENT_3D ( 'NONE', #201967, #25902, #203240 ) ;
#98927=ORIENTED_EDGE ( 'NONE', *, *, #188970, .T. ) ;
#98932=EDGE_LOOP ( 'NONE', ( #159065, #164772, #255706, #49927 ) ) ;
#98944=CIRCLE ( 'NONE', #132285, 0.09999999999998708533 ) ;
#98962=CARTESIAN_POINT ( 'NONE',  ( -23.15000000000000213, 74.07476635515223506, -123.7928639513981892 ) ) ;
#98966=AXIS2_PLACEMENT_3D ( 'NONE', #131699, #228245, #52144 ) ;
#98999=DIRECTION ( 'NONE',  ( 0.000000000000000000, 0.000000000000000000, 1.000000000000000000 ) ) ;
#99010=CYLINDRICAL_SURFACE ( 'NONE', #223829, 0.09999999999999939493 ) ;
#99046=FACE_OUTER_BOUND ( 'NONE', #149719, .T. ) ;
#99071=DIRECTION ( 'NONE',  ( -3.440080580676165868E-14, 0.1298341882520054891, 0.9915357197604850459 ) ) ;
#99082=CARTESIAN_POINT ( 'NONE',  ( -21.05000000000000071, 87.39257802171759693, -106.0970570643561501 ) ) ;
#99084=CIRCLE ( 'NONE', #28418, 0.5000000000000004441 ) ;
#99101=DIRECTION ( 'NONE',  ( 1.000000000000000000, -0.000000000000000000, 0.000000000000000000 ) ) ;
#99104=CARTESIAN_POINT ( 'NONE',  ( 23.14999999999999858, 76.00000000001190870, -103.0231074845243029 ) ) ;
#99116=CIRCLE ( 'NONE', #99674, 0.9750000000000036415 ) ;
#99129=EDGE_CURVE ( 'NONE', #33201, #17884, #220972, .T. ) ;
#99134=CARTESIAN_POINT ( 'NONE',  ( -21.55000000000000071, 68.65000000001205649, -124.2731074845243455 ) ) ;
#99140=DIRECTION ( 'NONE',  ( 0.000000000000000000, -0.4999999999999088507, 0.8660254037844913322 ) ) ;
#99152=CARTESIAN_POINT ( 'NONE',  ( 21.14999999999999503, 76.10000000001222986, -148.1726782920690937 ) ) ;
#99162=LINE ( 'NONE', #241286, #56220 ) ;
#99191=AXIS2_PLACEMENT_3D ( 'NONE', #6063, #85568, #129569 ) ;
#99199=AXIS2_PLACEMENT_3D ( 'NONE', #64009, #219218, #22340 ) ;
#99212=VERTEX_POINT ( 'NONE', #4989 ) ;
#99240=AXIS2_PLACEMENT_3D ( 'NONE', #242738, #107084, #182803 ) ;
#99262=ADVANCED_FACE ( 'NONE', ( #7585 ), #89669, .T. ) ;
#99263=CIRCLE ( 'NONE', #224170, 0.09999999999999939493 ) ;
#99284=DIRECTION ( 'NONE',  ( 0.000000000000000000, -1.000000000000000000, -7.105427357601001859E-15 ) ) ;
#99295=SPHERICAL_SURFACE ( 'NONE', #195080, 0.1000000000000000056 ) ;
#99304=AXIS2_PLACEMENT_3D ( 'NONE', #13693, #114070, #208070 ) ;
#99324=DIRECTION ( 'NONE',  ( 1.000000000000000000, 0.000000000000000000, 0.000000000000000000 ) ) ;
#99345=ORIENTED_EDGE ( 'NONE', *, *, #166847, .F. ) ;
#99346=ADVANCED_FACE ( 'NONE', ( #246199 ), #151499, .T. ) ;
#99368=DIRECTION ( 'NONE',  ( 1.000000000000000000, -3.265361837132813093E-16, -2.280189983783949500E-30 ) ) ;
#99377=DIRECTION ( 'NONE',  ( 1.000000000000000000, 0.000000000000000000, 0.000000000000000000 ) ) ;
#99392=LINE ( 'NONE', #237648, #226627 ) ;
#99420=DIRECTION ( 'NONE',  ( -3.265361837132813093E-16, -1.000000000000000000, 7.445645354460596589E-46 ) ) ;
#99480=ORIENTED_EDGE ( 'NONE', *, *, #67315, .T. ) ;
#99499=VERTEX_POINT ( 'NONE', #97350 ) ;
#99549=ADVANCED_FACE ( 'NONE', ( #153565 ), #93532, .F. ) ;
#99577=ORIENTED_EDGE ( 'NONE', *, *, #112491, .F. ) ;
#99609=EDGE_CURVE ( 'NONE', #231430, #62705, #200326, .T. ) ;
#99613=FACE_OUTER_BOUND ( 'NONE', #54784, .T. ) ;
#99627=( BOUNDED_CURVE ( )  B_SPLINE_CURVE ( 3, ( #93660, #94930, #214887, #50659 ),
 .UNSPECIFIED., .F., .F. ) 
 B_SPLINE_CURVE_WITH_KNOTS ( ( 4, 4 ),
 ( 3.141592653589778461, 4.712388980384686121 ),
 .UNSPECIFIED. ) 
 CURVE ( )  GEOMETRIC_REPRESENTATION_ITEM ( )  RATIONAL_B_SPLINE_CURVE ( ( 1.000000000000000000, 0.8047378541243622729, 0.8047378541243622729, 1.000000000000000000 ) ) 
 REPRESENTATION_ITEM ( '' )  );
#99640=EDGE_CURVE ( 'NONE', #163587, #207643, #20439, .T. ) ;
#99641=CARTESIAN_POINT ( 'NONE',  ( -21.52071067811865746, 68.22071067813065781, -115.2731074845243455 ) ) ;
#99661=EDGE_CURVE ( 'NONE', #224224, #60977, #208726, .T. ) ;
#99674=AXIS2_PLACEMENT_3D ( 'NONE', #253800, #15223, #137698 ) ;
#99731=AXIS2_PLACEMENT_3D ( 'NONE', #15663, #195572, #134273 ) ;
#99732=CIRCLE ( 'NONE', #191379, 0.5000000000000004441 ) ;
#99775=EDGE_LOOP ( 'NONE', ( #248514, #30908, #93942, #200953 ) ) ;
#99802=DIRECTION ( 'NONE',  ( 1.000000000000000000, 0.000000000000000000, 0.000000000000000000 ) ) ;
#99827=VECTOR ( 'NONE', #65748, 1000.000000000000000 ) ;
#99837=CIRCLE ( 'NONE', #220689, 0.1000000000000028644 ) ;
#99961=LINE ( 'NONE', #80389, #96023 ) ;
#99985=ORIENTED_EDGE ( 'NONE', *, *, #237813, .T. ) ;
#99997=CIRCLE ( 'NONE', #220825, 0.1000000000000043771 ) ;
#100005=CARTESIAN_POINT ( 'NONE',  ( 21.14999999999999858, 87.75000000001205080, -124.2731074845242176 ) ) ;
#100026=ADVANCED_FACE ( 'NONE', ( #99613 ), #159626, .F. ) ;
#100029=LINE ( 'NONE', #161336, #181350 ) ;
#100044=DIRECTION ( 'NONE',  ( 0.000000000000000000, -7.056502275159890832E-15, 1.000000000000000000 ) ) ;
#100053=DIRECTION ( 'NONE',  ( 0.000000000000000000, 0.9908441862701420355, 0.1350103645453197554 ) ) ;
#100066=CIRCLE ( 'NONE', #245836, 0.5000000000000004441 ) ;
#100087=TOROIDAL_SURFACE ( 'NONE', #183510, 11.70000000000000639, 0.1000000000000000056 ) ;
#100089=LINE ( 'NONE', #86623, #76504 ) ;
#100094=AXIS2_PLACEMENT_3D ( 'NONE', #9545, #167374, #49956 ) ;
#100122=AXIS2_PLACEMENT_3D ( 'NONE', #180386, #28736, #105622 ) ;
#100129=ORIENTED_EDGE ( 'NONE', *, *, #144291, .T. ) ;
#100138=DIRECTION ( 'NONE',  ( 0.000000000000000000, 0.000000000000000000, 1.000000000000000000 ) ) ;
#100168=ADVANCED_FACE ( 'NONE', ( #106038 ), #29851, .T. ) ;
#100215=ADVANCED_FACE ( 'NONE', ( #184308 ), #166074, .T. ) ;
#100237=CARTESIAN_POINT ( 'NONE',  ( -20.54999999999999716, 85.00000000001207923, -126.6291383618717816 ) ) ;
#100239=AXIS2_PLACEMENT_3D ( 'NONE', #128568, #110272, #11188 ) ;
#100247=EDGE_LOOP ( 'NONE', ( #239371, #15829, #48785, #114721 ) ) ;
#100270=CARTESIAN_POINT ( 'NONE',  ( 23.24999999999999289, 80.15000000001214175, -136.5231074845242460 ) ) ;
#100289=CARTESIAN_POINT ( 'NONE',  ( 18.47654891039378455, 85.46527494839439498, -129.3971315793295958 ) ) ;
#100303=AXIS2_PLACEMENT_3D ( 'NONE', #29789, #43718, #125812 ) ;
#100306=DIRECTION ( 'NONE',  ( -0.000000000000000000, 1.000000000000000000, 7.525063763929033127E-15 ) ) ;
#100342=ADVANCED_FACE ( 'NONE', ( #11850 ), #84101, .F. ) ;
#100372=CARTESIAN_POINT ( 'NONE',  ( 20.59588692710267921, 65.63127657884298571, -128.8840263900139576 ) ) ;
#100385=DIRECTION ( 'NONE',  ( 2.940209281316621016E-16, 1.000000000000000000, 7.056502275159890832E-15 ) ) ;
#100420=DIRECTION ( 'NONE',  ( 1.000000000000000000, 0.000000000000000000, 0.000000000000000000 ) ) ;
#100444=DIRECTION ( 'NONE',  ( 0.000000000000000000, -1.000000000000000000, 0.000000000000000000 ) ) ;
#100452=ORIENTED_EDGE ( 'NONE', *, *, #130525, .T. ) ;
#100454=VECTOR ( 'NONE', #170304, 1000.000000000000000 ) ;
#100461=ORIENTED_EDGE ( 'NONE', *, *, #40915, .T. ) ;
#100495=ORIENTED_EDGE ( 'NONE', *, *, #150660, .T. ) ;
#100518=ORIENTED_EDGE ( 'NONE', *, *, #210232, .F. ) ;
#100528=CARTESIAN_POINT ( 'NONE',  ( 21.05000000000000071, 75.96513199699909080, -142.7931933482134070 ) ) ;
#100537=EDGE_CURVE ( 'NONE', #162828, #114115, #146498, .T. ) ;
#100561=DIRECTION ( 'NONE',  ( 0.000000000000000000, -7.272083257015735086E-15, 1.000000000000000000 ) ) ;
#100568=DIRECTION ( 'NONE',  ( 0.000000000000000000, -6.467318590049456648E-15, 1.000000000000000000 ) ) ;
#100578=VERTEX_POINT ( 'NONE', #258083 ) ;
#100583=EDGE_CURVE ( 'NONE', #18233, #51864, #242410, .T. ) ;
#100596=CARTESIAN_POINT ( 'NONE',  ( -23.15000000000000213, 85.60000000001198828, -112.9170766071766820 ) ) ;
#100615=ORIENTED_EDGE ( 'NONE', *, *, #146188, .F. ) ;
#100619=CIRCLE ( 'NONE', #121540, 11.80000000000000426 ) ;
#100643=EDGE_LOOP ( 'NONE', ( #255345, #157295, #148913, #240694, #92130, #177795, #51644 ) ) ;
#100679=EDGE_LOOP ( 'NONE', ( #65555, #241916, #144150, #209105, #247902 ) ) ;
#100686=DIRECTION ( 'NONE',  ( 0.000000000000000000, 6.982962677686266711E-15, -1.000000000000000000 ) ) ;
#100688=EDGE_CURVE ( 'NONE', #85966, #37312, #34310, .T. ) ;
#100758=EDGE_LOOP ( 'NONE', ( #60112, #173988, #235925, #77896 ) ) ;
#100776=DIRECTION ( 'NONE',  ( 0.000000000000000000, 0.000000000000000000, 1.000000000000000000 ) ) ;
#100792=EDGE_LOOP ( 'NONE', ( #87240, #32861, #213424, #29098 ) ) ;
#100816=CARTESIAN_POINT ( 'NONE',  ( 23.14999999999999858, 64.35000000001195986, -110.0379132551783243 ) ) ;
#100830=EDGE_CURVE ( 'NONE', #207360, #89242, #200867, .T. ) ;
#100864=AXIS2_PLACEMENT_3D ( 'NONE', #20188, #176698, #77550 ) ;
#100893=ADVANCED_FACE ( 'NONE', ( #126981 ), #101035, .F. ) ;
#100917=CARTESIAN_POINT ( 'NONE',  ( 18.60000000000000142, 85.32100840337338354, -129.2871692354463278 ) ) ;
#100922=DIRECTION ( 'NONE',  ( 1.000000000000000000, -0.000000000000000000, 0.000000000000000000 ) ) ;
#100953=AXIS2_PLACEMENT_3D ( 'NONE', #192890, #53371, #174657 ) ;
#100956=CYLINDRICAL_SURFACE ( 'NONE', #223703, 0.09999999999999939493 ) ;
#100983=CARTESIAN_POINT ( 'NONE',  ( 23.14999999999998437, 87.75000000001213607, -136.5231074845242176 ) ) ;
#100995=EDGE_CURVE ( 'NONE', #140961, #118915, #76141, .T. ) ;
#101035=TOROIDAL_SURFACE ( 'NONE', #96957, 0.2000000000000000111, 0.1000000000000000056 ) ;
#101089=AXIS2_PLACEMENT_3D ( 'NONE', #197685, #19059, #257609 ) ;
#101095=EDGE_LOOP ( 'NONE', ( #233493, #190979, #177966 ) ) ;
#101103=CARTESIAN_POINT ( 'NONE',  ( -23.25000000000000000, 64.25000000001222134, -148.2731074845243882 ) ) ;
#101105=CARTESIAN_POINT ( 'NONE',  ( 18.49999999999999645, 76.00000000001190870, -103.0231074845243029 ) ) ;
#101125=CIRCLE ( 'NONE', #246926, 0.09999999999998900047 ) ;
#101161=CARTESIAN_POINT ( 'NONE',  ( 21.07928932188134397, 76.00000000001213607, -136.5231074845242745 ) ) ;
#101171=CYLINDRICAL_SURFACE ( 'NONE', #13844, 0.5000000000000004441 ) ;
#101191=DIRECTION ( 'NONE',  ( -1.000000000000000000, 0.000000000000000000, -0.000000000000000000 ) ) ;
#101211=DIRECTION ( 'NONE',  ( 1.000000000000000000, 0.000000000000000000, 0.000000000000000000 ) ) ;
#101224=DIRECTION ( 'NONE',  ( 0.000000000000000000, -6.467318590049456648E-15, 1.000000000000000000 ) ) ;
#101245=CIRCLE ( 'NONE', #147071, 0.2000000000000057288 ) ;
#101264=EDGE_LOOP ( 'NONE', ( #114531, #212326, #212200, #223372 ) ) ;
#101408=CIRCLE ( 'NONE', #168155, 1.899999999999999023 ) ;
#101432=AXIS2_PLACEMENT_3D ( 'NONE', #130301, #248997, #70375 ) ;
#101442=AXIS2_PLACEMENT_3D ( 'NONE', #196283, #257483, #61918 ) ;
#101475=EDGE_CURVE ( 'NONE', #82597, #164288, #242919, .T. ) ;
#101477=CARTESIAN_POINT ( 'NONE',  ( -20.54999999999999716, 84.66355140188123585, -126.9990063664569391 ) ) ;
#101492=CARTESIAN_POINT ( 'NONE',  ( 20.94999999999999929, 76.00000000001192291, -104.9231074845242944 ) ) ;
#101499=EDGE_CURVE ( 'NONE', #125207, #24834, #197134, .T. ) ;
#101547=DIRECTION ( 'NONE',  ( 1.000000000000000000, -3.265361837132813093E-16, -2.280189983783949500E-30 ) ) ;
#101582=VERTEX_POINT ( 'NONE', #135644 ) ;
#101583=CARTESIAN_POINT ( 'NONE',  ( -22.47120815636973745, 75.97109617810833981, -148.1730394732777825 ) ) ;
#101593=CARTESIAN_POINT ( 'NONE',  ( -22.39999999999999858, 64.35000000001214460, -136.4231074845243938 ) ) ;
#101595=CARTESIAN_POINT ( 'NONE',  ( 20.85000000000000142, 87.75000000001190870, -106.0231074845242176 ) ) ;
#101629=TOROIDAL_SURFACE ( 'NONE', #189160, 0.2000000000000000111, 0.1000000000000000056 ) ;
#101683=ORIENTED_EDGE ( 'NONE', *, *, #180761, .T. ) ;
#101701=FACE_OUTER_BOUND ( 'NONE', #189113, .T. ) ;
#101725=EDGE_CURVE ( 'NONE', #208687, #68456, #18264, .T. ) ;
#101731=AXIS2_PLACEMENT_3D ( 'NONE', #119466, #193863, #256321 ) ;
#101744=ADVANCED_FACE ( 'NONE', ( #239907 ), #118215, .T. ) ;
#101755=CARTESIAN_POINT ( 'NONE',  ( 20.94999999999999929, 85.00000000001197975, -112.9170766071766820 ) ) ;
#101800=EDGE_LOOP ( 'NONE', ( #169132, #55340, #151400, #151645 ) ) ;
#101829=CARTESIAN_POINT ( 'NONE',  ( -20.54999999999999716, 71.65000000001199965, -115.3731074845243256 ) ) ;
#101833=CARTESIAN_POINT ( 'NONE',  ( -21.10320863425827298, 75.97497774878509347, -142.9233848709835115 ) ) ;
#101847=DIRECTION ( 'NONE',  ( 0.000000000000000000, 0.000000000000000000, -1.000000000000000000 ) ) ;
#101861=CARTESIAN_POINT ( 'NONE',  ( -23.25000000000000000, 77.83585931145546510, -91.51866831572576189 ) ) ;
#101862=DIRECTION ( 'NONE',  ( -0.7071067811865475727, 0.7071067811865475727, 4.937700262164531476E-15 ) ) ;
#101863=DIRECTION ( 'NONE',  ( 0.000000000000000000, -1.000000000000000000, -6.982962677686265922E-15 ) ) ;
#101878=AXIS2_PLACEMENT_3D ( 'NONE', #199885, #40823, #22532 ) ;
#101887=DIRECTION ( 'NONE',  ( 0.000000000000000000, -0.5000000000000016653, 0.8660254037844377084 ) ) ;
#101900=FACE_OUTER_BOUND ( 'NONE', #160185, .T. ) ;
#101920=CARTESIAN_POINT ( 'NONE',  ( 22.45463910399149299, 76.00000000001311662, -148.1726782947081631 ) ) ;
#101922=ORIENTED_EDGE ( 'NONE', *, *, #58949, .T. ) ;
#101988=ORIENTED_EDGE ( 'NONE', *, *, #19494, .F. ) ;
#102016=VECTOR ( 'NONE', #139839, 1000.000000000000000 ) ;
#102042=EDGE_CURVE ( 'NONE', #6106, #157579, #85039, .T. ) ;
#102053=ORIENTED_EDGE ( 'NONE', *, *, #7181, .T. ) ;
#102058=VECTOR ( 'NONE', #140487, 999.9999999999998863 ) ;
#102063=ORIENTED_EDGE ( 'NONE', *, *, #217061, .T. ) ;
#102067=VERTEX_POINT ( 'NONE', #180899 ) ;
#102082=CARTESIAN_POINT ( 'NONE',  ( -23.25000000000000000, 85.68240343348826116, -96.36626410711143365 ) ) ;
#102107=CARTESIAN_POINT ( 'NONE',  ( 22.39999999999999503, 76.00000000001219291, -144.3138870828976792 ) ) ;
#102122=AXIS2_PLACEMENT_3D ( 'NONE', #258101, #119960, #42963 ) ;
#102137=AXIS2_PLACEMENT_3D ( 'NONE', #58606, #199447, #61194 ) ;
#102155=AXIS2_PLACEMENT_3D ( 'NONE', #245789, #167560, #87964 ) ;
#102189=EDGE_LOOP ( 'NONE', ( #193885, #196551, #158489, #83318 ) ) ;
#102194=AXIS2_PLACEMENT_3D ( 'NONE', #215340, #198348, #36748 ) ;
#102199=ORIENTED_EDGE ( 'NONE', *, *, #37160, .F. ) ;
#102218=CARTESIAN_POINT ( 'NONE',  ( 18.59999999999999432, 74.73821383144705521, -128.4366085209788366 ) ) ;
#102263=CARTESIAN_POINT ( 'NONE',  ( -18.59999999999999787, 74.14897176987119565, -124.8691942151018139 ) ) ;
#102272=DIRECTION ( 'NONE',  ( 1.000000000000000000, 0.000000000000000000, 0.000000000000000000 ) ) ;
#102273=DIRECTION ( 'NONE',  ( -1.000000000000000000, 0.000000000000000000, 0.000000000000000000 ) ) ;
#102279=VECTOR ( 'NONE', #168285, 999.9999999999998863 ) ;
#102291=VERTEX_POINT ( 'NONE', #66072 ) ;
#102313=ORIENTED_EDGE ( 'NONE', *, *, #37160, .T. ) ;
#102322=CARTESIAN_POINT ( 'NONE',  ( 20.94999999999999929, 71.00000000001199396, -115.4283735034374274 ) ) ;
#102346=ORIENTED_EDGE ( 'NONE', *, *, #188029, .T. ) ;
#102414=CARTESIAN_POINT ( 'NONE',  ( -21.13422380239120457, 76.00000000001219291, -143.0164339993295073 ) ) ;
#102468=FACE_OUTER_BOUND ( 'NONE', #173126, .T. ) ;
#102478=TOROIDAL_SURFACE ( 'NONE', #90034, 0.2000000000000000111, 0.1000000000000000056 ) ;
#102483=EDGE_LOOP ( 'NONE', ( #195245, #14409, #3566, #12886, #185896, #100495, #193536, #115053, #61589, #128679, #169935, #119775, #164586, #56239, #140633, #218924 ) ) ;
#102499=CARTESIAN_POINT ( 'NONE',  ( -20.94999999999999929, 76.00000000001213607, -136.5231074845242745 ) ) ;
#102511=VERTEX_POINT ( 'NONE', #225789 ) ;
#102517=DIRECTION ( 'NONE',  ( -1.000000000000000000, 0.000000000000000000, -0.000000000000000000 ) ) ;
#102529=DIRECTION ( 'NONE',  ( 0.000000000000000000, -0.5000000000000209832, -0.8660254037844264952 ) ) ;
#102541=CARTESIAN_POINT ( 'NONE',  ( -18.50000000000000000, 68.87972903831429505, -99.36354444268502561 ) ) ;
#102548=DIRECTION ( 'NONE',  ( 1.000000000000000000, -2.952720810173289112E-16, -2.061873921506763405E-30 ) ) ;
#102575=CIRCLE ( 'NONE', #202563, 7.900000000000003908 ) ;
#102586=EDGE_CURVE ( 'NONE', #3185, #230388, #32790, .T. ) ;
#102590=DIRECTION ( 'NONE',  ( 3.469446951953514477E-14, 0.9999176327611370985, 0.01283462868040226822 ) ) ;
#102591=DIRECTION ( 'NONE',  ( -1.000000000000000000, 0.000000000000000000, 0.000000000000000000 ) ) ;
#102597=ADVANCED_FACE ( 'NONE', ( #112301 ), #111005, .T. ) ;
#102608=ADVANCED_FACE ( 'NONE', ( #208824 ), #152732, .T. ) ;
#102637=CIRCLE ( 'NONE', #69373, 0.09999999999998986089 ) ;
#102644=CARTESIAN_POINT ( 'NONE',  ( -20.00857864376270001, 66.85000000001205933, -124.1731074845243512 ) ) ;
#102650=DIRECTION ( 'NONE',  ( -0.7071067811865475727, 0.7071067811865475727, 4.937700262164531476E-15 ) ) ;
#102655=ADVANCED_FACE ( 'NONE', ( #48456 ), #246650, .F. ) ;
#102756=VERTEX_POINT ( 'NONE', #216518 ) ;
#102768=DIRECTION ( 'NONE',  ( 7.304098846218134667E-16, 1.000000000000000000, 6.982962677686266711E-15 ) ) ;
#102809=DIRECTION ( 'NONE',  ( 0.000000000000000000, -7.124650136758292359E-15, 1.000000000000000000 ) ) ;
#102813=DIRECTION ( 'NONE',  ( -1.000000000000000000, 0.000000000000000000, -0.000000000000000000 ) ) ;
#102838=DIRECTION ( 'NONE',  ( 0.000000000000000000, 0.000000000000000000, 1.000000000000000000 ) ) ;
#102871=CARTESIAN_POINT ( 'NONE',  ( 21.93642651522410603, 68.67283376068634482, -136.5231074845243313 ) ) ;
#102885=CIRCLE ( 'NONE', #23833, 0.3999999999999975797 ) ;
#102888=ORIENTED_EDGE ( 'NONE', *, *, #181332, .T. ) ;
#102909=CARTESIAN_POINT ( 'NONE',  ( -23.15000000000000213, 71.75000000001205080, -124.2731074845243313 ) ) ;
#102921=VERTEX_POINT ( 'NONE', #140840 ) ;
#102924=EDGE_CURVE ( 'NONE', #135040, #60684, #147812, .T. ) ;
#102933=ORIENTED_EDGE ( 'NONE', *, *, #27489, .F. ) ;
#102967=EDGE_LOOP ( 'NONE', ( #217859, #157437, #78965 ) ) ;
#103015=AXIS2_PLACEMENT_3D ( 'NONE', #252370, #153337, #33383 ) ;
#103022=CARTESIAN_POINT ( 'NONE',  ( 20.94999999999999574, 74.16465844978765176, -124.9679561919613207 ) ) ;
#103037=CARTESIAN_POINT ( 'NONE',  ( -20.94999999999999929, 87.75000000001192291, -106.1231074845242262 ) ) ;
#103092=DIRECTION ( 'NONE',  ( 1.000000000000000000, 0.000000000000000000, 0.000000000000000000 ) ) ;
#103111=DIRECTION ( 'NONE',  ( 0.000000000000000000, 0.000000000000000000, -1.000000000000000000 ) ) ;
#103117=EDGE_CURVE ( 'NONE', #14587, #22794, #10443, .T. ) ;
#103130=CARTESIAN_POINT ( 'NONE',  ( -21.08198257630413508, 75.92735667622760332, -142.8597042185393491 ) ) ;
#103139=CIRCLE ( 'NONE', #90672, 0.2000000000000057288 ) ;
#103144=DIRECTION ( 'NONE',  ( 0.000000000000000000, -6.938893903907222067E-15, 1.000000000000000000 ) ) ;
#103145=CARTESIAN_POINT ( 'NONE',  ( 21.05000000000000071, 77.36087058720413268, -128.4501095574333362 ) ) ;
#103162=DIRECTION ( 'NONE',  ( 0.7071067811865475727, -0.7071067811865475727, -4.937700262164531476E-15 ) ) ;
#103213=CARTESIAN_POINT ( 'NONE',  ( 22.50046968638157807, 75.95483015287236128, -148.2731526389930252 ) ) ;
#103230=DIRECTION ( 'NONE',  ( 0.000000000000000000, 0.000000000000000000, 1.000000000000000000 ) ) ;
#103251=ORIENTED_EDGE ( 'NONE', *, *, #105227, .F. ) ;
#103265=EDGE_CURVE ( 'NONE', #76926, #111084, #15462, .T. ) ;
#103270=ORIENTED_EDGE ( 'NONE', *, *, #205510, .F. ) ;
#103284=EDGE_CURVE ( 'NONE', #82597, #8870, #93992, .T. ) ;
#103319=AXIS2_PLACEMENT_3D ( 'NONE', #106614, #47936, #187481 ) ;
#103332=EDGE_CURVE ( 'NONE', #192766, #188576, #152298, .T. ) ;
#103354=CARTESIAN_POINT ( 'NONE',  ( 20.94999999999999574, 74.26374286841466699, -124.9544551555068068 ) ) ;
#103367=DIRECTION ( 'NONE',  ( 1.000000000000000000, 0.000000000000000000, 0.000000000000000000 ) ) ;
#103410=DIRECTION ( 'NONE',  ( 1.000000000000000000, 0.000000000000000000, 0.000000000000000000 ) ) ;
#103417=ORIENTED_EDGE ( 'NONE', *, *, #243551, .F. ) ;
#103457=CIRCLE ( 'NONE', #203444, 2.000000000000001776 ) ;
#103471=ORIENTED_EDGE ( 'NONE', *, *, #241188, .F. ) ;
#103492=DIRECTION ( 'NONE',  ( 0.000000000000000000, 0.8700118002898393765, -0.4930308989875104575 ) ) ;
#103499=DIRECTION ( 'NONE',  ( 0.000000000000000000, -7.086529944415894657E-15, 1.000000000000000000 ) ) ;
#103502=CIRCLE ( 'NONE', #211865, 0.1000000000000016431 ) ;
#103503=EDGE_LOOP ( 'NONE', ( #94483, #246340, #33167, #252397 ) ) ;
#103514=DIRECTION ( 'NONE',  ( 1.000000000000000000, 0.000000000000000000, 0.000000000000000000 ) ) ;
#103524=DIRECTION ( 'NONE',  ( 0.000000000000000000, -6.454785026890489601E-15, 1.000000000000000000 ) ) ;
#103529=EDGE_LOOP ( 'NONE', ( #181671, #2738, #148528, #201377 ) ) ;
#103556=DIRECTION ( 'NONE',  ( 0.000000000000000000, -0.9915357197604982575, 0.1298341882519033486 ) ) ;
#103559=EDGE_LOOP ( 'NONE', ( #127662, #190698, #90922, #29845 ) ) ;
#103563=CARTESIAN_POINT ( 'NONE',  ( 21.05000000000000071, 65.27628289530454708, -124.3619171903969374 ) ) ;
#103564=CYLINDRICAL_SURFACE ( 'NONE', #133376, 12.87499999999999822 ) ;
#103580=LINE ( 'NONE', #65764, #141989 ) ;
#103603=DIRECTION ( 'NONE',  ( -6.938893903907222067E-15, -1.000000000000000000, -7.272083257015735086E-15 ) ) ;
#103604=DIRECTION ( 'NONE',  ( -1.836970198721029934E-16, -1.000000000000000000, -6.982962677686266711E-15 ) ) ;
#103618=DIRECTION ( 'NONE',  ( 1.000000000000000000, 0.000000000000000000, 0.000000000000000000 ) ) ;
#103668=ORIENTED_EDGE ( 'NONE', *, *, #143330, .T. ) ;
#103697=VERTEX_POINT ( 'NONE', #119377 ) ;
#103699=DIRECTION ( 'NONE',  ( 0.000000000000000000, -6.982962677686266711E-15, 1.000000000000000000 ) ) ;
#103760=CARTESIAN_POINT ( 'NONE',  ( -23.15000000000000213, 71.75000000001199396, -115.3731074845243256 ) ) ;
#103765=AXIS2_PLACEMENT_3D ( 'NONE', #87661, #69417, #246737 ) ;
#103776=DIRECTION ( 'NONE',  ( -1.000000000000000000, 0.000000000000000000, 0.000000000000000000 ) ) ;
#103809=CIRCLE ( 'NONE', #153778, 0.09999999999999939493 ) ;
#103821=ADVANCED_FACE ( 'NONE', ( #206605 ), #228754, .T. ) ;
#103884=DIRECTION ( 'NONE',  ( 0.000000000000000000, -7.116814260417668513E-15, 1.000000000000000000 ) ) ;
#103894=DIRECTION ( 'NONE',  ( 0.000000000000000000, 0.9915357197604804940, -0.1298341882520397950 ) ) ;
#103943=EDGE_CURVE ( 'NONE', #55329, #14291, #81134, .T. ) ;
#103966=ORIENTED_EDGE ( 'NONE', *, *, #38552, .T. ) ;
#104037=ORIENTED_EDGE ( 'NONE', *, *, #69279, .F. ) ;
#104064=DIRECTION ( 'NONE',  ( 0.000000000000000000, 0.000000000000000000, -1.000000000000000000 ) ) ;
#104129=CARTESIAN_POINT ( 'NONE',  ( 18.49999999999999645, 76.00000000001213607, -136.5231074845242745 ) ) ;
#104131=DIRECTION ( 'NONE',  ( -0.000000000000000000, 0.8660254037844377084, 0.5000000000000016653 ) ) ;
#104170=CARTESIAN_POINT ( 'NONE',  ( -18.59999999999999787, 77.63717271298244782, -124.9409541190522788 ) ) ;
#104197=VERTEX_POINT ( 'NONE', #195140 ) ;
#104224=DIRECTION ( 'NONE',  ( 0.000000000000000000, -0.9876197685951265681, -0.1568667991644790149 ) ) ;
#104249=EDGE_CURVE ( 'NONE', #79334, #98643, #81548, .T. ) ;
#104273=AXIS2_PLACEMENT_3D ( 'NONE', #258017, #63715, #140687 ) ;
#104285=DIRECTION ( 'NONE',  ( -3.265361837132813093E-16, -1.000000000000000000, -6.982962677686266711E-15 ) ) ;
#104288=ADVANCED_FACE ( 'NONE', ( #118141 ), #159854, .T. ) ;
#104299=ORIENTED_EDGE ( 'NONE', *, *, #194553, .T. ) ;
#104375=ORIENTED_EDGE ( 'NONE', *, *, #250201, .T. ) ;
#104415=ADVANCED_FACE ( 'NONE', ( #163698 ), #172956, .F. ) ;
#104434=DIRECTION ( 'NONE',  ( 0.000000000000000000, -6.853228547068871147E-15, 1.000000000000000000 ) ) ;
#104455=ADVANCED_FACE ( 'NONE', ( #7164 ), #26775, .F. ) ;
#104466=CARTESIAN_POINT ( 'NONE',  ( 21.14999999999999858, 76.00000000001205080, -124.3731074845242972 ) ) ;
#104471=DIRECTION ( 'NONE',  ( 0.000000000000000000, -1.000000000000000000, 0.000000000000000000 ) ) ;
#104488=CARTESIAN_POINT ( 'NONE',  ( -21.05000000000000071, 76.10000000001218723, -143.0637644362255401 ) ) ;
#104524=CARTESIAN_POINT ( 'NONE',  ( 23.24999999999999289, 70.05000000001197691, -113.3288097895591591 ) ) ;
#104525=AXIS2_PLACEMENT_3D ( 'NONE', #157581, #160125, #237073 ) ;
#104627=DIRECTION ( 'NONE',  ( -1.000000000000000000, 0.000000000000000000, 0.000000000000000000 ) ) ;
#104643=ORIENTED_EDGE ( 'NONE', *, *, #106361, .T. ) ;
#104662=EDGE_CURVE ( 'NONE', #34419, #232297, #181488, .T. ) ;
#104668=DIRECTION ( 'NONE',  ( 1.000000000000000000, 0.000000000000000000, 0.000000000000000000 ) ) ;
#104713=DIRECTION ( 'NONE',  ( 0.000000000000000000, -1.000000000000000000, -6.860497997771532351E-15 ) ) ;
#104737=ORIENTED_EDGE ( 'NONE', *, *, #256472, .F. ) ;
#104738=ADVANCED_FACE ( 'NONE', ( #244186 ), #225890, .F. ) ;
#104744=DIRECTION ( 'NONE',  ( 0.000000000000000000, -6.982962677686266711E-15, 1.000000000000000000 ) ) ;
#104753=DIRECTION ( 'NONE',  ( 0.000000000000000000, -6.982962677686266711E-15, 1.000000000000000000 ) ) ;
#104790=DIRECTION ( 'NONE',  ( -1.000000000000000000, -0.000000000000000000, -0.000000000000000000 ) ) ;
#104803=CARTESIAN_POINT ( 'NONE',  ( 21.14999999999999858, 76.00000000001205080, -124.3731074845242972 ) ) ;
#104807=ORIENTED_EDGE ( 'NONE', *, *, #251411, .T. ) ;
#104812=CIRCLE ( 'NONE', #138146, 0.1000000000000028644 ) ;
#104819=VECTOR ( 'NONE', #19221, 1000.000000000000000 ) ;
#104849=DIRECTION ( 'NONE',  ( 1.000000000000000000, 0.000000000000000000, 0.000000000000000000 ) ) ;
#104890=EDGE_CURVE ( 'NONE', #196680, #211746, #160656, .T. ) ;
#104893=VECTOR ( 'NONE', #31039, 1000.000000000000000 ) ;
#104907=ORIENTED_EDGE ( 'NONE', *, *, #96388, .T. ) ;
#104926=CARTESIAN_POINT ( 'NONE',  ( -21.44999999999999929, 68.75000000001205080, -124.1731074845243370 ) ) ;
#104929=DIRECTION ( 'NONE',  ( -0.000000000000000000, -1.000000000000000000, -6.982962677686266711E-15 ) ) ;
#104938=DIRECTION ( 'NONE',  ( 1.000000000000000000, 0.000000000000000000, 0.000000000000000000 ) ) ;
#105012=VERTEX_POINT ( 'NONE', #233642 ) ;
#105036=ORIENTED_EDGE ( 'NONE', *, *, #184137, .T. ) ;
#105040=VERTEX_POINT ( 'NONE', #154138 ) ;
#105055=DIRECTION ( 'NONE',  ( 4.504528286903032433E-15, 0.1298341882520054891, 0.9915357197604850459 ) ) ;
#105079=VERTEX_POINT ( 'NONE', #116263 ) ;
#105088=CARTESIAN_POINT ( 'NONE',  ( 21.05000000000000071, 76.00000000001190870, -103.0231074845243029 ) ) ;
#105109=LINE ( 'NONE', #163848, #11671 ) ;
#105215=AXIS2_PLACEMENT_3D ( 'NONE', #38221, #82430, #139853 ) ;
#105227=EDGE_CURVE ( 'NONE', #197443, #56953, #2576, .T. ) ;
#105228=AXIS2_PLACEMENT_3D ( 'NONE', #83815, #139958, #117840 ) ;
#105240=AXIS2_PLACEMENT_3D ( 'NONE', #41868, #200916, #181379 ) ;
#105264=CARTESIAN_POINT ( 'NONE',  ( -20.94999999999999929, 77.16270174995010223, -128.4231074845242802 ) ) ;
#105294=VERTEX_POINT ( 'NONE', #31310 ) ;
#105295=ORIENTED_EDGE ( 'NONE', *, *, #200566, .T. ) ;
#105303=ORIENTED_EDGE ( 'NONE', *, *, #175041, .F. ) ;
#105325=VERTEX_POINT ( 'NONE', #168262 ) ;
#105348=LINE ( 'NONE', #88367, #149685 ) ;
#105378=EDGE_CURVE ( 'NONE', #227184, #82680, #123395, .T. ) ;
#105387=ORIENTED_EDGE ( 'NONE', *, *, #176478, .T. ) ;
#105393=EDGE_CURVE ( 'NONE', #192091, #61013, #153839, .T. ) ;
#105438=DIRECTION ( 'NONE',  ( 0.000000000000000000, 6.982962677686266711E-15, -1.000000000000000000 ) ) ;
#105441=B_SPLINE_CURVE_WITH_KNOTS ( 'NONE', 3,
 ( #83596, #61512, #78482, #163185, #242699, #64068, #216721, #141052, #178922, #220585, #38105, #117627, #197151, #198442, #18529, #158088, #79754, #159343, #87470 ),
 .UNSPECIFIED., .F., .F.,
 ( 4, 3, 3, 3, 3, 3, 4 ),
 ( 0.000000000000000000, 2.646747978908423797E-05, 5.271166642128778001E-05, 9.008788829884103923E-05, 0.0001426648776561041253, 0.0001897378458659842060, 0.0001917382627806401836 ),
 .UNSPECIFIED. ) ;
#105456=AXIS2_PLACEMENT_3D ( 'NONE', #197020, #236162, #234895 ) ;
#105458=CARTESIAN_POINT ( 'NONE',  ( -18.39999999999999858, 85.60000000001187459, -96.42291809330220076 ) ) ;
#105480=CARTESIAN_POINT ( 'NONE',  ( 20.94999999999999574, 87.75000000001210765, -133.6231074845242119 ) ) ;
#105502=ORIENTED_EDGE ( 'NONE', *, *, #178945, .T. ) ;
#105512=CARTESIAN_POINT ( 'NONE',  ( 20.12500000000000000, 66.25000000001209344, -128.4113362024100979 ) ) ;
#105536=AXIS2_PLACEMENT_3D ( 'NONE', #195957, #216775, #99377 ) ;
#105584=ORIENTED_EDGE ( 'NONE', *, *, #108329, .F. ) ;
#105586=EDGE_CURVE ( 'NONE', #24834, #3363, #202673, .T. ) ;
#105588=VERTEX_POINT ( 'NONE', #141911 ) ;
#105596=ORIENTED_EDGE ( 'NONE', *, *, #207818, .T. ) ;
#105607=AXIS2_PLACEMENT_3D ( 'NONE', #191519, #207217, #225455 ) ;
#105608=PLANE ( 'NONE',  #17997 ) ;
#105622=DIRECTION ( 'NONE',  ( 0.000000000000000000, -7.086529944415894657E-15, 1.000000000000000000 ) ) ;
#105645=DIRECTION ( 'NONE',  ( 0.000000000000000000, -6.853228547068871147E-15, 1.000000000000000000 ) ) ;
#105656=AXIS2_PLACEMENT_3D ( 'NONE', #81212, #121673, #224590 ) ;
#105685=CARTESIAN_POINT ( 'NONE',  ( -21.11101077989000530, 75.98471473109790963, -142.9467922192504261 ) ) ;
#105714=DIRECTION ( 'NONE',  ( 0.000000000000000000, -0.3738317757008748909, -0.9274965247785733613 ) ) ;
#105743=DIRECTION ( 'NONE',  ( 6.484947573744954877E-15, -0.9274965247785555977, 0.3738317757009190223 ) ) ;
#105774=CARTESIAN_POINT ( 'NONE',  ( -22.50014994444007854, 64.25028026811983750, -136.6061876412430820 ) ) ;
#105783=CARTESIAN_POINT ( 'NONE',  ( -18.59999999999999787, 85.32100840337338354, -129.2871692354463562 ) ) ;
#105805=TOROIDAL_SURFACE ( 'NONE', #9968, 7.800000000000000711, 0.1000000000000000056 ) ;
#105819=CARTESIAN_POINT ( 'NONE',  ( -20.64999999999999858, 85.00000000001197975, -112.9170766071766820 ) ) ;
#105832=EDGE_CURVE ( 'NONE', #111084, #246341, #211248, .T. ) ;
#105840=ORIENTED_EDGE ( 'NONE', *, *, #201253, .T. ) ;
#105848=ORIENTED_EDGE ( 'NONE', *, *, #24902, .T. ) ;
#105851=DIRECTION ( 'NONE',  ( 0.000000000000000000, -7.172728831056617961E-15, 1.000000000000000000 ) ) ;
#105881=EDGE_CURVE ( 'NONE', #191930, #153656, #40592, .T. ) ;
#105888=ORIENTED_EDGE ( 'NONE', *, *, #33281, .T. ) ;
#105889=VECTOR ( 'NONE', #166906, 1000.000000000000114 ) ;
#105930=CARTESIAN_POINT ( 'NONE',  ( 18.49999999999999289, 65.71984138295523792, -111.7985354133230516 ) ) ;
#105981=AXIS2_PLACEMENT_3D ( 'NONE', #111365, #12286, #91801 ) ;
#106012=DIRECTION ( 'NONE',  ( 1.734723475976817507E-14, 1.000000000000000000, 6.982962677686266711E-15 ) ) ;
#106014=DIRECTION ( 'NONE',  ( 0.000000000000000000, -7.086529944415894657E-15, 1.000000000000000000 ) ) ;
#106019=DIRECTION ( 'NONE',  ( 0.000000000000000000, 0.000000000000000000, -1.000000000000000000 ) ) ;
#106028=EDGE_CURVE ( 'NONE', #8771, #30882, #28099, .T. ) ;
#106038=FACE_OUTER_BOUND ( 'NONE', #211676, .T. ) ;
#106054=FACE_OUTER_BOUND ( 'NONE', #40335, .T. ) ;
#106061=CIRCLE ( 'NONE', #22909, 4.049999999999998046 ) ;
#106078=CARTESIAN_POINT ( 'NONE',  ( -20.94983749550516450, 65.70233904877009934, -97.54874109119680270 ) ) ;
#106080=EDGE_CURVE ( 'NONE', #164153, #93761, #102885, .T. ) ;
#106081=CARTESIAN_POINT ( 'NONE',  ( 18.59999999999999076, 68.92903212821303782, -99.27654326265604823 ) ) ;
#106116=ADVANCED_FACE ( 'NONE', ( #134547 ), #90424, .T. ) ;
#106117=AXIS2_PLACEMENT_3D ( 'NONE', #240880, #118371, #100044 ) ;
#106125=CARTESIAN_POINT ( 'NONE',  ( 23.24999999999999289, 64.25000000001213607, -136.4231074845243938 ) ) ;
#106145=EDGE_LOOP ( 'NONE', ( #90585, #159277, #1374, #88197 ) ) ;
#106150=CARTESIAN_POINT ( 'NONE',  ( -21.05000000000000071, 87.75000000001192291, -106.1231074845242262 ) ) ;
#106161=VERTEX_POINT ( 'NONE', #195855 ) ;
#106183=CARTESIAN_POINT ( 'NONE',  ( -20.00857864376270001, 66.85000000001200249, -115.3731074845243683 ) ) ;
#106199=EDGE_LOOP ( 'NONE', ( #134240, #246822, #94798, #95986 ) ) ;
#106202=ORIENTED_EDGE ( 'NONE', *, *, #31392, .T. ) ;
#106220=EDGE_CURVE ( 'NONE', #13368, #112033, #219779, .T. ) ;
#106262=VECTOR ( 'NONE', #118807, 1000.000000000000000 ) ;
#106323=FACE_OUTER_BOUND ( 'NONE', #35397, .T. ) ;
#106357=DIRECTION ( 'NONE',  ( 1.000000000000000000, -0.000000000000000000, 0.000000000000000000 ) ) ;
#106361=EDGE_CURVE ( 'NONE', #19723, #173980, #86489, .T. ) ;
#106372=DIRECTION ( 'NONE',  ( 0.000000000000000000, 6.982962677686266711E-15, -1.000000000000000000 ) ) ;
#106408=EDGE_CURVE ( 'NONE', #8334, #53190, #44831, .T. ) ;
#106424=ORIENTED_EDGE ( 'NONE', *, *, #238598, .T. ) ;
#106439=VECTOR ( 'NONE', #154982, 1000.000000000000000 ) ;
#106445=FACE_OUTER_BOUND ( 'NONE', #84672, .T. ) ;
#106451=LINE ( 'NONE', #244694, #134624 ) ;
#106508=EDGE_CURVE ( 'NONE', #71963, #87941, #153389, .T. ) ;
#106524=ORIENTED_EDGE ( 'NONE', *, *, #217114, .F. ) ;
#106528=CYLINDRICAL_SURFACE ( 'NONE', #238805, 12.87499999999999822 ) ;
#106531=CARTESIAN_POINT ( 'NONE',  ( -20.54999999999999716, 76.00000000001192291, -104.9231074845242944 ) ) ;
#106551=ORIENTED_EDGE ( 'NONE', *, *, #238232, .T. ) ;
#106566=DIRECTION ( 'NONE',  ( 0.000000000000000000, 0.000000000000000000, 1.000000000000000000 ) ) ;
#106611=ORIENTED_EDGE ( 'NONE', *, *, #156357, .T. ) ;
#106614=CARTESIAN_POINT ( 'NONE',  ( -18.50000000000000000, 68.97833521811179480, -99.18954208262705663 ) ) ;
#106632=CIRCLE ( 'NONE', #202335, 0.1999999999999987899 ) ;
#106690=ORIENTED_EDGE ( 'NONE', *, *, #207160, .T. ) ;
#106698=EDGE_LOOP ( 'NONE', ( #92414, #15460, #250126, #135575 ) ) ;
#106726=AXIS2_PLACEMENT_3D ( 'NONE', #112398, #56242, #91544 ) ;
#106744=ADVANCED_FACE ( 'NONE', ( #157410 ), #16600, .F. ) ;
#106769=AXIS2_PLACEMENT_3D ( 'NONE', #85182, #49940, #206455 ) ;
#106806=ORIENTED_EDGE ( 'NONE', *, *, #91095, .F. ) ;
#106810=DIRECTION ( 'NONE',  ( -1.000000000000000000, -7.304098846218163263E-16, 4.217023435051627211E-16 ) ) ;
#106836=ADVANCED_FACE ( 'NONE', ( #76539 ), #193943, .F. ) ;
#106858=AXIS2_PLACEMENT_3D ( 'NONE', #123041, #141311, #125596 ) ;
#106871=ORIENTED_EDGE ( 'NONE', *, *, #22389, .F. ) ;
#106885=DIRECTION ( 'NONE',  ( 0.000000000000000000, 0.000000000000000000, -1.000000000000000000 ) ) ;
#106934=EDGE_LOOP ( 'NONE', ( #16375, #52007, #113928, #119854 ) ) ;
#106949=EDGE_CURVE ( 'NONE', #186279, #163243, #153584, .T. ) ;
#106953=AXIS2_PLACEMENT_3D ( 'NONE', #163620, #44954, #245722 ) ;
#106962=DIRECTION ( 'NONE',  ( -1.000000000000000000, 2.952720810173289112E-16, 2.061873921506763405E-30 ) ) ;
#106976=AXIS2_PLACEMENT_3D ( 'NONE', #120882, #200391, #8304 ) ;
#107015=DIRECTION ( 'NONE',  ( 0.000000000000000000, 1.000000000000000000, 0.000000000000000000 ) ) ;
#107041=CARTESIAN_POINT ( 'NONE',  ( -23.15000000000000213, 71.65000000001207070, -124.3731074845243256 ) ) ;
#107043=CARTESIAN_POINT ( 'NONE',  ( 23.14999999999999858, 71.22429906543254674, -114.8718755885703047 ) ) ;
#107050=CARTESIAN_POINT ( 'NONE',  ( -21.04999999999999716, 69.72991413632300350, -136.5579754875374192 ) ) ;
#107059=SURFACE_STYLE_USAGE ( .BOTH. , #33685 ) ;
#107066=LINE ( 'NONE', #246577, #63211 ) ;
#107068=DIRECTION ( 'NONE',  ( -2.827886303505249259E-16, -0.8660254037844378194, -0.5000000000000016653 ) ) ;
#107084=DIRECTION ( 'NONE',  ( 1.000000000000000000, -0.000000000000000000, 0.000000000000000000 ) ) ;
#107113=CARTESIAN_POINT ( 'NONE',  ( -23.15000000000000213, 85.00000000001197975, -112.9170766071766820 ) ) ;
#107131=DIRECTION ( 'NONE',  ( -0.000000000000000000, 1.000000000000000000, 6.982962677686266711E-15 ) ) ;
#107135=PLANE ( 'NONE',  #89747 ) ;
#107166=AXIS2_PLACEMENT_3D ( 'NONE', #106183, #149208, #226121 ) ;
#107171=ORIENTED_EDGE ( 'NONE', *, *, #210680, .F. ) ;
#107177=VERTEX_POINT ( 'NONE', #94506 ) ;
#107206=AXIS2_PLACEMENT_3D ( 'NONE', #148085, #105055, #144209 ) ;
#107213=ORIENTED_EDGE ( 'NONE', *, *, #235997, .T. ) ;
#107235=DIRECTION ( 'NONE',  ( 0.000000000000000000, 0.000000000000000000, 1.000000000000000000 ) ) ;
#107244=FACE_OUTER_BOUND ( 'NONE', #108430, .T. ) ;
#107271=CYLINDRICAL_SURFACE ( 'NONE', #143475, 0.1000000000000028644 ) ;
#107311=DIRECTION ( 'NONE',  ( 0.000000000000000000, -7.116814260417668513E-15, 1.000000000000000000 ) ) ;
#107325=CARTESIAN_POINT ( 'NONE',  ( 23.14999999999999503, 64.35000000001204512, -124.3731074845243825 ) ) ;
#107340=CARTESIAN_POINT ( 'NONE',  ( -23.25000000000000000, 76.00000000001189449, -100.9231074845242944 ) ) ;
#107363=ORIENTED_EDGE ( 'NONE', *, *, #181995, .T. ) ;
#107367=EDGE_CURVE ( 'NONE', #153790, #155470, #233316, .T. ) ;
#107369=DIRECTION ( 'NONE',  ( -1.000000000000000000, 2.952720810173289112E-16, 2.061873921506763405E-30 ) ) ;
#107384=CARTESIAN_POINT ( 'NONE',  ( -20.85882249326303040, 65.66751761918668251, -97.42826094061121012 ) ) ;
#107423=TOROIDAL_SURFACE ( 'NONE', #253161, 6.258578643762712446, 0.1000000000000000056 ) ;
#107439=CARTESIAN_POINT ( 'NONE',  ( 21.14261333020286315, 65.28430735075716029, -124.2731074845241466 ) ) ;
#107442=ORIENTED_EDGE ( 'NONE', *, *, #143330, .F. ) ;
#107484=CIRCLE ( 'NONE', #140809, 0.09999999999998898659 ) ;
#107505=DIRECTION ( 'NONE',  ( -0.000000000000000000, 6.982962677686266711E-15, -1.000000000000000000 ) ) ;
#107524=EDGE_LOOP ( 'NONE', ( #85318, #688, #233593, #8135 ) ) ;
#107535=DIRECTION ( 'NONE',  ( 0.000000000000000000, 0.000000000000000000, 1.000000000000000000 ) ) ;
#107540=VERTEX_POINT ( 'NONE', #118560 ) ;
#107580=CARTESIAN_POINT ( 'NONE',  ( 23.14999999999998437, 76.00000000001213607, -136.5231074845242745 ) ) ;
#107581=VECTOR ( 'NONE', #85930, 1000.000000000000000 ) ;
#107637=ADVANCED_FACE ( 'NONE', ( #63685 ), #21119, .T. ) ;
#107664=VERTEX_POINT ( 'NONE', #253868 ) ;
#107787=DIRECTION ( 'NONE',  ( -0.8660254037844653530, 0.000000000000000000, -0.4999999999999539257 ) ) ;
#107831=ORIENTED_EDGE ( 'NONE', *, *, #86803, .T. ) ;
#107869=ORIENTED_EDGE ( 'NONE', *, *, #68109, .T. ) ;
#107885=AXIS2_PLACEMENT_3D ( 'NONE', #245270, #26227, #105714 ) ;
#107893=CARTESIAN_POINT ( 'NONE',  ( -20.94999999999999929, 70.15000000001198543, -113.1556047088022723 ) ) ;
#107929=ORIENTED_EDGE ( 'NONE', *, *, #93950, .F. ) ;
#107930=DIRECTION ( 'NONE',  ( -2.561896900575096011E-15, 0.5907332058517336115, -0.8068669527896984439 ) ) ;
#107975=CARTESIAN_POINT ( 'NONE',  ( 21.14999999999999858, 69.35000000001205933, -124.1731074845243370 ) ) ;
#107981=ORIENTED_EDGE ( 'NONE', *, *, #22995, .T. ) ;
#108007=CARTESIAN_POINT ( 'NONE',  ( -22.59999999999999432, 64.25012875563564307, -136.5885370755380279 ) ) ;
#108061=CARTESIAN_POINT ( 'NONE',  ( -23.25000000000000000, 76.00000000001190870, -103.0231074845243029 ) ) ;
#108110=CARTESIAN_POINT ( 'NONE',  ( -20.85000000000000142, 77.83585931145546510, -91.51866831572576189 ) ) ;
#108122=AXIS2_PLACEMENT_3D ( 'NONE', #133299, #52450, #132007 ) ;
#108147=EDGE_CURVE ( 'NONE', #165923, #156363, #209304, .T. ) ;
#108160=AXIS2_PLACEMENT_3D ( 'NONE', #206766, #170257, #247159 ) ;
#108175=EDGE_CURVE ( 'NONE', #1620, #232297, #152528, .T. ) ;
#108250=DIRECTION ( 'NONE',  ( 0.000000000000000000, -1.000000000000000000, -6.352154140967427193E-15 ) ) ;
#108274=LINE ( 'NONE', #24900, #102279 ) ;
#108279=VECTOR ( 'NONE', #82956, 1000.000000000000000 ) ;
#108280=CARTESIAN_POINT ( 'NONE',  ( 23.14999999999999858, 64.40000000001194280, -109.9513107147998880 ) ) ;
#108289=ORIENTED_EDGE ( 'NONE', *, *, #50743, .T. ) ;
#108319=DIRECTION ( 'NONE',  ( -0.7071067811865389130, 4.937700262164590641E-15, -0.7071067811865561215 ) ) ;
#108329=EDGE_CURVE ( 'NONE', #14291, #103697, #32078, .T. ) ;
#108415=DIRECTION ( 'NONE',  ( 1.000000000000000000, 0.000000000000000000, 0.000000000000000000 ) ) ;
#108430=EDGE_LOOP ( 'NONE', ( #32645, #133459, #125616, #211150, #34815 ) ) ;
#108438=CIRCLE ( 'NONE', #250263, 0.1000000000000028644 ) ;
#108443=CARTESIAN_POINT ( 'NONE',  ( 18.54148534481893762, 65.67467670974414773, -97.45317318268841689 ) ) ;
#108466=CARTESIAN_POINT ( 'NONE',  ( 18.59999999999999076, 69.45000000001199680, -115.2731074845243455 ) ) ;
#108467=EDGE_LOOP ( 'NONE', ( #136690, #60377, #115117, #91155 ) ) ;
#108469=PLANE ( 'NONE',  #29804 ) ;
#108481=AXIS2_PLACEMENT_3D ( 'NONE', #242997, #224711, #124351 ) ;
#108516=ORIENTED_EDGE ( 'NONE', *, *, #111742, .F. ) ;
#108523=EDGE_CURVE ( 'NONE', #102291, #75479, #133331, .T. ) ;
#108540=ORIENTED_EDGE ( 'NONE', *, *, #32133, .F. ) ;
#108543=ORIENTED_EDGE ( 'NONE', *, *, #67104, .T. ) ;
#108548=AXIS2_PLACEMENT_3D ( 'NONE', #154082, #134445, #36690 ) ;
#108553=EDGE_CURVE ( 'NONE', #155438, #186897, #185158, .T. ) ;
#108555=ORIENTED_EDGE ( 'NONE', *, *, #42418, .T. ) ;
#108560=VERTEX_POINT ( 'NONE', #100270 ) ;
#108564=CARTESIAN_POINT ( 'NONE',  ( 20.94999999999999929, 76.00000000001190870, -103.0231074845243029 ) ) ;
#108568=DIRECTION ( 'NONE',  ( 0.000000000000000000, 6.982962677686266711E-15, -1.000000000000000000 ) ) ;
#108572=DIRECTION ( 'NONE',  ( 1.000000000000000000, 0.000000000000000000, 0.000000000000000000 ) ) ;
#108604=LINE ( 'NONE', #250675, #173744 ) ;
#108605=DIRECTION ( 'NONE',  ( 0.000000000000000000, -1.000000000000000000, 0.000000000000000000 ) ) ;
#108611=DIRECTION ( 'NONE',  ( 1.000000000000000000, 0.000000000000000000, 0.000000000000000000 ) ) ;
#108626=CARTESIAN_POINT ( 'NONE',  ( -21.05000000000000071, 76.00000000001210765, -133.6231074845243256 ) ) ;
#108627=ORIENTED_EDGE ( 'NONE', *, *, #14115, .T. ) ;
#108642=ORIENTED_EDGE ( 'NONE', *, *, #195691, .T. ) ;
#108644=DIRECTION ( 'NONE',  ( -0.000000000000000000, 1.000000000000000000, 6.982962677686266711E-15 ) ) ;
#108656=EDGE_CURVE ( 'NONE', #191930, #190621, #190490, .T. ) ;
#108669=CARTESIAN_POINT ( 'NONE',  ( 20.95512820512820440, 65.37615131630012399, -115.2731074845243739 ) ) ;
#108679=CARTESIAN_POINT ( 'NONE',  ( -20.89192007715127986, 65.67101464000501210, -97.44043916224792667 ) ) ;
#108699=ORIENTED_EDGE ( 'NONE', *, *, #242190, .T. ) ;
#108700=EDGE_CURVE ( 'NONE', #170795, #43436, #173766, .T. ) ;
#108783=CIRCLE ( 'NONE', #237962, 0.2000000000000057288 ) ;
#108784=DIRECTION ( 'NONE',  ( 0.000000000000000000, 0.000000000000000000, 1.000000000000000000 ) ) ;
#108808=FACE_OUTER_BOUND ( 'NONE', #21622, .T. ) ;
#108810=CARTESIAN_POINT ( 'NONE',  ( 22.39999999999999858, 75.90000000001219860, -144.3138870828976792 ) ) ;
#108830=AXIS2_PLACEMENT_3D ( 'NONE', #228608, #30408, #205155 ) ;
#108873=DIRECTION ( 'NONE',  ( 0.000000000000000000, -6.982962677686266711E-15, 1.000000000000000000 ) ) ;
#108957=CARTESIAN_POINT ( 'NONE',  ( -18.50000000000000000, 76.00000000001190870, -103.0231074845243029 ) ) ;
#108963=CARTESIAN_POINT ( 'NONE',  ( -20.85000000000000142, 76.00000000001190870, -103.0231074845243029 ) ) ;
#108975=CARTESIAN_POINT ( 'NONE',  ( -20.64999999999999858, 68.75000000001205080, -124.1731074845243370 ) ) ;
#108985=FACE_OUTER_BOUND ( 'NONE', #114368, .T. ) ;
#109019=AXIS2_PLACEMENT_3D ( 'NONE', #143907, #64387, #5658 ) ;
#109020=DIRECTION ( 'NONE',  ( -1.000000000000000000, 7.304098846218134667E-16, 5.100424963727255829E-30 ) ) ;
#109023=AXIS2_PLACEMENT_3D ( 'NONE', #90792, #192479, #169102 ) ;
#109045=AXIS2_PLACEMENT_3D ( 'NONE', #29825, #92322, #51894 ) ;
#109086=ORIENTED_EDGE ( 'NONE', *, *, #187727, .F. ) ;
#109092=DIRECTION ( 'NONE',  ( 0.000000000000000000, -6.982962677686266711E-15, 1.000000000000000000 ) ) ;
#109099=EDGE_CURVE ( 'NONE', #76926, #224952, #3176, .T. ) ;
#109102=CIRCLE ( 'NONE', #34150, 0.09999999999999939493 ) ;
#109128=B_SPLINE_CURVE_WITH_KNOTS ( 'NONE', 3,
 ( #189863, #86883, #171618, #209415, #8657, #47760, #169055, #12532 ),
 .UNSPECIFIED., .F., .F.,
 ( 4, 2, 2, 4 ),
 ( 0.000000000000000000, 0.0002181133598168873079, 0.0003271700397253444331, 0.0004362267196338015583 ),
 .UNSPECIFIED. ) ;
#109129=VERTEX_POINT ( 'NONE', #184648 ) ;
#109140=ORIENTED_EDGE ( 'NONE', *, *, #229983, .F. ) ;
#109146=ADVANCED_FACE ( 'NONE', ( #12457 ), #94525, .T. ) ;
#109176=ADVANCED_FACE ( 'NONE', ( #149406 ), #134917, .F. ) ;
#109192=DIRECTION ( 'NONE',  ( 0.000000000000000000, -1.000000000000000000, -6.982962677686266711E-15 ) ) ;
#109238=CARTESIAN_POINT ( 'NONE',  ( 22.49999999999999645, 64.35012909624795441, -136.6056273753972903 ) ) ;
#109293=AXIS2_PLACEMENT_3D ( 'NONE', #95275, #99101, #219059 ) ;
#109306=LINE ( 'NONE', #28559, #171636 ) ;
#109315=FACE_OUTER_BOUND ( 'NONE', #62022, .T. ) ;
#109342=ORIENTED_EDGE ( 'NONE', *, *, #247463, .F. ) ;
#109365=AXIS2_PLACEMENT_3D ( 'NONE', #186470, #83475, #24855 ) ;
#109368=DIRECTION ( 'NONE',  ( 0.000000000000000000, 0.000000000000000000, -1.000000000000000000 ) ) ;
#109378=DIRECTION ( 'NONE',  ( -0.000000000000000000, -0.1350103645451945777, 0.9908441862701590219 ) ) ;
#109408=DIRECTION ( 'NONE',  ( 0.000000000000000000, 7.116814260417668513E-15, -1.000000000000000000 ) ) ;
#109413=DIRECTION ( 'NONE',  ( 1.000000000000000000, 0.000000000000000000, 0.000000000000000000 ) ) ;
#109420=CIRCLE ( 'NONE', #255117, 4.000000000000003553 ) ;
#109434=EDGE_CURVE ( 'NONE', #137392, #25096, #132566, .T. ) ;
#109436=CIRCLE ( 'NONE', #1085, 0.1000000000000028644 ) ;
#109442=ADVANCED_FACE ( 'NONE', ( #65677 ), #190862, .F. ) ;
#109447=EDGE_CURVE ( 'NONE', #158778, #35933, #170028, .T. ) ;
#109452=ADVANCED_FACE ( 'NONE', ( #25294, #202625 ), #224741, .F. ) ;
#109501=ORIENTED_EDGE ( 'NONE', *, *, #145090, .F. ) ;
#109528=FACE_OUTER_BOUND ( 'NONE', #69550, .T. ) ;
#109557=TOROIDAL_SURFACE ( 'NONE', #176228, 0.2000000000000000111, 0.1000000000000000056 ) ;
#109602=ORIENTED_EDGE ( 'NONE', *, *, #114393, .F. ) ;
#109664=ADVANCED_FACE ( 'NONE', ( #10855 ), #130787, .F. ) ;
#109671=DIRECTION ( 'NONE',  ( -1.000000000000000000, -0.000000000000000000, -0.000000000000000000 ) ) ;
#109677=EDGE_CURVE ( 'NONE', #182088, #60637, #36738, .T. ) ;
#109679=FACE_OUTER_BOUND ( 'NONE', #24878, .T. ) ;
#109680=LINE ( 'NONE', #30180, #73915 ) ;
#109704=DIRECTION ( 'NONE',  ( 1.000000000000000000, 0.000000000000000000, 0.000000000000000000 ) ) ;
#109706=CARTESIAN_POINT ( 'NONE',  ( 18.55807992284871588, 65.67101464000501210, -97.44043916224792667 ) ) ;
#109717=CARTESIAN_POINT ( 'NONE',  ( -20.54999999999999716, 71.75000000001205080, -124.1731074845243228 ) ) ;
#109772=EDGE_LOOP ( 'NONE', ( #201766, #256167, #250502, #234180 ) ) ;
#109774=ORIENTED_EDGE ( 'NONE', *, *, #113080, .T. ) ;
#109795=DIRECTION ( 'NONE',  ( 0.000000000000000000, 6.938893903907222067E-15, -1.000000000000000000 ) ) ;
#109802=ADVANCED_FACE ( 'NONE', ( #62809 ), #161810, .T. ) ;
#109803=DIRECTION ( 'NONE',  ( 0.000000000000000000, -6.938893903907222067E-15, 1.000000000000000000 ) ) ;
#109821=DIRECTION ( 'NONE',  ( 0.000000000000000000, 0.8660254037844420383, -0.4999999999999943379 ) ) ;
#109828=EDGE_CURVE ( 'NONE', #177518, #213781, #166101, .T. ) ;
#109852=DIRECTION ( 'NONE',  ( -1.000000000000000000, -0.000000000000000000, -0.000000000000000000 ) ) ;
#109853=ORIENTED_EDGE ( 'NONE', *, *, #19151, .T. ) ;
#109863=CARTESIAN_POINT ( 'NONE',  ( 21.00000000000000000, 66.25000000001199396, -115.2731074845243597 ) ) ;
#109887=CARTESIAN_POINT ( 'NONE',  ( -21.08479644141223019, 69.65496134228024516, -136.5816619270885326 ) ) ;
#109898=AXIS2_PLACEMENT_3D ( 'NONE', #26701, #144036, #243150 ) ;
#109906=LINE ( 'NONE', #249450, #115165 ) ;
#109910=SPHERICAL_SURFACE ( 'NONE', #154170, 0.1000000000000000056 ) ;
#109924=EDGE_LOOP ( 'NONE', ( #20034, #42063, #11373 ) ) ;
#109941=DIRECTION ( 'NONE',  ( -2.252264143451594314E-15, 0.1298341882520054891, 0.9915357197604850459 ) ) ;
#109953=CARTESIAN_POINT ( 'NONE',  ( -20.86777300164945004, 65.66799936921530900, -97.42993998886008455 ) ) ;
#109954=CIRCLE ( 'NONE', #234870, 11.89999999999999325 ) ;
#110002=CARTESIAN_POINT ( 'NONE',  ( 20.12500000000000000, 66.25000000001209344, -128.4113362024100979 ) ) ;
#110012=CARTESIAN_POINT ( 'NONE',  ( 18.50000000000000000, 85.40000000001208491, -129.5238218066853904 ) ) ;
#110020=EDGE_LOOP ( 'NONE', ( #84878, #166337, #221249, #211824 ) ) ;
#110033=ORIENTED_EDGE ( 'NONE', *, *, #220336, .T. ) ;
#110067=EDGE_CURVE ( 'NONE', #107540, #241350, #103502, .T. ) ;
#110078=ORIENTED_EDGE ( 'NONE', *, *, #17351, .T. ) ;
#110080=CARTESIAN_POINT ( 'NONE',  ( 22.39999999999999503, 76.00000000001219291, -144.3138870828976792 ) ) ;
#110089=CARTESIAN_POINT ( 'NONE',  ( 18.58703555225034876, 85.40633674080100946, -129.3981628432775892 ) ) ;
#110099=CARTESIAN_POINT ( 'NONE',  ( 20.85000000000000142, 68.97833521811179480, -99.18954208262705663 ) ) ;
#110127=ORIENTED_EDGE ( 'NONE', *, *, #226404, .F. ) ;
#110175=CARTESIAN_POINT ( 'NONE',  ( -23.25000000000000000, 71.65000000001199965, -115.1731074845243370 ) ) ;
#110193=CIRCLE ( 'NONE', #185224, 0.09999999999999939493 ) ;
#110200=CARTESIAN_POINT ( 'NONE',  ( -21.05000000000000071, 70.10000000001213039, -126.3040077198679398 ) ) ;
#110230=DIRECTION ( 'NONE',  ( -0.000000000000000000, -6.982962677686266711E-15, 1.000000000000000000 ) ) ;
#110231=DIRECTION ( 'NONE',  ( -0.000000000000000000, 0.1350103645451945777, -0.9908441862701590219 ) ) ;
#110272=DIRECTION ( 'NONE',  ( 1.000000000000000000, 0.000000000000000000, 0.000000000000000000 ) ) ;
#110280=PLANE ( 'NONE',  #5971 ) ;
#110319=EDGE_CURVE ( 'NONE', #72948, #134440, #131138, .T. ) ;
#110326=ADVANCED_FACE ( 'NONE', ( #35917 ), #153827, .F. ) ;
#110401=CIRCLE ( 'NONE', #93840, 0.1000000000000028644 ) ;
#110420=DIRECTION ( 'NONE',  ( 0.000000000000000000, 0.000000000000000000, 1.000000000000000000 ) ) ;
#110460=CARTESIAN_POINT ( 'NONE',  ( -22.39999999999999858, 68.20922040163873135, -136.5231074845243313 ) ) ;
#110471=EDGE_LOOP ( 'NONE', ( #68052, #29426, #146866, #179212, #252915, #129084, #117205 ) ) ;
#110477=ORIENTED_EDGE ( 'NONE', *, *, #12072, .F. ) ;
#110487=AXIS2_PLACEMENT_3D ( 'NONE', #133527, #228791, #154419 ) ;
#110529=DIRECTION ( 'NONE',  ( 1.000000000000000000, -7.304098846218135653E-16, -5.100424963727256530E-30 ) ) ;
#110546=CARTESIAN_POINT ( 'NONE',  ( -20.94999999999999929, 74.83729825007408465, -128.6231074845242972 ) ) ;
#110548=AXIS2_PLACEMENT_3D ( 'NONE', #168035, #186286, #7642 ) ;
#110553=LINE ( 'NONE', #87129, #223971 ) ;
#110573=AXIS2_PLACEMENT_3D ( 'NONE', #183502, #240912, #162663 ) ;
#110723=DIRECTION ( 'NONE',  ( 0.000000000000000000, 0.9999631594459055250, 0.008583690987131395445 ) ) ;
#110737=CARTESIAN_POINT ( 'NONE',  ( 23.24999999999999289, 64.35000000001221565, -148.2731074845243882 ) ) ;
#110746=DIRECTION ( 'NONE',  ( 1.000000000000000000, 0.000000000000000000, 0.000000000000000000 ) ) ;
#110752=ADVANCED_FACE ( 'NONE', ( #166997 ), #66582, .T. ) ;
#110809=AXIS2_PLACEMENT_3D ( 'NONE', #139619, #118815, #238747 ) ;
#110812=CARTESIAN_POINT ( 'NONE',  ( -20.64999999999999858, 71.65000000001199965, -115.3731074845243256 ) ) ;
#110822=DIRECTION ( 'NONE',  ( 0.000000000000000000, 0.4930308989875575865, 0.8700118002898125091 ) ) ;
#110842=CARTESIAN_POINT ( 'NONE',  ( -20.85000000000000142, 77.26327546522911405, -95.12124281777788326 ) ) ;
#110845=EDGE_CURVE ( 'NONE', #37720, #109129, #224672, .T. ) ;
#110909=DIRECTION ( 'NONE',  ( 1.000000000000000000, 0.000000000000000000, 0.000000000000000000 ) ) ;
#110914=CARTESIAN_POINT ( 'NONE',  ( -21.05000000000000426, 69.52295361822230291, -136.4231074845243938 ) ) ;
#110917=ORIENTED_EDGE ( 'NONE', *, *, #169747, .F. ) ;
#110925=VERTEX_POINT ( 'NONE', #236219 ) ;
#110941=EDGE_CURVE ( 'NONE', #170896, #105294, #149969, .T. ) ;
#110968=AXIS2_PLACEMENT_3D ( 'NONE', #48778, #167476, #207890 ) ;
#111005=CYLINDRICAL_SURFACE ( 'NONE', #31141, 0.09999999999998898659 ) ;
#111010=EDGE_CURVE ( 'NONE', #207631, #63258, #137450, .T. ) ;
#111033=DIRECTION ( 'NONE',  ( 1.000000000000000000, 0.000000000000000000, 0.000000000000000000 ) ) ;
#111040=ORIENTED_EDGE ( 'NONE', *, *, #166310, .T. ) ;
#111042=ORIENTED_EDGE ( 'NONE', *, *, #136565, .T. ) ;
#111084=VERTEX_POINT ( 'NONE', #83536 ) ;
#111101=FACE_OUTER_BOUND ( 'NONE', #54697, .T. ) ;
#111107=VERTEX_POINT ( 'NONE', #240085 ) ;
#111119=ORIENTED_EDGE ( 'NONE', *, *, #72087, .T. ) ;
#111121=AXIS2_PLACEMENT_3D ( 'NONE', #63010, #4313, #222058 ) ;
#111133=CARTESIAN_POINT ( 'NONE',  ( 20.95496329884391784, 65.43256679391905095, -128.9487975522395402 ) ) ;
#111134=FACE_OUTER_BOUND ( 'NONE', #114218, .T. ) ;
#111144=EDGE_CURVE ( 'NONE', #231702, #70035, #65902, .T. ) ;
#111152=ADVANCED_FACE ( 'NONE', ( #4030 ), #161792, .T. ) ;
#111184=FACE_OUTER_BOUND ( 'NONE', #132083, .T. ) ;
#111203=AXIS2_PLACEMENT_3D ( 'NONE', #3732, #57266, #102809 ) ;
#111205=ORIENTED_EDGE ( 'NONE', *, *, #10243, .T. ) ;
#111230=DIRECTION ( 'NONE',  ( 0.000000000000000000, -2.775557561562888827E-14, 1.000000000000000000 ) ) ;
#111249=VECTOR ( 'NONE', #76064, 1000.000000000000000 ) ;
#111263=CARTESIAN_POINT ( 'NONE',  ( 22.00411653962156677, 68.74655713164199256, -136.6221455902929733 ) ) ;
#111267=CARTESIAN_POINT ( 'NONE',  ( -18.59999999999999787, 77.83585931145546510, -91.51866831572576189 ) ) ;
#111283=DIRECTION ( 'NONE',  ( 0.000000000000000000, 0.4999999999999689138, 0.8660254037844565822 ) ) ;
#111289=DIRECTION ( 'NONE',  ( -1.000000000000000000, 2.952720810173289112E-16, 2.061873921506763405E-30 ) ) ;
#111302=ORIENTED_EDGE ( 'NONE', *, *, #130757, .F. ) ;
#111313=DIRECTION ( 'NONE',  ( 0.000000000000000000, 6.982962677686266711E-15, -1.000000000000000000 ) ) ;
#111324=CIRCLE ( 'NONE', #15673, 11.74999999999999645 ) ;
#111335=CIRCLE ( 'NONE', #198990, 0.1000000000000028644 ) ;
#111342=DIRECTION ( 'NONE',  ( 1.000000000000000000, 0.000000000000000000, 0.000000000000000000 ) ) ;
#111359=AXIS2_PLACEMENT_3D ( 'NONE', #120183, #79707, #159285 ) ;
#111365=CARTESIAN_POINT ( 'NONE',  ( -2.995603634470891112E-16, 69.35000000001200249, -115.3731074845243398 ) ) ;
#111372=DIRECTION ( 'NONE',  ( 0.000000000000000000, 0.000000000000000000, 1.000000000000000000 ) ) ;
#111381=CIRCLE ( 'NONE', #157199, 11.90000000000000746 ) ;
#111386=CARTESIAN_POINT ( 'NONE',  ( 18.51565452909259690, 85.35285933884755138, -129.3281981632919440 ) ) ;
#111413=AXIS2_PLACEMENT_3D ( 'NONE', #227073, #247922, #47135 ) ;
#111431=DIRECTION ( 'NONE',  ( 0.000000000000000000, -1.000000000000000000, -6.982962677686266711E-15 ) ) ;
#111446=ORIENTED_EDGE ( 'NONE', *, *, #194896, .T. ) ;
#111491=ORIENTED_EDGE ( 'NONE', *, *, #187401, .T. ) ;
#111492=EDGE_CURVE ( 'NONE', #107664, #214613, #143219, .T. ) ;
#111509=ORIENTED_EDGE ( 'NONE', *, *, #207870, .T. ) ;
#111528=CARTESIAN_POINT ( 'NONE',  ( -20.94999999999999929, 74.25000000001205080, -124.8535959266226598 ) ) ;
#111552=LINE ( 'NONE', #191113, #255014 ) ;
#111567=LINE ( 'NONE', #71172, #198767 ) ;
#111568=ORIENTED_EDGE ( 'NONE', *, *, #100537, .T. ) ;
#111576=DIRECTION ( 'NONE',  ( 0.000000000000000000, -1.000000000000000000, -6.982962677686265922E-15 ) ) ;
#111586=DIRECTION ( 'NONE',  ( 0.000000000000000000, 7.026728003956683390E-15, -1.000000000000000000 ) ) ;
#111589=CARTESIAN_POINT ( 'NONE',  ( 20.94999999999999929, 76.00000000001190870, -103.0231074845243029 ) ) ;
#111675=DIRECTION ( 'NONE',  ( -0.000000000000000000, 6.982962677686266711E-15, -1.000000000000000000 ) ) ;
#111678=EDGE_CURVE ( 'NONE', #226855, #2981, #105348, .T. ) ;
#111687=ORIENTED_EDGE ( 'NONE', *, *, #239585, .F. ) ;
#111689=AXIS2_PLACEMENT_3D ( 'NONE', #255704, #34174, #171130 ) ;
#111704=EDGE_LOOP ( 'NONE', ( #71299, #242854, #176066 ) ) ;
#111706=CARTESIAN_POINT ( 'NONE',  ( -20.94999999999999929, 64.35000000001195986, -109.8069731475024753 ) ) ;
#111724=CIRCLE ( 'NONE', #199218, 0.09999999999998900047 ) ;
#111729=DIRECTION ( 'NONE',  ( -2.342056488767301376E-15, 0.1350103645451974088, -0.9908441862701587999 ) ) ;
#111735=CIRCLE ( 'NONE', #40846, 0.09999999999999939493 ) ;
#111738=CIRCLE ( 'NONE', #240750, 0.5000000000000004441 ) ;
#111742=EDGE_CURVE ( 'NONE', #246153, #155941, #37109, .T. ) ;
#111851=VERTEX_POINT ( 'NONE', #141320 ) ;
#111859=CARTESIAN_POINT ( 'NONE',  ( 20.85000000000000142, 76.00000000001190870, -103.0231074845243029 ) ) ;
#111861=LINE ( 'NONE', #133971, #242459 ) ;
#111864=FACE_OUTER_BOUND ( 'NONE', #211595, .T. ) ;
#111865=CYLINDRICAL_SURFACE ( 'NONE', #70983, 0.1000000000000028644 ) ;
#111890=CARTESIAN_POINT ( 'NONE',  ( 21.05543885634738643, 67.22422895316451275, -124.3387230138096697 ) ) ;
#111919=VERTEX_POINT ( 'NONE', #87749 ) ;
#111929=DIRECTION ( 'NONE',  ( -2.940209281316621016E-16, -1.000000000000000000, -7.056502275159890832E-15 ) ) ;
#111945=EDGE_CURVE ( 'NONE', #65006, #139626, #45622, .T. ) ;
#111946=CARTESIAN_POINT ( 'NONE',  ( 20.85000000000000142, 69.15387683765929694, -99.28538121767448388 ) ) ;
#111963=FACE_OUTER_BOUND ( 'NONE', #201584, .T. ) ;
#111976=ORIENTED_EDGE ( 'NONE', *, *, #112928, .T. ) ;
#112008=DIRECTION ( 'NONE',  ( -1.000000000000000000, 0.000000000000000000, -0.000000000000000000 ) ) ;
#112027=CARTESIAN_POINT ( 'NONE',  ( -18.59999999999999787, 66.65000000001205649, -124.1731074845243654 ) ) ;
#112033=VERTEX_POINT ( 'NONE', #90319 ) ;
#112056=ORIENTED_EDGE ( 'NONE', *, *, #60257, .T. ) ;
#112059=ORIENTED_EDGE ( 'NONE', *, *, #28504, .T. ) ;
#112060=LINE ( 'NONE', #214988, #142714 ) ;
#112078=EDGE_LOOP ( 'NONE', ( #70769, #39690, #86734, #21022, #134422, #50594 ) ) ;
#112096=ORIENTED_EDGE ( 'NONE', *, *, #248543, .F. ) ;
#112113=DIRECTION ( 'NONE',  ( 1.000000000000000000, 7.304098846218135653E-16, 5.100424963727256530E-30 ) ) ;
#112121=CARTESIAN_POINT ( 'NONE',  ( 18.36493879433201570, 85.50000080620250742, -96.10095882417341784 ) ) ;
#112133=EDGE_CURVE ( 'NONE', #154304, #76954, #153996, .T. ) ;
#112148=AXIS2_PLACEMENT_3D ( 'NONE', #101755, #256963, #78367 ) ;
#112162=FACE_OUTER_BOUND ( 'NONE', #238729, .T. ) ;
#112165=ORIENTED_EDGE ( 'NONE', *, *, #181332, .F. ) ;
#112169=CARTESIAN_POINT ( 'NONE',  ( -23.25000000000000000, 87.65000000001222702, -148.2731074845242176 ) ) ;
#112185=FACE_OUTER_BOUND ( 'NONE', #73885, .T. ) ;
#112192=CARTESIAN_POINT ( 'NONE',  ( -20.94999999999999929, 76.00000000001213607, -136.5231074845242745 ) ) ;
#112194=AXIS2_PLACEMENT_3D ( 'NONE', #186552, #64024, #225632 ) ;
#112225=CARTESIAN_POINT ( 'NONE',  ( 20.94999999999999929, 85.00000000001207923, -126.6291383618717816 ) ) ;
#112229=ORIENTED_EDGE ( 'NONE', *, *, #183122, .F. ) ;
#112267=VECTOR ( 'NONE', #120926, 1000.000000000000000 ) ;
#112283=DIRECTION ( 'NONE',  ( 0.000000000000000000, -1.000000000000000000, 0.000000000000000000 ) ) ;
#112291=CARTESIAN_POINT ( 'NONE',  ( 21.05000000000000071, 65.37127968600773897, -128.8581939154367717 ) ) ;
#112297=DIRECTION ( 'NONE',  ( 1.000000000000000000, 0.000000000000000000, 0.000000000000000000 ) ) ;
#112301=FACE_OUTER_BOUND ( 'NONE', #11235, .T. ) ;
#112354=DIRECTION ( 'NONE',  ( 0.000000000000000000, 0.000000000000000000, 1.000000000000000000 ) ) ;
#112357=CIRCLE ( 'NONE', #78986, 0.1000000000000028644 ) ;
#112369=VERTEX_POINT ( 'NONE', #47033 ) ;
#112395=CARTESIAN_POINT ( 'NONE',  ( -22.39999999999999858, 76.10085836911093793, -148.2726746080136877 ) ) ;
#112398=CARTESIAN_POINT ( 'NONE',  ( 18.59999999999999076, 64.35000000001197407, -111.6731074845243796 ) ) ;
#112408=CIRCLE ( 'NONE', #166586, 0.09999999999999939493 ) ;
#112422=ORIENTED_EDGE ( 'NONE', *, *, #246622, .F. ) ;
#112427=ORIENTED_EDGE ( 'NONE', *, *, #39142, .T. ) ;
#112431=CARTESIAN_POINT ( 'NONE',  ( 20.95420533658165141, 65.45413552525251077, -128.9556014638311296 ) ) ;
#112462=CARTESIAN_POINT ( 'NONE',  ( -20.85000000000000142, 77.16412189325305349, -95.30825939895268561 ) ) ;
#112464=ORIENTED_EDGE ( 'NONE', *, *, #110941, .F. ) ;
#112491=EDGE_CURVE ( 'NONE', #130380, #75842, #112616, .T. ) ;
#112523=DIRECTION ( 'NONE',  ( 0.000000000000000000, -1.000000000000000000, -6.860497997771532351E-15 ) ) ;
#112558=DIRECTION ( 'NONE',  ( 1.000000000000000000, 0.000000000000000000, 0.000000000000000000 ) ) ;
#112592=AXIS2_PLACEMENT_3D ( 'NONE', #209656, #230510, #90983 ) ;
#112593=EDGE_LOOP ( 'NONE', ( #120479, #164374, #186435, #124583 ) ) ;
#112599=ORIENTED_EDGE ( 'NONE', *, *, #7343, .T. ) ;
#112616=CIRCLE ( 'NONE', #254071, 0.09999999999999939493 ) ;
#112624=ORIENTED_EDGE ( 'NONE', *, *, #102042, .F. ) ;
#112625=EDGE_CURVE ( 'NONE', #64533, #165923, #243662, .T. ) ;
#112636=CARTESIAN_POINT ( 'NONE',  ( -21.12642695952773764, 69.62434007797698143, -136.6220107677137037 ) ) ;
#112662=CARTESIAN_POINT ( 'NONE',  ( 21.05000000000000071, 65.27628288308592630, -124.3468678833861958 ) ) ;
#112663=CARTESIAN_POINT ( 'NONE',  ( 21.07094088545369814, 75.90110629745997528, -142.8432747064414627 ) ) ;
#112677=ORIENTED_EDGE ( 'NONE', *, *, #30368, .T. ) ;
#112722=DIRECTION ( 'NONE',  ( 0.000000000000000000, 1.000000000000000000, 6.982962677686266711E-15 ) ) ;
#112726=CARTESIAN_POINT ( 'NONE',  ( 18.49999999999999289, 65.79142135624927334, -111.7559501969989668 ) ) ;
#112759=CARTESIAN_POINT ( 'NONE',  ( -21.07928932188134041, 75.90110485435778287, -142.8516241409176075 ) ) ;
#112785=CARTESIAN_POINT ( 'NONE',  ( 21.05000000000000071, 77.84908441863908024, -124.8670969630771594 ) ) ;
#112793=AXIS2_PLACEMENT_3D ( 'NONE', #243808, #182575, #100420 ) ;
#112817=DIRECTION ( 'NONE',  ( 1.000000000000000000, -3.265361837132813093E-16, -2.280189983783949500E-30 ) ) ;
#112837=CARTESIAN_POINT ( 'NONE',  ( 18.59999999999999432, 77.16270174995010223, -128.5231074845242745 ) ) ;
#112847=DIRECTION ( 'NONE',  ( 0.000000000000000000, 6.982962677686266711E-15, -1.000000000000000000 ) ) ;
#112874=FACE_OUTER_BOUND ( 'NONE', #183851, .T. ) ;
#112887=ORIENTED_EDGE ( 'NONE', *, *, #96499, .T. ) ;
#112892=CIRCLE ( 'NONE', #200381, 0.1000000000000028644 ) ;
#112896=AXIS2_PLACEMENT_3D ( 'NONE', #21130, #257090, #238867 ) ;
#112900=CARTESIAN_POINT ( 'NONE',  ( -22.50485643085238863, 76.07878633908943300, -148.2729024236967064 ) ) ;
#112919=ORIENTED_EDGE ( 'NONE', *, *, #4507, .F. ) ;
#112928=EDGE_CURVE ( 'NONE', #207643, #185852, #99961, .T. ) ;
#112938=ORIENTED_EDGE ( 'NONE', *, *, #137034, .F. ) ;
#112942=ADVANCED_FACE ( 'NONE', ( #118281 ), #179551, .F. ) ;
#112951=VECTOR ( 'NONE', #154780, 1000.000000000000000 ) ;
#112961=FACE_OUTER_BOUND ( 'NONE', #120943, .T. ) ;
#112979=VERTEX_POINT ( 'NONE', #62155 ) ;
#112983=CIRCLE ( 'NONE', #133813, 1.899999999999999023 ) ;
#112996=CARTESIAN_POINT ( 'NONE',  ( -20.99780126800948565, 64.39461131213509759, -109.9357549128190641 ) ) ;
#113002=CARTESIAN_POINT ( 'NONE',  ( -18.59999999999999787, 77.26178616857710324, -128.4366085209788366 ) ) ;
#113008=CIRCLE ( 'NONE', #146316, 0.1999999999999987899 ) ;
#113015=EDGE_CURVE ( 'NONE', #230368, #253291, #23049, .T. ) ;
#113034=CARTESIAN_POINT ( 'NONE',  ( 23.14999999999999858, 70.10000000001197407, -113.2422072491807086 ) ) ;
#113037=ADVANCED_FACE ( 'NONE', ( #158713 ), #41330, .F. ) ;
#113064=LINE ( 'NONE', #12706, #44882 ) ;
#113069=CARTESIAN_POINT ( 'NONE',  ( 18.49999999999999645, 77.83534155023646406, -124.9679561919613064 ) ) ;
#113080=EDGE_CURVE ( 'NONE', #19112, #73683, #112983, .T. ) ;
#113099=CYLINDRICAL_SURFACE ( 'NONE', #11110, 0.09999999999999939493 ) ;
#113102=ORIENTED_EDGE ( 'NONE', *, *, #28504, .F. ) ;
#113133=ORIENTED_EDGE ( 'NONE', *, *, #50252, .T. ) ;
#113135=DIRECTION ( 'NONE',  ( 1.000000000000000000, 0.000000000000000000, 0.000000000000000000 ) ) ;
#113151=DIRECTION ( 'NONE',  ( 0.000000000000000000, -0.4999999999999689138, 0.8660254037844565822 ) ) ;
#113178=ORIENTED_EDGE ( 'NONE', *, *, #104890, .T. ) ;
#113179=CARTESIAN_POINT ( 'NONE',  ( 23.15000000000000213, 87.75000000001197975, -115.1731074845242233 ) ) ;
#113199=LINE ( 'NONE', #71532, #210321 ) ;
#113201=ORIENTED_EDGE ( 'NONE', *, *, #193121, .T. ) ;
#113265=CARTESIAN_POINT ( 'NONE',  ( -20.54999999999999716, 76.00000000001205080, -123.5481074845242802 ) ) ;
#113279=DIRECTION ( 'NONE',  ( 0.000000000000000000, 7.086529944415894657E-15, -1.000000000000000000 ) ) ;
#113287=ORIENTED_EDGE ( 'NONE', *, *, #169747, .T. ) ;
#113288=DIRECTION ( 'NONE',  ( 0.000000000000000000, -0.9999631594459057471, 0.008583690987121077309 ) ) ;
#113304=CARTESIAN_POINT ( 'NONE',  ( -22.39999999999999858, 68.20922040163873135, -136.5231074845243313 ) ) ;
#113334=VERTEX_POINT ( 'NONE', #137500 ) ;
#113350=ORIENTED_EDGE ( 'NONE', *, *, #199680, .F. ) ;
#113367=ORIENTED_EDGE ( 'NONE', *, *, #60981, .T. ) ;
#113387=DIRECTION ( 'NONE',  ( -0.000000000000000000, 6.982962677686266711E-15, -1.000000000000000000 ) ) ;
#113397=CARTESIAN_POINT ( 'NONE',  ( 20.04142135623730070, 64.35000000001198828, -115.2731074845243739 ) ) ;
#113400=CYLINDRICAL_SURFACE ( 'NONE', #5655, 0.1000000000000028644 ) ;
#113402=ADVANCED_FACE ( 'NONE', ( #67936 ), #151352, .F. ) ;
#113435=ORIENTED_EDGE ( 'NONE', *, *, #83875, .T. ) ;
#113469=ORIENTED_EDGE ( 'NONE', *, *, #228041, .T. ) ;
#113539=CARTESIAN_POINT ( 'NONE',  ( 23.15000000000000213, 87.75000000001192291, -106.1231074845242262 ) ) ;
#113564=ORIENTED_EDGE ( 'NONE', *, *, #60219, .T. ) ;
#113595=ORIENTED_EDGE ( 'NONE', *, *, #135951, .T. ) ;
#113684=CARTESIAN_POINT ( 'NONE',  ( 18.59999999999999076, 77.85161776048073534, -91.41991776492061206 ) ) ;
#113707=CARTESIAN_POINT ( 'NONE',  ( 22.47809213839789066, 75.96246293238370129, -148.1730808193121049 ) ) ;
#113708=EDGE_CURVE ( 'NONE', #38706, #221411, #125625, .T. ) ;
#113745=CARTESIAN_POINT ( 'NONE',  ( -21.07928932188134041, 69.67148334361884565, -136.6220026301787414 ) ) ;
#113806=DIRECTION ( 'NONE',  ( 0.000000000000000000, -0.9999631594459057471, 0.008583690987121077309 ) ) ;
#113812=FACE_OUTER_BOUND ( 'NONE', #139919, .T. ) ;
#113844=EDGE_CURVE ( 'NONE', #13286, #188914, #109306, .T. ) ;
#113869=DIRECTION ( 'NONE',  ( 0.000000000000000000, 1.000000000000000000, -5.551115123125777653E-14 ) ) ;
#113898=EDGE_LOOP ( 'NONE', ( #114412, #244136, #19706, #49937 ) ) ;
#113928=ORIENTED_EDGE ( 'NONE', *, *, #36772, .F. ) ;
#113936=ORIENTED_EDGE ( 'NONE', *, *, #112928, .F. ) ;
#113964=DIRECTION ( 'NONE',  ( 1.000000000000000000, 0.000000000000000000, 0.000000000000000000 ) ) ;
#113983=CARTESIAN_POINT ( 'NONE',  ( -18.59999999999999787, 64.35000000001198828, -115.1731074845243796 ) ) ;
#114000=CARTESIAN_POINT ( 'NONE',  ( 22.47071067811865319, 76.00000000001213607, -136.5231074845242745 ) ) ;
#114005=EDGE_LOOP ( 'NONE', ( #210186, #5637, #230825 ) ) ;
#114012=FACE_OUTER_BOUND ( 'NONE', #161208, .T. ) ;
#114070=DIRECTION ( 'NONE',  ( -1.000000000000000000, -0.000000000000000000, -0.000000000000000000 ) ) ;
#114085=CARTESIAN_POINT ( 'NONE',  ( -20.94999999999999929, 70.15000000001211333, -126.3906102602463619 ) ) ;
#114092=CARTESIAN_POINT ( 'NONE',  ( 20.94999999999999929, 74.16465844978765176, -124.9679561919613207 ) ) ;
#114107=SPHERICAL_SURFACE ( 'NONE', #218251, 0.1000000000000000056 ) ;
#114115=VERTEX_POINT ( 'NONE', #43907 ) ;
#114129=CIRCLE ( 'NONE', #84874, 0.09999999999998898659 ) ;
#114218=EDGE_LOOP ( 'NONE', ( #96066, #243992, #9792, #42782 ) ) ;
#114237=CARTESIAN_POINT ( 'NONE',  ( -21.14999999999999858, 76.00000000001213607, -136.5231074845242745 ) ) ;
#114245=ORIENTED_EDGE ( 'NONE', *, *, #4367, .F. ) ;
#114315=DIRECTION ( 'NONE',  ( -1.000000000000000000, 0.000000000000000000, 0.000000000000000000 ) ) ;
#114316=CIRCLE ( 'NONE', #180969, 0.3999999999999975797 ) ;
#114336=LINE ( 'NONE', #2065, #15748 ) ;
#114347=LINE ( 'NONE', #32266, #66724 ) ;
#114357=ORIENTED_EDGE ( 'NONE', *, *, #45778, .F. ) ;
#114361=ORIENTED_EDGE ( 'NONE', *, *, #21529, .T. ) ;
#114368=EDGE_LOOP ( 'NONE', ( #208431, #63936, #190963, #115622 ) ) ;
#114378=CARTESIAN_POINT ( 'NONE',  ( 21.05000000000000071, 67.22371710471961137, -127.9644784893834100 ) ) ;
#114393=EDGE_CURVE ( 'NONE', #231702, #162766, #80163, .T. ) ;
#114411=ORIENTED_EDGE ( 'NONE', *, *, #20214, .T. ) ;
#114412=ORIENTED_EDGE ( 'NONE', *, *, #207385, .F. ) ;
#114490=AXIS2_PLACEMENT_3D ( 'NONE', #65763, #243112, #147883 ) ;
#114531=ORIENTED_EDGE ( 'NONE', *, *, #98695, .T. ) ;
#114544=CYLINDRICAL_SURFACE ( 'NONE', #36126, 7.900000000000003908 ) ;
#114545=CYLINDRICAL_SURFACE ( 'NONE', #51978, 0.09999999999999939493 ) ;
#114589=EDGE_LOOP ( 'NONE', ( #167193, #174265, #143335, #6474 ) ) ;
#114647=AXIS2_PLACEMENT_3D ( 'NONE', #67608, #66338, #168042 ) ;
#114663=ORIENTED_EDGE ( 'NONE', *, *, #63221, .F. ) ;
#114666=CARTESIAN_POINT ( 'NONE',  ( -21.05000000000000426, 76.02103547655231353, -142.8275633064719443 ) ) ;
#114673=CIRCLE ( 'NONE', #231218, 0.1999999999999987899 ) ;
#114700=EDGE_CURVE ( 'NONE', #25805, #87941, #220419, .T. ) ;
#114721=ORIENTED_EDGE ( 'NONE', *, *, #151213, .F. ) ;
#114746=ORIENTED_EDGE ( 'NONE', *, *, #12791, .F. ) ;
#114760=EDGE_LOOP ( 'NONE', ( #62272, #28269, #213411, #30557 ) ) ;
#114763=EDGE_LOOP ( 'NONE', ( #254451, #156229, #29545, #130042, #111302, #162113, #106806, #172734, #219482, #164283, #234253, #210480, #117246, #178348, #9103, #185523, #102313, #104807, #106202, #229439, #63407, #40873, #183193 ) ) ;
#114767=AXIS2_PLACEMENT_3D ( 'NONE', #51132, #12060, #190705 ) ;
#114793=CARTESIAN_POINT ( 'NONE',  ( -23.15000000000000213, 76.00000000001190870, -103.0231074845243029 ) ) ;
#114812=DIRECTION ( 'NONE',  ( 0.000000000000000000, -0.9915357197604804940, 0.1298341882520397950 ) ) ;
#114822=DIRECTION ( 'NONE',  ( 1.000000000000000000, 0.000000000000000000, 0.000000000000000000 ) ) ;
#114877=ORIENTED_EDGE ( 'NONE', *, *, #253302, .T. ) ;
#114884=DIRECTION ( 'NONE',  ( 1.000000000000000000, 0.000000000000000000, 0.000000000000000000 ) ) ;
#114896=VERTEX_POINT ( 'NONE', #27385 ) ;
#114928=ADVANCED_FACE ( 'NONE', ( #50721 ), #84429, .T. ) ;
#114949=CIRCLE ( 'NONE', #214898, 0.1000000000000070832 ) ;
#115036=CARTESIAN_POINT ( 'NONE',  ( -20.00857864376270001, 66.65000000001198543, -115.2731074845243597 ) ) ;
#115053=ORIENTED_EDGE ( 'NONE', *, *, #40727, .T. ) ;
#115110=CARTESIAN_POINT ( 'NONE',  ( 21.53752568617689178, 69.21319212550830002, -136.6220819458087306 ) ) ;
#115117=ORIENTED_EDGE ( 'NONE', *, *, #136042, .T. ) ;
#115132=DIRECTION ( 'NONE',  ( 1.000000000000000000, 0.000000000000000000, 0.000000000000000000 ) ) ;
#115141=DIRECTION ( 'NONE',  ( 0.000000000000000000, 0.8660254037844420383, -0.4999999999999941713 ) ) ;
#115156=CARTESIAN_POINT ( 'NONE',  ( 23.15000000000000213, 85.00000000001207923, -126.6291383618717816 ) ) ;
#115162=ADVANCED_FACE ( 'NONE', ( #242213 ), #25063, .F. ) ;
#115165=VECTOR ( 'NONE', #185610, 1000.000000000000000 ) ;
#115195=DIRECTION ( 'NONE',  ( 0.000000000000000000, 0.8700118002898357128, -0.4930308989875170633 ) ) ;
#115196=FACE_OUTER_BOUND ( 'NONE', #47934, .T. ) ;
#115198=LINE ( 'NONE', #154371, #111249 ) ;
#115204=AXIS2_PLACEMENT_3D ( 'NONE', #237588, #219293, #198450 ) ;
#115223=DIRECTION ( 'NONE',  ( 0.000000000000000000, -6.308085367188367561E-15, 1.000000000000000000 ) ) ;
#115234=AXIS2_PLACEMENT_3D ( 'NONE', #229900, #109941, #129519 ) ;
#115243=DIRECTION ( 'NONE',  ( 0.000000000000000000, 0.000000000000000000, 1.000000000000000000 ) ) ;
#115256=DIRECTION ( 'NONE',  ( 0.000000000000000000, 1.000000000000000000, 6.982962677686266711E-15 ) ) ;
#115278=LINE ( 'NONE', #190995, #221776 ) ;
#115292=DIRECTION ( 'NONE',  ( 0.000000000000000000, -8.987377189994711700E-15, 1.000000000000000000 ) ) ;
#115314=CARTESIAN_POINT ( 'NONE',  ( -21.07971444708686093, 75.91217656369435929, -142.8528995661508532 ) ) ;
#115350=CIRCLE ( 'NONE', #106976, 0.1000000000000028644 ) ;
#115353=CARTESIAN_POINT ( 'NONE',  ( 18.49999999999999289, 64.35000000001221565, -148.2731074845243882 ) ) ;
#115421=DIRECTION ( 'NONE',  ( 0.000000000000000000, -7.429790795770652649E-15, 1.000000000000000000 ) ) ;
#115425=DIRECTION ( 'NONE',  ( 1.000000000000000000, 0.000000000000000000, 0.000000000000000000 ) ) ;
#115435=CARTESIAN_POINT ( 'NONE',  ( -21.04999999999999716, 85.60000000001210196, -129.4910380878245633 ) ) ;
#115440=CARTESIAN_POINT ( 'NONE',  ( 20.94999999999999574, 77.73625713160946304, -124.9544551555067926 ) ) ;
#115446=CIRCLE ( 'NONE', #111359, 0.1000000000000064587 ) ;
#115480=FACE_OUTER_BOUND ( 'NONE', #218648, .T. ) ;
#115493=ORIENTED_EDGE ( 'NONE', *, *, #41723, .F. ) ;
#115498=DIRECTION ( 'NONE',  ( 1.000000000000000000, 0.000000000000000000, 0.000000000000000000 ) ) ;
#115528=CIRCLE ( 'NONE', #36468, 0.1000000000000046685 ) ;
#115545=B_SPLINE_CURVE_WITH_KNOTS ( 'NONE', 3,
 ( #221617, #132480, #128638, #33418, #229021, #252402, #188590, #54212 ),
 .UNSPECIFIED., .F., .F.,
 ( 4, 2, 2, 4 ),
 ( 0.000000000000000000, 0.0001306511400391407042, 0.0001959767100587063806, 0.0002613022800782720300 ),
 .UNSPECIFIED. ) ;
#115548=CARTESIAN_POINT ( 'NONE',  ( -20.85000000106584750, 64.25000000001195133, -109.8676028280505790 ) ) ;
#115556=ORIENTED_EDGE ( 'NONE', *, *, #178987, .F. ) ;
#115561=ORIENTED_EDGE ( 'NONE', *, *, #201541, .T. ) ;
#115607=( BOUNDED_CURVE ( )  B_SPLINE_CURVE ( 3, ( #38771, #118311, #197827, #19200 ),
 .UNSPECIFIED., .F., .F. ) 
 B_SPLINE_CURVE_WITH_KNOTS ( ( 4, 4 ),
 ( 3.141592653589791784, 4.712388980384628390 ),
 .UNSPECIFIED. ) 
 CURVE ( )  GEOMETRIC_REPRESENTATION_ITEM ( )  RATIONAL_B_SPLINE_CURVE ( ( 1.000000000000000000, 0.8047378541243791483, 0.8047378541243791483, 1.000000000000000000 ) ) 
 REPRESENTATION_ITEM ( '' )  );
#115622=ORIENTED_EDGE ( 'NONE', *, *, #191504, .F. ) ;
#115625=DIRECTION ( 'NONE',  ( 0.7071359030028288029, 0.000000000000000000, 0.7070776581708504427 ) ) ;
#115635=DIRECTION ( 'NONE',  ( -0.000000000000000000, -1.000000000000000000, -8.609265936414532828E-15 ) ) ;
#115701=CARTESIAN_POINT ( 'NONE',  ( 19.88284271247461987, 64.30857864377466626, -111.7731074845243739 ) ) ;
#115727=DIRECTION ( 'NONE',  ( 0.000000000000000000, -6.530723674265620862E-15, 1.000000000000000000 ) ) ;
#115757=DIRECTION ( 'NONE',  ( 0.000000000000000000, 7.026728003956683390E-15, -1.000000000000000000 ) ) ;
#115764=CARTESIAN_POINT ( 'NONE',  ( -18.59999999999999787, 66.65000000001205649, -124.1731074845243654 ) ) ;
#115802=CARTESIAN_POINT ( 'NONE',  ( -23.25000000000000000, 76.00000000001185185, -95.12310748452429721 ) ) ;
#115843=EDGE_CURVE ( 'NONE', #8334, #216369, #182616, .T. ) ;
#115865=DIRECTION ( 'NONE',  ( -1.000000000000000000, -0.000000000000000000, -0.000000000000000000 ) ) ;
#115930=ORIENTED_EDGE ( 'NONE', *, *, #84122, .T. ) ;
#115956=VERTEX_POINT ( 'NONE', #135445 ) ;
#115958=ORIENTED_EDGE ( 'NONE', *, *, #180082, .F. ) ;
#115968=EDGE_CURVE ( 'NONE', #185096, #17682, #112060, .T. ) ;
#115988=CARTESIAN_POINT ( 'NONE',  ( -23.25000000000000000, 76.00000000001213607, -136.5231074845242745 ) ) ;
#116009=DIRECTION ( 'NONE',  ( 0.000000000000000000, 0.000000000000000000, 1.000000000000000000 ) ) ;
#116055=DIRECTION ( 'NONE',  ( 0.000000000000000000, 0.000000000000000000, -1.000000000000000000 ) ) ;
#116058=VERTEX_POINT ( 'NONE', #74241 ) ;
#116076=CYLINDRICAL_SURFACE ( 'NONE', #18133, 0.09999999999998898659 ) ;
#116079=DIRECTION ( 'NONE',  ( 0.000000000000000000, -6.352154140967427193E-15, 1.000000000000000000 ) ) ;
#116108=ORIENTED_EDGE ( 'NONE', *, *, #69145, .F. ) ;
#116111=DIRECTION ( 'NONE',  ( 1.000000000000000000, -2.952720810173289112E-16, -2.061873921506763405E-30 ) ) ;
#116151=AXIS2_PLACEMENT_3D ( 'NONE', #93104, #252172, #115243 ) ;
#116174=CARTESIAN_POINT ( 'NONE',  ( 18.59999999999999076, 69.45000000001199680, -115.3731074845243398 ) ) ;
#116191=EDGE_LOOP ( 'NONE', ( #16565, #117164, #132714, #138847 ) ) ;
#116206=ORIENTED_EDGE ( 'NONE', *, *, #31808, .T. ) ;
#116263=CARTESIAN_POINT ( 'NONE',  ( 23.14999999999999858, 70.50000000001205080, -124.1178414656112352 ) ) ;
#116276=DIRECTION ( 'NONE',  ( 0.000000000000000000, 6.938893903907222067E-15, -1.000000000000000000 ) ) ;
#116284=DIRECTION ( 'NONE',  ( 1.000000000000000000, 7.304098846218105085E-16, 4.217023435051676515E-16 ) ) ;
#116296=CARTESIAN_POINT ( 'NONE',  ( 21.05000000000000071, 76.10000000001215881, -143.0001538663141503 ) ) ;
#116302=EDGE_LOOP ( 'NONE', ( #166533, #56922, #84421, #113102 ) ) ;
#116326=ADVANCED_FACE ( 'NONE', ( #6201 ), #229117, .F. ) ;
#116367=CARTESIAN_POINT ( 'NONE',  ( 20.99142135623731065, 64.40000000001194280, -109.9513107147998880 ) ) ;
#116409=DIRECTION ( 'NONE',  ( 1.000000000000000000, -0.000000000000000000, 0.000000000000000000 ) ) ;
#116425=EDGE_CURVE ( 'NONE', #234281, #139747, #30511, .T. ) ;
#116451=ORIENTED_EDGE ( 'NONE', *, *, #87919, .F. ) ;
#116465=DIRECTION ( 'NONE',  ( 1.000000000000000000, 0.000000000000000000, 0.000000000000000000 ) ) ;
#116474=ORIENTED_EDGE ( 'NONE', *, *, #109828, .F. ) ;
#116478=CARTESIAN_POINT ( 'NONE',  ( -23.15000000000000213, 76.00000000001190870, -103.0231074845243029 ) ) ;
#116487=CARTESIAN_POINT ( 'NONE',  ( -22.01447462590973103, 68.73619979878222352, -136.6221444845839130 ) ) ;
#116490=AXIS2_PLACEMENT_3D ( 'NONE', #157533, #55779, #180907 ) ;
#116516=ORIENTED_EDGE ( 'NONE', *, *, #198057, .F. ) ;
#116519=CIRCLE ( 'NONE', #49868, 12.97499999999999964 ) ;
#116574=AXIS2_PLACEMENT_3D ( 'NONE', #121860, #20192, #222203 ) ;
#116577=B_SPLINE_CURVE_WITH_KNOTS ( 'NONE', 3,
 ( #169864, #66863, #145099, #224638, #51123, #146373, #248064, #49858 ),
 .UNSPECIFIED., .F., .F.,
 ( 4, 2, 2, 4 ),
 ( 0.000000000000000000, 0.0001049670497869988235, 0.0002099340995739976470, 0.0004198681991479772963 ),
 .UNSPECIFIED. ) ;
#116578=AXIS2_PLACEMENT_3D ( 'NONE', #196728, #160205, #239720 ) ;
#116602=CYLINDRICAL_SURFACE ( 'NONE', #38134, 0.09999999999998898659 ) ;
#116611=DIRECTION ( 'NONE',  ( 0.000000000000000000, -0.8700118002898357128, 0.4930308989875170633 ) ) ;
#116631=CARTESIAN_POINT ( 'NONE',  ( 21.05000000000000071, 70.60000000001200249, -115.4283735034374274 ) ) ;
#116658=CARTESIAN_POINT ( 'NONE',  ( -22.39999999999999858, 76.00000000001219291, -144.3138870828977076 ) ) ;
#116698=EDGE_CURVE ( 'NONE', #1820, #257983, #164979, .T. ) ;
#116699=DIRECTION ( 'NONE',  ( 0.000000000000000000, -0.8660254037844343777, 0.5000000000000074385 ) ) ;
#116719=CARTESIAN_POINT ( 'NONE',  ( 20.94999999999999929, 71.00000000001205080, -124.1178414656112352 ) ) ;
#116773=CARTESIAN_POINT ( 'NONE',  ( -20.64999999999999858, 76.00000000001199396, -115.8981074845243029 ) ) ;
#116782=DIRECTION ( 'NONE',  ( -1.000000000000000000, 0.000000000000000000, 0.000000000000000000 ) ) ;
#116787=EDGE_CURVE ( 'NONE', #74814, #132343, #197266, .T. ) ;
#116838=AXIS2_PLACEMENT_3D ( 'NONE', #80396, #158722, #238216 ) ;
#116841=CARTESIAN_POINT ( 'NONE',  ( -21.05000000000000071, 64.25000000001195133, -110.0379132551783243 ) ) ;
#116850=CARTESIAN_POINT ( 'NONE',  ( 21.14999999999999503, 87.65000000001221281, -148.2731074845242176 ) ) ;
#116931=CARTESIAN_POINT ( 'NONE',  ( 20.85000000000000142, 77.14957036958755054, -95.20719500002232394 ) ) ;
#116939=ORIENTED_EDGE ( 'NONE', *, *, #248792, .T. ) ;
#116969=ORIENTED_EDGE ( 'NONE', *, *, #173557, .F. ) ;
#116970=ORIENTED_EDGE ( 'NONE', *, *, #26286, .F. ) ;
#116977=LINE ( 'NONE', #196499, #50964 ) ;
#116978=EDGE_LOOP ( 'NONE', ( #118943, #253141, #17455, #41914 ) ) ;
#117030=VECTOR ( 'NONE', #129535, 999.9999999999998863 ) ;
#117082=CARTESIAN_POINT ( 'NONE',  ( -18.50000000000000711, 64.25000000001210765, -129.5083017138703667 ) ) ;
#117084=ORIENTED_EDGE ( 'NONE', *, *, #50270, .T. ) ;
#117086=CARTESIAN_POINT ( 'NONE',  ( 21.05000000000000071, 67.22371710471958295, -124.3731074845243683 ) ) ;
#117097=EDGE_LOOP ( 'NONE', ( #73559, #69905, #164148, #18110, #84000, #185567, #139367, #249559, #72393, #243432, #67776, #50795, #115561, #253097 ) ) ;
#117103=CARTESIAN_POINT ( 'NONE',  ( 23.25000000000000000, 87.75000000001222134, -148.2731074845242176 ) ) ;
#117113=DIRECTION ( 'NONE',  ( 0.000000000000000000, -6.982962677686266711E-15, 1.000000000000000000 ) ) ;
#117122=CARTESIAN_POINT ( 'NONE',  ( -22.49231231312463208, 64.35001509633487160, -136.5841603721257513 ) ) ;
#117131=DIRECTION ( 'NONE',  ( -1.000000000000000000, 0.000000000000000000, 0.000000000000000000 ) ) ;
#117137=ORIENTED_EDGE ( 'NONE', *, *, #88066, .T. ) ;
#117164=ORIENTED_EDGE ( 'NONE', *, *, #136335, .F. ) ;
#117178=SPHERICAL_SURFACE ( 'NONE', #164034, 0.1000000000000000056 ) ;
#117202=ORIENTED_EDGE ( 'NONE', *, *, #109828, .T. ) ;
#117205=ORIENTED_EDGE ( 'NONE', *, *, #91827, .T. ) ;
#117245=LINE ( 'NONE', #101477, #146744 ) ;
#117246=ORIENTED_EDGE ( 'NONE', *, *, #134080, .T. ) ;
#117284=DIRECTION ( 'NONE',  ( 0.000000000000000000, -6.982962677686266711E-15, 1.000000000000000000 ) ) ;
#117292=DIRECTION ( 'NONE',  ( -1.000000000000000000, 0.000000000000000000, -0.000000000000000000 ) ) ;
#117317=ORIENTED_EDGE ( 'NONE', *, *, #3683, .F. ) ;
#117324=FACE_OUTER_BOUND ( 'NONE', #21412, .T. ) ;
#117334=CARTESIAN_POINT ( 'NONE',  ( -21.05000000000000071, 74.25000000001205080, -124.8535959266226598 ) ) ;
#117404=DIRECTION ( 'NONE',  ( 1.000000000000000000, 0.000000000000000000, 0.000000000000000000 ) ) ;
#117406=ORIENTED_EDGE ( 'NONE', *, *, #127185, .T. ) ;
#117412=CARTESIAN_POINT ( 'NONE',  ( 21.05000000000000071, 71.18691588786253988, -124.5815897280005089 ) ) ;
#117418=CARTESIAN_POINT ( 'NONE',  ( 20.94999999999999929, 76.00000000001190870, -103.0231074845243029 ) ) ;
#117432=ORIENTED_EDGE ( 'NONE', *, *, #106220, .T. ) ;
#117434=DIRECTION ( 'NONE',  ( 1.000000000000000000, 0.000000000000000000, 0.000000000000000000 ) ) ;
#117474=AXIS2_PLACEMENT_3D ( 'NONE', #64026, #223090, #44477 ) ;
#117475=CARTESIAN_POINT ( 'NONE',  ( 18.49999999999999645, 74.27191306321776665, -149.6386724793565577 ) ) ;
#117499=ORIENTED_EDGE ( 'NONE', *, *, #136756, .F. ) ;
#117503=EDGE_CURVE ( 'NONE', #236918, #111107, #172733, .T. ) ;
#117525=LINE ( 'NONE', #159240, #20119 ) ;
#117577=FACE_OUTER_BOUND ( 'NONE', #176186, .T. ) ;
#117599=EDGE_CURVE ( 'NONE', #102921, #213545, #114347, .T. ) ;
#117609=CIRCLE ( 'NONE', #146613, 0.1000000000000043771 ) ;
#117612=AXIS2_PLACEMENT_3D ( 'NONE', #180837, #223789, #222493 ) ;
#117627=CARTESIAN_POINT ( 'NONE',  ( -18.51024323315077424, 65.68895814178239334, -97.50265578621379348 ) ) ;
#117663=CARTESIAN_POINT ( 'NONE',  ( 21.00000000000000000, 66.25000000001199396, -115.3731074845243683 ) ) ;
#117683=ADVANCED_FACE ( 'NONE', ( #196435 ), #20960, .F. ) ;
#117705=VERTEX_POINT ( 'NONE', #97306 ) ;
#117715=ADVANCED_FACE ( 'NONE', ( #192601 ), #13973, .T. ) ;
#117753=DIRECTION ( 'NONE',  ( 0.000000000000000000, -6.982962677686267499E-15, 1.000000000000000000 ) ) ;
#117757=CARTESIAN_POINT ( 'NONE',  ( -18.50000000000000355, 85.40000000001207070, -129.2258477248609552 ) ) ;
#117792=DIRECTION ( 'NONE',  ( 1.000000000000000000, 0.000000000000000000, 0.000000000000000000 ) ) ;
#117794=DIRECTION ( 'NONE',  ( 0.000000000000000000, 0.000000000000000000, 1.000000000000000000 ) ) ;
#117798=CARTESIAN_POINT ( 'NONE',  ( 18.52165635395186172, 85.48115071129440423, -129.4982699016618994 ) ) ;
#117808=ORIENTED_EDGE ( 'NONE', *, *, #82074, .T. ) ;
#117840=DIRECTION ( 'NONE',  ( -1.000000000000000000, 0.000000000000000000, 0.000000000000000000 ) ) ;
#117852=DIRECTION ( 'NONE',  ( 0.000000000000000000, 1.000000000000000000, 6.982962677686266711E-15 ) ) ;
#117864=DIRECTION ( 'NONE',  ( 0.000000000000000000, -7.086529944415894657E-15, 1.000000000000000000 ) ) ;
#117940=CYLINDRICAL_SURFACE ( 'NONE', #36071, 11.74999999999999645 ) ;
#117950=CARTESIAN_POINT ( 'NONE',  ( -20.54999999999999716, 74.05981308412415842, -115.8522266955776416 ) ) ;
#117969=AXIS2_PLACEMENT_3D ( 'NONE', #166103, #209045, #111230 ) ;
#117980=PLANE ( 'NONE',  #13561 ) ;
#117981=DIRECTION ( 'NONE',  ( 0.000000000000000000, 6.608470384673558123E-15, -1.000000000000000000 ) ) ;
#117985=DIRECTION ( 'NONE',  ( 0.000000000000000000, 6.982962677686266711E-15, -1.000000000000000000 ) ) ;
#118006=EDGE_LOOP ( 'NONE', ( #233620, #141068, #71152, #88047 ) ) ;
#118034=EDGE_CURVE ( 'NONE', #95961, #235551, #43365, .T. ) ;
#118082=ORIENTED_EDGE ( 'NONE', *, *, #50010, .T. ) ;
#118141=FACE_OUTER_BOUND ( 'NONE', #45392, .T. ) ;
#118158=EDGE_LOOP ( 'NONE', ( #46677, #256358, #142502, #184408, #188849 ) ) ;
#118159=EDGE_CURVE ( 'NONE', #139066, #31859, #30226, .T. ) ;
#118215=TOROIDAL_SURFACE ( 'NONE', #51535, 3.899999999999999467, 0.1000000000000000056 ) ;
#118236=ADVANCED_FACE ( 'NONE', ( #211196 ), #148413, .T. ) ;
#118239=DIRECTION ( 'NONE',  ( 1.000000000000000000, 0.000000000000000000, 0.000000000000000000 ) ) ;
#118271=CARTESIAN_POINT ( 'NONE',  ( 19.97071067811864609, 64.27928932189330169, -111.8731074845243825 ) ) ;
#118281=FACE_OUTER_BOUND ( 'NONE', #167070, .T. ) ;
#118290=ORIENTED_EDGE ( 'NONE', *, *, #9305, .F. ) ;
#118299=ORIENTED_EDGE ( 'NONE', *, *, #79105, .F. ) ;
#118300=DIRECTION ( 'NONE',  ( 0.000000000000000000, -1.000000000000000000, -6.982962677686265922E-15 ) ) ;
#118308=( BOUNDED_SURFACE ( )  B_SPLINE_SURFACE ( 3, 2, ( 
 ( #122949, #82494, #182931 ),
 ( #242882, #198614, #202480 ),
 ( #39586, #119093, #162086 ),
 ( #241601, #120411, #163359 ),
 ( #85057, #159512, #25145 ),
 ( #20006, #223304, #164643 ) ),
 .UNSPECIFIED., .F., .F., .T. ) 
 B_SPLINE_SURFACE_WITH_KNOTS ( ( 4, 2, 4 ),
 ( 3, 3 ),
 ( 0.0001792624049599557520, 0.0003686986002124449983, 0.0005581347954649342174 ),
 ( 0.000000000000000000, 1.000000000000000000 ),
 .UNSPECIFIED. ) 
 GEOMETRIC_REPRESENTATION_ITEM ( )  RATIONAL_B_SPLINE_SURFACE ( (
 ( 1.000000000000000000, 0.9238795325112856283, 1.000000000000000000),
 ( 1.000000000000000000, 0.9229318695239514536, 1.000000000000000000),
 ( 1.000000000000000000, 0.8926288119229253137, 1.000000000000000000),
 ( 1.000000000000000000, 0.8123777807272960505, 1.000000000000000000),
 ( 1.000000000000000000, 0.7629087100930475041, 1.000000000000000000),
 ( 1.000000000000000000, 0.7071067811865475727, 1.000000000000000000) ) ) 
 REPRESENTATION_ITEM ( '' )  SURFACE ( )  );
#118311=CARTESIAN_POINT ( 'NONE',  ( -20.93284271247462414, 64.25000000001196554, -110.0379132551783243 ) ) ;
#118313=CARTESIAN_POINT ( 'NONE',  ( -23.15000000000000213, 76.00000000001190870, -103.0231074845243029 ) ) ;
#118318=ORIENTED_EDGE ( 'NONE', *, *, #147899, .F. ) ;
#118332=CARTESIAN_POINT ( 'NONE',  ( -23.25000000000000000, 76.00000000001213607, -136.5231074845242745 ) ) ;
#118355=DIRECTION ( 'NONE',  ( -4.336808689942052446E-15, 0.8660254037844445918, 0.4999999999999896194 ) ) ;
#118366=ORIENTED_EDGE ( 'NONE', *, *, #11028, .F. ) ;
#118371=DIRECTION ( 'NONE',  ( 1.000000000000000000, 0.000000000000000000, 0.000000000000000000 ) ) ;
#118389=ORIENTED_EDGE ( 'NONE', *, *, #65338, .F. ) ;
#118403=EDGE_LOOP ( 'NONE', ( #254368, #48938, #242614, #28589 ) ) ;
#118432=DIRECTION ( 'NONE',  ( 0.000000000000000000, -6.938893903907222067E-15, 1.000000000000000000 ) ) ;
#118451=DIRECTION ( 'NONE',  ( 4.377807931758639578E-15, -0.2605042016806606298, -0.9654727137038736640 ) ) ;
#118472=CARTESIAN_POINT ( 'NONE',  ( -18.59999999999999787, 77.16270174995010223, -128.4231074845242802 ) ) ;
#118483=ORIENTED_EDGE ( 'NONE', *, *, #19334, .F. ) ;
#118494=AXIS2_PLACEMENT_3D ( 'NONE', #131193, #171651, #210740 ) ;
#118504=ORIENTED_EDGE ( 'NONE', *, *, #192322, .T. ) ;
#118522=CARTESIAN_POINT ( 'NONE',  ( 20.94999999999999929, 76.00000000001205080, -123.6481074845242887 ) ) ;
#118560=CARTESIAN_POINT ( 'NONE',  ( 18.50000000000000000, 85.40000000001185754, -96.14106563635155567 ) ) ;
#118594=CARTESIAN_POINT ( 'NONE',  ( 21.05000000000000071, 67.22371710471958295, -124.3731074845243683 ) ) ;
#118615=ORIENTED_EDGE ( 'NONE', *, *, #198057, .T. ) ;
#118618=DIRECTION ( 'NONE',  ( 1.000000000000000000, -2.952720810173289112E-16, -2.061873921506763405E-30 ) ) ;
#118619=ADVANCED_FACE ( 'NONE', ( #114012 ), #159581, .F. ) ;
#118637=ADVANCED_FACE ( 'NONE', ( #26500 ), #183006, .T. ) ;
#118642=CIRCLE ( 'NONE', #6168, 0.1000000000000028644 ) ;
#118650=AXIS2_PLACEMENT_3D ( 'NONE', #146148, #125318, #107015 ) ;
#118663=DIRECTION ( 'NONE',  ( 0.000000000000000000, -1.000000000000000000, -6.982962677686265922E-15 ) ) ;
#118676=DIRECTION ( 'NONE',  ( -0.000000000000000000, -6.982962677686266711E-15, 1.000000000000000000 ) ) ;
#118678=ORIENTED_EDGE ( 'NONE', *, *, #185744, .T. ) ;
#118685=AXIS2_PLACEMENT_3D ( 'NONE', #24120, #103604, #183185 ) ;
#118688=AXIS2_PLACEMENT_3D ( 'NONE', #84846, #168327, #6627 ) ;
#118708=EDGE_LOOP ( 'NONE', ( #140696, #16966, #105036, #209038 ) ) ;
#118716=CARTESIAN_POINT ( 'NONE',  ( 21.05000000000000071, 65.57661458509917907, -129.0310555606542664 ) ) ;
#118755=VERTEX_POINT ( 'NONE', #25220 ) ;
#118759=CARTESIAN_POINT ( 'NONE',  ( -21.05000000000000071, 77.83534155023646406, -124.8679561919613121 ) ) ;
#118771=CYLINDRICAL_SURFACE ( 'NONE', #178522, 0.1000000000000028644 ) ;
#118807=DIRECTION ( 'NONE',  ( 0.000000000000000000, 6.982962677686266711E-15, -1.000000000000000000 ) ) ;
#118815=DIRECTION ( 'NONE',  ( -1.000000000000000000, -0.000000000000000000, -0.000000000000000000 ) ) ;
#118828=CIRCLE ( 'NONE', #223037, 0.09999999999999939493 ) ;
#118833=EDGE_CURVE ( 'NONE', #49212, #235424, #228550, .T. ) ;
#118871=AXIS2_PLACEMENT_3D ( 'NONE', #18192, #217645, #61166 ) ;
#118913=TOROIDAL_SURFACE ( 'NONE', #89649, 11.65000000000000036, 0.1000000000000000056 ) ;
#118915=VERTEX_POINT ( 'NONE', #212839 ) ;
#118938=CYLINDRICAL_SURFACE ( 'NONE', #189682, 0.09999999999999939493 ) ;
#118943=ORIENTED_EDGE ( 'NONE', *, *, #79782, .T. ) ;
#118966=CYLINDRICAL_SURFACE ( 'NONE', #86368, 0.1000000000000028644 ) ;
#118981=CARTESIAN_POINT ( 'NONE',  ( 23.24999999999999645, 70.40000000001199965, -115.4283735034374274 ) ) ;
#118988=ORIENTED_EDGE ( 'NONE', *, *, #229821, .T. ) ;
#119005=DIRECTION ( 'NONE',  ( -3.787827842127534447E-15, -0.7397360091702729346, -0.6728971962616859814 ) ) ;
#119010=ORIENTED_EDGE ( 'NONE', *, *, #153326, .T. ) ;
#119017=ORIENTED_EDGE ( 'NONE', *, *, #176655, .T. ) ;
#119034=CARTESIAN_POINT ( 'NONE',  ( 23.24999999999999289, 69.55000000001206217, -124.1731074845243370 ) ) ;
#119042=CYLINDRICAL_SURFACE ( 'NONE', #44523, 0.09999999999999939493 ) ;
#119058=CARTESIAN_POINT ( 'NONE',  ( -18.54159361262947314, 85.46313213550527621, -129.4739852682314449 ) ) ;
#119061=ADVANCED_FACE ( 'NONE', ( #1474 ), #144831, .F. ) ;
#119074=AXIS2_PLACEMENT_3D ( 'NONE', #150938, #68846, #209624 ) ;
#119092=ORIENTED_EDGE ( 'NONE', *, *, #122709, .F. ) ;
#119093=CARTESIAN_POINT ( 'NONE',  ( 21.05000000000000071, 69.65564095796861466, -136.5379631194182650 ) ) ;
#119117=FACE_OUTER_BOUND ( 'NONE', #153408, .T. ) ;
#119122=AXIS2_PLACEMENT_3D ( 'NONE', #165982, #167270, #25181 ) ;
#119179=CIRCLE ( 'NONE', #177657, 11.64999999999999325 ) ;
#119197=CIRCLE ( 'NONE', #110809, 4.049999999999998046 ) ;
#119217=AXIS2_PLACEMENT_3D ( 'NONE', #185775, #9697, #168828 ) ;
#119230=CARTESIAN_POINT ( 'NONE',  ( 21.07928932188134397, 75.90110485435755550, -142.8516241409230076 ) ) ;
#119235=DIRECTION ( 'NONE',  ( 0.000000000000000000, -6.982962677686267499E-15, 1.000000000000000000 ) ) ;
#119243=CIRCLE ( 'NONE', #44232, 0.09999999999998898659 ) ;
#119250=CARTESIAN_POINT ( 'NONE',  ( -23.25000000000000000, 77.16412189325305349, -95.10825939895268277 ) ) ;
#119251=DIRECTION ( 'NONE',  ( 0.000000000000000000, 6.982962677686266711E-15, -1.000000000000000000 ) ) ;
#119259=ADVANCED_FACE ( 'NONE', ( #138104 ), #37764, .T. ) ;
#119283=CIRCLE ( 'NONE', #206749, 0.09999999999998898659 ) ;
#119304=ORIENTED_EDGE ( 'NONE', *, *, #3317, .T. ) ;
#119307=CARTESIAN_POINT ( 'NONE',  ( -21.05000000000000071, 75.74389420791992222, -136.5580039261965908 ) ) ;
#119340=EDGE_CURVE ( 'NONE', #11251, #140147, #71004, .T. ) ;
#119341=AXIS2_PLACEMENT_3D ( 'NONE', #154966, #93678, #15445 ) ;
#119344=CARTESIAN_POINT ( 'NONE',  ( -23.15000000000000213, 85.00000000001207923, -126.6291383618717816 ) ) ;
#119360=EDGE_CURVE ( 'NONE', #155283, #133238, #129419, .T. ) ;
#119361=VERTEX_POINT ( 'NONE', #98962 ) ;
#119375=ORIENTED_EDGE ( 'NONE', *, *, #108700, .F. ) ;
#119377=CARTESIAN_POINT ( 'NONE',  ( 18.49999999999999645, 77.16270174995010223, -128.4231074845242802 ) ) ;
#119378=CIRCLE ( 'NONE', #194234, 4.049999999999998046 ) ;
#119393=AXIS2_PLACEMENT_3D ( 'NONE', #34236, #194592, #175051 ) ;
#119413=VECTOR ( 'NONE', #210051, 1000.000000000000000 ) ;
#119424=EDGE_CURVE ( 'NONE', #157942, #66650, #59250, .T. ) ;
#119438=DIRECTION ( 'NONE',  ( 0.000000000000000000, 6.982962677686266711E-15, -1.000000000000000000 ) ) ;
#119462=CARTESIAN_POINT ( 'NONE',  ( -21.07954763557471267, 75.93412408139377590, -142.8523984745623636 ) ) ;
#119466=CARTESIAN_POINT ( 'NONE',  ( 21.05000000000000071, 76.00000000001213607, -136.5231074845242745 ) ) ;
#119474=ORIENTED_EDGE ( 'NONE', *, *, #203677, .F. ) ;
#119477=ORIENTED_EDGE ( 'NONE', *, *, #250955, .T. ) ;
#119480=ORIENTED_EDGE ( 'NONE', *, *, #1930, .T. ) ;
#119507=EDGE_CURVE ( 'NONE', #114896, #4010, #154582, .T. ) ;
#119529=ORIENTED_EDGE ( 'NONE', *, *, #46488, .T. ) ;
#119534=VERTEX_POINT ( 'NONE', #184951 ) ;
#119546=CYLINDRICAL_SURFACE ( 'NONE', #49822, 11.74999999999999645 ) ;
#119569=CARTESIAN_POINT ( 'NONE',  ( -20.94999999999999929, 74.16465844978765176, -124.9679561919613207 ) ) ;
#119574=EDGE_CURVE ( 'NONE', #76926, #220426, #131646, .T. ) ;
#119577=DIRECTION ( 'NONE',  ( 1.000000000000000000, 0.000000000000000000, 0.000000000000000000 ) ) ;
#119626=DIRECTION ( 'NONE',  ( 0.000000000000000000, 0.000000000000000000, 1.000000000000000000 ) ) ;
#119635=TOROIDAL_SURFACE ( 'NONE', #236143, 12.77499999999999858, 0.1000000000000000056 ) ;
#119657=ORIENTED_EDGE ( 'NONE', *, *, #21652, .F. ) ;
#119668=ORIENTED_EDGE ( 'NONE', *, *, #215531, .F. ) ;
#119677=DIRECTION ( 'NONE',  ( -1.000000000000000000, 2.952720810173289112E-16, 2.061873921506763405E-30 ) ) ;
#119678=CARTESIAN_POINT ( 'NONE',  ( 21.05000000000000071, 76.10000000001218723, -143.0637644362255401 ) ) ;
#119705=CARTESIAN_POINT ( 'NONE',  ( -20.54999999999999716, 74.05981308412420105, -123.6939882734709926 ) ) ;
#119719=AXIS2_PLACEMENT_3D ( 'NONE', #190366, #13018, #10433 ) ;
#119724=CIRCLE ( 'NONE', #7265, 0.09999999999998712696 ) ;
#119743=EDGE_LOOP ( 'NONE', ( #10996, #228486, #187069, #94102 ) ) ;
#119744=ADVANCED_FACE ( 'NONE', ( #195251 ), #153580, .T. ) ;
#119745=EDGE_CURVE ( 'NONE', #3082, #243260, #193951, .T. ) ;
#119752=LINE ( 'NONE', #137990, #138853 ) ;
#119775=ORIENTED_EDGE ( 'NONE', *, *, #221841, .T. ) ;
#119778=AXIS2_PLACEMENT_3D ( 'NONE', #16918, #56000, #155169 ) ;
#119790=ORIENTED_EDGE ( 'NONE', *, *, #122973, .F. ) ;
#119801=CARTESIAN_POINT ( 'NONE',  ( 23.15000000000000213, 85.00000000001207923, -126.6291383618717816 ) ) ;
#119854=ORIENTED_EDGE ( 'NONE', *, *, #48330, .F. ) ;
#119885=CARTESIAN_POINT ( 'NONE',  ( 20.85000000000000142, 76.00000000001190870, -103.0231074845243029 ) ) ;
#119907=FACE_OUTER_BOUND ( 'NONE', #195770, .T. ) ;
#119912=CARTESIAN_POINT ( 'NONE',  ( 18.46858270002953262, 85.47420267472266175, -129.4210855498203614 ) ) ;
#119940=CARTESIAN_POINT ( 'NONE',  ( -22.50000000000000000, 75.90000000001222702, -148.1726782920690937 ) ) ;
#119946=AXIS2_PLACEMENT_3D ( 'NONE', #82643, #146486, #223458 ) ;
#119960=DIRECTION ( 'NONE',  ( 0.000000000000000000, 6.982962677686266711E-15, -1.000000000000000000 ) ) ;
#119964=ORIENTED_EDGE ( 'NONE', *, *, #210955, .F. ) ;
#119976=VERTEX_POINT ( 'NONE', #166398 ) ;
#119982=VECTOR ( 'NONE', #29281, 1000.000000000000000 ) ;
#119988=FACE_OUTER_BOUND ( 'NONE', #130193, .T. ) ;
#120015=CARTESIAN_POINT ( 'NONE',  ( 21.14999999999999858, 64.35000000001214460, -136.4231074845243938 ) ) ;
#120033=CARTESIAN_POINT ( 'NONE',  ( -18.59999999999999787, 64.35000000001198828, -115.2731074845243739 ) ) ;
#120050=CYLINDRICAL_SURFACE ( 'NONE', #48536, 0.1000000000000028644 ) ;
#120060=CARTESIAN_POINT ( 'NONE',  ( 18.49999999999998934, 69.45000000001206786, -126.5060803140843291 ) ) ;
#120092=CARTESIAN_POINT ( 'NONE',  ( -23.25000000000000000, 71.65000000001207070, -124.2731074845243313 ) ) ;
#120164=DIRECTION ( 'NONE',  ( 0.000000000000000000, -7.026728003956683390E-15, 1.000000000000000000 ) ) ;
#120169=DIRECTION ( 'NONE',  ( -5.603264701231743991E-32, -7.172728831056617961E-15, 1.000000000000000000 ) ) ;
#120183=CARTESIAN_POINT ( 'NONE',  ( 20.85000000000000142, 77.36242903720516040, -95.13422623660308375 ) ) ;
#120191=FILL_AREA_STYLE_COLOUR ( '', #2038 ) ;
#120218=ORIENTED_EDGE ( 'NONE', *, *, #205976, .F. ) ;
#120223=ADVANCED_FACE ( 'NONE', ( #10523 ), #11826, .T. ) ;
#120249=FACE_OUTER_BOUND ( 'NONE', #40195, .T. ) ;
#120260=DIRECTION ( 'NONE',  ( 0.000000000000000000, 0.000000000000000000, -1.000000000000000000 ) ) ;
#120263=DIRECTION ( 'NONE',  ( 0.000000000000000000, 0.000000000000000000, -1.000000000000000000 ) ) ;
#120269=CARTESIAN_POINT ( 'NONE',  ( -21.05000000000000071, 76.10000000001222986, -148.1726782920690937 ) ) ;
#120290=EDGE_CURVE ( 'NONE', #214613, #85598, #109102, .T. ) ;
#120307=FACE_OUTER_BOUND ( 'NONE', #98482, .T. ) ;
#120308=EDGE_LOOP ( 'NONE', ( #168976, #202677 ) ) ;
#120325=CARTESIAN_POINT ( 'NONE',  ( 23.14999999999999858, 76.00000000001189449, -101.0231074845243029 ) ) ;
#120396=EDGE_LOOP ( 'NONE', ( #224603, #33241, #22790, #257259 ) ) ;
#120411=CARTESIAN_POINT ( 'NONE',  ( 21.05000000000000071, 69.55891531154095730, -136.5053880512155331 ) ) ;
#120475=VECTOR ( 'NONE', #254467, 1000.000000000000000 ) ;
#120479=ORIENTED_EDGE ( 'NONE', *, *, #32657, .F. ) ;
#120487=PLANE ( 'NONE',  #192953 ) ;
#120491=CARTESIAN_POINT ( 'NONE',  ( -18.33981767444241484, 85.56957578981651125, -96.20394564079951749 ) ) ;
#120496=FACE_OUTER_BOUND ( 'NONE', #184560, .T. ) ;
#120530=CARTESIAN_POINT ( 'NONE',  ( -20.94999999999999929, 76.00000000001190870, -103.0231074845243029 ) ) ;
#120535=ADVANCED_FACE ( 'NONE', ( #121204 ), #241137, .T. ) ;
#120542=CARTESIAN_POINT ( 'NONE',  ( -18.50000000000000000, 85.40000000001187175, -96.14106563635156988 ) ) ;
#120601=ORIENTED_EDGE ( 'NONE', *, *, #103117, .F. ) ;
#120608=DIRECTION ( 'NONE',  ( 0.000000000000000000, -0.1350103645451945777, 0.9908441862701590219 ) ) ;
#120611=EDGE_CURVE ( 'NONE', #219486, #130620, #5043, .T. ) ;
#120620=DIRECTION ( 'NONE',  ( -1.000000000000000000, -1.387778780781454006E-13, 0.000000000000000000 ) ) ;
#120625=DIRECTION ( 'NONE',  ( 0.000000000000000000, -6.467318590049456648E-15, 1.000000000000000000 ) ) ;
#120638=AXIS2_PLACEMENT_3D ( 'NONE', #141733, #221259, #143002 ) ;
#120653=CARTESIAN_POINT ( 'NONE',  ( -18.49499033040906326, 85.43814877175674383, -129.3249542586007976 ) ) ;
#120668=DIRECTION ( 'NONE',  ( -0.000000000000000000, 0.8660254037844424824, 0.4999999999999934497 ) ) ;
#120674=DIRECTION ( 'NONE',  ( -0.000000000000000000, 6.982962677686266711E-15, -1.000000000000000000 ) ) ;
#120684=DIRECTION ( 'NONE',  ( 0.000000000000000000, 0.000000000000000000, -1.000000000000000000 ) ) ;
#120705=ORIENTED_EDGE ( 'NONE', *, *, #60257, .F. ) ;
#120733=CARTESIAN_POINT ( 'NONE',  ( 22.60000000000000142, 64.25043287652275126, -136.6239658536230763 ) ) ;
#120744=CYLINDRICAL_SURFACE ( 'NONE', #156852, 0.1000000000000028644 ) ;
#120771=ORIENTED_EDGE ( 'NONE', *, *, #53787, .F. ) ;
#120778=AXIS2_PLACEMENT_3D ( 'NONE', #257814, #196604, #60941 ) ;
#120805=CIRCLE ( 'NONE', #45945, 7.800000000000001599 ) ;
#120815=AXIS2_PLACEMENT_3D ( 'NONE', #44827, #103492, #183065 ) ;
#120840=ADVANCED_FACE ( 'NONE', ( #60872 ), #180840, .T. ) ;
#120843=AXIS2_PLACEMENT_3D ( 'NONE', #242975, #42225, #219551 ) ;
#120850=EDGE_CURVE ( 'NONE', #196680, #45647, #197817, .T. ) ;
#120851=DIRECTION ( 'NONE',  ( -1.000000000000000000, -0.000000000000000000, -0.000000000000000000 ) ) ;
#120882=CARTESIAN_POINT ( 'NONE',  ( -20.85000000000000142, 77.83585931145546510, -91.51866831572576189 ) ) ;
#120886=FACE_OUTER_BOUND ( 'NONE', #208076, .T. ) ;
#120926=DIRECTION ( 'NONE',  ( 0.000000000000000000, -6.982962677686266711E-15, 1.000000000000000000 ) ) ;
#120943=EDGE_LOOP ( 'NONE', ( #55977, #182824, #20972, #30053 ) ) ;
#120985=DIRECTION ( 'NONE',  ( 1.000000000000000000, 0.000000000000000000, 0.000000000000000000 ) ) ;
#120990=CIRCLE ( 'NONE', #241755, 11.70000000000000284 ) ;
#120994=ORIENTED_EDGE ( 'NONE', *, *, #45632, .T. ) ;
#120998=AXIS2_PLACEMENT_3D ( 'NONE', #90049, #125344, #87479 ) ;
#121004=CIRCLE ( 'NONE', #71107, 0.09999999999999459321 ) ;
#121007=ORIENTED_EDGE ( 'NONE', *, *, #96677, .T. ) ;
#121073=CARTESIAN_POINT ( 'NONE',  ( -21.14999999999999858, 87.65000000001214175, -136.5231074845242176 ) ) ;
#121080=CARTESIAN_POINT ( 'NONE',  ( 20.04142135623730070, 64.35000000001198828, -115.1731074845243796 ) ) ;
#121081=DIRECTION ( 'NONE',  ( -1.000000000000000000, -9.012599976027990443E-15, -6.882867235861669241E-14 ) ) ;
#121092=VERTEX_POINT ( 'NONE', #191129 ) ;
#121151=CARTESIAN_POINT ( 'NONE',  ( -21.05000000000000071, 69.74218538953603286, -136.6208977758331287 ) ) ;
#121155=AXIS2_PLACEMENT_3D ( 'NONE', #215783, #116699, #77545 ) ;
#121181=CYLINDRICAL_SURFACE ( 'NONE', #44462, 0.09999999999999939493 ) ;
#121184=CARTESIAN_POINT ( 'NONE',  ( -18.59999999999999787, 68.97833521811179480, -99.18954208262705663 ) ) ;
#121193=CIRCLE ( 'NONE', #29595, 2.000000000000001776 ) ;
#121204=FACE_OUTER_BOUND ( 'NONE', #155192, .T. ) ;
#121285=DIRECTION ( 'NONE',  ( 0.000000000000000000, 6.577889128801576950E-15, -1.000000000000000000 ) ) ;
#121292=CARTESIAN_POINT ( 'NONE',  ( 20.72390388899090041, 65.41003688158804152, -129.0117591887780577 ) ) ;
#121310=CIRCLE ( 'NONE', #42171, 0.1999999999999987899 ) ;
#121314=ORIENTED_EDGE ( 'NONE', *, *, #76410, .T. ) ;
#121335=CARTESIAN_POINT ( 'NONE',  ( 22.48660254037844197, 64.35000000001213039, -136.5731074845243995 ) ) ;
#121377=EDGE_LOOP ( 'NONE', ( #15251, #49516, #122871, #172797 ) ) ;
#121397=AXIS2_PLACEMENT_3D ( 'NONE', #115764, #177047, #213575 ) ;
#121400=PLANE ( 'NONE',  #112148 ) ;
#121418=VERTEX_POINT ( 'NONE', #26612 ) ;
#121436=EDGE_LOOP ( 'NONE', ( #223200, #251598, #198502, #226541 ) ) ;
#121437=DIRECTION ( 'NONE',  ( -1.000000000000000000, -0.000000000000000000, 0.000000000000000000 ) ) ;
#121455=VERTEX_POINT ( 'NONE', #55108 ) ;
#121485=FACE_OUTER_BOUND ( 'NONE', #16156, .T. ) ;
#121512=CYLINDRICAL_SURFACE ( 'NONE', #158937, 0.09999999999999939493 ) ;
#121528=ADVANCED_FACE ( 'NONE', ( #52559 ), #173860, .F. ) ;
#121531=ADVANCED_FACE ( 'NONE', ( #172579 ), #74750, .T. ) ;
#121540=AXIS2_PLACEMENT_3D ( 'NONE', #257379, #142611, #240451 ) ;
#121556=ORIENTED_EDGE ( 'NONE', *, *, #114700, .F. ) ;
#121557=CARTESIAN_POINT ( 'NONE',  ( -20.94999999999999929, 64.40000000001208491, -129.5949042542488314 ) ) ;
#121559=CARTESIAN_POINT ( 'NONE',  ( -20.54999999999999716, 73.50000000001205080, -123.2984855617622202 ) ) ;
#121560=DIRECTION ( 'NONE',  ( -3.265361837132813093E-16, -1.000000000000000000, -6.982962677686266711E-15 ) ) ;
#121586=VERTEX_POINT ( 'NONE', #257139 ) ;
#121589=CARTESIAN_POINT ( 'NONE',  ( 21.30740335185485890, 69.44334207798414127, -136.6220420103001914 ) ) ;
#121602=FACE_OUTER_BOUND ( 'NONE', #148546, .T. ) ;
#121611=VERTEX_POINT ( 'NONE', #118981 ) ;
#121642=ADVANCED_FACE ( 'NONE', ( #237974 ), #201240, .T. ) ;
#121654=DIRECTION ( 'NONE',  ( 1.000000000000000000, -0.000000000000000000, 0.000000000000000000 ) ) ;
#121669=EDGE_CURVE ( 'NONE', #199005, #61045, #30583, .T. ) ;
#121673=DIRECTION ( 'NONE',  ( 1.000000000000000000, 0.000000000000000000, 0.000000000000000000 ) ) ;
#121699=CIRCLE ( 'NONE', #9251, 0.1000000000000028644 ) ;
#121700=VERTEX_POINT ( 'NONE', #39820 ) ;
#121705=EDGE_LOOP ( 'NONE', ( #112165, #123916, #81972, #102063, #250044, #223590, #252019 ) ) ;
#121711=DIRECTION ( 'NONE',  ( 0.000000000000000000, 6.982962677686266711E-15, -1.000000000000000000 ) ) ;
#121712=AXIS2_PLACEMENT_3D ( 'NONE', #238168, #156115, #139043 ) ;
#121753=DIRECTION ( 'NONE',  ( -1.000000000000000000, 0.000000000000000000, 0.000000000000000000 ) ) ;
#121756=ORIENTED_EDGE ( 'NONE', *, *, #159921, .F. ) ;
#121768=DIRECTION ( 'NONE',  ( 0.000000000000000000, -6.938893903907222067E-15, 1.000000000000000000 ) ) ;
#121778=CARTESIAN_POINT ( 'NONE',  ( -20.85000000000000142, 68.97833521811179480, -99.18954208262705663 ) ) ;
#121781=CARTESIAN_POINT ( 'NONE',  ( 23.24999999999999289, 69.35000000001200249, -115.1731074845243512 ) ) ;
#121847=ORIENTED_EDGE ( 'NONE', *, *, #123775, .F. ) ;
#121858=ORIENTED_EDGE ( 'NONE', *, *, #198268, .F. ) ;
#121860=CARTESIAN_POINT ( 'NONE',  ( 23.14999999999999503, 69.35000000001200249, -115.3731074845243398 ) ) ;
#121874=DIRECTION ( 'NONE',  ( -1.000000000000000000, 0.000000000000000000, 0.000000000000000000 ) ) ;
#121913=AXIS2_PLACEMENT_3D ( 'NONE', #151745, #195995, #56450 ) ;
#121942=ORIENTED_EDGE ( 'NONE', *, *, #45412, .F. ) ;
#121950=CARTESIAN_POINT ( 'NONE',  ( 21.05000000000000071, 70.15000000001211333, -126.3906102602463619 ) ) ;
#122000=AXIS2_PLACEMENT_3D ( 'NONE', #81910, #107930, #150910 ) ;
#122012=FACE_OUTER_BOUND ( 'NONE', #181921, .T. ) ;
#122017=CARTESIAN_POINT ( 'NONE',  ( -21.11833042828144613, 75.99289949095295071, -142.9687521783799014 ) ) ;
#122032=EDGE_CURVE ( 'NONE', #29489, #149997, #22391, .T. ) ;
#122044=FACE_OUTER_BOUND ( 'NONE', #109924, .T. ) ;
#122058=VERTEX_POINT ( 'NONE', #137290 ) ;
#122081=VERTEX_POINT ( 'NONE', #119034 ) ;
#122089=VECTOR ( 'NONE', #159178, 1000.000000000000114 ) ;
#122119=ADVANCED_FACE ( 'NONE', ( #2909 ), #22512, .F. ) ;
#122131=CARTESIAN_POINT ( 'NONE',  ( -18.50000000000000000, 77.16412189325305349, -95.10825939895268277 ) ) ;
#122177=DIRECTION ( 'NONE',  ( -1.000000000000000000, -0.000000000000000000, -0.000000000000000000 ) ) ;
#122188=VECTOR ( 'NONE', #256924, 1000.000000000000114 ) ;
#122200=CARTESIAN_POINT ( 'NONE',  ( -22.39999999999999858, 68.20922040163873135, -136.6231074845243540 ) ) ;
#122255=AXIS2_PLACEMENT_3D ( 'NONE', #236454, #94365, #117794 ) ;
#122272=CARTESIAN_POINT ( 'NONE',  ( -20.64999999999999858, 76.00000000001190870, -103.0231074845243029 ) ) ;
#122274=ORIENTED_EDGE ( 'NONE', *, *, #182710, .T. ) ;
#122351=CIRCLE ( 'NONE', #247413, 0.1000000000000028644 ) ;
#122361=AXIS2_PLACEMENT_3D ( 'NONE', #224700, #66922, #86455 ) ;
#122382=CARTESIAN_POINT ( 'NONE',  ( 18.39999999999999858, 85.50000000001209344, -129.4910380878245633 ) ) ;
#122396=AXIS2_PLACEMENT_3D ( 'NONE', #65798, #181902, #184456 ) ;
#122448=B_SPLINE_CURVE_WITH_KNOTS ( 'NONE', 3,
 ( #251379, #175724, #17894, #77865, #111890, #214817, #94867, #16641, #96142, #233138, #235658, #256446, #216095, #131431, #210982, #32376 ),
 .UNSPECIFIED., .F., .F.,
 ( 4, 3, 3, 3, 3, 4 ),
 ( 0.000000000000000000, 2.372700795693547977E-05, 5.739057815866958510E-05, 9.073899019179559378E-05, 0.0001243544287365697066, 0.0001585386695601189160 ),
 .UNSPECIFIED. ) ;
#122453=CIRCLE ( 'NONE', #26597, 0.09999999999998898659 ) ;
#122504=EDGE_CURVE ( 'NONE', #33201, #59064, #204651, .T. ) ;
#122529=DIRECTION ( 'NONE',  ( 1.836970198721029934E-16, 1.000000000000000000, 6.982962677686266711E-15 ) ) ;
#122533=AXIS2_PLACEMENT_3D ( 'NONE', #152166, #135118, #193840 ) ;
#122538=CARTESIAN_POINT ( 'NONE',  ( -20.94999999999999929, 77.16270174995010223, -128.5231074845242745 ) ) ;
#122540=DIRECTION ( 'NONE',  ( 1.000000000000000000, 0.000000000000000000, 0.000000000000000000 ) ) ;
#122565=DIRECTION ( 'NONE',  ( -1.000000000000000000, 0.000000000000000000, -0.000000000000000000 ) ) ;
#122577=FACE_OUTER_BOUND ( 'NONE', #207183, .T. ) ;
#122598=DIRECTION ( 'NONE',  ( 0.000000000000000000, -0.7397360091702823714, 0.6728971962616756564 ) ) ;
#122638=AXIS2_PLACEMENT_3D ( 'NONE', #247394, #150872, #30963 ) ;
#122646=DIRECTION ( 'NONE',  ( 1.000000000000000000, 0.000000000000000000, 0.000000000000000000 ) ) ;
#122663=DIRECTION ( 'NONE',  ( 0.000000000000000000, -6.938893903907222067E-15, 1.000000000000000000 ) ) ;
#122671=DIRECTION ( 'NONE',  ( -1.000000000000000000, 0.000000000000000000, -0.000000000000000000 ) ) ;
#122709=EDGE_CURVE ( 'NONE', #197247, #182665, #147635, .T. ) ;
#122743=DIRECTION ( 'NONE',  ( -1.000000000000000000, -0.000000000000000000, -0.000000000000000000 ) ) ;
#122769=CYLINDRICAL_SURFACE ( 'NONE', #206920, 0.1000000000000038219 ) ;
#122790=ORIENTED_EDGE ( 'NONE', *, *, #80581, .T. ) ;
#122808=CARTESIAN_POINT ( 'NONE',  ( 21.14999999999999503, 76.10000000001222986, -148.1726782920690937 ) ) ;
#122817=CARTESIAN_POINT ( 'NONE',  ( 22.50927854361892244, 76.10085807354001020, -148.2726746105511779 ) ) ;
#122821=CARTESIAN_POINT ( 'NONE',  ( -20.54999999999999716, 76.00000000001189449, -101.0231074845243029 ) ) ;
#122822=ORIENTED_EDGE ( 'NONE', *, *, #194042, .F. ) ;
#122829=CARTESIAN_POINT ( 'NONE',  ( -18.50000000000000000, 66.75000000001199396, -115.3731074845243683 ) ) ;
#122858=VERTEX_POINT ( 'NONE', #97516 ) ;
#122871=ORIENTED_EDGE ( 'NONE', *, *, #167574, .T. ) ;
#122877=AXIS2_PLACEMENT_3D ( 'NONE', #5142, #160431, #239949 ) ;
#122902=EDGE_CURVE ( 'NONE', #181206, #122058, #167947, .T. ) ;
#122949=CARTESIAN_POINT ( 'NONE',  ( 21.07928932188134397, 69.67148334361883144, -136.6220026301787698 ) ) ;
#122953=AXIS2_PLACEMENT_3D ( 'NONE', #186762, #66798, #203742 ) ;
#122971=CARTESIAN_POINT ( 'NONE',  ( -18.59999999999999787, 66.65000000001198543, -115.3731074845243683 ) ) ;
#122973=EDGE_CURVE ( 'NONE', #156274, #220426, #100089, .T. ) ;
#122985=DIRECTION ( 'NONE',  ( 0.000000000000000000, -1.000000000000000000, 0.000000000000000000 ) ) ;
#122997=CIRCLE ( 'NONE', #247884, 0.09999999999999939493 ) ;
#123016=CARTESIAN_POINT ( 'NONE',  ( -21.14999999999999858, 87.75000000001213607, -136.5231074845242176 ) ) ;
#123025=DIRECTION ( 'NONE',  ( -2.952720810173289112E-16, -1.000000000000000000, -6.982962677686266711E-15 ) ) ;
#123041=CARTESIAN_POINT ( 'NONE',  ( 20.94999999999999929, 70.15000000001211333, -126.3906102602463619 ) ) ;
#123089=CARTESIAN_POINT ( 'NONE',  ( -20.54999999999999716, 74.00000000001205080, -123.2984855617622060 ) ) ;
#123122=EDGE_CURVE ( 'NONE', #243534, #87303, #94342, .T. ) ;
#123151=CARTESIAN_POINT ( 'NONE',  ( -21.14999999999999858, 76.10000000001222986, -148.1726782920690937 ) ) ;
#123158=EDGE_LOOP ( 'NONE', ( #102933, #256794, #74545, #193727 ) ) ;
#123161=FACE_OUTER_BOUND ( 'NONE', #169250, .T. ) ;
#123171=DIRECTION ( 'NONE',  ( -0.000000000000000000, 6.982962677686266711E-15, -1.000000000000000000 ) ) ;
#123179=CARTESIAN_POINT ( 'NONE',  ( 23.14999999999999858, 76.00000000001190870, -103.0231074845243029 ) ) ;
#123194=CARTESIAN_POINT ( 'NONE',  ( -20.64999999999999858, 71.75000000001205080, -124.1731074845243228 ) ) ;
#123204=CARTESIAN_POINT ( 'NONE',  ( 23.14999999999999503, 64.35000000001195986, -109.9379132551783158 ) ) ;
#123259=DIRECTION ( 'NONE',  ( 1.000000000000000000, 0.000000000000000000, 0.000000000000000000 ) ) ;
#123295=DIRECTION ( 'NONE',  ( -0.000000000000000000, -6.982962677686266711E-15, 1.000000000000000000 ) ) ;
#123349=DIRECTION ( 'NONE',  ( 1.224646799147353207E-16, -1.000000000000000000, -6.982962677686266711E-15 ) ) ;
#123386=ORIENTED_EDGE ( 'NONE', *, *, #201092, .F. ) ;
#123395=CIRCLE ( 'NONE', #10968, 12.87499999999999822 ) ;
#123406=ORIENTED_EDGE ( 'NONE', *, *, #53537, .T. ) ;
#123456=ORIENTED_EDGE ( 'NONE', *, *, #56872, .F. ) ;
#123471=CARTESIAN_POINT ( 'NONE',  ( 21.05000000000000071, 84.66355140188112216, -112.5472086025915388 ) ) ;
#123476=DIRECTION ( 'NONE',  ( 1.000000000000000000, 0.000000000000000000, 0.000000000000000000 ) ) ;
#123490=ORIENTED_EDGE ( 'NONE', *, *, #206678, .F. ) ;
#123528=DIRECTION ( 'NONE',  ( 0.000000000000000000, -1.000000000000000000, 0.000000000000000000 ) ) ;
#123535=ORIENTED_EDGE ( 'NONE', *, *, #164466, .T. ) ;
#123560=VECTOR ( 'NONE', #45565, 1000.000000000000000 ) ;
#123575=ORIENTED_EDGE ( 'NONE', *, *, #134138, .F. ) ;
#123583=ORIENTED_EDGE ( 'NONE', *, *, #103284, .F. ) ;
#123616=CIRCLE ( 'NONE', #156957, 0.1000000000000028644 ) ;
#123656=ORIENTED_EDGE ( 'NONE', *, *, #257505, .F. ) ;
#123711=VECTOR ( 'NONE', #43620, 1000.000000000000114 ) ;
#123768=AXIS2_PLACEMENT_3D ( 'NONE', #214110, #251945, #72041 ) ;
#123775=EDGE_CURVE ( 'NONE', #246341, #219596, #12954, .T. ) ;
#123819=EDGE_CURVE ( 'NONE', #19771, #105588, #226716, .T. ) ;
#123827=EDGE_LOOP ( 'NONE', ( #151875, #211790, #204438, #233375, #57494, #2100, #6199, #167364, #119477, #182015 ) ) ;
#123858=EDGE_CURVE ( 'NONE', #131694, #130891, #64415, .T. ) ;
#123870=CARTESIAN_POINT ( 'NONE',  ( 21.14999999999999858, 65.28660755661216797, -124.2731074845243739 ) ) ;
#123882=DIRECTION ( 'NONE',  ( 0.000000000000000000, 0.000000000000000000, 1.000000000000000000 ) ) ;
#123884=ORIENTED_EDGE ( 'NONE', *, *, #250943, .F. ) ;
#123889=DIRECTION ( 'NONE',  ( 1.000000000000000000, 0.000000000000000000, 0.000000000000000000 ) ) ;
#123916=ORIENTED_EDGE ( 'NONE', *, *, #215531, .T. ) ;
#123929=DIRECTION ( 'NONE',  ( 0.000000000000000000, -6.454785026890489601E-15, 1.000000000000000000 ) ) ;
#123943=FACE_OUTER_BOUND ( 'NONE', #120308, .T. ) ;
#123953=CIRCLE ( 'NONE', #116151, 0.6000000000000033085 ) ;
#123987=ORIENTED_EDGE ( 'NONE', *, *, #49983, .T. ) ;
#124002=VERTEX_POINT ( 'NONE', #162720 ) ;
#124017=ORIENTED_EDGE ( 'NONE', *, *, #24690, .F. ) ;
#124042=DIRECTION ( 'NONE',  ( 1.000000000000000000, 0.000000000000000000, 0.000000000000000000 ) ) ;
#124059=CYLINDRICAL_SURFACE ( 'NONE', #203338, 0.09999999999998898659 ) ;
#124063=EDGE_LOOP ( 'NONE', ( #160727, #64996, #141280, #61361 ) ) ;
#124083=LINE ( 'NONE', #24992, #23944 ) ;
#124085=ORIENTED_EDGE ( 'NONE', *, *, #92462, .F. ) ;
#124121=AXIS2_PLACEMENT_3D ( 'NONE', #98108, #119005, #318 ) ;
#124213=ADVANCED_FACE ( 'NONE', ( #76427 ), #33508, .T. ) ;
#124219=ADVANCED_FACE ( 'NONE', ( #234215 ), #39514, .F. ) ;
#124229=VECTOR ( 'NONE', #65431, 1000.000000000000000 ) ;
#124252=CARTESIAN_POINT ( 'NONE',  ( -21.05000000000000071, 69.45934304831089889, -136.4231074845243654 ) ) ;
#124254=AXIS2_PLACEMENT_3D ( 'NONE', #36608, #95257, #128307 ) ;
#124347=EDGE_CURVE ( 'NONE', #174398, #1620, #152156, .T. ) ;
#124351=DIRECTION ( 'NONE',  ( -1.000000000000000000, 0.000000000000000000, 0.000000000000000000 ) ) ;
#124370=AXIS2_PLACEMENT_3D ( 'NONE', #159390, #241485, #141104 ) ;
#124399=CARTESIAN_POINT ( 'NONE',  ( -20.94788355080264353, 65.69792220476320210, -97.53355541284612684 ) ) ;
#124406=DIRECTION ( 'NONE',  ( 2.952720810173289112E-16, 1.000000000000000000, 6.938893903907222067E-15 ) ) ;
#124422=LINE ( 'NONE', #201372, #34369 ) ;
#124504=CARTESIAN_POINT ( 'NONE',  ( -20.85000000000000142, 76.32388570108224712, -103.0655178952103199 ) ) ;
#124536=B_SPLINE_CURVE_WITH_KNOTS ( 'NONE', 3,
 ( #48378, #66675, #227018, #211320, #129215, #208761, #91377, #126642, #70554, #30132 ),
 .UNSPECIFIED., .F., .F.,
 ( 4, 2, 2, 2, 4 ),
 ( 0.000000000000000000, 0.0001660831991682472993, 0.0002491247987523721144, 0.0002906455985444166869, 0.0003321663983364612593 ),
 .UNSPECIFIED. ) ;
#124558=ADVANCED_FACE ( 'NONE', ( #230074 ), #73011, .F. ) ;
#124567=CARTESIAN_POINT ( 'NONE',  ( -23.25000000000000000, 76.00000000001193712, -106.9231074845242944 ) ) ;
#124583=ORIENTED_EDGE ( 'NONE', *, *, #45778, .T. ) ;
#124610=EDGE_LOOP ( 'NONE', ( #130513, #36363, #31792, #50691 ) ) ;
#124614=DIRECTION ( 'NONE',  ( 0.000000000000000000, -1.000000000000000000, 0.000000000000000000 ) ) ;
#124620=ORIENTED_EDGE ( 'NONE', *, *, #206645, .F. ) ;
#124632=AXIS2_PLACEMENT_3D ( 'NONE', #252903, #50830, #71723 ) ;
#124634=DIRECTION ( 'NONE',  ( -0.7071067811865474617, 0.7071067811865474617, 4.937700262164531476E-15 ) ) ;
#124699=EDGE_CURVE ( 'NONE', #25096, #22494, #171426, .T. ) ;
#124701=AXIS2_PLACEMENT_3D ( 'NONE', #5671, #219598, #41006 ) ;
#124760=EDGE_CURVE ( 'NONE', #93991, #16075, #52709, .T. ) ;
#124768=ADVANCED_FACE ( 'NONE', ( #123943 ), #63959, .F. ) ;
#124806=CARTESIAN_POINT ( 'NONE',  ( -20.64999999999999858, 71.75000000001199396, -115.3731074845243256 ) ) ;
#124850=CARTESIAN_POINT ( 'NONE',  ( 21.46681500598269565, 76.00000000001219291, -143.3806186439480825 ) ) ;
#124893=ORIENTED_EDGE ( 'NONE', *, *, #236451, .F. ) ;
#124933=LINE ( 'NONE', #204446, #236408 ) ;
#125007=DIRECTION ( 'NONE',  ( 0.000000000000000000, -0.1350103645451945777, 0.9908441862701590219 ) ) ;
#125026=CARTESIAN_POINT ( 'NONE',  ( 20.85000000000000142, 68.92903212821303782, -99.27654326265604823 ) ) ;
#125030=EDGE_CURVE ( 'NONE', #128716, #252010, #64950, .T. ) ;
#125032=AXIS2_PLACEMENT_3D ( 'NONE', #113069, #217272, #197728 ) ;
#125035=CARTESIAN_POINT ( 'NONE',  ( 20.94999999999999929, 85.50000000001197975, -112.9170766071766820 ) ) ;
#125074=CIRCLE ( 'NONE', #50046, 4.100000000000006750 ) ;
#125118=FACE_OUTER_BOUND ( 'NONE', #118158, .T. ) ;
#125129=SPHERICAL_SURFACE ( 'NONE', #168319, 0.1000000000000000056 ) ;
#125130=CARTESIAN_POINT ( 'NONE',  ( -21.05000000000000071, 74.16465844978765176, -124.8679561919613263 ) ) ;
#125135=CARTESIAN_POINT ( 'NONE',  ( -20.85000000000000142, 87.65000000001191438, -103.0231074845242176 ) ) ;
#125207=VERTEX_POINT ( 'NONE', #174205 ) ;
#125221=CIRCLE ( 'NONE', #58556, 0.1000000000000028644 ) ;
#125256=ORIENTED_EDGE ( 'NONE', *, *, #102924, .T. ) ;
#125258=DIRECTION ( 'NONE',  ( -0.000000000000000000, 6.982962677686266711E-15, -1.000000000000000000 ) ) ;
#125262=EDGE_LOOP ( 'NONE', ( #178927, #25464, #245891, #228207 ) ) ;
#125265=DIRECTION ( 'NONE',  ( 0.000000000000000000, 6.982962677686266711E-15, -1.000000000000000000 ) ) ;
#125290=LINE ( 'NONE', #186554, #17490 ) ;
#125316=DIRECTION ( 'NONE',  ( -0.000000000000000000, 6.982962677686266711E-15, -1.000000000000000000 ) ) ;
#125318=DIRECTION ( 'NONE',  ( 3.616040088954490704E-32, 7.105427357601001859E-15, -1.000000000000000000 ) ) ;
#125334=CARTESIAN_POINT ( 'NONE',  ( -18.59999999999999787, 74.83729825007408465, -128.5231074845243029 ) ) ;
#125338=ORIENTED_EDGE ( 'NONE', *, *, #223657, .F. ) ;
#125339=DIRECTION ( 'NONE',  ( 0.000000000000000000, -0.8660254037844377084, -0.5000000000000016653 ) ) ;
#125344=DIRECTION ( 'NONE',  ( 1.000000000000000000, 0.000000000000000000, 0.000000000000000000 ) ) ;
#125361=VERTEX_POINT ( 'NONE', #120269 ) ;
#125363=CARTESIAN_POINT ( 'NONE',  ( 21.09551895715238246, 65.37856267284368528, -124.2859828186246745 ) ) ;
#125375=CARTESIAN_POINT ( 'NONE',  ( -22.49544290803740054, 64.25012976215485594, -136.5884194437824419 ) ) ;
#125381=CARTESIAN_POINT ( 'NONE',  ( -21.00448002041582640, 64.25000000001207923, -129.6747666222131556 ) ) ;
#125407=EDGE_LOOP ( 'NONE', ( #149342, #96606, #51965, #213059 ) ) ;
#125422=FACE_OUTER_BOUND ( 'NONE', #92702, .T. ) ;
#125438=DIRECTION ( 'NONE',  ( 0.000000000000000000, 0.000000000000000000, 1.000000000000000000 ) ) ;
#125454=CARTESIAN_POINT ( 'NONE',  ( -21.14999999999999858, 76.10000000001218723, -143.0637644362255401 ) ) ;
#125500=CARTESIAN_POINT ( 'NONE',  ( -23.25000000000000000, 76.00000000001190870, -103.0231074845243029 ) ) ;
#125523=CARTESIAN_POINT ( 'NONE',  ( 18.49999999999999289, 65.79142135392881130, -111.8206006188944315 ) ) ;
#125530=DIRECTION ( 'NONE',  ( 1.000000000000000000, 0.000000000000000000, 0.000000000000000000 ) ) ;
#125571=DIRECTION ( 'NONE',  ( 0.000000000000000000, -0.9999631594459053030, -0.008583690987162452199 ) ) ;
#125596=DIRECTION ( 'NONE',  ( 0.000000000000000000, 0.4999999999999088507, -0.8660254037844913322 ) ) ;
#125599=CYLINDRICAL_SURFACE ( 'NONE', #120843, 0.09999999999998898659 ) ;
#125616=ORIENTED_EDGE ( 'NONE', *, *, #12072, .T. ) ;
#125625=CIRCLE ( 'NONE', #109045, 0.1000000000000052097 ) ;
#125654=DIRECTION ( 'NONE',  ( 0.000000000000000000, -7.056502275159890043E-15, 1.000000000000000000 ) ) ;
#125698=EDGE_CURVE ( 'NONE', #91270, #257751, #186127, .T. ) ;
#125702=EDGE_CURVE ( 'NONE', #243534, #213669, #98595, .T. ) ;
#125719=LINE ( 'NONE', #180568, #223812 ) ;
#125752=DIRECTION ( 'NONE',  ( 0.000000000000000000, -1.000000000000000000, 0.000000000000000000 ) ) ;
#125786=DIRECTION ( 'NONE',  ( 1.000000000000000000, 0.000000000000000000, 0.000000000000000000 ) ) ;
#125807=CARTESIAN_POINT ( 'NONE',  ( -21.05000000000000071, 77.83534155023646406, -124.8679561919613121 ) ) ;
#125810=DIRECTION ( 'NONE',  ( 0.000000000000000000, 0.000000000000000000, -1.000000000000000000 ) ) ;
#125812=DIRECTION ( 'NONE',  ( 0.000000000000000000, 0.000000000000000000, -1.000000000000000000 ) ) ;
#125819=AXIS2_PLACEMENT_3D ( 'NONE', #196798, #192970, #116009 ) ;
#125861=CARTESIAN_POINT ( 'NONE',  ( -20.94999999999999929, 64.40000000001209912, -129.5949042542488314 ) ) ;
#125864=EDGE_CURVE ( 'NONE', #57850, #168985, #248489, .T. ) ;
#125932=DIRECTION ( 'NONE',  ( -1.000000000000000000, 0.000000000000000000, 0.000000000000000000 ) ) ;
#125934=EDGE_LOOP ( 'NONE', ( #140620, #179171, #31083, #83735 ) ) ;
#126001=ADVANCED_FACE ( 'NONE', ( #112874 ), #162288, .T. ) ;
#126017=ADVANCED_FACE ( 'NONE', ( #24066 ), #100956, .T. ) ;
#126029=VERTEX_POINT ( 'NONE', #179294 ) ;
#126049=AXIS2_PLACEMENT_3D ( 'NONE', #114000, #73634, #115292 ) ;
#126069=CIRCLE ( 'NONE', #226010, 0.1000000000000026007 ) ;
#126141=ORIENTED_EDGE ( 'NONE', *, *, #103943, .F. ) ;
#126169=DIRECTION ( 'NONE',  ( 0.000000000000000000, -6.982962677686266711E-15, 1.000000000000000000 ) ) ;
#126174=CARTESIAN_POINT ( 'NONE',  ( -21.14999999999999858, 69.45934304831089889, -136.5231074845243313 ) ) ;
#126247=EDGE_LOOP ( 'NONE', ( #241676, #44337, #88651, #189771 ) ) ;
#126251=DIRECTION ( 'NONE',  ( -1.000000000000000000, 0.000000000000000000, -0.000000000000000000 ) ) ;
#126277=EDGE_CURVE ( 'NONE', #236302, #89014, #73477, .T. ) ;
#126292=AXIS2_PLACEMENT_3D ( 'NONE', #189231, #57059, #148826 ) ;
#126301=CARTESIAN_POINT ( 'NONE',  ( -18.50000000000000000, 77.68707439010378835, -149.3376804510659213 ) ) ;
#126314=CIRCLE ( 'NONE', #59843, 0.1999999999999987899 ) ;
#126327=DIRECTION ( 'NONE',  ( 0.000000000000000000, 0.000000000000000000, 1.000000000000000000 ) ) ;
#126353=DIRECTION ( 'NONE',  ( -1.000000000000000000, 0.000000000000000000, 0.000000000000000000 ) ) ;
#126354=DIRECTION ( 'NONE',  ( 0.000000000000000000, -6.982962677686266711E-15, 1.000000000000000000 ) ) ;
#126381=DIRECTION ( 'NONE',  ( -1.000000000000000000, 0.000000000000000000, -0.000000000000000000 ) ) ;
#126388=ORIENTED_EDGE ( 'NONE', *, *, #191429, .T. ) ;
#126389=CARTESIAN_POINT ( 'NONE',  ( 23.14999999999999858, 76.00000000001205080, -123.6481074845242887 ) ) ;
#126433=CARTESIAN_POINT ( 'NONE',  ( 18.59999999999999787, 87.75000000001197975, -115.1731074845242233 ) ) ;
#126438=EDGE_CURVE ( 'NONE', #155470, #102511, #109680, .T. ) ;
#126470=ORIENTED_EDGE ( 'NONE', *, *, #96311, .F. ) ;
#126497=ORIENTED_EDGE ( 'NONE', *, *, #241429, .T. ) ;
#126523=CARTESIAN_POINT ( 'NONE',  ( -21.65000000000000213, 68.29142135624935861, -124.1731074845243512 ) ) ;
#126547=CARTESIAN_POINT ( 'NONE',  ( -20.64999999999999858, 73.60000000001200249, -116.2477294072864140 ) ) ;
#126557=ORIENTED_EDGE ( 'NONE', *, *, #200652, .T. ) ;
#126561=ORIENTED_EDGE ( 'NONE', *, *, #181995, .F. ) ;
#126589=DIRECTION ( 'NONE',  ( 0.000000000000000000, -7.056502275159890832E-15, 1.000000000000000000 ) ) ;
#126596=SPHERICAL_SURFACE ( 'NONE', #153745, 0.1000000000000000056 ) ;
#126638=VECTOR ( 'NONE', #123889, 1000.000000000000000 ) ;
#126641=CIRCLE ( 'NONE', #193298, 0.09999999999999939493 ) ;
#126642=CARTESIAN_POINT ( 'NONE',  ( 18.42636655943171320, 85.49694431578251397, -96.41402691336872977 ) ) ;
#126698=VERTEX_POINT ( 'NONE', #156560 ) ;
#126739=DIRECTION ( 'NONE',  ( 1.000000000000000000, 0.000000000000000000, 0.000000000000000000 ) ) ;
#126783=CARTESIAN_POINT ( 'NONE',  ( -23.15000000000000213, 64.25000000001222134, -148.2731074845243882 ) ) ;
#126844=FACE_OUTER_BOUND ( 'NONE', #231138, .T. ) ;
#126853=CIRCLE ( 'NONE', #243550, 0.2000000000000057288 ) ;
#126860=CARTESIAN_POINT ( 'NONE',  ( -23.15000000000000213, 64.35000000001195986, -110.0379132551783243 ) ) ;
#126863=CARTESIAN_POINT ( 'NONE',  ( -22.59999999999999787, 64.35042919246734527, -136.6231074845243825 ) ) ;
#126866=CARTESIAN_POINT ( 'NONE',  ( -23.25000000000000000, 87.48912529308798014, -106.1231074845242262 ) ) ;
#126870=AXIS2_PLACEMENT_3D ( 'NONE', #180745, #98585, #3360 ) ;
#126887=CARTESIAN_POINT ( 'NONE',  ( -20.94999999999999929, 77.26178616857710324, -128.4366085209788366 ) ) ;
#126916=VERTEX_POINT ( 'NONE', #192783 ) ;
#126917=LINE ( 'NONE', #206447, #237482 ) ;
#126941=AXIS2_PLACEMENT_3D ( 'NONE', #16943, #255486, #156477 ) ;
#126947=ORIENTED_EDGE ( 'NONE', *, *, #180082, .T. ) ;
#126958=CARTESIAN_POINT ( 'NONE',  ( -20.94999999999999929, 65.70711192142366031, -97.56510546851220056 ) ) ;
#126964=DIRECTION ( 'NONE',  ( -1.000000000000000000, -0.000000000000000000, -0.000000000000000000 ) ) ;
#126972=CARTESIAN_POINT ( 'NONE',  ( 18.49999999999998934, 69.45000000001199680, -115.3731074845243398 ) ) ;
#126977=CARTESIAN_POINT ( 'NONE',  ( 20.94999999999999574, 74.83729825007408465, -128.4231074845243086 ) ) ;
#126981=FACE_OUTER_BOUND ( 'NONE', #132141, .T. ) ;
#127005=CARTESIAN_POINT ( 'NONE',  ( 21.11701782572533048, 65.27839088400459389, -124.2780700550131598 ) ) ;
#127052=VECTOR ( 'NONE', #207718, 1000.000000000000114 ) ;
#127064=ADVANCED_FACE ( 'NONE', ( #218730 ), #157976, .T. ) ;
#127090=CARTESIAN_POINT ( 'NONE',  ( 18.48536876927988359, 85.46352724987957572, -129.4744892194416366 ) ) ;
#127139=CARTESIAN_POINT ( 'NONE',  ( -21.44999999999999929, 68.75000000001199396, -115.2731074845243455 ) ) ;
#127154=DIRECTION ( 'NONE',  ( 0.000000000000000000, 1.000000000000000000, 6.982962677686266711E-15 ) ) ;
#127155=CARTESIAN_POINT ( 'NONE',  ( -20.85000000000000142, 64.25000000001196554, -109.8069731475024895 ) ) ;
#127185=EDGE_CURVE ( 'NONE', #53595, #111851, #74930, .T. ) ;
#127206=ORIENTED_EDGE ( 'NONE', *, *, #157776, .F. ) ;
#127208=ORIENTED_EDGE ( 'NONE', *, *, #14435, .F. ) ;
#127216=ORIENTED_EDGE ( 'NONE', *, *, #58426, .T. ) ;
#127271=DIRECTION ( 'NONE',  ( 0.000000000000000000, 0.000000000000000000, 1.000000000000000000 ) ) ;
#127274=LINE ( 'NONE', #49012, #237965 ) ;
#127307=ADVANCED_FACE ( 'NONE', ( #252416 ), #58122, .T. ) ;
#127313=ORIENTED_EDGE ( 'NONE', *, *, #197709, .T. ) ;
#127330=ORIENTED_EDGE ( 'NONE', *, *, #79439, .F. ) ;
#127333=DIRECTION ( 'NONE',  ( 1.000000000000000000, -2.952720810173289112E-16, -2.061873921506763405E-30 ) ) ;
#127346=EDGE_CURVE ( 'NONE', #133238, #164153, #174927, .T. ) ;
#127369=CARTESIAN_POINT ( 'NONE',  ( 21.05000000000000071, 77.73625713160946304, -124.9544551555067926 ) ) ;
#127378=DIRECTION ( 'NONE',  ( 0.000000000000000000, 0.000000000000000000, 1.000000000000000000 ) ) ;
#127387=CARTESIAN_POINT ( 'NONE',  ( 22.39999999999999503, 75.90000000001219860, -144.3138870828976792 ) ) ;
#127398=DIRECTION ( 'NONE',  ( 1.000000000000000000, 0.000000000000000000, -0.000000000000000000 ) ) ;
#127399=CIRCLE ( 'NONE', #81563, 11.70000000000000284 ) ;
#127405=PLANE ( 'NONE',  #156843 ) ;
#127428=DIRECTION ( 'NONE',  ( -3.265361837132813093E-16, -1.000000000000000000, -6.982962677686266711E-15 ) ) ;
#127437=CYLINDRICAL_SURFACE ( 'NONE', #197519, 0.1000000000000028644 ) ;
#127477=ORIENTED_EDGE ( 'NONE', *, *, #5662, .T. ) ;
#127492=VERTEX_POINT ( 'NONE', #116773 ) ;
#127497=VERTEX_POINT ( 'NONE', #10639 ) ;
#127499=EDGE_LOOP ( 'NONE', ( #170265, #55437, #48477, #223290 ) ) ;
#127514=ORIENTED_EDGE ( 'NONE', *, *, #224498, .T. ) ;
#127534=CARTESIAN_POINT ( 'NONE',  ( 22.59066674512275696, 64.25000000001213607, -136.5536116081545401 ) ) ;
#127576=CIRCLE ( 'NONE', #44199, 0.1000000000000028644 ) ;
#127582=CARTESIAN_POINT ( 'NONE',  ( -20.94999999999999929, 87.41227409416161720, -105.9231074845242091 ) ) ;
#127588=AXIS2_PLACEMENT_3D ( 'NONE', #166795, #202040, #65090 ) ;
#127593=CIRCLE ( 'NONE', #60934, 0.09999999999999939493 ) ;
#127594=LINE ( 'NONE', #46753, #239551 ) ;
#127615=LINE ( 'NONE', #29827, #216939 ) ;
#127626=CARTESIAN_POINT ( 'NONE',  ( -23.15000000000000213, 71.65000000001199965, -115.3731074845243256 ) ) ;
#127640=CYLINDRICAL_SURFACE ( 'NONE', #140025, 4.000000000000003553 ) ;
#127662=ORIENTED_EDGE ( 'NONE', *, *, #232940, .T. ) ;
#127664=VERTEX_POINT ( 'NONE', #65466 ) ;
#127665=EDGE_CURVE ( 'NONE', #199002, #14594, #194692, .T. ) ;
#127686=DIRECTION ( 'NONE',  ( 0.000000000000000000, 6.982962677686266711E-15, -1.000000000000000000 ) ) ;
#127689=CARTESIAN_POINT ( 'NONE',  ( 21.14999999999999858, 64.35000000001204512, -124.3731074845243825 ) ) ;
#127712=DIRECTION ( 'NONE',  ( 1.000000000000000000, 0.000000000000000000, 0.000000000000000000 ) ) ;
#127727=ORIENTED_EDGE ( 'NONE', *, *, #51988, .F. ) ;
#127737=CYLINDRICAL_SURFACE ( 'NONE', #65536, 0.1000000000000028644 ) ;
#127755=ORIENTED_EDGE ( 'NONE', *, *, #219239, .T. ) ;
#127769=EDGE_CURVE ( 'NONE', #113334, #138262, #57446, .T. ) ;
#127792=CARTESIAN_POINT ( 'NONE',  ( -20.64999999999999858, 76.00000000001213607, -136.5231074845242745 ) ) ;
#127794=AXIS2_PLACEMENT_3D ( 'NONE', #66908, #146426, #108605 ) ;
#127805=VERTEX_POINT ( 'NONE', #37925 ) ;
#127813=CARTESIAN_POINT ( 'NONE',  ( 20.94999999999997442, 77.26327546522911405, -95.12124281777788326 ) ) ;
#127851=ORIENTED_EDGE ( 'NONE', *, *, #205510, .T. ) ;
#127866=AXIS2_PLACEMENT_3D ( 'NONE', #224668, #27803, #65600 ) ;
#127879=DIRECTION ( 'NONE',  ( 0.000000000000000000, 0.000000000000000000, 1.000000000000000000 ) ) ;
#127893=DIRECTION ( 'NONE',  ( -1.000000000000000000, 0.000000000000000000, 0.000000000000000000 ) ) ;
#127904=TOROIDAL_SURFACE ( 'NONE', #36341, 11.65000000000000036, 0.1000000000000000056 ) ;
#127906=CARTESIAN_POINT ( 'NONE',  ( -23.15000000000000213, 87.65000000001214175, -136.5231074845242176 ) ) ;
#127964=ORIENTED_EDGE ( 'NONE', *, *, #49983, .F. ) ;
#127966=ORIENTED_EDGE ( 'NONE', *, *, #63923, .F. ) ;
#127981=DIRECTION ( 'NONE',  ( 0.000000000000000000, -0.9999631594459053030, -0.008583690987162452199 ) ) ;
#127982=DIRECTION ( 'NONE',  ( -0.000000000000000000, -1.000000000000000000, -6.982962677686266711E-15 ) ) ;
#127996=FACE_OUTER_BOUND ( 'NONE', #137491, .T. ) ;
#128011=EDGE_CURVE ( 'NONE', #182615, #153127, #54581, .T. ) ;
#128035=DIRECTION ( 'NONE',  ( -1.000000000000000000, 0.000000000000000000, -0.000000000000000000 ) ) ;
#128076=DIRECTION ( 'NONE',  ( -0.7071067811865127117, -0.7071067811865821007, 0.000000000000000000 ) ) ;
#128080=EDGE_CURVE ( 'NONE', #19771, #13368, #62288, .T. ) ;
#128092=DIRECTION ( 'NONE',  ( -0.000000000000000000, 1.000000000000000000, 6.982962677686266711E-15 ) ) ;
#128101=DIRECTION ( 'NONE',  ( 1.000000000000000000, 0.000000000000000000, 0.000000000000000000 ) ) ;
#128113=B_SPLINE_CURVE_WITH_KNOTS ( 'NONE', 3,
 ( #185799, #48853, #26753, #188369, #89257, #9722, #226169, #145380, #166273, #46273 ),
 .UNSPECIFIED., .F., .F.,
 ( 4, 3, 3, 4 ),
 ( 0.000000000000000000, 3.394313611810396763E-05, 6.779740500698037422E-05, 0.0001049857339142504432 ),
 .UNSPECIFIED. ) ;
#128125=AXIS2_PLACEMENT_3D ( 'NONE', #100816, #216943, #215657 ) ;
#128132=ADVANCED_FACE ( 'NONE', ( #221336 ), #140663, .F. ) ;
#128205=( BOUNDED_CURVE ( )  B_SPLINE_CURVE ( 3, ( #18778, #177880, #59156, #239123 ),
 .UNSPECIFIED., .F., .T. ) 
 B_SPLINE_CURVE_WITH_KNOTS ( ( 4, 4 ),
 ( 3.141592653589793116, 4.712388980384689674 ),
 .UNSPECIFIED. ) 
 CURVE ( )  GEOMETRIC_REPRESENTATION_ITEM ( )  RATIONAL_B_SPLINE_CURVE ( ( 1.000000000000000000, 0.8047378541243649375, 0.8047378541243649375, 1.000000000000000000 ) ) 
 REPRESENTATION_ITEM ( '' )  );
#128213=CARTESIAN_POINT ( 'NONE',  ( -23.15000000000000213, 76.00000000001188027, -99.12310748452429721 ) ) ;
#128307=DIRECTION ( 'NONE',  ( 0.000000000000000000, 0.000000000000000000, 1.000000000000000000 ) ) ;
#128311=DIRECTION ( 'NONE',  ( -0.000000000000000000, -1.000000000000000000, -6.982962677686266711E-15 ) ) ;
#128325=VERTEX_POINT ( 'NONE', #160960 ) ;
#128365=AXIS2_PLACEMENT_3D ( 'NONE', #92939, #228629, #91665 ) ;
#128386=CARTESIAN_POINT ( 'NONE',  ( 22.39999999999999858, 76.00000000001213607, -136.5231074845242745 ) ) ;
#128391=CARTESIAN_POINT ( 'NONE',  ( -18.50000000000000000, 77.73625713160946304, -124.9544551555067926 ) ) ;
#128398=FACE_OUTER_BOUND ( 'NONE', #230165, .T. ) ;
#128401=ORIENTED_EDGE ( 'NONE', *, *, #111742, .T. ) ;
#128422=AXIS2_PLACEMENT_3D ( 'NONE', #21099, #180159, #61484 ) ;
#128542=LINE ( 'NONE', #3444, #108279 ) ;
#128550=LINE ( 'NONE', #208107, #221058 ) ;
#128556=CYLINDRICAL_SURFACE ( 'NONE', #80262, 0.1000000000000028644 ) ;
#128565=FACE_OUTER_BOUND ( 'NONE', #186947, .T. ) ;
#128568=CARTESIAN_POINT ( 'NONE',  ( -20.64999999999999858, 85.00000000001207923, -126.6291383618717816 ) ) ;
#128572=DIRECTION ( 'NONE',  ( 0.000000000000000000, 0.000000000000000000, 1.000000000000000000 ) ) ;
#128609=VECTOR ( 'NONE', #136853, 1000.000000000000000 ) ;
#128625=DIRECTION ( 'NONE',  ( 2.978066053179069723E-16, 1.000000000000000000, 9.529811370173023114E-15 ) ) ;
#128638=CARTESIAN_POINT ( 'NONE',  ( 21.12230431290520372, 75.99479014832319024, -142.9806741378172887 ) ) ;
#128669=CIRCLE ( 'NONE', #8057, 0.09999999999999938105 ) ;
#128670=AXIS2_PLACEMENT_3D ( 'NONE', #156316, #118451, #197962 ) ;
#128671=FACE_OUTER_BOUND ( 'NONE', #191667, .T. ) ;
#128679=ORIENTED_EDGE ( 'NONE', *, *, #181227, .F. ) ;
#128694=EDGE_LOOP ( 'NONE', ( #231335, #187248, #134620, #212918 ) ) ;
#128698=FACE_OUTER_BOUND ( 'NONE', #219254, .T. ) ;
#128710=ORIENTED_EDGE ( 'NONE', *, *, #1149, .F. ) ;
#128716=VERTEX_POINT ( 'NONE', #196077 ) ;
#128719=LINE ( 'NONE', #25760, #189249 ) ;
#128739=AXIS2_PLACEMENT_3D ( 'NONE', #254537, #193326, #217984 ) ;
#128746=CYLINDRICAL_SURFACE ( 'NONE', #178855, 4.049999999999998046 ) ;
#128787=DIRECTION ( 'NONE',  ( 0.000000000000000000, -6.982962677686266711E-15, 1.000000000000000000 ) ) ;
#128813=ORIENTED_EDGE ( 'NONE', *, *, #252432, .F. ) ;
#128832=EDGE_CURVE ( 'NONE', #173897, #189309, #176597, .T. ) ;
#128912=DIRECTION ( 'NONE',  ( 1.000000000000000000, 0.000000000000000000, 0.000000000000000000 ) ) ;
#128916=CARTESIAN_POINT ( 'NONE',  ( -20.64999999999999858, 68.85000000001205933, -124.1731074845243370 ) ) ;
#128930=CARTESIAN_POINT ( 'NONE',  ( 18.59999999999999076, 69.60000000001207354, -126.5926828544627654 ) ) ;
#128934=CARTESIAN_POINT ( 'NONE',  ( 22.39999999999999503, 64.35000000001213039, -136.5231074845243597 ) ) ;
#128951=CARTESIAN_POINT ( 'NONE',  ( 20.94999999999999929, 69.55000000001207638, -126.5060803140843291 ) ) ;
#128955=FACE_OUTER_BOUND ( 'NONE', #62374, .T. ) ;
#128960=CARTESIAN_POINT ( 'NONE',  ( 20.97565083910961548, 65.52538259873327320, -128.9451643079358405 ) ) ;
#128962=VERTEX_POINT ( 'NONE', #124252 ) ;
#128995=DIRECTION ( 'NONE',  ( 0.000000000000000000, 0.000000000000000000, 1.000000000000000000 ) ) ;
#129025=DIRECTION ( 'NONE',  ( 0.7071067811865475727, 0.7071067811865475727, 4.937700262164531476E-15 ) ) ;
#129039=VECTOR ( 'NONE', #122646, 1000.000000000000000 ) ;
#129046=CARTESIAN_POINT ( 'NONE',  ( 20.94999999999999929, 77.83534155023646406, -124.9679561919612922 ) ) ;
#129068=EDGE_CURVE ( 'NONE', #200753, #92332, #240989, .T. ) ;
#129075=ADVANCED_FACE ( 'NONE', ( #208906 ), #147652, .T. ) ;
#129082=ORIENTED_EDGE ( 'NONE', *, *, #225598, .F. ) ;
#129084=ORIENTED_EDGE ( 'NONE', *, *, #247463, .T. ) ;
#129116=DIRECTION ( 'NONE',  ( 0.000000000000000000, 0.8700118002898393765, -0.4930308989875104575 ) ) ;
#129129=ORIENTED_EDGE ( 'NONE', *, *, #81127, .T. ) ;
#129151=CARTESIAN_POINT ( 'NONE',  ( -21.05000000000000071, 77.25000000001209344, -128.5231074845242745 ) ) ;
#129159=DIRECTION ( 'NONE',  ( 0.000000000000000000, 0.000000000000000000, -1.000000000000000000 ) ) ;
#129167=CARTESIAN_POINT ( 'NONE',  ( 21.30000000000002558, 76.00000000001216449, -140.5731074845242858 ) ) ;
#129175=EDGE_LOOP ( 'NONE', ( #194277, #165572, #164793, #87762 ) ) ;
#129188=DIRECTION ( 'NONE',  ( 0.000000000000000000, -6.467318590049456648E-15, 1.000000000000000000 ) ) ;
#129203=CARTESIAN_POINT ( 'NONE',  ( -21.05000000000000071, 69.58624026620188374, -136.4374944237204375 ) ) ;
#129215=CARTESIAN_POINT ( 'NONE',  ( 18.46905048506370406, 85.47374425739423032, -96.34712119226884397 ) ) ;
#129248=VECTOR ( 'NONE', #192005, 1000.000000000000000 ) ;
#129258=DIRECTION ( 'NONE',  ( -1.000000000000000000, -0.000000000000000000, -0.000000000000000000 ) ) ;
#129271=ORIENTED_EDGE ( 'NONE', *, *, #100537, .F. ) ;
#129373=CARTESIAN_POINT ( 'NONE',  ( 18.59999999999999076, 65.50857864377465489, -111.7731074845243597 ) ) ;
#129398=ADVANCED_FACE ( 'NONE', ( #169180 ), #128746, .F. ) ;
#129419=CIRCLE ( 'NONE', #104273, 12.97499999999999964 ) ;
#129437=CARTESIAN_POINT ( 'NONE',  ( -18.59999999999999787, 66.75000000001205080, -124.2731074845243597 ) ) ;
#129486=EDGE_CURVE ( 'NONE', #102511, #191930, #99116, .T. ) ;
#129509=CIRCLE ( 'NONE', #200231, 4.149999999999987033 ) ;
#129515=CARTESIAN_POINT ( 'NONE',  ( 20.94999999999999929, 87.48912529308798014, -106.1231074845242262 ) ) ;
#129519=DIRECTION ( 'NONE',  ( 0.000000000000000000, 0.9915357197604804940, -0.1298341882520397950 ) ) ;
#129528=EDGE_CURVE ( 'NONE', #31859, #14872, #156026, .T. ) ;
#129533=CARTESIAN_POINT ( 'NONE',  ( -20.87600722750343252, 65.66887361445333227, -97.43298459182690863 ) ) ;
#129535=DIRECTION ( 'NONE',  ( -0.000000000000000000, -0.1350103645451807555, -0.9908441862701610203 ) ) ;
#129563=AXIS2_PLACEMENT_3D ( 'NONE', #192750, #158770, #255219 ) ;
#129569=DIRECTION ( 'NONE',  ( 0.000000000000000000, 0.3738317757009942399, -0.9274965247785252886 ) ) ;
#129587=CARTESIAN_POINT ( 'NONE',  ( -18.59999999999999787, 66.65000000001198543, -115.3731074845243683 ) ) ;
#129590=ORIENTED_EDGE ( 'NONE', *, *, #164768, .T. ) ;
#129591=LINE ( 'NONE', #110012, #42611 ) ;
#129608=ADVANCED_FACE ( 'NONE', ( #200268, #20365, #122012 ), #24214, .F. ) ;
#129622=LINE ( 'NONE', #151776, #218309 ) ;
#129625=DIRECTION ( 'NONE',  ( -1.000000000000000000, 2.952720810173289112E-16, 2.061873921506763405E-30 ) ) ;
#129629=AXIS2_PLACEMENT_3D ( 'NONE', #205003, #8123, #225841 ) ;
#129631=FACE_OUTER_BOUND ( 'NONE', #68604, .T. ) ;
#129645=ORIENTED_EDGE ( 'NONE', *, *, #20427, .F. ) ;
#129648=CARTESIAN_POINT ( 'NONE',  ( -20.94999999999999929, 74.16465844978765176, -124.9679561919613207 ) ) ;
#129660=CARTESIAN_POINT ( 'NONE',  ( 18.49351773456780634, 85.44302569515717494, -129.3377819584974020 ) ) ;
#129667=DIRECTION ( 'NONE',  ( 1.000000000000000000, 0.000000000000000000, 0.000000000000000000 ) ) ;
#129711=CARTESIAN_POINT ( 'NONE',  ( 20.94999999999999929, 76.00000000001193712, -105.9231074845242944 ) ) ;
#129718=DIRECTION ( 'NONE',  ( 0.000000000000000000, -0.4999999999999689138, -0.8660254037844565822 ) ) ;
#129781=AXIS2_PLACEMENT_3D ( 'NONE', #16365, #174181, #48091 ) ;
#129792=CARTESIAN_POINT ( 'NONE',  ( -20.54999999999999716, 85.40000000001198543, -112.9170766071766820 ) ) ;
#129799=CARTESIAN_POINT ( 'NONE',  ( 21.00000000000000000, 66.25000000001206502, -124.1731074845243654 ) ) ;
#129815=CIRCLE ( 'NONE', #254675, 0.09999999999999939493 ) ;
#129816=DIRECTION ( 'NONE',  ( 1.000000000000000000, -0.000000000000000000, 0.000000000000000000 ) ) ;
#129841=FACE_OUTER_BOUND ( 'NONE', #45992, .T. ) ;
#129844=AXIS2_PLACEMENT_3D ( 'NONE', #79644, #139611, #40581 ) ;
#129907=DIRECTION ( 'NONE',  ( 0.000000000000000000, -7.086529944415894657E-15, 1.000000000000000000 ) ) ;
#129910=VERTEX_POINT ( 'NONE', #151877 ) ;
#129938=DIRECTION ( 'NONE',  ( 1.000000000000000000, 0.000000000000000000, 0.000000000000000000 ) ) ;
#129950=VECTOR ( 'NONE', #216805, 1000.000000000000000 ) ;
#129979=CARTESIAN_POINT ( 'NONE',  ( 23.14999999999999858, 70.40000000001207070, -124.1178414656112352 ) ) ;
#129986=EDGE_LOOP ( 'NONE', ( #106424, #155013, #68407, #51054 ) ) ;
#130006=AXIS2_PLACEMENT_3D ( 'NONE', #72013, #231096, #193238 ) ;
#130028=ORIENTED_EDGE ( 'NONE', *, *, #55718, .T. ) ;
#130042=ORIENTED_EDGE ( 'NONE', *, *, #151213, .T. ) ;
#130083=AXIS2_PLACEMENT_3D ( 'NONE', #157426, #23037, #21737 ) ;
#130107=FACE_OUTER_BOUND ( 'NONE', #199501, .T. ) ;
#130181=CARTESIAN_POINT ( 'NONE',  ( 20.94999999999999574, 77.26178616857710324, -128.4366085209788366 ) ) ;
#130182=CYLINDRICAL_SURFACE ( 'NONE', #153002, 0.09999999999998898659 ) ;
#130193=EDGE_LOOP ( 'NONE', ( #80213, #95784, #223459, #35452, #43203 ) ) ;
#130225=ORIENTED_EDGE ( 'NONE', *, *, #213877, .T. ) ;
#130230=AXIS2_PLACEMENT_3D ( 'NONE', #169434, #226789, #149850 ) ;
#130243=ORIENTED_EDGE ( 'NONE', *, *, #79876, .F. ) ;
#130266=EDGE_LOOP ( 'NONE', ( #168321, #134015, #113287, #52024 ) ) ;
#130301=CARTESIAN_POINT ( 'NONE',  ( 18.59999999999999432, 74.27191306321776665, -149.6386724793565577 ) ) ;
#130302=DIRECTION ( 'NONE',  ( -0.000000000000000000, -6.982962677686266711E-15, 1.000000000000000000 ) ) ;
#130312=EDGE_CURVE ( 'NONE', #160823, #65006, #78634, .T. ) ;
#130324=VECTOR ( 'NONE', #109378, 1000.000000000000114 ) ;
#130344=ORIENTED_EDGE ( 'NONE', *, *, #246489, .T. ) ;
#130362=ADVANCED_FACE ( 'NONE', ( #111134 ), #191983, .F. ) ;
#130380=VERTEX_POINT ( 'NONE', #198372 ) ;
#130408=AXIS2_PLACEMENT_3D ( 'NONE', #104170, #220302, #20825 ) ;
#130427=ADVANCED_FACE ( 'NONE', ( #18454 ), #158011, .T. ) ;
#130433=CARTESIAN_POINT ( 'NONE',  ( -23.15000000000000213, 71.65000000001207070, -124.1731074845243228 ) ) ;
#130453=DIRECTION ( 'NONE',  ( -1.000000000000000000, 0.000000000000000000, 0.000000000000000000 ) ) ;
#130484=CARTESIAN_POINT ( 'NONE',  ( -23.25000000000000000, 87.75000000001192291, -106.1231074845242262 ) ) ;
#130504=CARTESIAN_POINT ( 'NONE',  ( 19.81427058490527315, 64.33143601963020330, -111.7731074845243739 ) ) ;
#130505=EDGE_CURVE ( 'NONE', #54263, #198296, #186528, .T. ) ;
#130513=ORIENTED_EDGE ( 'NONE', *, *, #210064, .T. ) ;
#130515=CIRCLE ( 'NONE', #88807, 0.1000000000000052097 ) ;
#130525=EDGE_CURVE ( 'NONE', #82698, #130620, #20409, .T. ) ;
#130529=AXIS2_PLACEMENT_3D ( 'NONE', #51090, #128101, #109803 ) ;
#130532=DIRECTION ( 'NONE',  ( 1.000000000000000000, -3.265361837132813093E-16, -2.280189983783949500E-30 ) ) ;
#130551=TOROIDAL_SURFACE ( 'NONE', #209673, 12.77499999999999858, 0.1000000000000000056 ) ;
#130560=CARTESIAN_POINT ( 'NONE',  ( 18.50016250449482413, 65.70233904877112252, -97.54874109119650427 ) ) ;
#130583=AXIS2_PLACEMENT_3D ( 'NONE', #146091, #106962, #163117 ) ;
#130609=EDGE_CURVE ( 'NONE', #137344, #87320, #166355, .T. ) ;
#130620=VERTEX_POINT ( 'NONE', #135510 ) ;
#130678=CIRCLE ( 'NONE', #43218, 0.1000000000000028783 ) ;
#130696=ADVANCED_FACE ( 'NONE', ( #232084 ), #228866, .F. ) ;
#130717=FACE_OUTER_BOUND ( 'NONE', #157201, .T. ) ;
#130722=DIRECTION ( 'NONE',  ( 1.000000000000000000, -7.304098846218134667E-16, -5.100424963727256530E-30 ) ) ;
#130724=CIRCLE ( 'NONE', #184888, 0.1999999999999987899 ) ;
#130749=EDGE_LOOP ( 'NONE', ( #3799, #204913, #31153, #177829 ) ) ;
#130750=EDGE_LOOP ( 'NONE', ( #123406, #63714, #102888, #243860 ) ) ;
#130757=EDGE_CURVE ( 'NONE', #40198, #244668, #83069, .T. ) ;
#130784=AXIS2_PLACEMENT_3D ( 'NONE', #234536, #191600, #35100 ) ;
#130787=PLANE ( 'NONE',  #174120 ) ;
#130891=VERTEX_POINT ( 'NONE', #39013 ) ;
#130901=CIRCLE ( 'NONE', #147473, 2.000000000000001776 ) ;
#130933=CARTESIAN_POINT ( 'NONE',  ( 20.95512820512820440, 65.37615131630018084, -124.3731074845243825 ) ) ;
#130974=ORIENTED_EDGE ( 'NONE', *, *, #205976, .T. ) ;
#131059=DIRECTION ( 'NONE',  ( -1.000000000000000000, 2.952720810173289112E-16, 2.061873921506763405E-30 ) ) ;
#131064=AXIS2_PLACEMENT_3D ( 'NONE', #233628, #77105, #197039 ) ;
#131086=CIRCLE ( 'NONE', #193636, 0.09999999999998712696 ) ;
#131117=CARTESIAN_POINT ( 'NONE',  ( 20.85000000000000142, 87.65000000001190017, -103.0231074845242176 ) ) ;
#131137=EDGE_CURVE ( 'NONE', #60014, #122058, #141310, .T. ) ;
#131138=LINE ( 'NONE', #214518, #174498 ) ;
#131158=EDGE_LOOP ( 'NONE', ( #35301, #63636, #248716 ) ) ;
#131193=CARTESIAN_POINT ( 'NONE',  ( -18.50000000000000000, 66.65000000001205649, -124.1731074845243654 ) ) ;
#131196=DIRECTION ( 'NONE',  ( 1.000000000000000000, 0.000000000000000000, 0.000000000000000000 ) ) ;
#131236=LINE ( 'NONE', #253738, #204683 ) ;
#131248=CARTESIAN_POINT ( 'NONE',  ( -20.15000000000000568, 66.70857864377468616, -115.2731074845243597 ) ) ;
#131250=ORIENTED_EDGE ( 'NONE', *, *, #96677, .F. ) ;
#131254=DIRECTION ( 'NONE',  ( 0.000000000000000000, -6.547589603894034005E-15, 1.000000000000000000 ) ) ;
#131301=DIRECTION ( 'NONE',  ( -0.000000000000000000, 1.000000000000000000, 6.982962677686267499E-15 ) ) ;
#131315=ORIENTED_EDGE ( 'NONE', *, *, #109099, .T. ) ;
#131388=ORIENTED_EDGE ( 'NONE', *, *, #7963, .T. ) ;
#131402=VERTEX_POINT ( 'NONE', #251964 ) ;
#131404=PLANE ( 'NONE',  #208762 ) ;
#131408=CARTESIAN_POINT ( 'NONE',  ( -23.15000000000000213, 64.35000000001205933, -124.3731074845243825 ) ) ;
#131414=DIRECTION ( 'NONE',  ( 0.000000000000000000, 6.982962677686266711E-15, -1.000000000000000000 ) ) ;
#131426=DIRECTION ( 'NONE',  ( 0.000000000000000000, 0.8660254037844378194, 0.5000000000000016653 ) ) ;
#131431=CARTESIAN_POINT ( 'NONE',  ( 21.12802099929860944, 67.21944740978983646, -124.2749174995927461 ) ) ;
#131497=AXIS2_PLACEMENT_3D ( 'NONE', #33835, #169490, #50751 ) ;
#131517=DIRECTION ( 'NONE',  ( 0.000000000000000000, 0.000000000000000000, 1.000000000000000000 ) ) ;
#131522=ORIENTED_EDGE ( 'NONE', *, *, #208554, .T. ) ;
#131555=CARTESIAN_POINT ( 'NONE',  ( 21.00000000000000000, 66.25000000001199396, -115.2731074845243597 ) ) ;
#131586=ORIENTED_EDGE ( 'NONE', *, *, #69902, .F. ) ;
#131603=EDGE_LOOP ( 'NONE', ( #215101, #255149, #118483, #249070, #249442 ) ) ;
#131610=DIRECTION ( 'NONE',  ( -1.000000000000000000, 0.000000000000000000, 0.000000000000000000 ) ) ;
#131626=AXIS2_PLACEMENT_3D ( 'NONE', #96529, #255575, #91429 ) ;
#131646=( BOUNDED_CURVE ( )  B_SPLINE_CURVE ( 3, ( #70169, #7598, #68876, #187546 ),
 .UNSPECIFIED., .F., .F. ) 
 B_SPLINE_CURVE_WITH_KNOTS ( ( 4, 4 ),
 ( 4.712388980384690562, 6.283185307179586232 ),
 .UNSPECIFIED. ) 
 CURVE ( )  GEOMETRIC_REPRESENTATION_ITEM ( )  RATIONAL_B_SPLINE_CURVE ( ( 1.000000000000000000, 0.8047378541243652705, 0.8047378541243652705, 1.000000000000000000 ) ) 
 REPRESENTATION_ITEM ( '' )  );
#131659=CARTESIAN_POINT ( 'NONE',  ( 18.50000000000000355, 85.42107434499847329, -96.19863542509438048 ) ) ;
#131672=EDGE_LOOP ( 'NONE', ( #119529, #43523 ) ) ;
#131694=VERTEX_POINT ( 'NONE', #208711 ) ;
#131699=CARTESIAN_POINT ( 'NONE',  ( -20.64999999999999858, 71.65000000001207070, -124.1731074845243228 ) ) ;
#131777=DIRECTION ( 'NONE',  ( -1.000000000000000000, 0.000000000000000000, 0.000000000000000000 ) ) ;
#131795=CARTESIAN_POINT ( 'NONE',  ( 19.97071067811865674, 64.27928932189330169, -111.8731074845243825 ) ) ;
#131831=AXIS2_PLACEMENT_3D ( 'NONE', #245577, #43526, #203863 ) ;
#131840=EDGE_CURVE ( 'NONE', #161509, #130891, #153908, .T. ) ;
#131849=ORIENTED_EDGE ( 'NONE', *, *, #150753, .F. ) ;
#131850=CARTESIAN_POINT ( 'NONE',  ( 18.50000972452444969, 65.70673848566960373, -97.56382523348291613 ) ) ;
#131854=CARTESIAN_POINT ( 'NONE',  ( 23.15000000000000213, 84.66355140188112216, -112.5472086025915388 ) ) ;
#131872=ORIENTED_EDGE ( 'NONE', *, *, #256992, .T. ) ;
#131904=EDGE_CURVE ( 'NONE', #257751, #225759, #179851, .T. ) ;
#131922=ORIENTED_EDGE ( 'NONE', *, *, #231621, .T. ) ;
#131928=ORIENTED_EDGE ( 'NONE', *, *, #198714, .F. ) ;
#131943=CARTESIAN_POINT ( 'NONE',  ( -22.39999999999999858, 76.00000000001222134, -148.1726782920690937 ) ) ;
#131981=CARTESIAN_POINT ( 'NONE',  ( 21.05000000000000071, 76.00000000001192291, -105.0231074845243029 ) ) ;
#132002=EDGE_LOOP ( 'NONE', ( #3756, #44237, #68859, #176548, #227015 ) ) ;
#132007=DIRECTION ( 'NONE',  ( 0.000000000000000000, 0.000000000000000000, 1.000000000000000000 ) ) ;
#132083=EDGE_LOOP ( 'NONE', ( #199682, #38699, #36719, #189555 ) ) ;
#132127=FACE_OUTER_BOUND ( 'NONE', #256165, .T. ) ;
#132141=EDGE_LOOP ( 'NONE', ( #202849, #65879, #200863, #65441 ) ) ;
#132150=ADVANCED_FACE ( 'NONE', ( #234354 ), #96297, .T. ) ;
#132163=EDGE_CURVE ( 'NONE', #80026, #60977, #112892, .T. ) ;
#132164=DIRECTION ( 'NONE',  ( 1.836970198721029934E-16, 1.000000000000000000, 6.982962677686266711E-15 ) ) ;
#132190=DIRECTION ( 'NONE',  ( 0.000000000000000000, 0.4930308989875575865, 0.8700118002898125091 ) ) ;
#132191=CARTESIAN_POINT ( 'NONE',  ( -18.59999999999999787, 64.35000000001198828, -115.1731074845243796 ) ) ;
#132196=ADVANCED_FACE ( 'NONE', ( #93566 ), #131404, .F. ) ;
#132218=CARTESIAN_POINT ( 'NONE',  ( 21.05000012384953223, 65.37127970113643016, -124.3451301544889702 ) ) ;
#132222=DIRECTION ( 'NONE',  ( -0.000000000000000000, -6.982962677686266711E-15, 1.000000000000000000 ) ) ;
#132227=VERTEX_POINT ( 'NONE', #50125 ) ;
#132239=DIRECTION ( 'NONE',  ( 0.000000000000000000, -1.000000000000000000, -6.982962677686265922E-15 ) ) ;
#132249=FACE_OUTER_BOUND ( 'NONE', #111704, .T. ) ;
#132256=CARTESIAN_POINT ( 'NONE',  ( -20.94999999999999929, 87.65000000001192859, -106.0231074845242176 ) ) ;
#132266=ADVANCED_FACE ( 'NONE', ( #5851 ), #137991, .F. ) ;
#132272=CARTESIAN_POINT ( 'NONE',  ( -20.94999999999999929, 70.10000000001213039, -126.3040077198679398 ) ) ;
#132277=EDGE_CURVE ( 'NONE', #220426, #14895, #71401, .T. ) ;
#132285=AXIS2_PLACEMENT_3D ( 'NONE', #134035, #250148, #173227 ) ;
#132333=ORIENTED_EDGE ( 'NONE', *, *, #253030, .T. ) ;
#132343=VERTEX_POINT ( 'NONE', #86660 ) ;
#132352=AXIS2_PLACEMENT_3D ( 'NONE', #180372, #60406, #219477 ) ;
#132363=CARTESIAN_POINT ( 'NONE',  ( 22.45305468355011058, 76.10085836911193269, -148.2726746080140288 ) ) ;
#132396=CIRCLE ( 'NONE', #236437, 0.2000000000000057288 ) ;
#132397=EDGE_CURVE ( 'NONE', #49989, #200718, #121310, .T. ) ;
#132408=CARTESIAN_POINT ( 'NONE',  ( 23.24999999999999289, 71.85000000001214460, -136.5231074845243029 ) ) ;
#132453=AXIS2_PLACEMENT_3D ( 'NONE', #1561, #99368, #121560 ) ;
#132478=DIRECTION ( 'NONE',  ( 0.000000000000000000, -0.1350103645451807555, -0.9908441862701610203 ) ) ;
#132480=CARTESIAN_POINT ( 'NONE',  ( 21.13614978966382196, 76.00000000001217870, -143.0222121863580753 ) ) ;
#132504=CARTESIAN_POINT ( 'NONE',  ( 20.94999999999999929, 69.45000000001206786, -126.5060803140843291 ) ) ;
#132509=DIRECTION ( 'NONE',  ( 0.000000000000000000, -0.1350103645451807555, -0.9908441862701610203 ) ) ;
#132566=CIRCLE ( 'NONE', #119946, 0.5000000000000004441 ) ;
#132594=ADVANCED_FACE ( 'NONE', ( #56455 ), #19711, .T. ) ;
#132630=ORIENTED_EDGE ( 'NONE', *, *, #207385, .T. ) ;
#132670=ORIENTED_EDGE ( 'NONE', *, *, #154423, .T. ) ;
#132685=DIRECTION ( 'NONE',  ( 0.000000000000000000, 0.000000000000000000, 1.000000000000000000 ) ) ;
#132704=ORIENTED_EDGE ( 'NONE', *, *, #237450, .F. ) ;
#132710=DIRECTION ( 'NONE',  ( 0.000000000000000000, -7.026728003956683390E-15, 1.000000000000000000 ) ) ;
#132714=ORIENTED_EDGE ( 'NONE', *, *, #132163, .F. ) ;
#132719=FACE_OUTER_BOUND ( 'NONE', #185130, .T. ) ;
#132751=EDGE_LOOP ( 'NONE', ( #187686, #631, #224616, #165623 ) ) ;
#132767=VECTOR ( 'NONE', #104938, 1000.000000000000000 ) ;
#132768=AXIS2_PLACEMENT_3D ( 'NONE', #24994, #224442, #221855 ) ;
#132776=DIRECTION ( 'NONE',  ( -1.000000000000000000, 0.000000000000000000, -0.000000000000000000 ) ) ;
#132782=DIRECTION ( 'NONE',  ( 0.000000000000000000, 0.000000000000000000, -1.000000000000000000 ) ) ;
#132784=EDGE_CURVE ( 'NONE', #174818, #13368, #150332, .T. ) ;
#132787=DIRECTION ( 'NONE',  ( 0.000000000000000000, 1.000000000000000000, 6.982962677686266711E-15 ) ) ;
#132798=ADVANCED_FACE ( 'NONE', ( #187986 ), #25768, .T. ) ;
#132810=CARTESIAN_POINT ( 'NONE',  ( 20.97462148592276776, 67.12526242356146611, -124.2684631527937000 ) ) ;
#132841=ORIENTED_EDGE ( 'NONE', *, *, #10501, .T. ) ;
#132852=ORIENTED_EDGE ( 'NONE', *, *, #113015, .T. ) ;
#132889=CIRCLE ( 'NONE', #53763, 7.800000000000001599 ) ;
#132909=ORIENTED_EDGE ( 'NONE', *, *, #187947, .T. ) ;
#132914=ORIENTED_EDGE ( 'NONE', *, *, #74493, .F. ) ;
#132920=AXIS2_PLACEMENT_3D ( 'NONE', #97759, #78218, #157812 ) ;
#132950=EDGE_LOOP ( 'NONE', ( #1980, #163807, #196665, #254050 ) ) ;
#132986=EDGE_CURVE ( 'NONE', #231766, #211151, #250807, .T. ) ;
#133022=CARTESIAN_POINT ( 'NONE',  ( -18.50000000000000000, 64.25000000001199396, -115.1731074845243796 ) ) ;
#133028=DIRECTION ( 'NONE',  ( 0.000000000000000000, -7.056502275159890043E-15, 1.000000000000000000 ) ) ;
#133044=DIRECTION ( 'NONE',  ( 0.000000000000000000, -7.147358527629759053E-15, 1.000000000000000000 ) ) ;
#133056=ADVANCED_FACE ( 'NONE', ( #122577 ), #209115, .T. ) ;
#133114=CARTESIAN_POINT ( 'NONE',  ( 18.59999999999999076, 76.00000000001190870, -103.0231074845243029 ) ) ;
#133133=DIRECTION ( 'NONE',  ( 0.000000000000000000, -1.000000000000000000, -6.982962677686266711E-15 ) ) ;
#133141=CARTESIAN_POINT ( 'NONE',  ( 18.52643265882457868, 65.68026841930898740, -97.47257401318893244 ) ) ;
#133170=ORIENTED_EDGE ( 'NONE', *, *, #94094, .T. ) ;
#133177=AXIS2_PLACEMENT_3D ( 'NONE', #227728, #131196, #129907 ) ;
#133202=DIRECTION ( 'NONE',  ( 0.000000000000000000, -1.000000000000000000, -6.982962677686265922E-15 ) ) ;
#133234=CARTESIAN_POINT ( 'NONE',  ( 19.58285714285715073, 66.98499851036351060, -128.1024546684426468 ) ) ;
#133236=ORIENTED_EDGE ( 'NONE', *, *, #150311, .F. ) ;
#133238=VERTEX_POINT ( 'NONE', #113265 ) ;
#133257=EDGE_CURVE ( 'NONE', #17884, #88196, #171999, .T. ) ;
#133267=CARTESIAN_POINT ( 'NONE',  ( 20.95520789717937404, 65.42306940062712783, -128.9428745106495171 ) ) ;
#133268=DIRECTION ( 'NONE',  ( -0.7071067811865127117, -0.7071067811865821007, 0.000000000000000000 ) ) ;
#133273=CARTESIAN_POINT ( 'NONE',  ( 21.14999999999999858, 76.10000000001222986, -148.1726782920690937 ) ) ;
#133276=CARTESIAN_POINT ( 'NONE',  ( 22.49436431346199683, 75.93309647028996778, -148.1730584321777542 ) ) ;
#133299=CARTESIAN_POINT ( 'NONE',  ( -20.54999999999999716, 71.65000000001207070, -124.1731074845243228 ) ) ;
#133331=LINE ( 'NONE', #108626, #161063 ) ;
#133333=EDGE_CURVE ( 'NONE', #99212, #11251, #234224, .T. ) ;
#133367=VERTEX_POINT ( 'NONE', #233237 ) ;
#133371=EDGE_LOOP ( 'NONE', ( #176795, #163841, #16169, #225999 ) ) ;
#133376=AXIS2_PLACEMENT_3D ( 'NONE', #192142, #170037, #188263 ) ;
#133390=ORIENTED_EDGE ( 'NONE', *, *, #134336, .F. ) ;
#133410=EDGE_CURVE ( 'NONE', #58209, #127492, #9376, .T. ) ;
#133417=CARTESIAN_POINT ( 'NONE',  ( -23.25000000000000000, 76.10000000001222986, -148.1726782920690937 ) ) ;
#133439=EDGE_CURVE ( 'NONE', #70203, #164631, #126069, .T. ) ;
#133459=ORIENTED_EDGE ( 'NONE', *, *, #171165, .T. ) ;
#133473=CARTESIAN_POINT ( 'NONE',  ( 21.05000000000000071, 65.27628289530457550, -128.8581939154367717 ) ) ;
#133486=DIRECTION ( 'NONE',  ( 1.000000000000000000, 0.000000000000000000, 0.000000000000000000 ) ) ;
#133489=CARTESIAN_POINT ( 'NONE',  ( 18.59999999999999432, 77.16270174995010223, -128.4231074845242802 ) ) ;
#133517=ADVANCED_FACE ( 'NONE', ( #6129 ), #145644, .F. ) ;
#133520=PLANE ( 'NONE',  #70472 ) ;
#133527=CARTESIAN_POINT ( 'NONE',  ( -18.59999999999999787, 77.16412189325305349, -95.30825939895268561 ) ) ;
#133546=ORIENTED_EDGE ( 'NONE', *, *, #245838, .T. ) ;
#133579=CARTESIAN_POINT ( 'NONE',  ( 18.59999999999999432, 77.29973367124300410, -146.4949779616548824 ) ) ;
#133594=CARTESIAN_POINT ( 'NONE',  ( -21.08035267497491816, 75.91731137523616724, -142.8548143243073696 ) ) ;
#133603=DIRECTION ( 'NONE',  ( 1.000000000000000000, -3.265361837132813093E-16, -2.280189983783949500E-30 ) ) ;
#133645=LINE ( 'NONE', #232764, #217350 ) ;
#133654=ORIENTED_EDGE ( 'NONE', *, *, #184450, .T. ) ;
#133665=DIRECTION ( 'NONE',  ( 0.000000000000000000, -0.9908441862701791170, 0.1350103645450472789 ) ) ;
#133688=CARTESIAN_POINT ( 'NONE',  ( -20.64999999999999858, 71.65000000001207070, -124.1731074845243228 ) ) ;
#133705=CARTESIAN_POINT ( 'NONE',  ( -20.64999999999999858, 76.00000000001190870, -103.0231074845243029 ) ) ;
#133714=ORIENTED_EDGE ( 'NONE', *, *, #36519, .F. ) ;
#133727=AXIS2_PLACEMENT_3D ( 'NONE', #201733, #217426, #77928 ) ;
#133735=CARTESIAN_POINT ( 'NONE',  ( -22.60000000000080789, 75.95218301954683682, -148.2731299156770319 ) ) ;
#133784=CIRCLE ( 'NONE', #50572, 0.5000000000000004441 ) ;
#133787=EDGE_LOOP ( 'NONE', ( #48371, #33849, #237358, #76684 ) ) ;
#133795=CARTESIAN_POINT ( 'NONE',  ( -23.25000000000000000, 64.35000000001195986, -110.0379132551783385 ) ) ;
#133813=AXIS2_PLACEMENT_3D ( 'NONE', #209351, #9870, #184651 ) ;
#133831=CARTESIAN_POINT ( 'NONE',  ( -20.85000000000000142, 64.25000000001195133, -109.8069731475024753 ) ) ;
#133836=ORIENTED_EDGE ( 'NONE', *, *, #199872, .T. ) ;
#133859=AXIS2_PLACEMENT_3D ( 'NONE', #48653, #47356, #23984 ) ;
#133934=ORIENTED_EDGE ( 'NONE', *, *, #214175, .T. ) ;
#133948=ORIENTED_EDGE ( 'NONE', *, *, #53352, .F. ) ;
#133971=CARTESIAN_POINT ( 'NONE',  ( 20.94999999999999929, 64.35000000001195986, -109.8647081744214233 ) ) ;
#133977=CIRCLE ( 'NONE', #96544, 0.1000000000000028644 ) ;
#133982=AXIS2_PLACEMENT_3D ( 'NONE', #169127, #33472, #247332 ) ;
#133985=DIRECTION ( 'NONE',  ( 0.000000000000000000, -0.1568667991644355497, -0.9876197685951332295 ) ) ;
#134015=ORIENTED_EDGE ( 'NONE', *, *, #133257, .T. ) ;
#134018=CIRCLE ( 'NONE', #117474, 11.65000000000000746 ) ;
#134035=CARTESIAN_POINT ( 'NONE',  ( -21.14999999999999858, 75.90220970870339556, -142.7809220950004203 ) ) ;
#134061=FACE_OUTER_BOUND ( 'NONE', #161598, .T. ) ;
#134073=CARTESIAN_POINT ( 'NONE',  ( -23.15000000000000213, 70.10000000001197407, -113.2422072491807086 ) ) ;
#134080=EDGE_CURVE ( 'NONE', #207709, #103697, #196985, .T. ) ;
#134092=ORIENTED_EDGE ( 'NONE', *, *, #74097, .T. ) ;
#134104=LINE ( 'NONE', #49774, #63067 ) ;
#134111=ORIENTED_EDGE ( 'NONE', *, *, #174089, .F. ) ;
#134138=EDGE_CURVE ( 'NONE', #3363, #85598, #63925, .T. ) ;
#134175=FACE_OUTER_BOUND ( 'NONE', #141887, .T. ) ;
#134176=CIRCLE ( 'NONE', #21780, 0.1000000000000028644 ) ;
#134189=EDGE_LOOP ( 'NONE', ( #132852, #144934, #228542, #177224 ) ) ;
#134205=CARTESIAN_POINT ( 'NONE',  ( -22.39999999999999858, 64.35000000001214460, -136.6231074845243825 ) ) ;
#134211=ORIENTED_EDGE ( 'NONE', *, *, #39954, .T. ) ;
#134240=ORIENTED_EDGE ( 'NONE', *, *, #136531, .F. ) ;
#134273=DIRECTION ( 'NONE',  ( 1.000000000000000000, 0.000000000000000000, 0.000000000000000000 ) ) ;
#134299=CARTESIAN_POINT ( 'NONE',  ( -20.94999999999999929, 77.16270174995010223, -128.4231074845242802 ) ) ;
#134316=DIRECTION ( 'NONE',  ( 0.000000000000000000, -1.000000000000000000, -6.982962677686266711E-15 ) ) ;
#134320=EDGE_LOOP ( 'NONE', ( #140778, #235857 ) ) ;
#134325=AXIS2_PLACEMENT_3D ( 'NONE', #96454, #100306, #138151 ) ;
#134329=CARTESIAN_POINT ( 'NONE',  ( -23.25000000000000000, 64.25000000001215028, -136.5231074845243597 ) ) ;
#134336=EDGE_CURVE ( 'NONE', #221411, #13648, #255400, .T. ) ;
#134365=CARTESIAN_POINT ( 'NONE',  ( 21.59780538579341780, 75.90102133041420984, -143.3701980144675474 ) ) ;
#134367=CARTESIAN_POINT ( 'NONE',  ( 21.00000000000000000, 66.25000000001199396, -115.2731074845243597 ) ) ;
#134388=FACE_OUTER_BOUND ( 'NONE', #163548, .T. ) ;
#134401=CARTESIAN_POINT ( 'NONE',  ( 21.05000000000000071, 76.00000000001193712, -107.0231074845243029 ) ) ;
#134413=CARTESIAN_POINT ( 'NONE',  ( 22.57320508075687115, 64.25000000001215028, -136.5231074845243597 ) ) ;
#134422=ORIENTED_EDGE ( 'NONE', *, *, #154504, .F. ) ;
#134428=ADVANCED_FACE ( 'NONE', ( #250250 ), #231993, .F. ) ;
#134440=VERTEX_POINT ( 'NONE', #113304 ) ;
#134445=DIRECTION ( 'NONE',  ( 1.000000000000000000, 0.000000000000000000, 0.000000000000000000 ) ) ;
#134469=ORIENTED_EDGE ( 'NONE', *, *, #220639, .F. ) ;
#134500=EDGE_LOOP ( 'NONE', ( #11360, #161898, #10186, #154341 ) ) ;
#134504=DIRECTION ( 'NONE',  ( -1.000000000000000000, 0.000000000000000000, -0.000000000000000000 ) ) ;
#134527=CARTESIAN_POINT ( 'NONE',  ( -22.39999999999999858, 64.35000000001214460, -136.6231074845243825 ) ) ;
#134533=CARTESIAN_POINT ( 'NONE',  ( 22.42196299218230493, 75.99755832602491523, -148.1727191871737830 ) ) ;
#134544=FACE_OUTER_BOUND ( 'NONE', #47012, .T. ) ;
#134547=FACE_OUTER_BOUND ( 'NONE', #11735, .T. ) ;
#134580=AXIS2_PLACEMENT_3D ( 'NONE', #156542, #152689, #236037 ) ;
#134595=CARTESIAN_POINT ( 'NONE',  ( -20.94999999999999929, 87.65000000001191438, -103.0231074845242176 ) ) ;
#134599=DIRECTION ( 'NONE',  ( 0.000000000000000000, 0.000000000000000000, 1.000000000000000000 ) ) ;
#134620=ORIENTED_EDGE ( 'NONE', *, *, #202244, .T. ) ;
#134624=VECTOR ( 'NONE', #148173, 1000.000000000000000 ) ;
#134629=CARTESIAN_POINT ( 'NONE',  ( -21.00023020733502932, 76.00000000001219291, -142.9139767297926369 ) ) ;
#134676=AXIS2_PLACEMENT_3D ( 'NONE', #220510, #177561, #21037 ) ;
#134757=CARTESIAN_POINT ( 'NONE',  ( -23.25000000000000000, 74.00000000001199396, -116.2477294072864140 ) ) ;
#134769=CARTESIAN_POINT ( 'NONE',  ( -20.94999999999999929, 87.65000000001192859, -105.9231074845242091 ) ) ;
#134785=CYLINDRICAL_SURFACE ( 'NONE', #81355, 0.09999999999998898659 ) ;
#134809=AXIS2_PLACEMENT_3D ( 'NONE', #25671, #127333, #128625 ) ;
#134813=ORIENTED_EDGE ( 'NONE', *, *, #42546, .F. ) ;
#134831=CARTESIAN_POINT ( 'NONE',  ( 20.94999999999999929, 87.48912529308798014, -106.1231074845242262 ) ) ;
#134837=CARTESIAN_POINT ( 'NONE',  ( -23.25000000000000000, 84.59626168225496201, -112.4732350016745102 ) ) ;
#134843=CIRCLE ( 'NONE', #22478, 0.09999999999999938105 ) ;
#134875=ORIENTED_EDGE ( 'NONE', *, *, #82200, .F. ) ;
#134897=CARTESIAN_POINT ( 'NONE',  ( 21.05000000000000071, 76.10000000001218723, -143.0637644362255401 ) ) ;
#134902=EDGE_CURVE ( 'NONE', #182665, #183267, #34514, .T. ) ;
#134905=FACE_OUTER_BOUND ( 'NONE', #142819, .T. ) ;
#134917=SPHERICAL_SURFACE ( 'NONE', #236426, 0.1000000000000000056 ) ;
#134934=DIRECTION ( 'NONE',  ( 1.000000000000000000, 0.000000000000000000, 0.000000000000000000 ) ) ;
#134957=ORIENTED_EDGE ( 'NONE', *, *, #221011, .F. ) ;
#135004=CARTESIAN_POINT ( 'NONE',  ( 23.14999999999998792, 64.35000000001214460, -136.5231074845243597 ) ) ;
#135035=CARTESIAN_POINT ( 'NONE',  ( -21.14999999999999858, 76.00000000001219291, -143.0637644362255401 ) ) ;
#135040=VERTEX_POINT ( 'NONE', #241915 ) ;
#135064=EDGE_CURVE ( 'NONE', #92332, #119361, #184690, .T. ) ;
#135070=FACE_OUTER_BOUND ( 'NONE', #40287, .T. ) ;
#135101=ORIENTED_EDGE ( 'NONE', *, *, #100830, .F. ) ;
#135118=DIRECTION ( 'NONE',  ( 0.000000000000000000, 6.982962677686266711E-15, -1.000000000000000000 ) ) ;
#135160=DIRECTION ( 'NONE',  ( 0.000000000000000000, 0.000000000000000000, 1.000000000000000000 ) ) ;
#135171=DIRECTION ( 'NONE',  ( -0.7071067811865474617, 0.7071067811865474617, 4.937700262164531476E-15 ) ) ;
#135193=ORIENTED_EDGE ( 'NONE', *, *, #49468, .T. ) ;
#135210=CIRCLE ( 'NONE', #22827, 0.1000000000000072220 ) ;
#135225=ADVANCED_FACE ( 'NONE', ( #236482 ), #192903, .T. ) ;
#135254=AXIS2_PLACEMENT_3D ( 'NONE', #247427, #109192, #70112 ) ;
#135261=CARTESIAN_POINT ( 'NONE',  ( -20.94999999999999929, 68.92903212821303782, -99.27654326265604823 ) ) ;
#135269=CARTESIAN_POINT ( 'NONE',  ( -23.15000000000000213, 76.00000000001213607, -136.5231074845242745 ) ) ;
#135274=EDGE_CURVE ( 'NONE', #31859, #239007, #5604, .T. ) ;
#135339=CARTESIAN_POINT ( 'NONE',  ( 21.12400222705966257, 67.22148809293496186, -124.2731074845243597 ) ) ;
#135386=EDGE_LOOP ( 'NONE', ( #162215, #152051, #255717, #238256 ) ) ;
#135409=CARTESIAN_POINT ( 'NONE',  ( -20.54999999999999716, 76.00000000001190870, -103.0231074845243029 ) ) ;
#135419=ADVANCED_FACE ( 'NONE', ( #107244 ), #249344, .F. ) ;
#135435=ADVANCED_FACE ( 'NONE', ( #87669 ), #189363, .T. ) ;
#135439=AXIS2_PLACEMENT_3D ( 'NONE', #134527, #7194, #193247 ) ;
#135445=CARTESIAN_POINT ( 'NONE',  ( -18.59999999999999787, 77.73670573947940454, -91.50568489690056140 ) ) ;
#135483=CARTESIAN_POINT ( 'NONE',  ( -18.50000000000000000, 85.50000000001223555, -148.2731074845242460 ) ) ;
#135488=ORIENTED_EDGE ( 'NONE', *, *, #60846, .F. ) ;
#135490=CARTESIAN_POINT ( 'NONE',  ( 18.43630871534871218, 85.67980087481485896, -96.36247541654022086 ) ) ;
#135510=CARTESIAN_POINT ( 'NONE',  ( -20.64999999999999858, 73.50000000001199396, -116.2477294072864140 ) ) ;
#135531=DIRECTION ( 'NONE',  ( 0.000000000000000000, -1.000000000000000000, 0.000000000000000000 ) ) ;
#135544=DIRECTION ( 'NONE',  ( 0.000000000000000000, 0.000000000000000000, 1.000000000000000000 ) ) ;
#135564=CARTESIAN_POINT ( 'NONE',  ( 23.15000000000000213, 85.60000000001197407, -112.9170766071766820 ) ) ;
#135575=ORIENTED_EDGE ( 'NONE', *, *, #24902, .F. ) ;
#135644=CARTESIAN_POINT ( 'NONE',  ( 18.49999999999999289, 64.35000000001191722, -103.0231074845243882 ) ) ;
#135692=ADVANCED_FACE ( 'NONE', ( #2362 ), #191085, .T. ) ;
#135716=CARTESIAN_POINT ( 'NONE',  ( -21.05000000000000071, 64.35000000001208775, -129.7392418215462158 ) ) ;
#135717=ORIENTED_EDGE ( 'NONE', *, *, #161592, .T. ) ;
#135721=AXIS2_PLACEMENT_3D ( 'NONE', #64818, #85632, #89509 ) ;
#135739=TOROIDAL_SURFACE ( 'NONE', #89949, 11.65000000000000036, 0.1000000000000000056 ) ;
#135748=EDGE_LOOP ( 'NONE', ( #257294, #11347, #106690, #6544 ) ) ;
#135751=ORIENTED_EDGE ( 'NONE', *, *, #184861, .T. ) ;
#135755=EDGE_CURVE ( 'NONE', #239290, #132343, #186156, .T. ) ;
#135765=AXIS2_PLACEMENT_3D ( 'NONE', #252153, #132222, #193494 ) ;
#135767=CARTESIAN_POINT ( 'NONE',  ( -23.15000000000000213, 64.25000000001199396, -115.1731074845243796 ) ) ;
#135850=ADVANCED_FACE ( 'NONE', ( #38508 ), #158476, .T. ) ;
#135861=EDGE_CURVE ( 'NONE', #16840, #213344, #93297, .T. ) ;
#135928=DIRECTION ( 'NONE',  ( 2.952720810173289112E-16, 1.000000000000000000, -6.088138035986627436E-46 ) ) ;
#135941=CARTESIAN_POINT ( 'NONE',  ( -18.59999999999999787, 85.48068669529084218, -96.08199231576638510 ) ) ;
#135951=EDGE_CURVE ( 'NONE', #149997, #67927, #130901, .T. ) ;
#135963=CIRCLE ( 'NONE', #15183, 0.09999999999999939493 ) ;
#135972=ORIENTED_EDGE ( 'NONE', *, *, #182710, .F. ) ;
#135980=DIRECTION ( 'NONE',  ( 1.000000000000000000, -3.265361837132813093E-16, -2.280189983783949500E-30 ) ) ;
#135981=VERTEX_POINT ( 'NONE', #246964 ) ;
#135988=VECTOR ( 'NONE', #52788, 1000.000000000000000 ) ;
#136025=DIRECTION ( 'NONE',  ( 0.000000000000000000, 0.000000000000000000, -1.000000000000000000 ) ) ;
#136042=EDGE_CURVE ( 'NONE', #220397, #206536, #145289, .T. ) ;
#136049=DIRECTION ( 'NONE',  ( 0.000000000000000000, 0.000000000000000000, 1.000000000000000000 ) ) ;
#136053=CIRCLE ( 'NONE', #161033, 0.09999999999998898659 ) ;
#136059=DIRECTION ( 'NONE',  ( 1.000000000000000000, 0.000000000000000000, 0.000000000000000000 ) ) ;
#136061=DIRECTION ( 'NONE',  ( 0.000000000000000000, 0.000000000000000000, 1.000000000000000000 ) ) ;
#136067=DIRECTION ( 'NONE',  ( 1.000000000000000000, 0.000000000000000000, 0.000000000000000000 ) ) ;
#136083=CARTESIAN_POINT ( 'NONE',  ( -18.59999999999999787, 69.15387683765929694, -99.28538121767448388 ) ) ;
#136116=EDGE_CURVE ( 'NONE', #13808, #121700, #89201, .T. ) ;
#136136=ADVANCED_FACE ( 'NONE', ( #119988 ), #41720, .T. ) ;
#136137=CARTESIAN_POINT ( 'NONE',  ( -18.43634282235119670, 85.67978719993983816, -96.36245559907032998 ) ) ;
#136182=ORIENTED_EDGE ( 'NONE', *, *, #91438, .F. ) ;
#136196=EDGE_CURVE ( 'NONE', #236918, #143411, #193273, .T. ) ;
#136218=DIRECTION ( 'NONE',  ( 1.000000000000000000, -0.000000000000000000, 0.000000000000000000 ) ) ;
#136221=CARTESIAN_POINT ( 'NONE',  ( -18.50000000000000000, 74.36282728704168221, -124.9409541190522930 ) ) ;
#136250=DIRECTION ( 'NONE',  ( 0.000000000000000000, -6.938893903907222067E-15, 1.000000000000000000 ) ) ;
#136264=ORIENTED_EDGE ( 'NONE', *, *, #236828, .T. ) ;
#136310=ORIENTED_EDGE ( 'NONE', *, *, #47410, .F. ) ;
#136317=DIRECTION ( 'NONE',  ( 1.000000000000000000, -0.000000000000000000, 0.000000000000000000 ) ) ;
#136335=EDGE_CURVE ( 'NONE', #60977, #231942, #207210, .T. ) ;
#136340=EDGE_CURVE ( 'NONE', #147639, #220201, #99627, .T. ) ;
#136393=ORIENTED_EDGE ( 'NONE', *, *, #148218, .T. ) ;
#136415=EDGE_LOOP ( 'NONE', ( #229550, #213028, #92960, #60990 ) ) ;
#136420=EDGE_LOOP ( 'NONE', ( #199349, #88627, #255130, #17100, #251626 ) ) ;
#136457=CARTESIAN_POINT ( 'NONE',  ( 22.39999999999999858, 68.20922040163875977, -136.6231074845243540 ) ) ;
#136488=VERTEX_POINT ( 'NONE', #2238 ) ;
#136492=DIRECTION ( 'NONE',  ( 0.000000000000000000, 0.9999176327611370985, -0.01283462868041286391 ) ) ;
#136509=CARTESIAN_POINT ( 'NONE',  ( 22.60000000000000142, 76.00000000001213607, -136.5231074845242745 ) ) ;
#136531=EDGE_CURVE ( 'NONE', #73853, #153900, #231068, .T. ) ;
#136535=AXIS2_PLACEMENT_3D ( 'NONE', #159996, #239515, #101224 ) ;
#136543=ADVANCED_FACE ( 'NONE', ( #81757 ), #255242, .F. ) ;
#136565=EDGE_CURVE ( 'NONE', #189309, #50227, #37553, .T. ) ;
#136572=EDGE_LOOP ( 'NONE', ( #69645, #59538, #146272, #123987 ) ) ;
#136605=DIRECTION ( 'NONE',  ( 0.000000000000000000, -0.2605042016806740079, 0.9654727137038698892 ) ) ;
#136622=EDGE_LOOP ( 'NONE', ( #110033, #30185, #119092, #40404 ) ) ;
#136632=CARTESIAN_POINT ( 'NONE',  ( -22.59999999999999787, 76.00000000001213607, -136.5231074845242745 ) ) ;
#136650=CARTESIAN_POINT ( 'NONE',  ( 23.15000000000000213, 85.50000000001207923, -126.6291383618717816 ) ) ;
#136654=ORIENTED_EDGE ( 'NONE', *, *, #238732, .T. ) ;
#136673=CARTESIAN_POINT ( 'NONE',  ( -18.59999999999999787, 102.4393534156129562, -118.3815988770166427 ) ) ;
#136690=ORIENTED_EDGE ( 'NONE', *, *, #108147, .F. ) ;
#136740=ADVANCED_FACE ( 'NONE', ( #85604 ), #226414, .F. ) ;
#136756=EDGE_CURVE ( 'NONE', #221411, #183267, #196006, .T. ) ;
#136782=CARTESIAN_POINT ( 'NONE',  ( 18.50000000000000355, 85.48068669529082797, -96.08199231576635668 ) ) ;
#136821=DIRECTION ( 'NONE',  ( 0.000000000000000000, 0.000000000000000000, 1.000000000000000000 ) ) ;
#136853=DIRECTION ( 'NONE',  ( -0.000000000000000000, 1.000000000000000000, 6.982962677686266711E-15 ) ) ;
#136897=LINE ( 'NONE', #251711, #181722 ) ;
#136910=DIRECTION ( 'NONE',  ( 0.000000000000000000, -0.1298341882519953860, -0.9915357197604862671 ) ) ;
#136950=CARTESIAN_POINT ( 'NONE',  ( 21.07928932188134397, 75.90110485435778287, -142.8516241409176075 ) ) ;
#136973=CARTESIAN_POINT ( 'NONE',  ( -21.05000000000000071, 74.16465844978765176, -124.9679561919613207 ) ) ;
#137002=FACE_OUTER_BOUND ( 'NONE', #168605, .T. ) ;
#137034=EDGE_CURVE ( 'NONE', #182088, #51816, #177282, .T. ) ;
#137071=ORIENTED_EDGE ( 'NONE', *, *, #249540, .F. ) ;
#137089=CARTESIAN_POINT ( 'NONE',  ( -18.59999999999999787, 64.35000000001208775, -129.5083017138703667 ) ) ;
#137121=CARTESIAN_POINT ( 'NONE',  ( 21.05000000000000071, 87.48912529308817909, -133.4231074845242233 ) ) ;
#137132=CARTESIAN_POINT ( 'NONE',  ( 22.47110162079220785, 75.97120258720953245, -148.1730434212086323 ) ) ;
#137163=DIRECTION ( 'NONE',  ( 0.000000000000000000, -7.056502275159890043E-15, 1.000000000000000000 ) ) ;
#137164=DIRECTION ( 'NONE',  ( 1.000000000000000000, 0.000000000000000000, 0.000000000000000000 ) ) ;
#137181=CARTESIAN_POINT ( 'NONE',  ( 19.75857864376268935, 64.35000000001197407, -111.7731074845243739 ) ) ;
#137191=DIRECTION ( 'NONE',  ( 0.000000000000000000, 0.9915357197604862671, -0.1298341882519953583 ) ) ;
#137208=CARTESIAN_POINT ( 'NONE',  ( -23.15000000000000213, 64.35000000001205933, -124.3731074845243825 ) ) ;
#137214=DIRECTION ( 'NONE',  ( -0.1538461538461484146, -0.9880948137434723000, 0.000000000000000000 ) ) ;
#137219=FACE_OUTER_BOUND ( 'NONE', #162736, .T. ) ;
#137290=CARTESIAN_POINT ( 'NONE',  ( -20.94999999999999929, 87.48912529308817909, -133.5231074845242176 ) ) ;
#137308=CARTESIAN_POINT ( 'NONE',  ( 20.85000000000000142, 76.00000000001190870, -103.0231074845243029 ) ) ;
#137311=CARTESIAN_POINT ( 'NONE',  ( -18.50000000000000711, 85.42130820975080496, -129.2807442704737753 ) ) ;
#137312=CARTESIAN_POINT ( 'NONE',  ( -22.24259225415828567, 68.50806212944671358, -136.6221733679771830 ) ) ;
#137314=AXIS2_PLACEMENT_3D ( 'NONE', #128951, #248902, #33742 ) ;
#137340=ORIENTED_EDGE ( 'NONE', *, *, #104249, .T. ) ;
#137344=VERTEX_POINT ( 'NONE', #220393 ) ;
#137385=ORIENTED_EDGE ( 'NONE', *, *, #63724, .T. ) ;
#137389=ORIENTED_EDGE ( 'NONE', *, *, #77773, .F. ) ;
#137392=VERTEX_POINT ( 'NONE', #22199 ) ;
#137441=ADVANCED_FACE ( 'NONE', ( #87267 ), #217523, .F. ) ;
#137444=DIRECTION ( 'NONE',  ( -3.265361837132813093E-16, -1.000000000000000000, -6.938893903907222067E-15 ) ) ;
#137449=DIRECTION ( 'NONE',  ( -0.000000000000000000, 0.8700118002898356018, -0.4930308989875170078 ) ) ;
#137450=B_SPLINE_CURVE_WITH_KNOTS ( 'NONE', 3,
 ( #36783, #116296, #176279, #82249, #203525, #100528, #178862, #143535 ),
 .UNSPECIFIED., .F., .F.,
 ( 4, 2, 2, 4 ),
 ( 0.000000000000000000, 0.0001881495939909106339, 0.0002822243909863764405, 0.0003762991879818423013 ),
 .UNSPECIFIED. ) ;
#137464=AXIS2_PLACEMENT_3D ( 'NONE', #108963, #231504, #32033 ) ;
#137486=DIRECTION ( 'NONE',  ( 0.000000000000000000, 6.982962677686266711E-15, -1.000000000000000000 ) ) ;
#137491=EDGE_LOOP ( 'NONE', ( #232951, #114361, #175, #220916 ) ) ;
#137500=CARTESIAN_POINT ( 'NONE',  ( -21.55000000000000071, 68.65000000001199965, -115.3731074845243540 ) ) ;
#137532=CARTESIAN_POINT ( 'NONE',  ( 23.14999999999999503, 69.55000000001206217, -124.1731074845243370 ) ) ;
#137564=CARTESIAN_POINT ( 'NONE',  ( -23.15000000000000213, 64.25000000001206502, -124.3731074845243825 ) ) ;
#137565=ORIENTED_EDGE ( 'NONE', *, *, #138206, .T. ) ;
#137590=EDGE_CURVE ( 'NONE', #178773, #16075, #234272, .T. ) ;
#137606=CIRCLE ( 'NONE', #37701, 0.1000000000000028644 ) ;
#137634=ORIENTED_EDGE ( 'NONE', *, *, #29084, .F. ) ;
#137698=DIRECTION ( 'NONE',  ( 1.000000000000000000, 0.000000000000000000, 0.000000000000000000 ) ) ;
#137718=ORIENTED_EDGE ( 'NONE', *, *, #179991, .T. ) ;
#137778=ORIENTED_EDGE ( 'NONE', *, *, #135951, .F. ) ;
#137780=DIRECTION ( 'NONE',  ( -0.000000000000000000, -6.982962677686266711E-15, 1.000000000000000000 ) ) ;
#137782=FACE_OUTER_BOUND ( 'NONE', #226521, .T. ) ;
#137787=DIRECTION ( 'NONE',  ( 1.000000000000000000, 0.000000000000000000, 0.000000000000000000 ) ) ;
#137818=EDGE_CURVE ( 'NONE', #15448, #59827, #67882, .T. ) ;
#137860=DIRECTION ( 'NONE',  ( 0.000000000000000000, -8.338584948901395817E-15, 1.000000000000000000 ) ) ;
#137871=DIRECTION ( 'NONE',  ( 0.000000000000000000, 1.000000000000000000, 0.000000000000000000 ) ) ;
#137880=AXIS2_PLACEMENT_3D ( 'NONE', #117334, #250414, #32707 ) ;
#137899=AXIS2_PLACEMENT_3D ( 'NONE', #178332, #75384, #137871 ) ;
#137913=DIRECTION ( 'NONE',  ( 0.000000000000000000, -7.086529944415894657E-15, 1.000000000000000000 ) ) ;
#137990=CARTESIAN_POINT ( 'NONE',  ( 20.94999999999999574, 69.45000000001206786, -126.6792853948412159 ) ) ;
#137991=CONICAL_SURFACE ( 'NONE', #58882, 4.299999999999970512, 0.7853981633974466137 ) ;
#137997=DIRECTION ( 'NONE',  ( 0.000000000000000000, -7.487053152578127080E-15, 1.000000000000000000 ) ) ;
#138016=ADVANCED_FACE ( 'NONE', ( #38557 ), #47013, .T. ) ;
#138019=DIRECTION ( 'NONE',  ( 6.938893903907030216E-14, 0.000000000000000000, -1.000000000000000000 ) ) ;
#138057=ORIENTED_EDGE ( 'NONE', *, *, #215127, .F. ) ;
#138088=( BOUNDED_SURFACE ( )  B_SPLINE_SURFACE ( 3, 2, ( 
 ( #211778, #47529, #210490 ),
 ( #228773, #111386, #168833 ),
 ( #129660, #209190, #110089 ),
 ( #190945, #250877, #206625 ),
 ( #189643, #127090, #117798 ),
 ( #16164, #255972, #254694 ),
 ( #257257, #175253, #196063 ),
 ( #77372, #235186, #57808 ) ),
 .UNSPECIFIED., .F., .F., .T. ) 
 B_SPLINE_SURFACE_WITH_KNOTS ( ( 4, 2, 2, 4 ),
 ( 3, 3 ),
 ( 0.0001704874539069779586, 0.0003809798300636547323, 0.0004862260181419930920, 0.0005914722062203315060 ),
 ( 0.000000000000000000, 1.000000000000000000 ),
 .UNSPECIFIED. ) 
 GEOMETRIC_REPRESENTATION_ITEM ( )  RATIONAL_B_SPLINE_SURFACE ( (
 ( 1.000000000000000000, 0.7071067811865088260, 1.000000000000000000),
 ( 1.000000000000000000, 0.7670648383569527162, 1.000000000000000000),
 ( 1.000000000000000000, 0.8204820770261292973, 1.000000000000000000),
 ( 1.000000000000000000, 0.8877218296109479212, 1.000000000000000000),
 ( 1.000000000000000000, 0.9080815932664854095, 1.000000000000000000),
 ( 1.000000000000000000, 0.9395541505862110565, 1.000000000000000000),
 ( 1.000000000000000000, 0.9506520335378865205, 1.000000000000000000),
 ( 1.000000000000000000, 0.9504532311154486601, 1.000000000000000000) ) ) 
 REPRESENTATION_ITEM ( '' )  SURFACE ( )  );
#138095=CARTESIAN_POINT ( 'NONE',  ( -21.05000000000000071, 76.00000000001188027, -99.02310748452428868 ) ) ;
#138104=FACE_OUTER_BOUND ( 'NONE', #162504, .T. ) ;
#138142=AXIS2_PLACEMENT_3D ( 'NONE', #200708, #59881, #22083 ) ;
#138145=DIRECTION ( 'NONE',  ( 0.000000000000000000, -0.4999999999999608646, 0.8660254037844612451 ) ) ;
#138146=AXIS2_PLACEMENT_3D ( 'NONE', #171327, #70918, #91734 ) ;
#138151=DIRECTION ( 'NONE',  ( 0.000000000000000000, 0.000000000000000000, 1.000000000000000000 ) ) ;
#138154=CARTESIAN_POINT ( 'NONE',  ( -20.07928932188135107, 66.77928932189340117, -124.1731074845243654 ) ) ;
#138158=CARTESIAN_POINT ( 'NONE',  ( -22.43310005002225438, 75.99436305787135382, -148.1727696116587083 ) ) ;
#138167=DIRECTION ( 'NONE',  ( 0.000000000000000000, 0.5907332058517377193, -0.8068669527896954463 ) ) ;
#138178=SPHERICAL_SURFACE ( 'NONE', #3702, 0.1000000000000000056 ) ;
#138206=EDGE_CURVE ( 'NONE', #153790, #23751, #8422, .T. ) ;
#138262=VERTEX_POINT ( 'NONE', #249605 ) ;
#138268=ORIENTED_EDGE ( 'NONE', *, *, #128011, .F. ) ;
#138287=DIRECTION ( 'NONE',  ( 0.000000000000000000, -7.086529944415894657E-15, 1.000000000000000000 ) ) ;
#138291=CARTESIAN_POINT ( 'NONE',  ( -21.05000000000000071, 87.65000000001192859, -105.9231074845242091 ) ) ;
#138303=ORIENTED_EDGE ( 'NONE', *, *, #90457, .T. ) ;
#138390=CARTESIAN_POINT ( 'NONE',  ( -21.05000000000000071, 76.00000000001190870, -103.0231074845243029 ) ) ;
#138391=DIRECTION ( 'NONE',  ( -2.952720810173289605E-16, -1.000000000000000000, -7.086529944415894657E-15 ) ) ;
#138439=AXIS2_PLACEMENT_3D ( 'NONE', #114085, #154545, #171538 ) ;
#138443=EDGE_CURVE ( 'NONE', #153892, #9803, #22551, .T. ) ;
#138453=CARTESIAN_POINT ( 'NONE',  ( -18.59999999999999787, 74.73821383144705521, -128.4366085209788366 ) ) ;
#138458=DIRECTION ( 'NONE',  ( 0.000000000000000000, -6.982962677686266711E-15, 1.000000000000000000 ) ) ;
#138476=CARTESIAN_POINT ( 'NONE',  ( -22.47007471830798409, 76.00000000001219291, -144.2438181364507841 ) ) ;
#138480=CARTESIAN_POINT ( 'NONE',  ( 22.45380639572249137, 75.99999985734274333, -148.2735403756364008 ) ) ;
#138484=CARTESIAN_POINT ( 'NONE',  ( -18.59999999999999787, 66.65000000001205649, -124.3731074845243683 ) ) ;
#138496=CARTESIAN_POINT ( 'NONE',  ( -18.50000000000000000, 77.83534155023646406, -124.9679561919613064 ) ) ;
#138526=ORIENTED_EDGE ( 'NONE', *, *, #47410, .T. ) ;
#138549=CARTESIAN_POINT ( 'NONE',  ( 20.94560253601876809, 64.25000000001195133, -110.0130239720089094 ) ) ;
#138563=DIRECTION ( 'NONE',  ( -1.000000000000000000, -0.000000000000000000, -0.000000000000000000 ) ) ;
#138600=EDGE_CURVE ( 'NONE', #167228, #130891, #14103, .T. ) ;
#138703=CIRCLE ( 'NONE', #47149, 0.09999999999999939493 ) ;
#138736=CARTESIAN_POINT ( 'NONE',  ( 21.07954640115206857, 75.93399229287231833, -142.8523951805472052 ) ) ;
#138762=CIRCLE ( 'NONE', #42951, 12.87499999999999822 ) ;
#138781=CARTESIAN_POINT ( 'NONE',  ( 23.14999999999999858, 70.50000000001199396, -115.4283735034374274 ) ) ;
#138814=ORIENTED_EDGE ( 'NONE', *, *, #238732, .F. ) ;
#138819=ORIENTED_EDGE ( 'NONE', *, *, #7821, .T. ) ;
#138824=DIRECTION ( 'NONE',  ( 0.000000000000000000, 0.9893560106964510714, -0.1455152366551481502 ) ) ;
#138828=FACE_OUTER_BOUND ( 'NONE', #247559, .T. ) ;
#138835=AXIS2_PLACEMENT_3D ( 'NONE', #93957, #99071, #114812 ) ;
#138847=ORIENTED_EDGE ( 'NONE', *, *, #251391, .F. ) ;
#138853=VECTOR ( 'NONE', #37652, 1000.000000000000000 ) ;
#138887=ORIENTED_EDGE ( 'NONE', *, *, #217231, .F. ) ;
#138920=DIRECTION ( 'NONE',  ( 0.000000000000000000, 6.982962677686266711E-15, -1.000000000000000000 ) ) ;
#138946=EDGE_CURVE ( 'NONE', #146363, #236918, #128719, .T. ) ;
#138968=DIRECTION ( 'NONE',  ( 2.952720810173289112E-16, 1.000000000000000000, 6.938893903907222067E-15 ) ) ;
#138973=CARTESIAN_POINT ( 'NONE',  ( -21.05000000000000071, 76.00000000001220712, -143.0637644362255401 ) ) ;
#138998=ORIENTED_EDGE ( 'NONE', *, *, #4336, .F. ) ;
#139019=AXIS2_PLACEMENT_3D ( 'NONE', #23654, #122743, #22359 ) ;
#139043=DIRECTION ( 'NONE',  ( 0.000000000000000000, 0.000000000000000000, -1.000000000000000000 ) ) ;
#139066=VERTEX_POINT ( 'NONE', #16486 ) ;
#139097=AXIS2_PLACEMENT_3D ( 'NONE', #32769, #228371, #112283 ) ;
#139103=VERTEX_POINT ( 'NONE', #113002 ) ;
#139198=LINE ( 'NONE', #41432, #33366 ) ;
#139216=CARTESIAN_POINT ( 'NONE',  ( -22.50000000000000000, 64.35042919246734527, -136.6231074845243825 ) ) ;
#139234=ORIENTED_EDGE ( 'NONE', *, *, #180682, .T. ) ;
#139265=CARTESIAN_POINT ( 'NONE',  ( -18.59999999999999787, 66.75000000001199396, -115.3731074845243683 ) ) ;
#139266=AXIS2_PLACEMENT_3D ( 'NONE', #85678, #244778, #148259 ) ;
#139273=CARTESIAN_POINT ( 'NONE',  ( 18.59999999999999076, 65.50857864377465489, -111.6731074845243796 ) ) ;
#139352=ORIENTED_EDGE ( 'NONE', *, *, #208019, .T. ) ;
#139367=ORIENTED_EDGE ( 'NONE', *, *, #10817, .T. ) ;
#139368=ORIENTED_EDGE ( 'NONE', *, *, #20650, .F. ) ;
#139454=EDGE_CURVE ( 'NONE', #105012, #240054, #151274, .T. ) ;
#139498=CIRCLE ( 'NONE', #206154, 0.5000000000000004441 ) ;
#139500=CIRCLE ( 'NONE', #27120, 0.1000000000000028644 ) ;
#139519=ORIENTED_EDGE ( 'NONE', *, *, #172720, .F. ) ;
#139611=DIRECTION ( 'NONE',  ( 1.000000000000000000, -2.952720810173289112E-16, -2.061873921506763405E-30 ) ) ;
#139615=ORIENTED_EDGE ( 'NONE', *, *, #86803, .F. ) ;
#139619=CARTESIAN_POINT ( 'NONE',  ( -23.15000000000000213, 76.00000000001213607, -136.5231074845242745 ) ) ;
#139626=VERTEX_POINT ( 'NONE', #40893 ) ;
#139682=FACE_OUTER_BOUND ( 'NONE', #107524, .T. ) ;
#139721=TOROIDAL_SURFACE ( 'NONE', #64718, 0.4000000000000017431, 0.1000000000000000056 ) ;
#139747=VERTEX_POINT ( 'NONE', #54826 ) ;
#139766=CARTESIAN_POINT ( 'NONE',  ( -22.47071067811865319, 75.90090754530959316, -144.2431822290223806 ) ) ;
#139772=CARTESIAN_POINT ( 'NONE',  ( -22.59999999999999787, 64.25043287652275126, -136.6239658536231047 ) ) ;
#139774=VERTEX_POINT ( 'NONE', #152697 ) ;
#139778=DIRECTION ( 'NONE',  ( 1.000000000000000000, -1.836970198721029934E-16, -1.282749433769087582E-30 ) ) ;
#139783=CARTESIAN_POINT ( 'NONE',  ( 21.14999999999999503, 76.10000000001222986, -148.1726782920690937 ) ) ;
#139791=CARTESIAN_POINT ( 'NONE',  ( 21.03670563405601968, 65.37517631068381263, -124.1975605983152491 ) ) ;
#139839=DIRECTION ( 'NONE',  ( -0.000000000000000000, -6.982962677686266711E-15, 1.000000000000000000 ) ) ;
#139847=CARTESIAN_POINT ( 'NONE',  ( 21.02374657821584947, 64.39999999919209017, -109.9513107143265387 ) ) ;
#139848=EDGE_LOOP ( 'NONE', ( #189660, #162100, #153024, #73784 ) ) ;
#139853=DIRECTION ( 'NONE',  ( 0.000000000000000000, -6.417474130781252121E-15, 1.000000000000000000 ) ) ;
#139881=CIRCLE ( 'NONE', #2514, 0.09999999999999939493 ) ;
#139884=EDGE_LOOP ( 'NONE', ( #29696, #9138, #206718, #254802 ) ) ;
#139919=EDGE_LOOP ( 'NONE', ( #148714, #189188, #135101, #218444 ) ) ;
#139958=DIRECTION ( 'NONE',  ( 0.000000000000000000, -6.982962677686266711E-15, 1.000000000000000000 ) ) ;
#139961=LINE ( 'NONE', #176564, #223383 ) ;
#140000=CARTESIAN_POINT ( 'NONE',  ( -18.47130263965443220, 85.47115558597577945, -96.33970271904722438 ) ) ;
#140021=EDGE_CURVE ( 'NONE', #247118, #163587, #92724, .T. ) ;
#140025=AXIS2_PLACEMENT_3D ( 'NONE', #82051, #161652, #241179 ) ;
#140069=FACE_OUTER_BOUND ( 'NONE', #11429, .T. ) ;
#140131=CONICAL_SURFACE ( 'NONE', #244748, 6.250000000000005329, 0.7853981633974431720 ) ;
#140147=VERTEX_POINT ( 'NONE', #196959 ) ;
#140196=ORIENTED_EDGE ( 'NONE', *, *, #200054, .T. ) ;
#140252=CARTESIAN_POINT ( 'NONE',  ( -21.14999999999999858, 64.25000000001210765, -129.7969768484651922 ) ) ;
#140285=EDGE_CURVE ( 'NONE', #22276, #217558, #201684, .T. ) ;
#140309=CIRCLE ( 'NONE', #115204, 0.09999999999999739653 ) ;
#140336=DIRECTION ( 'NONE',  ( 1.000000000000000000, 0.000000000000000000, 0.000000000000000000 ) ) ;
#140341=ADVANCED_FACE ( 'NONE', ( #175521 ), #1755, .F. ) ;
#140471=CIRCLE ( 'NONE', #227980, 0.6000000000000033085 ) ;
#140487=DIRECTION ( 'NONE',  ( -0.000000000000000000, -0.8660254037844420383, 0.4999999999999943379 ) ) ;
#140522=EDGE_CURVE ( 'NONE', #231766, #54998, #147708, .T. ) ;
#140526=ORIENTED_EDGE ( 'NONE', *, *, #96418, .F. ) ;
#140556=AXIS2_PLACEMENT_3D ( 'NONE', #168402, #91387, #52231 ) ;
#140567=CARTESIAN_POINT ( 'NONE',  ( 21.14999999999999858, 69.35000000001205933, -124.3731074845243540 ) ) ;
#140620=ORIENTED_EDGE ( 'NONE', *, *, #99661, .T. ) ;
#140633=ORIENTED_EDGE ( 'NONE', *, *, #220577, .T. ) ;
#140639=ORIENTED_EDGE ( 'NONE', *, *, #145628, .F. ) ;
#140649=EDGE_CURVE ( 'NONE', #212214, #130380, #183207, .T. ) ;
#140659=EDGE_CURVE ( 'NONE', #186279, #216286, #56098, .T. ) ;
#140663=TOROIDAL_SURFACE ( 'NONE', #161535, 11.70000000000000107, 0.1000000000000000056 ) ;
#140665=ORIENTED_EDGE ( 'NONE', *, *, #191504, .T. ) ;
#140679=CARTESIAN_POINT ( 'NONE',  ( -18.50000000000000000, 66.85000000001221565, -148.2731074845243597 ) ) ;
#140683=VERTEX_POINT ( 'NONE', #250858 ) ;
#140687=DIRECTION ( 'NONE',  ( 0.000000000000000000, -7.487053152578127080E-15, 1.000000000000000000 ) ) ;
#140696=ORIENTED_EDGE ( 'NONE', *, *, #198474, .F. ) ;
#140698=EDGE_LOOP ( 'NONE', ( #34461, #214949, #242722, #79152 ) ) ;
#140700=DIRECTION ( 'NONE',  ( 0.000000000000000000, -7.026728003956683390E-15, 1.000000000000000000 ) ) ;
#140701=TOROIDAL_SURFACE ( 'NONE', #203046, 4.099999999999999645, 0.1000000000000000056 ) ;
#140716=EDGE_CURVE ( 'NONE', #116058, #252068, #135210, .T. ) ;
#140738=CIRCLE ( 'NONE', #174101, 2.000000000000001776 ) ;
#140742=( BOUNDED_SURFACE ( )  B_SPLINE_SURFACE ( 3, 2, ( 
 ( #39548, #220715, #196031 ),
 ( #79884, #77337, #1648 ),
 ( #40826, #160774, #255936 ),
 ( #141184, #215570, #218123 ),
 ( #17384, #177763, #119058 ),
 ( #96873, #236422, #57773 ),
 ( #137311, #216852, #38238 ),
 ( #117757, #197293, #18664 ) ),
 .UNSPECIFIED., .F., .F., .F. ) 
 B_SPLINE_SURFACE_WITH_KNOTS ( ( 4, 2, 2, 4 ),
 ( 3, 3 ),
 ( 0.0001723339234021429623, 0.0002782939632049932365, 0.0003842540030078435377, 0.0005961740826135441401 ),
 ( 0.000000000000000000, 1.000000000000000000 ),
 .UNSPECIFIED. ) 
 GEOMETRIC_REPRESENTATION_ITEM ( )  RATIONAL_B_SPLINE_SURFACE ( (
 ( 1.000000000000000000, 0.9504532311154486601, 1.000000000000000000),
 ( 1.000000000000000000, 0.9506023220705424048, 1.000000000000000000),
 ( 1.000000000000000000, 0.9395774818187647703, 1.000000000000000000),
 ( 1.000000000000000000, 0.9079328464641989171, 1.000000000000000000),
 ( 1.000000000000000000, 0.8875702416207198464, 1.000000000000000000),
 ( 1.000000000000000000, 0.8205919608037975932, 1.000000000000000000),
 ( 1.000000000000000000, 0.7666842783600120725, 1.000000000000000000),
 ( 1.000000000000000000, 0.7071067811865088260, 1.000000000000000000) ) ) 
 REPRESENTATION_ITEM ( '' )  SURFACE ( )  );
#140747=CARTESIAN_POINT ( 'NONE',  ( -22.47886152344871036, 75.96249906115053818, -148.1730961275722223 ) ) ;
#140763=ADVANCED_FACE ( 'NONE', ( #50096 ), #35322, .T. ) ;
#140765=DIRECTION ( 'NONE',  ( -0.000000000000000000, 6.982962677686266711E-15, -1.000000000000000000 ) ) ;
#140778=ORIENTED_EDGE ( 'NONE', *, *, #172806, .T. ) ;
#140787=LINE ( 'NONE', #159090, #214848 ) ;
#140796=ADVANCED_FACE ( 'NONE', ( #51349 ), #31857, .F. ) ;
#140809=AXIS2_PLACEMENT_3D ( 'NONE', #14158, #230624, #214893 ) ;
#140817=CARTESIAN_POINT ( 'NONE',  ( 20.41140022480505323, 65.58956915761045536, -128.9081061808921334 ) ) ;
#140840=CARTESIAN_POINT ( 'NONE',  ( -20.07928932188135107, 66.77928932189333011, -115.3731074845243683 ) ) ;
#140844=ORIENTED_EDGE ( 'NONE', *, *, #186929, .T. ) ;
#140855=EDGE_CURVE ( 'NONE', #230224, #73853, #139498, .T. ) ;
#140871=CARTESIAN_POINT ( 'NONE',  ( 21.05000000000000071, 87.48912529308817909, -133.6231074845242119 ) ) ;
#140882=ORIENTED_EDGE ( 'NONE', *, *, #53510, .F. ) ;
#140909=ORIENTED_EDGE ( 'NONE', *, *, #94076, .F. ) ;
#140920=AXIS2_PLACEMENT_3D ( 'NONE', #143364, #26001, #121285 ) ;
#140923=AXIS2_PLACEMENT_3D ( 'NONE', #137089, #190675, #12031 ) ;
#140951=ADVANCED_FACE ( 'NONE', ( #176490 ), #93724, .T. ) ;
#140955=VERTEX_POINT ( 'NONE', #48511 ) ;
#140961=VERTEX_POINT ( 'NONE', #184164 ) ;
#140973=ORIENTED_EDGE ( 'NONE', *, *, #12265, .F. ) ;
#141021=DIRECTION ( 'NONE',  ( 0.000000000000000000, 6.982962677686266711E-15, -1.000000000000000000 ) ) ;
#141052=CARTESIAN_POINT ( 'NONE',  ( -18.54148534481894472, 65.67467670974414773, -97.45317318268841689 ) ) ;
#141053=CARTESIAN_POINT ( 'NONE',  ( -21.05000000000000071, 61.95000000001210338, -131.0094124137634140 ) ) ;
#141062=CARTESIAN_POINT ( 'NONE',  ( 23.25000000000000000, 85.60000000001208775, -126.6291383618717816 ) ) ;
#141068=ORIENTED_EDGE ( 'NONE', *, *, #181323, .F. ) ;
#141090=DIRECTION ( 'NONE',  ( 1.000000000000000000, 0.000000000000000000, 0.000000000000000000 ) ) ;
#141104=DIRECTION ( 'NONE',  ( -7.304098846217948299E-16, -1.000000000000000000, 0.000000000000000000 ) ) ;
#141110=EDGE_LOOP ( 'NONE', ( #136264, #64258, #95922, #156631 ) ) ;
#141122=DIRECTION ( 'NONE',  ( 1.040834085586049673E-13, 0.7899159663865300551, 0.6132151058540831201 ) ) ;
#141145=DIRECTION ( 'NONE',  ( 0.000000000000000000, -6.853228547068871147E-15, 1.000000000000000000 ) ) ;
#141154=ORIENTED_EDGE ( 'NONE', *, *, #182802, .T. ) ;
#141158=CARTESIAN_POINT ( 'NONE',  ( 20.85000000000000142, 64.25000000001195133, -109.8069731475024753 ) ) ;
#141184=CARTESIAN_POINT ( 'NONE',  ( -18.46093223321778609, 85.48068296828660095, -129.4385569705975456 ) ) ;
#141205=EDGE_LOOP ( 'NONE', ( #149357, #249889, #226075, #215521 ) ) ;
#141206=AXIS2_PLACEMENT_3D ( 'NONE', #141053, #101887, #125339 ) ;
#141214=CARTESIAN_POINT ( 'NONE',  ( 20.94999999999999929, 67.12338541492499644, -128.1380270056797031 ) ) ;
#141226=CIRCLE ( 'NONE', #57995, 0.2000000000000057288 ) ;
#141235=CARTESIAN_POINT ( 'NONE',  ( 18.53691006697094679, 65.69784844286142800, -111.8209087672256885 ) ) ;
#141280=ORIENTED_EDGE ( 'NONE', *, *, #91863, .F. ) ;
#141281=AXIS2_PLACEMENT_3D ( 'NONE', #62438, #102813, #165388 ) ;
#141310=LINE ( 'NONE', #198711, #166534 ) ;
#141311=DIRECTION ( 'NONE',  ( 0.000000000000000000, -0.8660254037844468122, -0.4999999999999859557 ) ) ;
#141320=CARTESIAN_POINT ( 'NONE',  ( -21.05000000000000071, 75.90220970870339556, -142.7809220950004203 ) ) ;
#141341=DIRECTION ( 'NONE',  ( 0.000000000000000000, 0.000000000000000000, 1.000000000000000000 ) ) ;
#141356=ORIENTED_EDGE ( 'NONE', *, *, #45632, .F. ) ;
#141387=DIRECTION ( 'NONE',  ( -1.000000000000000000, 0.000000000000000000, -0.000000000000000000 ) ) ;
#141388=ADVANCED_FACE ( 'NONE', ( #6509 ), #243836, .F. ) ;
#141451=EDGE_CURVE ( 'NONE', #12375, #118755, #181325, .T. ) ;
#141452=ADVANCED_FACE ( 'NONE', ( #9088 ), #69079, .F. ) ;
#141458=AXIS2_PLACEMENT_3D ( 'NONE', #84326, #62257, #187355 ) ;
#141470=CARTESIAN_POINT ( 'NONE',  ( -18.50000000000000000, 85.40000000001209912, -129.2258477248609552 ) ) ;
#141472=DIRECTION ( 'NONE',  ( -1.000000000000000000, 0.000000000000000000, 0.000000000000000000 ) ) ;
#141510=EDGE_CURVE ( 'NONE', #35933, #64409, #173057, .T. ) ;
#141543=DIRECTION ( 'NONE',  ( 1.000000000000000000, -0.000000000000000000, 0.000000000000000000 ) ) ;
#141575=CARTESIAN_POINT ( 'NONE',  ( -21.05000000000000071, 75.90220970870339556, -142.7809220950004203 ) ) ;
#141600=VECTOR ( 'NONE', #141970, 1000.000000000000000 ) ;
#141603=CARTESIAN_POINT ( 'NONE',  ( 20.94403535211772294, 65.69367753730655579, -97.51892380663478832 ) ) ;
#141629=CIRCLE ( 'NONE', #62534, 11.80000000000000426 ) ;
#141702=AXIS2_PLACEMENT_3D ( 'NONE', #140567, #98847, #100138 ) ;
#141713=EDGE_CURVE ( 'NONE', #11251, #66400, #198139, .T. ) ;
#141716=AXIS2_PLACEMENT_3D ( 'NONE', #93487, #34836, #174367 ) ;
#141717=ADVANCED_FACE ( 'NONE', ( #160177 ), #98851, .F. ) ;
#141733=CARTESIAN_POINT ( 'NONE',  ( -21.14999999999999858, 64.35000000001214460, -136.4231074845243938 ) ) ;
#141778=ORIENTED_EDGE ( 'NONE', *, *, #236017, .F. ) ;
#141784=VECTOR ( 'NONE', #202598, 1000.000000000000000 ) ;
#141798=CARTESIAN_POINT ( 'NONE',  ( -18.59999999999999787, 64.35000000001208775, -129.5083017138703667 ) ) ;
#141872=ORIENTED_EDGE ( 'NONE', *, *, #218090, .F. ) ;
#141885=ADVANCED_FACE ( 'NONE', ( #23232 ), #2492, .T. ) ;
#141887=EDGE_LOOP ( 'NONE', ( #146923, #166960, #124893, #100452 ) ) ;
#141894=ORIENTED_EDGE ( 'NONE', *, *, #79105, .T. ) ;
#141911=CARTESIAN_POINT ( 'NONE',  ( 18.59999999999998721, 69.06610602788553877, -99.23746165015076315 ) ) ;
#141947=CARTESIAN_POINT ( 'NONE',  ( 23.14999999999999503, 69.45000000001199680, -115.3731074845243398 ) ) ;
#141962=ORIENTED_EDGE ( 'NONE', *, *, #122504, .T. ) ;
#141970=DIRECTION ( 'NONE',  ( 1.000000000000000000, -1.875376730785737719E-16, -1.309568571767809260E-30 ) ) ;
#141981=CARTESIAN_POINT ( 'NONE',  ( -22.14074124539699540, 75.90094710416812518, -143.9131853355680732 ) ) ;
#141984=DIRECTION ( 'NONE',  ( -0.000000000000000000, 1.000000000000000000, 6.982962677686266711E-15 ) ) ;
#141989=VECTOR ( 'NONE', #163591, 1000.000000000000000 ) ;
#142013=DIRECTION ( 'NONE',  ( 1.000000000000000000, 0.000000000000000000, 0.000000000000000000 ) ) ;
#142015=CIRCLE ( 'NONE', #129563, 0.1000000000000028644 ) ;
#142038=CIRCLE ( 'NONE', #58813, 11.70000000000000284 ) ;
#142073=ORIENTED_EDGE ( 'NONE', *, *, #152137, .F. ) ;
#142086=CARTESIAN_POINT ( 'NONE',  ( 20.77766267348356166, 65.55095760939339300, -128.9303985686466945 ) ) ;
#142105=ORIENTED_EDGE ( 'NONE', *, *, #230502, .T. ) ;
#142110=CARTESIAN_POINT ( 'NONE',  ( 21.10320863425824811, 69.59972261355297007, -136.5481297357514734 ) ) ;
#142114=EDGE_CURVE ( 'NONE', #19112, #56619, #244278, .T. ) ;
#142120=ADVANCED_FACE ( 'NONE', ( #2028 ), #120744, .T. ) ;
#142137=DIRECTION ( 'NONE',  ( 0.000000000000000000, -0.6728971962617102953, -0.7397360091702507301 ) ) ;
#142160=ORIENTED_EDGE ( 'NONE', *, *, #111144, .T. ) ;
#142170=AXIS2_PLACEMENT_3D ( 'NONE', #149028, #12092, #10785 ) ;
#142171=EDGE_CURVE ( 'NONE', #131694, #173897, #49839, .T. ) ;
#142208=LINE ( 'NONE', #221720, #182449 ) ;
#142215=EDGE_LOOP ( 'NONE', ( #182517, #94773, #118318 ) ) ;
#142222=ORIENTED_EDGE ( 'NONE', *, *, #246706, .F. ) ;
#142226=ADVANCED_FACE ( 'NONE', ( #111101 ), #211490, .T. ) ;
#142242=EDGE_CURVE ( 'NONE', #82189, #18420, #92809, .T. ) ;
#142263=ORIENTED_EDGE ( 'NONE', *, *, #149257, .T. ) ;
#142265=EDGE_CURVE ( 'NONE', #213669, #221570, #39542, .T. ) ;
#142273=DIRECTION ( 'NONE',  ( 1.000000000000000000, 0.000000000000000000, 0.000000000000000000 ) ) ;
#142292=DIRECTION ( 'NONE',  ( 0.000000000000000000, 0.000000000000000000, 1.000000000000000000 ) ) ;
#142295=CIRCLE ( 'NONE', #63175, 0.1000000000000028644 ) ;
#142311=DIRECTION ( 'NONE',  ( 0.000000000000000000, 0.000000000000000000, 1.000000000000000000 ) ) ;
#142326=FACE_OUTER_BOUND ( 'NONE', #186926, .T. ) ;
#142327=CARTESIAN_POINT ( 'NONE',  ( 20.95263205890728386, 67.10425989211800868, -128.0335990775827781 ) ) ;
#142356=CARTESIAN_POINT ( 'NONE',  ( -18.59999999999999787, 74.16465844978765176, -124.8679561919613263 ) ) ;
#142359=CARTESIAN_POINT ( 'NONE',  ( -21.05000000000000071, 64.36312671090797721, -129.7013482711997199 ) ) ;
#142363=AXIS2_PLACEMENT_3D ( 'NONE', #94112, #253188, #231092 ) ;
#142369=CARTESIAN_POINT ( 'NONE',  ( 20.95512820512820440, 65.37615131630018084, -124.3731074845243825 ) ) ;
#142372=DIRECTION ( 'NONE',  ( -1.000000000000000000, -0.000000000000000000, -0.000000000000000000 ) ) ;
#142409=DIRECTION ( 'NONE',  ( 0.000000000000000000, -6.530723674265620862E-15, 1.000000000000000000 ) ) ;
#142424=AXIS2_PLACEMENT_3D ( 'NONE', #233464, #134316, #157801 ) ;
#142456=CIRCLE ( 'NONE', #234033, 0.09999999999999939493 ) ;
#142463=CARTESIAN_POINT ( 'NONE',  ( -21.05000000000000071, 87.48912529308817909, -133.6231074845242119 ) ) ;
#142480=AXIS2_PLACEMENT_3D ( 'NONE', #133417, #58976, #17329 ) ;
#142493=VECTOR ( 'NONE', #239724, 1000.000000000000000 ) ;
#142500=CARTESIAN_POINT ( 'NONE',  ( 18.49999999999999289, 65.79142135624927334, -111.8731074845243683 ) ) ;
#142502=ORIENTED_EDGE ( 'NONE', *, *, #91827, .F. ) ;
#142509=ORIENTED_EDGE ( 'NONE', *, *, #18221, .T. ) ;
#142580=CARTESIAN_POINT ( 'NONE',  ( -23.25000000000000000, 76.00000000001190870, -103.0231074845243029 ) ) ;
#142602=CIRCLE ( 'NONE', #109293, 0.09999999999998898659 ) ;
#142611=DIRECTION ( 'NONE',  ( 1.000000000000000000, -0.000000000000000000, 0.000000000000000000 ) ) ;
#142631=CARTESIAN_POINT ( 'NONE',  ( 23.14999999999999858, 76.00000000001190870, -103.0231074845243029 ) ) ;
#142657=CARTESIAN_POINT ( 'NONE',  ( -21.05000000000000071, 76.00000000001190870, -103.0231074845243029 ) ) ;
#142698=CARTESIAN_POINT ( 'NONE',  ( 21.06490991615909536, 65.27510865242494731, -124.3193961309912510 ) ) ;
#142710=LINE ( 'NONE', #243105, #52233 ) ;
#142714=VECTOR ( 'NONE', #153795, 999.9999999999998863 ) ;
#142735=ORIENTED_EDGE ( 'NONE', *, *, #223029, .T. ) ;
#142743=DIRECTION ( 'NONE',  ( -0.000000000000000000, 0.8660254037844377084, 0.5000000000000016653 ) ) ;
#142752=CIRCLE ( 'NONE', #30363, 0.1000000000000000888 ) ;
#142776=ORIENTED_EDGE ( 'NONE', *, *, #4381, .F. ) ;
#142780=AXIS2_PLACEMENT_3D ( 'NONE', #85628, #84328, #204319 ) ;
#142782=DIRECTION ( 'NONE',  ( 0.000000000000000000, -0.9998779222360104635, -0.01562499999996343723 ) ) ;
#142812=DIRECTION ( 'NONE',  ( 1.000000000000000000, 0.000000000000000000, 0.000000000000000000 ) ) ;
#142819=EDGE_LOOP ( 'NONE', ( #123535, #134092, #252580, #2677 ) ) ;
#142832=DIRECTION ( 'NONE',  ( 1.000000000000000000, -2.952720810173289112E-16, -2.061873921506763405E-30 ) ) ;
#142860=CARTESIAN_POINT ( 'NONE',  ( 20.88420186297724257, 65.66974365629666011, -97.43601455626048846 ) ) ;
#142913=DIRECTION ( 'NONE',  ( 1.000000000000000000, 0.000000000000000000, 0.000000000000000000 ) ) ;
#142916=ORIENTED_EDGE ( 'NONE', *, *, #109434, .F. ) ;
#142925=ORIENTED_EDGE ( 'NONE', *, *, #21284, .F. ) ;
#142949=ORIENTED_EDGE ( 'NONE', *, *, #125030, .T. ) ;
#142965=CIRCLE ( 'NONE', #30589, 0.1000000000000052097 ) ;
#142997=AXIS2_PLACEMENT_3D ( 'NONE', #165598, #245120, #225520 ) ;
#143002=DIRECTION ( 'NONE',  ( -1.000000000000000000, 0.000000000000000000, 0.000000000000000000 ) ) ;
#143052=FACE_OUTER_BOUND ( 'NONE', #52244, .T. ) ;
#143071=DIRECTION ( 'NONE',  ( 0.000000000000000000, -6.467318590049456648E-15, 1.000000000000000000 ) ) ;
#143094=CARTESIAN_POINT ( 'NONE',  ( 23.24999999999999645, 76.00000000001213607, -136.5231074845242745 ) ) ;
#143097=EDGE_CURVE ( 'NONE', #215553, #254300, #53120, .T. ) ;
#143104=CARTESIAN_POINT ( 'NONE',  ( 21.07016717457012689, 76.00000000001219291, -142.8440483226252127 ) ) ;
#143137=ORIENTED_EDGE ( 'NONE', *, *, #193925, .T. ) ;
#143139=ADVANCED_FACE ( 'NONE', ( #190022 ), #40520, .T. ) ;
#143151=DIRECTION ( 'NONE',  ( -0.000000000000000000, 1.000000000000000000, 6.352154140967427193E-15 ) ) ;
#143172=AXIS2_PLACEMENT_3D ( 'NONE', #231588, #249859, #15106 ) ;
#143174=B_SPLINE_CURVE_WITH_KNOTS ( 'NONE', 3,
 ( #110460, #96021, #190009, #255040, #76462, #156036, #235536 ),
 .UNSPECIFIED., .F., .F.,
 ( 4, 3, 4 ),
 ( 0.000000000000000000, 0.0009834301579440022593, 0.001767853679402679300 ),
 .UNSPECIFIED. ) ;
#143189=CARTESIAN_POINT ( 'NONE',  ( 21.05000000000000071, 85.50000000001197975, -112.9170766071766820 ) ) ;
#143193=ORIENTED_EDGE ( 'NONE', *, *, #221796, .F. ) ;
#143203=EDGE_LOOP ( 'NONE', ( #42451, #111042, #254134, #137718, #63917, #207534, #19500, #240393, #26418 ) ) ;
#143216=LINE ( 'NONE', #203200, #36560 ) ;
#143219=LINE ( 'NONE', #20741, #45425 ) ;
#143221=CIRCLE ( 'NONE', #109898, 0.09999999999999939493 ) ;
#143308=CARTESIAN_POINT ( 'NONE',  ( -22.49917693094574389, 75.91477003579055349, -148.1729032690549559 ) ) ;
#143330=EDGE_CURVE ( 'NONE', #172048, #167228, #114336, .T. ) ;
#143335=ORIENTED_EDGE ( 'NONE', *, *, #55718, .F. ) ;
#143364=CARTESIAN_POINT ( 'NONE',  ( -21.07928932188134041, 76.00000000001213607, -136.5231074845242745 ) ) ;
#143383=DIRECTION ( 'NONE',  ( 1.000000000000000000, 0.000000000000000000, 0.000000000000000000 ) ) ;
#143411=VERTEX_POINT ( 'NONE', #86731 ) ;
#143413=CIRCLE ( 'NONE', #139097, 0.1000000000000028644 ) ;
#143414=AXIS2_PLACEMENT_3D ( 'NONE', #10356, #89862, #66461 ) ;
#143475=AXIS2_PLACEMENT_3D ( 'NONE', #75856, #116284, #197073 ) ;
#143492=DIRECTION ( 'NONE',  ( 0.000000000000000000, 1.000000000000000000, 0.000000000000000000 ) ) ;
#143515=AXIS2_PLACEMENT_3D ( 'NONE', #9078, #209858, #53338 ) ;
#143527=ORIENTED_EDGE ( 'NONE', *, *, #36825, .F. ) ;
#143535=CARTESIAN_POINT ( 'NONE',  ( 21.05000000000000071, 75.90220970870339556, -142.7809220950004203 ) ) ;
#143560=CARTESIAN_POINT ( 'NONE',  ( -18.59999999999999787, 76.00000000001213607, -136.5231074845242745 ) ) ;
#143571=ORIENTED_EDGE ( 'NONE', *, *, #180622, .F. ) ;
#143604=DIRECTION ( 'NONE',  ( 0.000000000000000000, 0.000000000000000000, 1.000000000000000000 ) ) ;
#143680=ORIENTED_EDGE ( 'NONE', *, *, #144790, .F. ) ;
#143686=AXIS2_PLACEMENT_3D ( 'NONE', #133489, #91796, #136025 ) ;
#143694=FACE_OUTER_BOUND ( 'NONE', #201191, .T. ) ;
#143711=STYLED_ITEM ( 'NONE', ( #177593 ), #179045 ) ;
#143776=ORIENTED_EDGE ( 'NONE', *, *, #209246, .F. ) ;
#143785=ORIENTED_EDGE ( 'NONE', *, *, #73739, .T. ) ;
#143792=CARTESIAN_POINT ( 'NONE',  ( -22.50000000000000000, 64.35042919246734527, -136.6231074845243825 ) ) ;
#143821=CARTESIAN_POINT ( 'NONE',  ( 20.94999999999999929, 76.00000000001205080, -123.5481074845242802 ) ) ;
#143828=CARTESIAN_POINT ( 'NONE',  ( -21.05000000000000426, 64.40000000001208491, -129.5949042542488314 ) ) ;
#143892=ADVANCED_FACE ( 'NONE', ( #83154 ), #78052, .F. ) ;
#143905=DIRECTION ( 'NONE',  ( -0.000000000000000000, -6.982962677686266711E-15, 1.000000000000000000 ) ) ;
#143907=CARTESIAN_POINT ( 'NONE',  ( -23.15000000000000213, 70.05000000001197691, -113.3288097895591591 ) ) ;
#143908=EDGE_LOOP ( 'NONE', ( #239155, #56212, #18408, #227732 ) ) ;
#143912=VERTEX_POINT ( 'NONE', #247392 ) ;
#143936=LINE ( 'NONE', #203912, #12044 ) ;
#143959=VECTOR ( 'NONE', #71965, 1000.000000000000000 ) ;
#143967=SPHERICAL_SURFACE ( 'NONE', #233133, 0.1000000000000000056 ) ;
#143973=CIRCLE ( 'NONE', #31597, 0.1000000000000028644 ) ;
#143994=CARTESIAN_POINT ( 'NONE',  ( -21.14999999999999858, 64.35000000001214460, -136.5231074845243597 ) ) ;
#144036=DIRECTION ( 'NONE',  ( -0.000000000000000000, -6.982962677686266711E-15, 1.000000000000000000 ) ) ;
#144049=CARTESIAN_POINT ( 'NONE',  ( 23.15000000000000213, 85.50000000001197975, -112.9170766071766820 ) ) ;
#144067=AXIS2_PLACEMENT_3D ( 'NONE', #183245, #147969, #64565 ) ;
#144069=CIRCLE ( 'NONE', #215003, 0.09999999999999939493 ) ;
#144082=CARTESIAN_POINT ( 'NONE',  ( -20.64999999999999858, 71.65000000001207070, -124.1731074845243228 ) ) ;
#144101=ORIENTED_EDGE ( 'NONE', *, *, #61860, .T. ) ;
#144144=VERTEX_POINT ( 'NONE', #213398 ) ;
#144150=ORIENTED_EDGE ( 'NONE', *, *, #119340, .T. ) ;
#144172=AXIS2_PLACEMENT_3D ( 'NONE', #115988, #195540, #13051 ) ;
#144209=DIRECTION ( 'NONE',  ( 0.000000000000000000, 0.9915357197604804940, -0.1298341882520397950 ) ) ;
#144211=ORIENTED_EDGE ( 'NONE', *, *, #97216, .T. ) ;
#144223=ORIENTED_EDGE ( 'NONE', *, *, #21938, .T. ) ;
#144249=ADVANCED_FACE ( 'NONE', ( #82847 ), #153014, .T. ) ;
#144263=AXIS2_PLACEMENT_3D ( 'NONE', #8196, #108568, #72022 ) ;
#144279=DIRECTION ( 'NONE',  ( 0.7071067811865474617, -0.7071067811865474617, -5.142139384388980375E-15 ) ) ;
#144291=EDGE_CURVE ( 'NONE', #140147, #216955, #217239, .T. ) ;
#144299=CIRCLE ( 'NONE', #81752, 0.4000000000000114575 ) ;
#144339=VECTOR ( 'NONE', #35553, 999.9999999999998863 ) ;
#144360=VERTEX_POINT ( 'NONE', #164991 ) ;
#144364=VERTEX_POINT ( 'NONE', #9766 ) ;
#144366=CARTESIAN_POINT ( 'NONE',  ( 20.94999999999999929, 77.83585931145546510, -91.51866831572576189 ) ) ;
#144411=ORIENTED_EDGE ( 'NONE', *, *, #221774, .T. ) ;
#144445=DIRECTION ( 'NONE',  ( -1.000000000000000000, 2.952720810173289112E-16, 2.061873921506763405E-30 ) ) ;
#144456=ORIENTED_EDGE ( 'NONE', *, *, #199125, .T. ) ;
#144457=EDGE_CURVE ( 'NONE', #47866, #8189, #19814, .T. ) ;
#144470=ORIENTED_EDGE ( 'NONE', *, *, #79743, .T. ) ;
#144481=ORIENTED_EDGE ( 'NONE', *, *, #131904, .F. ) ;
#144509=( BOUNDED_SURFACE ( )  B_SPLINE_SURFACE ( 3, 2, ( 
 ( #26258, #243995, #40713 ),
 ( #23711, #62803, #142327 ),
 ( #223146, #202313, #184026 ),
 ( #24986, #224434, #65367 ) ),
 .UNSPECIFIED., .F., .F., .F. ) 
 B_SPLINE_SURFACE_WITH_KNOTS ( ( 4, 4 ),
 ( 3, 3 ),
 ( 0.0002700421466196767546, 0.0004789321604330748668 ),
 ( 0.000000000000000000, 1.000000000000000000 ),
 .UNSPECIFIED. ) 
 GEOMETRIC_REPRESENTATION_ITEM ( )  RATIONAL_B_SPLINE_SURFACE ( (
 ( 1.000000000000000000, 0.7071067811865475727, 1.000000000000000000),
 ( 1.000000000000000000, 0.7163411249511738577, 1.000000000000000000),
 ( 1.000000000000000000, 0.7221957104842052777, 1.000000000000000000),
 ( 1.000000000000000000, 0.7250110520819876836, 1.000000000000000000) ) ) 
 REPRESENTATION_ITEM ( '' )  SURFACE ( )  );
#144515=EDGE_CURVE ( 'NONE', #28934, #156274, #24098, .T. ) ;
#144541=PLANE ( 'NONE',  #57237 ) ;
#144551=DIRECTION ( 'NONE',  ( -1.000000000000000000, 0.000000000000000000, 0.000000000000000000 ) ) ;
#144566=VECTOR ( 'NONE', #19632, 1000.000000000000000 ) ;
#144568=LINE ( 'NONE', #125035, #75552 ) ;
#144606=VECTOR ( 'NONE', #148217, 1000.000000000000000 ) ;
#144633=TOROIDAL_SURFACE ( 'NONE', #211292, 0.2000000000000000111, 0.1000000000000000056 ) ;
#144635=TOROIDAL_SURFACE ( 'NONE', #32245, 0.4000000000000005773, 0.1000000000000000056 ) ;
#144640=CARTESIAN_POINT ( 'NONE',  ( -23.25000000000000000, 76.00000000001205080, -123.7481074845242972 ) ) ;
#144648=CARTESIAN_POINT ( 'NONE',  ( 20.21494484322215968, 66.69682926214323970, -128.1828422927511610 ) ) ;
#144650=CARTESIAN_POINT ( 'NONE',  ( -23.15000000000000213, 87.75000000001222134, -148.2731074845242176 ) ) ;
#144658=CIRCLE ( 'NONE', #215396, 0.1000000000000028644 ) ;
#144674=EDGE_LOOP ( 'NONE', ( #42980, #82751, #142776, #38592 ) ) ;
#144685=DIRECTION ( 'NONE',  ( 0.000000000000000000, 6.982962677686266711E-15, -1.000000000000000000 ) ) ;
#144725=AXIS2_PLACEMENT_3D ( 'NONE', #221227, #42610, #23075 ) ;
#144731=CARTESIAN_POINT ( 'NONE',  ( -20.54999999999999716, 85.50000000001197975, -112.9170766071766820 ) ) ;
#144773=CARTESIAN_POINT ( 'NONE',  ( -22.39999999999999858, 64.25000000001215028, -136.4231074845243938 ) ) ;
#144790=EDGE_CURVE ( 'NONE', #202540, #139774, #149178, .T. ) ;
#144812=AXIS2_PLACEMENT_3D ( 'NONE', #136083, #197362, #38308 ) ;
#144819=TOROIDAL_SURFACE ( 'NONE', #211471, 0.2000000000000000111, 0.1000000000000000056 ) ;
#144824=AXIS2_PLACEMENT_3D ( 'NONE', #138496, #116409, #216773 ) ;
#144827=CARTESIAN_POINT ( 'NONE',  ( -21.08884785362073089, 75.95021690494546363, -142.8803008519499258 ) ) ;
#144831=SPHERICAL_SURFACE ( 'NONE', #50116, 0.1000000000000000056 ) ;
#144833=EDGE_CURVE ( 'NONE', #57112, #140955, #111735, .T. ) ;
#144834=DIRECTION ( 'NONE',  ( -0.000000000000000000, 6.982962677686266711E-15, -1.000000000000000000 ) ) ;
#144837=CIRCLE ( 'NONE', #103319, 0.2000000000000057288 ) ;
#144848=DIRECTION ( 'NONE',  ( 0.000000000000000000, -1.000000000000000000, 0.000000000000000000 ) ) ;
#144876=CARTESIAN_POINT ( 'NONE',  ( -20.85000000000000142, 68.97833521811179480, -99.38954208262707368 ) ) ;
#144932=VECTOR ( 'NONE', #244363, 1000.000000000000000 ) ;
#144934=ORIENTED_EDGE ( 'NONE', *, *, #28388, .T. ) ;
#144936=AXIS2_PLACEMENT_3D ( 'NONE', #21346, #1737, #243894 ) ;
#144945=CARTESIAN_POINT ( 'NONE',  ( 22.42357213249528769, 68.32706761365223258, -136.6221944485259030 ) ) ;
#144949=CARTESIAN_POINT ( 'NONE',  ( 22.59999999999999787, 64.35042919246734527, -136.6231074845243825 ) ) ;
#144992=ORIENTED_EDGE ( 'NONE', *, *, #189485, .T. ) ;
#145015=ADVANCED_FACE ( 'NONE', ( #17194 ), #197082, .T. ) ;
#145020=AXIS2_PLACEMENT_3D ( 'NONE', #186945, #24013, #125654 ) ;
#145039=VECTOR ( 'NONE', #24906, 1000.000000000000000 ) ;
#145048=ORIENTED_EDGE ( 'NONE', *, *, #152912, .F. ) ;
#145084=ORIENTED_EDGE ( 'NONE', *, *, #624, .T. ) ;
#145090=EDGE_CURVE ( 'NONE', #1620, #2705, #4026, .T. ) ;
#145099=CARTESIAN_POINT ( 'NONE',  ( -18.46902351632711614, 85.50947011869294556, -129.5366535502669478 ) ) ;
#145135=B_SPLINE_CURVE_WITH_KNOTS ( 'NONE', 3,
 ( #91784, #112636, #13539, #254663, #218125, #96874, #34404, #116487, #137312, #94335 ),
 .UNSPECIFIED., .F., .F.,
 ( 4, 3, 3, 4 ),
 ( 0.000000000000000000, 0.0002000000000008537104, 0.001000000000082977483, 0.001967863649483339323 ),
 .UNSPECIFIED. ) ;
#145138=VERTEX_POINT ( 'NONE', #183952 ) ;
#145207=DIRECTION ( 'NONE',  ( 0.000000000000000000, 1.000000000000000000, 6.938893903907222067E-15 ) ) ;
#145216=EDGE_CURVE ( 'NONE', #40198, #105588, #157771, .T. ) ;
#145228=CARTESIAN_POINT ( 'NONE',  ( -23.25000000000000000, 76.10085836911093793, -148.2726746080136877 ) ) ;
#145236=CYLINDRICAL_SURFACE ( 'NONE', #231756, 0.1000000000000028644 ) ;
#145261=VERTEX_POINT ( 'NONE', #108280 ) ;
#145283=VECTOR ( 'NONE', #209055, 1000.000000000000000 ) ;
#145289=LINE ( 'NONE', #167467, #251709 ) ;
#145302=ORIENTED_EDGE ( 'NONE', *, *, #134336, .T. ) ;
#145336=EDGE_CURVE ( 'NONE', #207643, #25751, #11986, .T. ) ;
#145337=CARTESIAN_POINT ( 'NONE',  ( -21.05000000000000071, 77.16270174995010223, -128.4231074845242802 ) ) ;
#145349=EDGE_LOOP ( 'NONE', ( #156637, #3963, #71264, #73086 ) ) ;
#145367=VECTOR ( 'NONE', #113387, 1000.000000000000000 ) ;
#145379=SPHERICAL_SURFACE ( 'NONE', #44389, 0.1000000000000000056 ) ;
#145380=CARTESIAN_POINT ( 'NONE',  ( 20.95443524775735611, 67.12144573613926468, -127.9893852089242188 ) ) ;
#145398=DIRECTION ( 'NONE',  ( 1.000000000000000000, 0.000000000000000000, 0.000000000000000000 ) ) ;
#145410=EDGE_CURVE ( 'NONE', #225759, #139066, #89333, .T. ) ;
#145431=EDGE_LOOP ( 'NONE', ( #151230, #176707, #33681, #150078 ) ) ;
#145451=CARTESIAN_POINT ( 'NONE',  ( 22.39999999999999503, 76.00000000001222134, -148.1726782920690937 ) ) ;
#145453=DIRECTION ( 'NONE',  ( 0.000000000000000000, -7.304098846218139203E-15, 1.000000000000000000 ) ) ;
#145481=CIRCLE ( 'NONE', #212139, 7.900000000000003908 ) ;
#145495=CARTESIAN_POINT ( 'NONE',  ( -23.25000000000000000, 76.00000000001190870, -103.0231074845243029 ) ) ;
#145503=CARTESIAN_POINT ( 'NONE',  ( 19.99999999999998934, 64.25000000001196554, -111.6731074845243796 ) ) ;
#145514=ORIENTED_EDGE ( 'NONE', *, *, #17060, .T. ) ;
#145525=DIRECTION ( 'NONE',  ( 0.000000000000000000, 6.982962677686266711E-15, -1.000000000000000000 ) ) ;
#145530=CIRCLE ( 'NONE', #74842, 0.1000000000000043771 ) ;
#145575=DIRECTION ( 'NONE',  ( 0.000000000000000000, 1.000000000000000000, 6.608470384673536824E-15 ) ) ;
#145586=EDGE_CURVE ( 'NONE', #151026, #205485, #73669, .T. ) ;
#145628=EDGE_CURVE ( 'NONE', #13286, #88928, #228650, .T. ) ;
#145633=CARTESIAN_POINT ( 'NONE',  ( -22.39999999999999858, 76.00000000001219291, -144.3138870828977076 ) ) ;
#145638=VERTEX_POINT ( 'NONE', #215696 ) ;
#145644=CYLINDRICAL_SURFACE ( 'NONE', #1179, 4.049999999999998046 ) ;
#145659=CARTESIAN_POINT ( 'NONE',  ( 20.12500000000000355, 66.74195072709477472, -128.1597686473819238 ) ) ;
#145695=DIRECTION ( 'NONE',  ( 0.000000000000000000, 6.982962677686266711E-15, -1.000000000000000000 ) ) ;
#145700=FACE_OUTER_BOUND ( 'NONE', #71332, .T. ) ;
#145843=CARTESIAN_POINT ( 'NONE',  ( -21.07016717456945898, 69.67905916191187998, -136.5231074845243597 ) ) ;
#145844=VERTEX_POINT ( 'NONE', #242976 ) ;
#145878=AXIS2_PLACEMENT_3D ( 'NONE', #110546, #227937, #210941 ) ;
#145900=CYLINDRICAL_SURFACE ( 'NONE', #246320, 0.09999999999998898659 ) ;
#145902=ADVANCED_FACE ( 'NONE', ( #184287 ), #207732, .T. ) ;
#145934=SPHERICAL_SURFACE ( 'NONE', #181822, 0.1000000000000000056 ) ;
#145954=CYLINDRICAL_SURFACE ( 'NONE', #39378, 0.09999999999999939493 ) ;
#145984=LINE ( 'NONE', #61326, #8932 ) ;
#145995=CARTESIAN_POINT ( 'NONE',  ( -20.54999999999999716, 68.85000000001205933, -124.1731074845243370 ) ) ;
#146007=EDGE_LOOP ( 'NONE', ( #243592, #191781, #40350, #101922, #90815, #46706, #255505, #10765, #53806, #46535, #251030, #161210 ) ) ;
#146024=VERTEX_POINT ( 'NONE', #115036 ) ;
#146050=TOROIDAL_SURFACE ( 'NONE', #179391, 0.2000000000000000111, 0.1000000000000000056 ) ;
#146055=EDGE_LOOP ( 'NONE', ( #35336, #122790, #174542, #160164 ) ) ;
#146060=ORIENTED_EDGE ( 'NONE', *, *, #59916, .T. ) ;
#146064=EDGE_LOOP ( 'NONE', ( #133170, #223014, #72658, #136310 ) ) ;
#146091=CARTESIAN_POINT ( 'NONE',  ( 23.14999999999999858, 71.00000000001205080, -124.1178414656112352 ) ) ;
#146148=CARTESIAN_POINT ( 'NONE',  ( 23.14999999999999858, 73.90000000001190017, -103.0231074845243171 ) ) ;
#146188=EDGE_CURVE ( 'NONE', #93761, #242949, #216328, .T. ) ;
#146272=ORIENTED_EDGE ( 'NONE', *, *, #36737, .F. ) ;
#146309=DIRECTION ( 'NONE',  ( 0.000000000000000000, -3.469446951953635015E-14, 1.000000000000000000 ) ) ;
#146310=ORIENTED_EDGE ( 'NONE', *, *, #10817, .F. ) ;
#146316=AXIS2_PLACEMENT_3D ( 'NONE', #188382, #248361, #91853 ) ;
#146333=DIRECTION ( 'NONE',  ( 1.000000000000000000, 0.000000000000000000, 0.000000000000000000 ) ) ;
#146348=CARTESIAN_POINT ( 'NONE',  ( 20.85000000000000142, 77.83585931145546510, -91.51866831572576189 ) ) ;
#146363=VERTEX_POINT ( 'NONE', #11810 ) ;
#146373=CARTESIAN_POINT ( 'NONE',  ( -18.58671080940899856, 85.40693285883877195, -129.3989530196196256 ) ) ;
#146404=VECTOR ( 'NONE', #203557, 1000.000000000000000 ) ;
#146417=LINE ( 'NONE', #68193, #127052 ) ;
#146426=DIRECTION ( 'NONE',  ( 1.000000000000000000, 7.304098846218133681E-16, 4.639676173203992654E-30 ) ) ;
#146428=CIRCLE ( 'NONE', #225714, 0.09999999999999939493 ) ;
#146486=DIRECTION ( 'NONE',  ( 1.000000000000000000, 0.000000000000000000, 0.000000000000000000 ) ) ;
#146489=DIRECTION ( 'NONE',  ( -1.000000000000000000, 0.000000000000000000, 0.000000000000000000 ) ) ;
#146496=CARTESIAN_POINT ( 'NONE',  ( -20.91682497891422798, 65.67736539654943329, -97.46251168765718376 ) ) ;
#146498=CIRCLE ( 'NONE', #142424, 0.09999999999998898659 ) ;
#146506=CARTESIAN_POINT ( 'NONE',  ( 20.94999999999999929, 69.35000000001207354, -126.5060803140843291 ) ) ;
#146516=FACE_OUTER_BOUND ( 'NONE', #235173, .T. ) ;
#146522=AXIS2_PLACEMENT_3D ( 'NONE', #74328, #243623, #83239 ) ;
#146526=DIRECTION ( 'NONE',  ( 0.000000000000000000, 0.000000000000000000, 1.000000000000000000 ) ) ;
#146528=CARTESIAN_POINT ( 'NONE',  ( -18.59999999999999787, 74.13328508995475374, -124.7704322382423072 ) ) ;
#146553=DIRECTION ( 'NONE',  ( 0.000000000000000000, -1.000000000000000000, 0.000000000000000000 ) ) ;
#146571=EDGE_CURVE ( 'NONE', #168985, #229125, #83211, .T. ) ;
#146584=CARTESIAN_POINT ( 'NONE',  ( -21.55000000000000426, 68.25000000001205080, -124.1731074845243512 ) ) ;
#146589=ADVANCED_FACE ( 'NONE', ( #61172 ), #35230, .T. ) ;
#146604=VECTOR ( 'NONE', #218916, 1000.000000000000000 ) ;
#146613=AXIS2_PLACEMENT_3D ( 'NONE', #189501, #113806, #193363 ) ;
#146629=CARTESIAN_POINT ( 'NONE',  ( 20.94999999999999574, 74.25000000001205080, -124.8535959266226598 ) ) ;
#146631=EDGE_LOOP ( 'NONE', ( #182755, #109342, #142073, #90886 ) ) ;
#146663=CARTESIAN_POINT ( 'NONE',  ( 23.14999999999999858, 69.35000000001205933, -124.1731074845243370 ) ) ;
#146670=VECTOR ( 'NONE', #41674, 1000.000000000000000 ) ;
#146686=VECTOR ( 'NONE', #218657, 1000.000000000000000 ) ;
#146718=ORIENTED_EDGE ( 'NONE', *, *, #68109, .F. ) ;
#146744=VECTOR ( 'NONE', #57242, 1000.000000000000000 ) ;
#146759=FACE_OUTER_BOUND ( 'NONE', #95131, .T. ) ;
#146792=DIRECTION ( 'NONE',  ( 1.000000000000000000, -0.000000000000000000, 0.000000000000000000 ) ) ;
#146796=AXIS2_PLACEMENT_3D ( 'NONE', #134299, #31408, #13107 ) ;
#146813=FACE_OUTER_BOUND ( 'NONE', #70165, .T. ) ;
#146822=CARTESIAN_POINT ( 'NONE',  ( -23.25000000000000000, 73.40000000001199965, -116.2477294072864140 ) ) ;
#146855=CARTESIAN_POINT ( 'NONE',  ( -20.05000000000000426, 66.75000000001205080, -124.1731074845243654 ) ) ;
#146863=DIRECTION ( 'NONE',  ( 1.301042606982683734E-14, 0.8660254037844367092, -0.5000000000000037748 ) ) ;
#146866=ORIENTED_EDGE ( 'NONE', *, *, #194335, .T. ) ;
#146876=ADVANCED_FACE ( 'NONE', ( #32353 ), #111865, .T. ) ;
#146895=EDGE_LOOP ( 'NONE', ( #244152, #95447, #35317, #224865, #214027, #199292, #180936, #3455, #126388, #225275, #101683, #182850 ) ) ;
#146903=DIRECTION ( 'NONE',  ( 1.000000000000000000, 0.000000000000000000, 0.000000000000000000 ) ) ;
#146911=AXIS2_PLACEMENT_3D ( 'NONE', #93259, #253608, #176676 ) ;
#146923=ORIENTED_EDGE ( 'NONE', *, *, #120611, .F. ) ;
#146936=PLANE ( 'NONE',  #79794 ) ;
#146958=VECTOR ( 'NONE', #47539, 1000.000000000000000 ) ;
#146960=VECTOR ( 'NONE', #163405, 1000.000000000000000 ) ;
#146982=ORIENTED_EDGE ( 'NONE', *, *, #70820, .T. ) ;
#146994=ORIENTED_EDGE ( 'NONE', *, *, #34015, .T. ) ;
#147000=DIRECTION ( 'NONE',  ( 0.000000000000000000, 1.000000000000000000, 6.982962677686266711E-15 ) ) ;
#147006=LINE ( 'NONE', #182317, #159857 ) ;
#147009=VECTOR ( 'NONE', #89542, 1000.000000000000000 ) ;
#147020=CARTESIAN_POINT ( 'NONE',  ( -21.05000000000000071, 69.69503888732714358, -136.5017219185863837 ) ) ;
#147022=DIRECTION ( 'NONE',  ( 0.000000000000000000, 0.000000000000000000, 1.000000000000000000 ) ) ;
#147024=VERTEX_POINT ( 'NONE', #51388 ) ;
#147031=TOROIDAL_SURFACE ( 'NONE', #92874, 4.149999999999999467, 0.1000000000000000056 ) ;
#147052=AXIS2_PLACEMENT_3D ( 'NONE', #238341, #8412, #204026 ) ;
#147056=ORIENTED_EDGE ( 'NONE', *, *, #161715, .T. ) ;
#147071=AXIS2_PLACEMENT_3D ( 'NONE', #254949, #136317, #213308 ) ;
#147077=CARTESIAN_POINT ( 'NONE',  ( 22.49999999999999645, 64.25043287652275126, -136.6239658536231332 ) ) ;
#147095=CARTESIAN_POINT ( 'NONE',  ( 20.94999999999999929, 84.73084112150731073, -112.6211822035085675 ) ) ;
#147136=DIRECTION ( 'NONE',  ( 0.000000000000000000, 1.000000000000000000, 6.938893903907222067E-15 ) ) ;
#147159=ORIENTED_EDGE ( 'NONE', *, *, #168509, .T. ) ;
#147164=VERTEX_POINT ( 'NONE', #180370 ) ;
#147203=DIRECTION ( 'NONE',  ( 0.000000000000000000, 7.086529944415894657E-15, -1.000000000000000000 ) ) ;
#147226=FACE_OUTER_BOUND ( 'NONE', #124063, .T. ) ;
#147235=DIRECTION ( 'NONE',  ( 1.000000000000000000, 0.000000000000000000, 0.000000000000000000 ) ) ;
#147288=PLANE ( 'NONE',  #97384 ) ;
#147301=DIRECTION ( 'NONE',  ( 0.000000000000000000, 0.000000000000000000, 1.000000000000000000 ) ) ;
#147312=ORIENTED_EDGE ( 'NONE', *, *, #237778, .F. ) ;
#147412=CARTESIAN_POINT ( 'NONE',  ( -21.08621493067320429, 75.94380516053614372, -142.8724017756962326 ) ) ;
#147460=TOROIDAL_SURFACE ( 'NONE', #35080, 0.2000000000000000111, 0.1000000000000000056 ) ;
#147467=CARTESIAN_POINT ( 'NONE',  ( -20.54999999999999716, 85.40000000001198543, -112.9170766071766820 ) ) ;
#147468=VERTEX_POINT ( 'NONE', #251488 ) ;
#147473=AXIS2_PLACEMENT_3D ( 'NONE', #123179, #86584, #48765 ) ;
#147489=CARTESIAN_POINT ( 'NONE',  ( 21.09793522318408066, 65.27537548979928772, -124.2838166135473017 ) ) ;
#147499=DIRECTION ( 'NONE',  ( 1.000000000000000000, 0.000000000000000000, 0.000000000000000000 ) ) ;
#147521=EDGE_CURVE ( 'NONE', #151038, #154603, #239784, .T. ) ;
#147534=CIRCLE ( 'NONE', #197585, 0.09999999999998898659 ) ;
#147571=ADVANCED_FACE ( 'NONE', ( #187696 ), #7763, .T. ) ;
#147632=CARTESIAN_POINT ( 'NONE',  ( -20.12071067811865888, 66.67928932189340685, -124.1731074845243654 ) ) ;
#147635=CIRCLE ( 'NONE', #67957, 0.09999999999998898659 ) ;
#147639=VERTEX_POINT ( 'NONE', #237069 ) ;
#147652=CYLINDRICAL_SURFACE ( 'NONE', #3849, 4.000000000000003553 ) ;
#147653=CARTESIAN_POINT ( 'NONE',  ( 18.49999999999999289, 65.50857864377465489, -111.6731074845243654 ) ) ;
#147705=CARTESIAN_POINT ( 'NONE',  ( -18.59999999999999787, 68.87972903831429505, -99.36354444268502561 ) ) ;
#147707=VERTEX_POINT ( 'NONE', #192822 ) ;
#147708=CIRCLE ( 'NONE', #185127, 0.09999999999998898659 ) ;
#147716=CARTESIAN_POINT ( 'NONE',  ( -23.25000000000000000, 64.25000000001190870, -103.0231074845243882 ) ) ;
#147743=CARTESIAN_POINT ( 'NONE',  ( -21.37071067811865532, 67.92928932189333580, -115.2731074845243455 ) ) ;
#147778=CIRCLE ( 'NONE', #222766, 0.1000000000000028644 ) ;
#147787=VERTEX_POINT ( 'NONE', #163955 ) ;
#147812=CIRCLE ( 'NONE', #122877, 7.900000000000003908 ) ;
#147817=CARTESIAN_POINT ( 'NONE',  ( -20.94999027547553894, 65.70673848566976005, -97.56382523348287350 ) ) ;
#147828=ORIENTED_EDGE ( 'NONE', *, *, #127769, .T. ) ;
#147845=TOROIDAL_SURFACE ( 'NONE', #35435, 0.6000000000000009770, 0.1000000000000000056 ) ;
#147876=DIRECTION ( 'NONE',  ( 0.000000000000000000, 0.000000000000000000, 1.000000000000000000 ) ) ;
#147883=DIRECTION ( 'NONE',  ( 1.000000000000000000, 0.000000000000000000, 0.000000000000000000 ) ) ;
#147899=EDGE_CURVE ( 'NONE', #161400, #102756, #144069, .T. ) ;
#147927=ADVANCED_FACE ( 'NONE', ( #248616 ), #51671, .F. ) ;
#147947=AXIS2_PLACEMENT_3D ( 'NONE', #167617, #189732, #11096 ) ;
#147969=DIRECTION ( 'NONE',  ( 1.000000000000000000, 0.000000000000000000, 0.000000000000000000 ) ) ;
#147988=ORIENTED_EDGE ( 'NONE', *, *, #80970, .F. ) ;
#147997=LINE ( 'NONE', #129711, #209962 ) ;
#148056=DIRECTION ( 'NONE',  ( 1.000000000000000000, -0.000000000000000000, 0.000000000000000000 ) ) ;
#148085=CARTESIAN_POINT ( 'NONE',  ( 18.59999999999999787, 77.36242903720516040, -95.13422623660308375 ) ) ;
#148136=VECTOR ( 'NONE', #144279, 1000.000000000000114 ) ;
#148173=DIRECTION ( 'NONE',  ( 1.000000000000000000, 0.000000000000000000, 0.000000000000000000 ) ) ;
#148174=VERTEX_POINT ( 'NONE', #121950 ) ;
#148194=AXIS2_PLACEMENT_3D ( 'NONE', #21026, #134504, #234921 ) ;
#148217=DIRECTION ( 'NONE',  ( 0.000000000000000000, -6.982962677686266711E-15, 1.000000000000000000 ) ) ;
#148218=EDGE_CURVE ( 'NONE', #33201, #45900, #240149, .T. ) ;
#148242=DIRECTION ( 'NONE',  ( -1.000000000000000000, 2.952720810173289112E-16, 2.061873921506763405E-30 ) ) ;
#148249=AXIS2_PLACEMENT_3D ( 'NONE', #157625, #58453, #137997 ) ;
#148259=DIRECTION ( 'NONE',  ( 0.000000000000000000, 0.1568667991644355497, 0.9876197685951332295 ) ) ;
#148288=EDGE_CURVE ( 'NONE', #153900, #211628, #198440, .T. ) ;
#148344=ORIENTED_EDGE ( 'NONE', *, *, #2888, .F. ) ;
#148362=EDGE_CURVE ( 'NONE', #221833, #94457, #165129, .T. ) ;
#148369=CARTESIAN_POINT ( 'NONE',  ( -20.94999999999999929, 74.75000000001207923, -128.5231074845243029 ) ) ;
#148380=ORIENTED_EDGE ( 'NONE', *, *, #140659, .F. ) ;
#148413=( BOUNDED_SURFACE ( )  B_SPLINE_SURFACE ( 3, 2, ( 
 ( #151241, #53407, #250322 ),
 ( #170844, #112121, #71708 ),
 ( #230781, #175951, #135490 ),
 ( #156394, #32604, #16863 ),
 ( #251607, #54684, #13025 ),
 ( #191669, #52104, #152544 ),
 ( #92520, #18132, #173410 ),
 ( #252882, #37721, #172117 ),
 ( #131659, #73007, #74289 ),
 ( #55948, #136782, #215048 ) ),
 .UNSPECIFIED., .F., .F., .F. ) 
 B_SPLINE_SURFACE_WITH_KNOTS ( ( 4, 2, 2, 2, 4 ),
 ( 3, 3 ),
 ( 0.0001701955120502373817, 0.0002247052511886135672, 0.0002792149903269897527, 0.0003882344686037421779, 0.0006062734251572470283 ),
 ( 0.000000000000000000, 1.000000000000000000 ),
 .UNSPECIFIED. ) 
 GEOMETRIC_REPRESENTATION_ITEM ( )  RATIONAL_B_SPLINE_SURFACE ( (
 ( 1.000000000000000000, 0.2966190024560231286, 1.000000000000000000),
 ( 1.000000000000000000, 0.2964522492704981804, 1.000000000000000000),
 ( 1.000000000000000000, 0.3059923531895626936, 1.000000000000000000),
 ( 1.000000000000000000, 0.3355751146933140805, 1.000000000000000000),
 ( 1.000000000000000000, 0.3550672384963000638, 1.000000000000000000),
 ( 1.000000000000000000, 0.4157034672182242652, 1.000000000000000000),
 ( 1.000000000000000000, 0.4588031877651267965, 1.000000000000000000),
 ( 1.000000000000000000, 0.5771441759666575688, 1.000000000000000000),
 ( 1.000000000000000000, 0.6469377121768220551, 1.000000000000000000),
 ( 1.000000000000000000, 0.7071067811865475727, 1.000000000000000000) ) ) 
 REPRESENTATION_ITEM ( '' )  SURFACE ( )  );
#148432=AXIS2_PLACEMENT_3D ( 'NONE', #25497, #127154, #164995 ) ;
#148439=LINE ( 'NONE', #127582, #33545 ) ;
#148454=VECTOR ( 'NONE', #168566, 1000.000000000000000 ) ;
#148511=ADVANCED_FACE ( 'NONE', ( #237735 ), #127904, .T. ) ;
#148528=ORIENTED_EDGE ( 'NONE', *, *, #52299, .F. ) ;
#148546=EDGE_LOOP ( 'NONE', ( #169393, #34195, #9142, #107929 ) ) ;
#148556=DIRECTION ( 'NONE',  ( 0.000000000000000000, -1.000000000000000000, -6.982962677686266711E-15 ) ) ;
#148559=ORIENTED_EDGE ( 'NONE', *, *, #206828, .T. ) ;
#148581=FACE_OUTER_BOUND ( 'NONE', #151813, .T. ) ;
#148587=TOROIDAL_SURFACE ( 'NONE', #81891, 0.9750000000000019762, 0.1000000000000000056 ) ;
#148606=B_SPLINE_CURVE_WITH_KNOTS ( 'NONE', 3,
 ( #73799, #33398, #112900, #192438, #133735, #94604 ),
 .UNSPECIFIED., .F., .F.,
 ( 4, 2, 4 ),
 ( 0.000000000000000000, 0.0001568709654583423218, 0.0003137419309166846436 ),
 .UNSPECIFIED. ) ;
#148617=LINE ( 'NONE', #144731, #29298 ) ;
#148680=DIRECTION ( 'NONE',  ( 0.000000000000000000, -0.9908441862701791170, 0.1350103645450472789 ) ) ;
#148700=AXIS2_PLACEMENT_3D ( 'NONE', #119569, #20468, #19160 ) ;
#148703=EDGE_LOOP ( 'NONE', ( #214961, #69789, #212960, #202225 ) ) ;
#148711=DIRECTION ( 'NONE',  ( 1.000000000000000000, 0.000000000000000000, 0.000000000000000000 ) ) ;
#148714=ORIENTED_EDGE ( 'NONE', *, *, #242615, .T. ) ;
#148741=DIRECTION ( 'NONE',  ( 0.000000000000000000, -1.000000000000000000, -6.982962677686265922E-15 ) ) ;
#148745=AXIS2_PLACEMENT_3D ( 'NONE', #59129, #40921, #1743 ) ;
#148766=ORIENTED_EDGE ( 'NONE', *, *, #179036, .T. ) ;
#148769=DIRECTION ( 'NONE',  ( 0.000000000000000000, -0.3738317757008748909, -0.9274965247785733613 ) ) ;
#148826=DIRECTION ( 'NONE',  ( 0.1538461538461484146, -0.9880948137434723000, 0.000000000000000000 ) ) ;
#148843=VERTEX_POINT ( 'NONE', #16488 ) ;
#148869=VERTEX_POINT ( 'NONE', #55552 ) ;
#148887=DIRECTION ( 'NONE',  ( 0.000000000000000000, 7.086529944415894657E-15, -1.000000000000000000 ) ) ;
#148913=ORIENTED_EDGE ( 'NONE', *, *, #206780, .T. ) ;
#148929=ORIENTED_EDGE ( 'NONE', *, *, #32895, .T. ) ;
#148932=DIRECTION ( 'NONE',  ( 0.000000000000000000, -6.997203936713175802E-15, 1.000000000000000000 ) ) ;
#148959=ORIENTED_EDGE ( 'NONE', *, *, #90077, .F. ) ;
#149024=ORIENTED_EDGE ( 'NONE', *, *, #37965, .F. ) ;
#149028=CARTESIAN_POINT ( 'NONE',  ( 20.94999999999999929, 87.29603075034741266, -133.4752083248603469 ) ) ;
#149100=CARTESIAN_POINT ( 'NONE',  ( -18.59999999999999787, 64.35000000001205933, -124.2731074845243882 ) ) ;
#149108=CARTESIAN_POINT ( 'NONE',  ( -20.94999999999999929, 65.70729864261004138, -97.56574559737244101 ) ) ;
#149118=ORIENTED_EDGE ( 'NONE', *, *, #9864, .F. ) ;
#149130=CIRCLE ( 'NONE', #99191, 0.1000000000000000888 ) ;
#149131=VERTEX_POINT ( 'NONE', #124567 ) ;
#149150=LINE ( 'NONE', #106125, #144932 ) ;
#149165=CYLINDRICAL_SURFACE ( 'NONE', #124254, 0.1000000000000028644 ) ;
#149178=CIRCLE ( 'NONE', #178402, 0.09999999999999799327 ) ;
#149208=DIRECTION ( 'NONE',  ( 0.000000000000000000, 6.982962677686267499E-15, -1.000000000000000000 ) ) ;
#149222=DIRECTION ( 'NONE',  ( -1.000000000000000000, 7.304098846218135653E-16, 4.639676173203994055E-30 ) ) ;
#149237=EDGE_CURVE ( 'NONE', #231485, #47571, #28146, .T. ) ;
#149257=EDGE_CURVE ( 'NONE', #131402, #207317, #15685, .T. ) ;
#149261=B_SPLINE_CURVE_WITH_KNOTS ( 'NONE', 3,
 ( #57689, #192105, #13456, #235072, #58957, #77256, #194687, #135941 ),
 .UNSPECIFIED., .F., .F.,
 ( 4, 2, 2, 4 ),
 ( 0.000000000000000000, 0.0001094981963948514188, 0.0002189963927897028376, 0.0004379927855794013927 ),
 .UNSPECIFIED. ) ;
#149298=DIRECTION ( 'NONE',  ( 0.000000000000000000, 0.000000000000000000, -1.000000000000000000 ) ) ;
#149312=CARTESIAN_POINT ( 'NONE',  ( -20.94999999999999929, 77.85102823015292017, -124.8691942151017855 ) ) ;
#149327=DIRECTION ( 'NONE',  ( -1.000000000000000000, -7.304098846218134667E-16, -5.311601492717084346E-30 ) ) ;
#149342=ORIENTED_EDGE ( 'NONE', *, *, #222018, .T. ) ;
#149356=CARTESIAN_POINT ( 'NONE',  ( 21.05000000000000071, 76.00000000001193712, -107.1231074845243114 ) ) ;
#149357=ORIENTED_EDGE ( 'NONE', *, *, #163792, .T. ) ;
#149369=AXIS2_PLACEMENT_3D ( 'NONE', #75026, #134934, #73735 ) ;
#149383=CARTESIAN_POINT ( 'NONE',  ( -23.25000000000000000, 64.35000000001222986, -148.2731074845243882 ) ) ;
#149406=FACE_OUTER_BOUND ( 'NONE', #90638, .T. ) ;
#149420=CIRCLE ( 'NONE', #61917, 4.300000000000025580 ) ;
#149423=DIRECTION ( 'NONE',  ( 3.469446951953635015E-14, 6.982962677686266711E-15, -1.000000000000000000 ) ) ;
#149435=AXIS2_PLACEMENT_3D ( 'NONE', #151092, #51959, #131517 ) ;
#149437=CARTESIAN_POINT ( 'NONE',  ( -20.64999999999999858, 71.65000000001199965, -115.3731074845243256 ) ) ;
#149449=EDGE_CURVE ( 'NONE', #135040, #206383, #28344, .T. ) ;
#149450=DIRECTION ( 'NONE',  ( 0.000000000000000000, -7.056502275159890832E-15, 1.000000000000000000 ) ) ;
#149489=DIRECTION ( 'NONE',  ( 0.000000000000000000, 0.000000000000000000, 1.000000000000000000 ) ) ;
#149504=FACE_OUTER_BOUND ( 'NONE', #166750, .T. ) ;
#149545=DIRECTION ( 'NONE',  ( 0.000000000000000000, 0.000000000000000000, 1.000000000000000000 ) ) ;
#149585=EDGE_LOOP ( 'NONE', ( #45177, #218732, #130974, #103966 ) ) ;
#149675=AXIS2_PLACEMENT_3D ( 'NONE', #241414, #125316, #240128 ) ;
#149676=VECTOR ( 'NONE', #245981, 1000.000000000000000 ) ;
#149685=VECTOR ( 'NONE', #247464, 1000.000000000000000 ) ;
#149689=DIRECTION ( 'NONE',  ( 0.000000000000000000, -1.000000000000000000, -6.352154140967427193E-15 ) ) ;
#149691=CARTESIAN_POINT ( 'NONE',  ( 21.05000000000000071, 67.22371710471966821, -136.5231074845243597 ) ) ;
#149706=CARTESIAN_POINT ( 'NONE',  ( 21.05000000000000071, 87.65000000001192859, -105.9231074845242091 ) ) ;
#149712=ORIENTED_EDGE ( 'NONE', *, *, #73739, .F. ) ;
#149719=EDGE_LOOP ( 'NONE', ( #134211, #171596, #232562 ) ) ;
#149724=ORIENTED_EDGE ( 'NONE', *, *, #211313, .F. ) ;
#149734=AXIS2_PLACEMENT_3D ( 'NONE', #142580, #108611, #106014 ) ;
#149737=ORIENTED_EDGE ( 'NONE', *, *, #165644, .T. ) ;
#149771=EDGE_CURVE ( 'NONE', #242949, #185471, #19563, .T. ) ;
#149795=EDGE_CURVE ( 'NONE', #59439, #161343, #28542, .T. ) ;
#149812=DIRECTION ( 'NONE',  ( 0.000000000000000000, -7.272083257015735086E-15, 1.000000000000000000 ) ) ;
#149827=ORIENTED_EDGE ( 'NONE', *, *, #38552, .F. ) ;
#149835=ADVANCED_FACE ( 'NONE', ( #194520 ), #156687, .T. ) ;
#149847=EDGE_CURVE ( 'NONE', #103697, #25805, #117525, .T. ) ;
#149850=DIRECTION ( 'NONE',  ( 0.000000000000000000, -1.000000000000000000, -7.272083257015735086E-15 ) ) ;
#149856=DIRECTION ( 'NONE',  ( 0.000000000000000000, 0.4930308989875575865, 0.8700118002898125091 ) ) ;
#149874=AXIS2_PLACEMENT_3D ( 'NONE', #117103, #119677, #17984 ) ;
#149883=DIRECTION ( 'NONE',  ( 0.7071067811865474617, -0.7071067811865474617, -4.937700262164531476E-15 ) ) ;
#149895=EDGE_LOOP ( 'NONE', ( #226861, #98927, #164922, #49652 ) ) ;
#149963=VECTOR ( 'NONE', #3184, 1000.000000000000000 ) ;
#149969=B_SPLINE_CURVE_WITH_KNOTS ( 'NONE', 3,
 ( #53734, #78426, #57569, #134533, #18463, #214095, #77144, #158022, #137132, #113707, #251932, #216659, #133276, #13333, #194561, #73333 ),
 .UNSPECIFIED., .F., .F.,
 ( 4, 3, 3, 3, 3, 4 ),
 ( 0.000000000000000000, 2.209833635978099498E-05, 5.595056164119025226E-05, 8.979992002654954499E-05, 0.0001236482757198867745, 0.0001574984039362969023 ),
 .UNSPECIFIED. ) ;
#149986=CARTESIAN_POINT ( 'NONE',  ( -21.55000000000000426, 68.25000000001199396, -115.3731074845243540 ) ) ;
#149997=VERTEX_POINT ( 'NONE', #186494 ) ;
#150009=EDGE_LOOP ( 'NONE', ( #224578, #29217, #232005, #115556 ) ) ;
#150056=ORIENTED_EDGE ( 'NONE', *, *, #64222, .F. ) ;
#150078=ORIENTED_EDGE ( 'NONE', *, *, #118159, .F. ) ;
#150140=CARTESIAN_POINT ( 'NONE',  ( -20.00857864376270001, 66.75000000001205080, -124.1731074845243654 ) ) ;
#150194=CARTESIAN_POINT ( 'NONE',  ( -18.59999999999999787, 64.40000000001208491, -129.5949042542488314 ) ) ;
#150209=ORIENTED_EDGE ( 'NONE', *, *, #32133, .T. ) ;
#150244=VECTOR ( 'NONE', #88312, 1000.000000000000000 ) ;
#150311=EDGE_CURVE ( 'NONE', #227184, #207317, #80630, .T. ) ;
#150325=AXIS2_PLACEMENT_3D ( 'NONE', #19836, #99324, #181477 ) ;
#150329=CARTESIAN_POINT ( 'NONE',  ( 21.30000000000002558, 76.00000000001210765, -132.4731074845242915 ) ) ;
#150330=ORIENTED_EDGE ( 'NONE', *, *, #38548, .T. ) ;
#150332=B_SPLINE_CURVE_WITH_KNOTS ( 'NONE', 3,
 ( #71897, #14505, #88850, #131850, #130560, #251799, #249245, #191863, #93997, #133141, #168471, #108443, #32793, #109706, #207556, #228401, #171036, #229677, #232262 ),
 .UNSPECIFIED., .F., .F.,
 ( 4, 3, 3, 3, 3, 3, 4 ),
 ( -2.000416914662652606E-06, 0.000000000000000000, 4.714008503746095890E-05, 9.979203887777572343E-05, 0.0001372215519229490546, 0.0001635031576220952632, 0.0001900083748504098548 ),
 .UNSPECIFIED. ) ;
#150338=ORIENTED_EDGE ( 'NONE', *, *, #200956, .F. ) ;
#150345=CARTESIAN_POINT ( 'NONE',  ( -23.15000000000000213, 76.00000000001210765, -132.3731074845242972 ) ) ;
#150351=ORIENTED_EDGE ( 'NONE', *, *, #160941, .F. ) ;
#150375=ADVANCED_FACE ( 'NONE', ( #164052 ), #61423, .T. ) ;
#150414=EDGE_CURVE ( 'NONE', #241350, #194536, #111324, .T. ) ;
#150417=ORIENTED_EDGE ( 'NONE', *, *, #39788, .F. ) ;
#150439=ORIENTED_EDGE ( 'NONE', *, *, #130609, .T. ) ;
#150468=VECTOR ( 'NONE', #15324, 1000.000000000000000 ) ;
#150483=DIRECTION ( 'NONE',  ( 0.000000000000000000, 6.769652589177772835E-15, -1.000000000000000000 ) ) ;
#150574=DIRECTION ( 'NONE',  ( 0.000000000000000000, -0.8660254037844420383, 0.4999999999999942824 ) ) ;
#150578=CARTESIAN_POINT ( 'NONE',  ( -22.50000000000000000, 76.00000000001217870, -142.7731074845243029 ) ) ;
#150616=CARTESIAN_POINT ( 'NONE',  ( -21.29999999999995808, 76.00000000001213607, -136.5231074845242745 ) ) ;
#150642=EDGE_CURVE ( 'NONE', #241360, #152046, #1757, .T. ) ;
#150660=EDGE_CURVE ( 'NONE', #145138, #118915, #20069, .T. ) ;
#150703=ORIENTED_EDGE ( 'NONE', *, *, #85910, .T. ) ;
#150713=AXIS2_PLACEMENT_3D ( 'NONE', #130433, #169616, #127879 ) ;
#150753=EDGE_CURVE ( 'NONE', #242104, #145844, #82423, .T. ) ;
#150823=EDGE_CURVE ( 'NONE', #236302, #8640, #240666, .T. ) ;
#150847=CIRCLE ( 'NONE', #217466, 0.09999999999999939493 ) ;
#150858=DIRECTION ( 'NONE',  ( 0.000000000000000000, -2.775557561562888827E-14, 1.000000000000000000 ) ) ;
#150872=DIRECTION ( 'NONE',  ( 1.000000000000000000, 0.000000000000000000, 0.000000000000000000 ) ) ;
#150910=DIRECTION ( 'NONE',  ( 0.000000000000000000, 0.8068669527896844551, 0.5907332058517525963 ) ) ;
#150938=CARTESIAN_POINT ( 'NONE',  ( 18.59999999999997655, 77.16412189325305349, -95.10825939895268277 ) ) ;
#150977=ADVANCED_FACE ( 'NONE', ( #137219 ), #34958, .F. ) ;
#151007=DIRECTION ( 'NONE',  ( -1.000000000000000000, -3.469446951953635015E-14, -2.422701857770461054E-28 ) ) ;
#151008=ORIENTED_EDGE ( 'NONE', *, *, #11236, .T. ) ;
#151026=VERTEX_POINT ( 'NONE', #242728 ) ;
#151031=VECTOR ( 'NONE', #95718, 1000.000000000000000 ) ;
#151038=VERTEX_POINT ( 'NONE', #165796 ) ;
#151046=CARTESIAN_POINT ( 'NONE',  ( 18.60000000000000497, 76.00000000001213607, -136.5231074845242745 ) ) ;
#151092=CARTESIAN_POINT ( 'NONE',  ( 21.05000000000000071, 85.00000000001197975, -112.5170766071766764 ) ) ;
#151142=ORIENTED_EDGE ( 'NONE', *, *, #13416, .T. ) ;
#151153=ADVANCED_FACE ( 'NONE', ( #9264 ), #88778, .F. ) ;
#151158=CARTESIAN_POINT ( 'NONE',  ( -20.05000000000000426, 66.75000000001199396, -115.2731074845243597 ) ) ;
#151168=CARTESIAN_POINT ( 'NONE',  ( 20.85000000000000142, 69.01799029515542827, -99.32695536626806643 ) ) ;
#151185=VERTEX_POINT ( 'NONE', #191788 ) ;
#151211=DIRECTION ( 'NONE',  ( -1.000000000000000000, 0.000000000000000000, 0.000000000000000000 ) ) ;
#151213=EDGE_CURVE ( 'NONE', #174818, #244668, #71826, .T. ) ;
#151230=ORIENTED_EDGE ( 'NONE', *, *, #2216, .T. ) ;
#151241=CARTESIAN_POINT ( 'NONE',  ( 18.39999999999999858, 85.50000000001185185, -96.42291809330218655 ) ) ;
#151249=ORIENTED_EDGE ( 'NONE', *, *, #181014, .T. ) ;
#151254=ADVANCED_FACE ( 'NONE', ( #99046 ), #138178, .T. ) ;
#151271=ORIENTED_EDGE ( 'NONE', *, *, #131904, .T. ) ;
#151274=CIRCLE ( 'NONE', #251181, 11.80000000000000426 ) ;
#151304=CARTESIAN_POINT ( 'NONE',  ( -21.14999999999999858, 64.25000000001215028, -136.5231074845243597 ) ) ;
#151352=PLANE ( 'NONE',  #183893 ) ;
#151384=CARTESIAN_POINT ( 'NONE',  ( 20.01093837587850288, 64.25000000001196554, -111.7687100499271793 ) ) ;
#151386=DIRECTION ( 'NONE',  ( 1.000000000000000000, 0.000000000000000000, 0.000000000000000000 ) ) ;
#151400=ORIENTED_EDGE ( 'NONE', *, *, #170334, .T. ) ;
#151405=AXIS2_PLACEMENT_3D ( 'NONE', #233920, #115256, #155702 ) ;
#151486=ORIENTED_EDGE ( 'NONE', *, *, #228041, .F. ) ;
#151499=( BOUNDED_SURFACE ( )  B_SPLINE_SURFACE ( 3, 2, ( 
 ( #90966, #147077, #47984 ),
 ( #226614, #250047, #109238 ),
 ( #127534, #85796, #167978 ),
 ( #71429, #25881, #188783 ) ),
 .UNSPECIFIED., .F., .F., .F. ) 
 B_SPLINE_SURFACE_WITH_KNOTS ( ( 4, 4 ),
 ( 3, 3 ),
 ( 0.0006461284895273780972, 0.0007503702773985890034 ),
 ( 0.000000000000000000, 1.000000000000000000 ),
 .UNSPECIFIED. ) 
 GEOMETRIC_REPRESENTATION_ITEM ( )  RATIONAL_B_SPLINE_SURFACE ( (
 ( 1.000000000000000000, 0.7071067811865475727, 1.000000000000000000),
 ( 1.000000000000000000, 0.7076476444648678310, 1.000000000000000000),
 ( 1.000000000000000000, 0.7075727925192238921, 1.000000000000000000),
 ( 1.000000000000000000, 0.7071067811865475727, 1.000000000000000000) ) ) 
 REPRESENTATION_ITEM ( '' )  SURFACE ( )  );
#151511=CARTESIAN_POINT ( 'NONE',  ( -21.05000000000000071, 77.16270174995010223, -128.4231074845242802 ) ) ;
#151526=DIRECTION ( 'NONE',  ( 0.000000000000000000, 6.982962677686266711E-15, -1.000000000000000000 ) ) ;
#151539=ORIENTED_EDGE ( 'NONE', *, *, #133439, .F. ) ;
#151544=EDGE_CURVE ( 'NONE', #29923, #45647, #182611, .T. ) ;
#151545=EDGE_CURVE ( 'NONE', #24249, #145638, #169362, .T. ) ;
#151616=VECTOR ( 'NONE', #50993, 1000.000000000000000 ) ;
#151645=ORIENTED_EDGE ( 'NONE', *, *, #148362, .F. ) ;
#151667=CIRCLE ( 'NONE', #39237, 0.1000000000000052097 ) ;
#151712=ORIENTED_EDGE ( 'NONE', *, *, #64661, .F. ) ;
#151720=ORIENTED_EDGE ( 'NONE', *, *, #190993, .T. ) ;
#151741=ORIENTED_EDGE ( 'NONE', *, *, #166078, .T. ) ;
#151745=CARTESIAN_POINT ( 'NONE',  ( 21.05000000000000071, 76.00000000001213607, -136.5231074845242745 ) ) ;
#151776=CARTESIAN_POINT ( 'NONE',  ( 20.94999999999999929, 70.10000000001197407, -113.2422072491807086 ) ) ;
#151800=CARTESIAN_POINT ( 'NONE',  ( 23.15000000000000213, 85.00000000001197975, -112.9170766071766820 ) ) ;
#151813=EDGE_LOOP ( 'NONE', ( #65842, #67810, #72912, #114663 ) ) ;
#151833=CARTESIAN_POINT ( 'NONE',  ( -21.06715728752538652, 64.25000000001209344, -129.5083017138703667 ) ) ;
#151846=ORIENTED_EDGE ( 'NONE', *, *, #34323, .T. ) ;
#151855=ORIENTED_EDGE ( 'NONE', *, *, #63382, .F. ) ;
#151858=ORIENTED_EDGE ( 'NONE', *, *, #77773, .T. ) ;
#151863=EDGE_CURVE ( 'NONE', #125361, #140961, #62163, .T. ) ;
#151875=ORIENTED_EDGE ( 'NONE', *, *, #221841, .F. ) ;
#151877=CARTESIAN_POINT ( 'NONE',  ( 23.14999999999999858, 80.00000000001190870, -103.0231074845242745 ) ) ;
#151892=DIRECTION ( 'NONE',  ( 0.000000000000000000, 6.982962677686266711E-15, -1.000000000000000000 ) ) ;
#151901=AXIS2_PLACEMENT_3D ( 'NONE', #145337, #30560, #108784 ) ;
#151909=CARTESIAN_POINT ( 'NONE',  ( -21.08078803292166725, 75.92081401285447839, -142.8561204489614624 ) ) ;
#151927=VECTOR ( 'NONE', #184953, 1000.000000000000000 ) ;
#151969=FACE_OUTER_BOUND ( 'NONE', #65779, .T. ) ;
#152016=ORIENTED_EDGE ( 'NONE', *, *, #111945, .T. ) ;
#152037=ORIENTED_EDGE ( 'NONE', *, *, #231044, .F. ) ;
#152045=AXIS2_PLACEMENT_3D ( 'NONE', #36601, #116111, #173558 ) ;
#152046=VERTEX_POINT ( 'NONE', #98105 ) ;
#152051=ORIENTED_EDGE ( 'NONE', *, *, #42764, .T. ) ;
#152059=ORIENTED_EDGE ( 'NONE', *, *, #221796, .T. ) ;
#152078=CARTESIAN_POINT ( 'NONE',  ( 21.30000000000002558, 76.00000000001216449, -140.5731074845242858 ) ) ;
#152083=CARTESIAN_POINT ( 'NONE',  ( 20.94999999999999929, 65.61821452928792553, -97.51526212064020172 ) ) ;
#152136=AXIS2_PLACEMENT_3D ( 'NONE', #115156, #177730, #113869 ) ;
#152137=EDGE_CURVE ( 'NONE', #7658, #3601, #178908, .T. ) ;
#152141=ORIENTED_EDGE ( 'NONE', *, *, #136340, .F. ) ;
#152156=LINE ( 'NONE', #53014, #247757 ) ;
#152166=CARTESIAN_POINT ( 'NONE',  ( 18.39999999999999858, 85.40000000001222702, -148.2731074845242460 ) ) ;
#152168=VERTEX_POINT ( 'NONE', #104524 ) ;
#152171=ADVANCED_FACE ( 'NONE', ( #184090 ), #62862, .T. ) ;
#152175=EDGE_CURVE ( 'NONE', #192091, #76825, #145530, .T. ) ;
#152179=VECTOR ( 'NONE', #187998, 1000.000000000000000 ) ;
#152196=FACE_OUTER_BOUND ( 'NONE', #101095, .T. ) ;
#152213=EDGE_LOOP ( 'NONE', ( #255001, #166095, #193945, #19853 ) ) ;
#152220=AXIS2_PLACEMENT_3D ( 'NONE', #158273, #197343, #123929 ) ;
#152260=FACE_OUTER_BOUND ( 'NONE', #246632, .T. ) ;
#152267=CYLINDRICAL_SURFACE ( 'NONE', #253980, 0.1000000000000028644 ) ;
#152271=CARTESIAN_POINT ( 'NONE',  ( -23.25000000000000000, 76.00000000001185185, -95.12310748452429721 ) ) ;
#152298=CIRCLE ( 'NONE', #110573, 4.100000000000006750 ) ;
#152330=ADVANCED_FACE ( 'NONE', ( #109679 ), #224637, .T. ) ;
#152340=DIRECTION ( 'NONE',  ( 0.000000000000000000, 1.000000000000000000, 0.000000000000000000 ) ) ;
#152358=DIRECTION ( 'NONE',  ( 3.265361837132813093E-16, 1.000000000000000000, 6.982962677686266711E-15 ) ) ;
#152391=ADVANCED_FACE ( 'NONE', ( #173573 ), #233511, .T. ) ;
#152488=ADVANCED_FACE ( 'NONE', ( #177401 ), #158234, .T. ) ;
#152516=CYLINDRICAL_SURFACE ( 'NONE', #187849, 0.09999999999999939493 ) ;
#152528=CIRCLE ( 'NONE', #40096, 0.09999999999999939493 ) ;
#152544=CARTESIAN_POINT ( 'NONE',  ( 18.52326479938722059, 85.64236444492735245, -96.30835007111858204 ) ) ;
#152574=VECTOR ( 'NONE', #191957, 1000.000000000000000 ) ;
#152597=CARTESIAN_POINT ( 'NONE',  ( -23.25000000000000000, 76.00000000001213607, -136.5231074845242745 ) ) ;
#152606=LINE ( 'NONE', #133022, #236937 ) ;
#152649=DIRECTION ( 'NONE',  ( 0.000000000000000000, 6.997203936713175802E-15, -1.000000000000000000 ) ) ;
#152651=AXIS2_PLACEMENT_3D ( 'NONE', #126523, #22311, #160541 ) ;
#152689=DIRECTION ( 'NONE',  ( -1.000000000000000000, -0.000000000000000000, -0.000000000000000000 ) ) ;
#152697=CARTESIAN_POINT ( 'NONE',  ( -20.85000000000000142, 69.06610602788553877, -99.23746165015076315 ) ) ;
#152704=CARTESIAN_POINT ( 'NONE',  ( 21.12642695952774119, 75.90109671682282055, -142.8987674065594717 ) ) ;
#152723=CARTESIAN_POINT ( 'NONE',  ( 21.05000000000000071, 65.57661458509919328, -129.0310555606542664 ) ) ;
#152732=PLANE ( 'NONE',  #156017 ) ;
#152734=CARTESIAN_POINT ( 'NONE',  ( -23.15000000000000213, 85.00000000001197975, -112.9170766071766820 ) ) ;
#152745=CIRCLE ( 'NONE', #111203, 7.791421356237338003 ) ;
#152762=VERTEX_POINT ( 'NONE', #254014 ) ;
#152798=ORIENTED_EDGE ( 'NONE', *, *, #79443, .T. ) ;
#152800=ORIENTED_EDGE ( 'NONE', *, *, #54959, .T. ) ;
#152821=ORIENTED_EDGE ( 'NONE', *, *, #111492, .F. ) ;
#152842=EDGE_LOOP ( 'NONE', ( #244479, #251058, #176523, #143785 ) ) ;
#152867=CARTESIAN_POINT ( 'NONE',  ( 20.95575313997065336, 65.38544669673724741, -128.9018167825795445 ) ) ;
#152868=CARTESIAN_POINT ( 'NONE',  ( -21.37071067811865532, 67.92928932189333580, -115.3731074845243540 ) ) ;
#152885=CIRCLE ( 'NONE', #173751, 0.2000000000000057288 ) ;
#152900=FACE_OUTER_BOUND ( 'NONE', #59372, .T. ) ;
#152912=EDGE_CURVE ( 'NONE', #199005, #47571, #43963, .T. ) ;
#152929=EDGE_LOOP ( 'NONE', ( #248111, #182194, #29991, #248755, #89680 ) ) ;
#152981=ORIENTED_EDGE ( 'NONE', *, *, #111678, .T. ) ;
#152987=CARTESIAN_POINT ( 'NONE',  ( -23.25000000000000000, 76.10085836911093793, -148.2726746080136877 ) ) ;
#153002=AXIS2_PLACEMENT_3D ( 'NONE', #51916, #132787, #12841 ) ;
#153014=( BOUNDED_SURFACE ( )  B_SPLINE_SURFACE ( 3, 2, ( 
 ( #161152, #201544, #141575 ),
 ( #119462, #22944, #79005 ),
 ( #157320, #80283, #158601 ),
 ( #122017, #238097, #17757 ),
 ( #102414, #196408, #239403 ),
 ( #180717, #138973, #2048 ) ),
 .UNSPECIFIED., .F., .F., .F. ) 
 B_SPLINE_SURFACE_WITH_KNOTS ( ( 4, 2, 4 ),
 ( 3, 3 ),
 ( 0.0001792624049599484879, 0.0003686986002124686881, 0.0005581347954649888612 ),
 ( 0.000000000000000000, 1.000000000000000000 ),
 .UNSPECIFIED. ) 
 GEOMETRIC_REPRESENTATION_ITEM ( )  RATIONAL_B_SPLINE_SURFACE ( (
 ( 1.000000000000000000, 0.9238795325112671986, 1.000000000000000000),
 ( 1.000000000000000000, 0.9229318695239959736, 1.000000000000000000),
 ( 1.000000000000000000, 0.8926288119229054407, 1.000000000000000000),
 ( 1.000000000000000000, 0.8123777807272675178, 1.000000000000000000),
 ( 1.000000000000000000, 0.7629087100930393994, 1.000000000000000000),
 ( 1.000000000000000000, 0.7071067811865352493, 1.000000000000000000) ) ) 
 REPRESENTATION_ITEM ( '' )  SURFACE ( )  );
#153016=CYLINDRICAL_SURFACE ( 'NONE', #142480, 0.09999999999998898659 ) ;
#153023=AXIS2_PLACEMENT_3D ( 'NONE', #216954, #473, #117864 ) ;
#153024=ORIENTED_EDGE ( 'NONE', *, *, #28237, .F. ) ;
#153050=ORIENTED_EDGE ( 'NONE', *, *, #95569, .F. ) ;
#153054=ORIENTED_EDGE ( 'NONE', *, *, #187207, .F. ) ;
#153072=ORIENTED_EDGE ( 'NONE', *, *, #132397, .T. ) ;
#153073=CIRCLE ( 'NONE', #223739, 0.1000000000000072220 ) ;
#153079=CIRCLE ( 'NONE', #169827, 1.899999999999999023 ) ;
#153114=CARTESIAN_POINT ( 'NONE',  ( -23.15000000000000213, 76.00000000001190870, -103.0231074845243029 ) ) ;
#153127=VERTEX_POINT ( 'NONE', #172943 ) ;
#153145=VERTEX_POINT ( 'NONE', #237993 ) ;
#153150=ORIENTED_EDGE ( 'NONE', *, *, #105378, .T. ) ;
#153193=AXIS2_PLACEMENT_3D ( 'NONE', #212540, #230823, #251646 ) ;
#153200=CARTESIAN_POINT ( 'NONE',  ( 18.59999999999997655, 76.00000000001185185, -95.12310748452429721 ) ) ;
#153220=EDGE_LOOP ( 'NONE', ( #55252, #96039, #151271, #207037, #202715 ) ) ;
#153250=ORIENTED_EDGE ( 'NONE', *, *, #192850, .F. ) ;
#153251=DIRECTION ( 'NONE',  ( 1.000000000000000000, 0.000000000000000000, 0.000000000000000000 ) ) ;
#153253=AXIS2_PLACEMENT_3D ( 'NONE', #234192, #236760, #254984 ) ;
#153282=DIRECTION ( 'NONE',  ( -0.000000000000000000, -6.982962677686266711E-15, 1.000000000000000000 ) ) ;
#153326=EDGE_CURVE ( 'NONE', #155807, #148843, #56461, .T. ) ;
#153337=DIRECTION ( 'NONE',  ( 0.000000000000000000, 6.982962677686266711E-15, -1.000000000000000000 ) ) ;
#153356=CARTESIAN_POINT ( 'NONE',  ( 20.85000000000000142, 76.00000000001185185, -95.12310748452429721 ) ) ;
#153385=ORIENTED_EDGE ( 'NONE', *, *, #211791, .T. ) ;
#153389=CIRCLE ( 'NONE', #157478, 0.2000000000000057288 ) ;
#153408=EDGE_LOOP ( 'NONE', ( #254362, #57230, #69863, #164750, #190340 ) ) ;
#153483=TOROIDAL_SURFACE ( 'NONE', #240923, 11.70000000000000462, 0.1000000000000000056 ) ;
#153497=FACE_OUTER_BOUND ( 'NONE', #173866, .T. ) ;
#153513=CARTESIAN_POINT ( 'NONE',  ( 0.000000000000000000, 0.000000000000000000, 0.000000000000000000 ) ) ;
#153516=ORIENTED_EDGE ( 'NONE', *, *, #21908, .T. ) ;
#153553=EDGE_CURVE ( 'NONE', #56965, #47601, #121193, .T. ) ;
#153565=FACE_OUTER_BOUND ( 'NONE', #245008, .T. ) ;
#153580=CYLINDRICAL_SURFACE ( 'NONE', #8802, 0.09999999999999867328 ) ;
#153584=CIRCLE ( 'NONE', #45188, 11.70000000000000284 ) ;
#153610=CARTESIAN_POINT ( 'NONE',  ( 20.94999999999999929, 76.00000000001189449, -101.1231074845242972 ) ) ;
#153614=CARTESIAN_POINT ( 'NONE',  ( -18.59999999999999787, 72.08710075277861051, -125.0412845115133678 ) ) ;
#153635=CARTESIAN_POINT ( 'NONE',  ( -20.85000000000000142, 64.25000000001190870, -103.0231074845243882 ) ) ;
#153638=SURFACE_STYLE_FILL_AREA ( #206175 ) ;
#153656=VERTEX_POINT ( 'NONE', #123870 ) ;
#153673=CYLINDRICAL_SURFACE ( 'NONE', #189646, 11.80000000000000426 ) ;
#153745=AXIS2_PLACEMENT_3D ( 'NONE', #246534, #148741, #228275 ) ;
#153769=DIRECTION ( 'NONE',  ( 0.000000000000000000, 0.000000000000000000, 1.000000000000000000 ) ) ;
#153778=AXIS2_PLACEMENT_3D ( 'NONE', #40943, #199996, #21374 ) ;
#153784=DIRECTION ( 'NONE',  ( 0.000000000000000000, -1.000000000000000000, -6.982962677686265922E-15 ) ) ;
#153790=VERTEX_POINT ( 'NONE', #204658 ) ;
#153795=DIRECTION ( 'NONE',  ( -0.000000000000000000, -0.1298341882519953583, -0.9915357197604862671 ) ) ;
#153818=DIRECTION ( 'NONE',  ( 1.000000000000000000, -2.952720810173289112E-16, -2.061873921506763405E-30 ) ) ;
#153824=ORIENTED_EDGE ( 'NONE', *, *, #211331, .T. ) ;
#153827=TOROIDAL_SURFACE ( 'NONE', #195316, 12.97499999999999609, 0.1000000000000000056 ) ;
#153839=LINE ( 'NONE', #55940, #252738 ) ;
#153858=( BOUNDED_SURFACE ( )  B_SPLINE_SURFACE ( 3, 2, ( 
 ( #199793, #180221, #21164 ),
 ( #61548, #103213, #197193 ),
 ( #101920, #138480, #122817 ),
 ( #62824, #1553, #43269 ) ),
 .UNSPECIFIED., .F., .F., .F. ) 
 B_SPLINE_SURFACE_WITH_KNOTS ( ( 4, 4 ),
 ( 3, 3 ),
 ( 3.239053990300444497E-18, 0.0003124336600439674345 ),
 ( 0.000000000000000000, 1.000000000000000000 ),
 .UNSPECIFIED. ) 
 GEOMETRIC_REPRESENTATION_ITEM ( )  RATIONAL_B_SPLINE_SURFACE ( (
 ( 1.000000000000000000, 0.7071067811865475727, 1.000000000000000000),
 ( 1.000000000000000000, 0.7089187706049921989, 1.000000000000000000),
 ( 1.000000000000000000, 0.7039288185051796320, 1.000000000000000000),
 ( 1.000000000000000000, 0.7040654476015839602, 1.000000000000000000) ) ) 
 REPRESENTATION_ITEM ( '' )  SURFACE ( )  );
#153874=EDGE_CURVE ( 'NONE', #2636, #246153, #33903, .T. ) ;
#153892=VERTEX_POINT ( 'NONE', #229388 ) ;
#153900=VERTEX_POINT ( 'NONE', #50705 ) ;
#153908=LINE ( 'NONE', #151304, #175286 ) ;
#153935=DIRECTION ( 'NONE',  ( 1.000000000000000000, 0.000000000000000000, 0.000000000000000000 ) ) ;
#153974=CARTESIAN_POINT ( 'NONE',  ( 18.52928932188133970, 65.72071067813064360, -115.1731074845243796 ) ) ;
#153980=AXIS2_PLACEMENT_3D ( 'NONE', #35858, #95789, #175381 ) ;
#153994=CIRCLE ( 'NONE', #257933, 0.09999999999999939493 ) ;
#153996=CIRCLE ( 'NONE', #58241, 0.09999999999998898659 ) ;
#154018=VERTEX_POINT ( 'NONE', #97527 ) ;
#154082=CARTESIAN_POINT ( 'NONE',  ( 20.94999999999999574, 87.48912529308817909, -133.4231074845242233 ) ) ;
#154109=ADVANCED_FACE ( 'NONE', ( #163963 ), #146936, .F. ) ;
#154114=ORIENTED_EDGE ( 'NONE', *, *, #251411, .F. ) ;
#154138=CARTESIAN_POINT ( 'NONE',  ( -23.25000000000000000, 84.59626168225506149, -127.0729799673739677 ) ) ;
#154170=AXIS2_PLACEMENT_3D ( 'NONE', #250711, #189471, #249452 ) ;
#154202=EDGE_CURVE ( 'NONE', #207317, #148869, #17456, .T. ) ;
#154244=CARTESIAN_POINT ( 'NONE',  ( 22.39999999999999503, 64.35000000001213039, -136.6231074845243825 ) ) ;
#154246=CARTESIAN_POINT ( 'NONE',  ( 20.94999999999999574, 76.00000000001213607, -136.5231074845242745 ) ) ;
#154270=CARTESIAN_POINT ( 'NONE',  ( -23.15000000000000213, 85.00000000001197975, -112.4170766071766678 ) ) ;
#154304=VERTEX_POINT ( 'NONE', #215890 ) ;
#154328=CIRCLE ( 'NONE', #132, 0.1999999999999987899 ) ;
#154340=CIRCLE ( 'NONE', #54308, 0.09999999999999520384 ) ;
#154341=ORIENTED_EDGE ( 'NONE', *, *, #22995, .F. ) ;
#154350=AXIS2_PLACEMENT_3D ( 'NONE', #31722, #190795, #91660 ) ;
#154371=CARTESIAN_POINT ( 'NONE',  ( -23.25000000000000000, 87.75000000001192291, -106.1231074845242262 ) ) ;
#154373=DIRECTION ( 'NONE',  ( 0.000000000000000000, 0.000000000000000000, 1.000000000000000000 ) ) ;
#154405=AXIS2_PLACEMENT_3D ( 'NONE', #251653, #117284, #75611 ) ;
#154418=CARTESIAN_POINT ( 'NONE',  ( -21.05000000000000071, 74.83729825007408465, -128.4231074845243086 ) ) ;
#154419=DIRECTION ( 'NONE',  ( 0.000000000000000000, 0.000000000000000000, 1.000000000000000000 ) ) ;
#154423=EDGE_CURVE ( 'NONE', #105294, #110925, #117609, .T. ) ;
#154428=VERTEX_POINT ( 'NONE', #74726 ) ;
#154441=ORIENTED_EDGE ( 'NONE', *, *, #2888, .T. ) ;
#154466=VERTEX_POINT ( 'NONE', #154270 ) ;
#154467=CIRCLE ( 'NONE', #79404, 0.09999999999999939493 ) ;
#154486=DIRECTION ( 'NONE',  ( 0.000000000000000000, 0.000000000000000000, -1.000000000000000000 ) ) ;
#154504=EDGE_CURVE ( 'NONE', #8134, #114896, #79969, .T. ) ;
#154521=VECTOR ( 'NONE', #42581, 1000.000000000000000 ) ;
#154532=DIRECTION ( 'NONE',  ( 0.000000000000000000, 7.147358527629759053E-15, -1.000000000000000000 ) ) ;
#154544=DIRECTION ( 'NONE',  ( 0.000000000000000000, -8.338584948901395817E-15, 1.000000000000000000 ) ) ;
#154545=DIRECTION ( 'NONE',  ( 0.000000000000000000, -0.8660254037844445918, -0.4999999999999897304 ) ) ;
#154563=DIRECTION ( 'NONE',  ( -1.000000000000000000, -0.000000000000000000, -0.000000000000000000 ) ) ;
#154573=DIRECTION ( 'NONE',  ( -1.000000000000000000, 0.000000000000000000, 0.000000000000000000 ) ) ;
#154582=CIRCLE ( 'NONE', #216891, 0.1000000000000028644 ) ;
#154603=VERTEX_POINT ( 'NONE', #129792 ) ;
#154615=CIRCLE ( 'NONE', #12573, 0.09999999999999939493 ) ;
#154637=ORIENTED_EDGE ( 'NONE', *, *, #141510, .T. ) ;
#154642=ORIENTED_EDGE ( 'NONE', *, *, #128011, .T. ) ;
#154643=DIRECTION ( 'NONE',  ( 1.000000000000000000, -1.875376730785737719E-16, -1.309568571767809260E-30 ) ) ;
#154660=EDGE_LOOP ( 'NONE', ( #93232, #86579, #91589, #155083 ) ) ;
#154663=CIRCLE ( 'NONE', #42209, 0.09999999999998898659 ) ;
#154679=VECTOR ( 'NONE', #117985, 1000.000000000000000 ) ;
#154691=ORIENTED_EDGE ( 'NONE', *, *, #99609, .F. ) ;
#154702=EDGE_CURVE ( 'NONE', #1482, #125207, #7272, .T. ) ;
#154719=ORIENTED_EDGE ( 'NONE', *, *, #75800, .T. ) ;
#154749=AXIS2_PLACEMENT_3D ( 'NONE', #88737, #249143, #169634 ) ;
#154765=EDGE_CURVE ( 'NONE', #71756, #208687, #154663, .T. ) ;
#154780=DIRECTION ( 'NONE',  ( 0.000000000000000000, 6.982962677686266711E-15, -1.000000000000000000 ) ) ;
#154799=DIRECTION ( 'NONE',  ( 1.000000000000000000, 0.000000000000000000, 0.000000000000000000 ) ) ;
#154802=EDGE_CURVE ( 'NONE', #110925, #207616, #28117, .T. ) ;
#154810=CARTESIAN_POINT ( 'NONE',  ( 20.94999999999999574, 77.83534155023646406, -124.9679561919613064 ) ) ;
#154834=ORIENTED_EDGE ( 'NONE', *, *, #28388, .F. ) ;
#154846=ORIENTED_EDGE ( 'NONE', *, *, #145336, .F. ) ;
#154860=VECTOR ( 'NONE', #104753, 1000.000000000000000 ) ;
#154903=FACE_OUTER_BOUND ( 'NONE', #67235, .T. ) ;
#154906=EDGE_CURVE ( 'NONE', #242104, #148843, #46281, .T. ) ;
#154924=DIRECTION ( 'NONE',  ( 0.000000000000000000, -7.056502275159890832E-15, 1.000000000000000000 ) ) ;
#154962=VERTEX_POINT ( 'NONE', #65659 ) ;
#154966=CARTESIAN_POINT ( 'NONE',  ( -20.54999999999999716, 85.00000000001197975, -112.9170766071766820 ) ) ;
#154982=DIRECTION ( 'NONE',  ( -0.000000000000000000, -6.982962677686266711E-15, 1.000000000000000000 ) ) ;
#154985=ORIENTED_EDGE ( 'NONE', *, *, #57035, .F. ) ;
#154992=DIRECTION ( 'NONE',  ( 1.000000000000000000, 0.000000000000000000, 0.000000000000000000 ) ) ;
#155004=B_SPLINE_CURVE_WITH_KNOTS ( 'NONE', 3,
 ( #113745, #15974, #109887, #172498, #10808, #228579, #52476, #69515 ),
 .UNSPECIFIED., .F., .F.,
 ( 4, 2, 2, 4 ),
 ( 0.000000000000000000, 6.534141206309662642E-05, 0.0001306828241261932528, 0.0002613656482524241275 ),
 .UNSPECIFIED. ) ;
#155009=TOROIDAL_SURFACE ( 'NONE', #130006, 12.77500000000000036, 0.1000000000000000056 ) ;
#155013=ORIENTED_EDGE ( 'NONE', *, *, #229771, .F. ) ;
#155034=EDGE_CURVE ( 'NONE', #205485, #255544, #236289, .T. ) ;
#155039=DIRECTION ( 'NONE',  ( -1.000000000000000000, 0.000000000000000000, -0.000000000000000000 ) ) ;
#155044=ORIENTED_EDGE ( 'NONE', *, *, #80581, .F. ) ;
#155083=ORIENTED_EDGE ( 'NONE', *, *, #78011, .F. ) ;
#155144=ORIENTED_EDGE ( 'NONE', *, *, #71112, .F. ) ;
#155169=DIRECTION ( 'NONE',  ( 0.000000000000000000, 0.000000000000000000, 1.000000000000000000 ) ) ;
#155192=EDGE_LOOP ( 'NONE', ( #106524, #170145, #127330, #6233 ) ) ;
#155198=VECTOR ( 'NONE', #254166, 999.9999999999998863 ) ;
#155209=CARTESIAN_POINT ( 'NONE',  ( 23.14999999999998437, 76.00000000001213607, -136.5231074845242745 ) ) ;
#155247=AXIS2_PLACEMENT_3D ( 'NONE', #111267, #112558, #168719 ) ;
#155248=ADVANCED_FACE ( 'NONE', ( #79758 ), #121512, .T. ) ;
#155283=VERTEX_POINT ( 'NONE', #88753 ) ;
#155304=ORIENTED_EDGE ( 'NONE', *, *, #17060, .F. ) ;
#155392=EDGE_CURVE ( 'NONE', #154603, #106161, #246553, .T. ) ;
#155420=ORIENTED_EDGE ( 'NONE', *, *, #136196, .T. ) ;
#155438=VERTEX_POINT ( 'NONE', #74390 ) ;
#155439=DIRECTION ( 'NONE',  ( 0.000000000000000000, -7.429790795770644761E-15, 1.000000000000000000 ) ) ;
#155464=EDGE_LOOP ( 'NONE', ( #109602, #142160, #76132, #120705 ) ) ;
#155466=( NAMED_UNIT ( * ) PLANE_ANGLE_UNIT ( ) SI_UNIT ( $, .RADIAN. ) );
#155470=VERTEX_POINT ( 'NONE', #193026 ) ;
#155515=CARTESIAN_POINT ( 'NONE',  ( 21.05000000000000071, 64.40000000001194280, -109.9513107147998880 ) ) ;
#155520=DIRECTION ( 'NONE',  ( 2.879366945564059217E-14, 0.9875055080513762684, -0.1575844902526679081 ) ) ;
#155540=CARTESIAN_POINT ( 'NONE',  ( -21.93340585900934414, 76.00000000001219291, -143.8472545066296391 ) ) ;
#155547=DIRECTION ( 'NONE',  ( 0.000000000000000000, -1.000000000000000000, 0.000000000000000000 ) ) ;
#155554=CARTESIAN_POINT ( 'NONE',  ( 21.07094088545303734, 69.67983277809565834, -136.6220011870765632 ) ) ;
#155583=DIRECTION ( 'NONE',  ( 0.000000000000000000, -6.982962677686266711E-15, 1.000000000000000000 ) ) ;
#155600=SPHERICAL_SURFACE ( 'NONE', #1531, 0.1000000000000000056 ) ;
#155637=FACE_OUTER_BOUND ( 'NONE', #250373, .T. ) ;
#155650=AXIS2_PLACEMENT_3D ( 'NONE', #220679, #100686, #184105 ) ;
#155672=CARTESIAN_POINT ( 'NONE',  ( -23.25000000000000000, 74.08971962618026907, -123.8917396293253717 ) ) ;
#155702=DIRECTION ( 'NONE',  ( 0.000000000000000000, 0.000000000000000000, 1.000000000000000000 ) ) ;
#155713=EDGE_LOOP ( 'NONE', ( #244982, #223835, #180387, #54844 ) ) ;
#155807=VERTEX_POINT ( 'NONE', #214825 ) ;
#155828=CARTESIAN_POINT ( 'NONE',  ( 18.49999999999999289, 65.70729864261004138, -97.56574559737244101 ) ) ;
#155839=CARTESIAN_POINT ( 'NONE',  ( -18.59999999999999787, 74.16465844978765176, -124.9679561919613207 ) ) ;
#155848=VERTEX_POINT ( 'NONE', #153635 ) ;
#155864=VECTOR ( 'NONE', #159385, 1000.000000000000000 ) ;
#155939=AXIS2_PLACEMENT_3D ( 'NONE', #121778, #4364, #240423 ) ;
#155941=VERTEX_POINT ( 'NONE', #80416 ) ;
#155943=CARTESIAN_POINT ( 'NONE',  ( 18.59999999999999076, 74.75000000001206502, -128.5231074845243029 ) ) ;
#155989=VERTEX_POINT ( 'NONE', #98693 ) ;
#156013=EDGE_CURVE ( 'NONE', #197068, #230546, #184209, .T. ) ;
#156014=ORIENTED_EDGE ( 'NONE', *, *, #164606, .T. ) ;
#156017=AXIS2_PLACEMENT_3D ( 'NONE', #191860, #92710, #11927 ) ;
#156026=LINE ( 'NONE', #213393, #41463 ) ;
#156036=CARTESIAN_POINT ( 'NONE',  ( -21.33487959338958362, 69.27444184810096317, -136.5231074845243313 ) ) ;
#156045=CARTESIAN_POINT ( 'NONE',  ( -23.15000000000000213, 87.75000000001192291, -106.1231074845242262 ) ) ;
#156085=DIRECTION ( 'NONE',  ( -1.000000000000000000, 0.000000000000000000, -0.000000000000000000 ) ) ;
#156115=DIRECTION ( 'NONE',  ( -1.000000000000000000, 0.000000000000000000, -0.000000000000000000 ) ) ;
#156155=ORIENTED_EDGE ( 'NONE', *, *, #20520, .T. ) ;
#156187=CARTESIAN_POINT ( 'NONE',  ( 23.24999999999999289, 69.35000000001200249, -115.3731074845243398 ) ) ;
#156198=CARTESIAN_POINT ( 'NONE',  ( 20.95512820512820440, 65.37615131630018084, -124.3731074845243825 ) ) ;
#156206=CARTESIAN_POINT ( 'NONE',  ( -22.59999999999999787, 75.89914163091351895, -148.2726746080136877 ) ) ;
#156229=ORIENTED_EDGE ( 'NONE', *, *, #18461, .T. ) ;
#156235=CARTESIAN_POINT ( 'NONE',  ( 21.06277459767465032, 67.12713756174342450, -124.3191082921676980 ) ) ;
#156258=VECTOR ( 'NONE', #240349, 1000.000000000000000 ) ;
#156265=AXIS2_PLACEMENT_3D ( 'NONE', #47812, #227748, #127378 ) ;
#156274=VERTEX_POINT ( 'NONE', #176390 ) ;
#156277=CARTESIAN_POINT ( 'NONE',  ( -22.48970261584618058, 64.35000000001214460, -136.5784769727417824 ) ) ;
#156286=ADVANCED_FACE ( 'NONE', ( #129841 ), #110280, .F. ) ;
#156299=DIRECTION ( 'NONE',  ( 1.000000000000000000, 0.000000000000000000, 0.000000000000000000 ) ) ;
#156301=CARTESIAN_POINT ( 'NONE',  ( -20.64999999999999858, 76.00000000001205080, -123.5481074845242802 ) ) ;
#156304=CIRCLE ( 'NONE', #43841, 0.1000000000000028644 ) ;
#156311=VERTEX_POINT ( 'NONE', #249808 ) ;
#156315=ORIENTED_EDGE ( 'NONE', *, *, #193568, .T. ) ;
#156316=CARTESIAN_POINT ( 'NONE',  ( -21.05000000000000071, 87.29603075034721371, -106.0710066441880883 ) ) ;
#156330=ORIENTED_EDGE ( 'NONE', *, *, #194990, .T. ) ;
#156357=EDGE_CURVE ( 'NONE', #76270, #185168, #43281, .T. ) ;
#156363=VERTEX_POINT ( 'NONE', #83642 ) ;
#156390=DIRECTION ( 'NONE',  ( 0.000000000000000000, -7.272083257015735086E-15, 1.000000000000000000 ) ) ;
#156394=CARTESIAN_POINT ( 'NONE',  ( 18.43466021071412797, 85.49419069046841457, -96.40604592439639475 ) ) ;
#156427=VERTEX_POINT ( 'NONE', #206201 ) ;
#156477=DIRECTION ( 'NONE',  ( 0.000000000000000000, 0.000000000000000000, 1.000000000000000000 ) ) ;
#156487=CYLINDRICAL_SURFACE ( 'NONE', #165548, 0.1000000000000106914 ) ;
#156506=ORIENTED_EDGE ( 'NONE', *, *, #116425, .F. ) ;
#156542=CARTESIAN_POINT ( 'NONE',  ( -20.00857864376270001, 66.65000000001205649, -124.1731074845243654 ) ) ;
#156557=DIRECTION ( 'NONE',  ( 0.000000000000000000, 6.982962677686266711E-15, -1.000000000000000000 ) ) ;
#156560=CARTESIAN_POINT ( 'NONE',  ( -20.85000000000000142, 87.75000000001190870, -103.0231074845242176 ) ) ;
#156582=FACE_OUTER_BOUND ( 'NONE', #123158, .T. ) ;
#156584=CARTESIAN_POINT ( 'NONE',  ( 20.94999999999999929, 87.39257802171759693, -106.0970570643561501 ) ) ;
#156631=ORIENTED_EDGE ( 'NONE', *, *, #254488, .F. ) ;
#156637=ORIENTED_EDGE ( 'NONE', *, *, #176789, .T. ) ;
#156654=ORIENTED_EDGE ( 'NONE', *, *, #217708, .T. ) ;
#156665=FACE_OUTER_BOUND ( 'NONE', #38750, .T. ) ;
#156678=DIRECTION ( 'NONE',  ( 0.7071067811865474617, -0.7071067811865474617, -4.937700262164531476E-15 ) ) ;
#156687=SPHERICAL_SURFACE ( 'NONE', #140923, 0.1000000000000000056 ) ;
#156713=DIRECTION ( 'NONE',  ( 0.000000000000000000, 0.9893560106964510714, -0.1455152366551481502 ) ) ;
#156761=DIRECTION ( 'NONE',  ( 0.000000000000000000, 0.000000000000000000, -1.000000000000000000 ) ) ;
#156839=DIRECTION ( 'NONE',  ( 1.000000000000000000, 0.000000000000000000, 0.000000000000000000 ) ) ;
#156843=AXIS2_PLACEMENT_3D ( 'NONE', #167839, #148242, #227776 ) ;
#156851=VERTEX_POINT ( 'NONE', #128934 ) ;
#156852=AXIS2_PLACEMENT_3D ( 'NONE', #162427, #21624, #167260 ) ;
#156871=ADVANCED_FACE ( 'NONE', ( #89781 ), #246307, .T. ) ;
#156876=CARTESIAN_POINT ( 'NONE',  ( 20.85000000000000142, 77.83585931145546510, -91.41866831572575336 ) ) ;
#156893=CARTESIAN_POINT ( 'NONE',  ( 21.04386569057533762, 64.25000000001236344, -109.8802701327437319 ) ) ;
#156925=CARTESIAN_POINT ( 'NONE',  ( 21.05000000000000071, 71.00000000001199396, -115.4283735034374274 ) ) ;
#156937=EDGE_CURVE ( 'NONE', #54007, #247013, #243500, .T. ) ;
#156957=AXIS2_PLACEMENT_3D ( 'NONE', #62813, #223159, #163212 ) ;
#156992=EDGE_LOOP ( 'NONE', ( #193224, #16332, #227990, #246082 ) ) ;
#157058=DIRECTION ( 'NONE',  ( 0.000000000000000000, 0.000000000000000000, 1.000000000000000000 ) ) ;
#157093=CARTESIAN_POINT ( 'NONE',  ( -23.25000000000000000, 76.00000000001213607, -136.5231074845242745 ) ) ;
#157105=EDGE_CURVE ( 'NONE', #54263, #24859, #197882, .T. ) ;
#157153=EDGE_CURVE ( 'NONE', #47571, #89242, #100029, .T. ) ;
#157164=EDGE_LOOP ( 'NONE', ( #88646, #240006, #85276 ) ) ;
#157174=EDGE_CURVE ( 'NONE', #31427, #195402, #31350, .T. ) ;
#157182=AXIS2_PLACEMENT_3D ( 'NONE', #66586, #32625, #10462 ) ;
#157187=VECTOR ( 'NONE', #62057, 1000.000000000000000 ) ;
#157191=ORIENTED_EDGE ( 'NONE', *, *, #18065, .F. ) ;
#157199=AXIS2_PLACEMENT_3D ( 'NONE', #233412, #213822, #215106 ) ;
#157201=EDGE_LOOP ( 'NONE', ( #146060, #235185, #29097, #13022 ) ) ;
#157205=EDGE_LOOP ( 'NONE', ( #102053, #71349, #95503, #142916, #133948 ) ) ;
#157268=ORIENTED_EDGE ( 'NONE', *, *, #164199, .F. ) ;
#157295=ORIENTED_EDGE ( 'NONE', *, *, #187082, .T. ) ;
#157307=DIRECTION ( 'NONE',  ( -0.000000000000000000, 7.272083257015735086E-15, -1.000000000000000000 ) ) ;
#157320=CARTESIAN_POINT ( 'NONE',  ( -21.09096482362049940, 75.96055172123797661, -142.8866518499284268 ) ) ;
#157327=ORIENTED_EDGE ( 'NONE', *, *, #124347, .F. ) ;
#157331=CARTESIAN_POINT ( 'NONE',  ( 21.98333005346336222, 76.00000000001219291, -143.8971828135809687 ) ) ;
#157341=EDGE_CURVE ( 'NONE', #154304, #30941, #148606, .T. ) ;
#157358=CARTESIAN_POINT ( 'NONE',  ( -20.64999999999999858, 76.00000000001192291, -105.0231074845243029 ) ) ;
#157384=CARTESIAN_POINT ( 'NONE',  ( 21.05000000000000071, 76.00000000001190870, -103.0231074845243029 ) ) ;
#157410=FACE_OUTER_BOUND ( 'NONE', #141110, .T. ) ;
#157426=CARTESIAN_POINT ( 'NONE',  ( 20.94999999999999929, 68.97833521811179480, -99.18954208262705663 ) ) ;
#157428=ORIENTED_EDGE ( 'NONE', *, *, #13416, .F. ) ;
#157437=ORIENTED_EDGE ( 'NONE', *, *, #188029, .F. ) ;
#157451=DIRECTION ( 'NONE',  ( -0.7071067811865389130, -5.024295867788141276E-15, 0.7071067811865561215 ) ) ;
#157457=VECTOR ( 'NONE', #36330, 1000.000000000000000 ) ;
#157478=AXIS2_PLACEMENT_3D ( 'NONE', #254194, #157733, #135531 ) ;
#157509=ORIENTED_EDGE ( 'NONE', *, *, #56454, .F. ) ;
#157533=CARTESIAN_POINT ( 'NONE',  ( -22.39999999999999503, 68.20922040163873135, -136.6231074845243540 ) ) ;
#157536=DIRECTION ( 'NONE',  ( 0.000000000000000000, -0.4999999999999689138, -0.8660254037844565822 ) ) ;
#157549=ORIENTED_EDGE ( 'NONE', *, *, #156937, .T. ) ;
#157579=VERTEX_POINT ( 'NONE', #100983 ) ;
#157581=CARTESIAN_POINT ( 'NONE',  ( -20.64999999999999858, 74.05981308412420105, -123.6939882734709926 ) ) ;
#157582=FACE_OUTER_BOUND ( 'NONE', #38550, .T. ) ;
#157587=CIRCLE ( 'NONE', #211729, 11.65000000000000746 ) ;
#157603=ORIENTED_EDGE ( 'NONE', *, *, #231786, .T. ) ;
#157625=CARTESIAN_POINT ( 'NONE',  ( -20.54999999999999716, 76.00000000001190870, -103.0231074845243029 ) ) ;
#157675=ADVANCED_FACE ( 'NONE', ( #43639 ), #22813, .T. ) ;
#157686=PLANE ( 'NONE',  #13664 ) ;
#157692=DIRECTION ( 'NONE',  ( 0.000000000000000000, -6.982962677686266711E-15, 1.000000000000000000 ) ) ;
#157695=TOROIDAL_SURFACE ( 'NONE', #182606, 1.900000000000002576, 0.1000000000000000056 ) ;
#157733=DIRECTION ( 'NONE',  ( -1.000000000000000000, 3.265361837132813093E-16, 2.280189983783949500E-30 ) ) ;
#157754=ORIENTED_EDGE ( 'NONE', *, *, #29664, .T. ) ;
#157766=DIRECTION ( 'NONE',  ( -4.391705002472927119E-16, -1.000000000000000000, -7.026728003956683390E-15 ) ) ;
#157771=CIRCLE ( 'NONE', #249304, 0.09999999999999799327 ) ;
#157776=EDGE_CURVE ( 'NONE', #34583, #16075, #110193, .T. ) ;
#157787=ORIENTED_EDGE ( 'NONE', *, *, #243413, .T. ) ;
#157801=DIRECTION ( 'NONE',  ( 0.000000000000000000, 0.000000000000000000, -1.000000000000000000 ) ) ;
#157812=DIRECTION ( 'NONE',  ( 1.000000000000000000, 0.000000000000000000, 0.000000000000000000 ) ) ;
#157843=CARTESIAN_POINT ( 'NONE',  ( 21.14999999999999858, 69.45000000001205365, -124.3731074845243540 ) ) ;
#157848=CARTESIAN_POINT ( 'NONE',  ( 21.17356465864818915, 75.90108875899831276, -142.9459106107659920 ) ) ;
#157851=CARTESIAN_POINT ( 'NONE',  ( -20.85000000000000142, 68.97833521811179480, -99.18954208262705663 ) ) ;
#157862=AXIS2_PLACEMENT_3D ( 'NONE', #14465, #109671, #191826 ) ;
#157866=CARTESIAN_POINT ( 'NONE',  ( 23.14999999999999503, 64.25000000001205080, -124.3731074845243825 ) ) ;
#157872=DIRECTION ( 'NONE',  ( 0.000000000000000000, -6.982962677686266711E-15, 1.000000000000000000 ) ) ;
#157877=DIRECTION ( 'NONE',  ( -2.827886303505248766E-16, -0.8660254037844377084, -0.5000000000000015543 ) ) ;
#157880=VERTEX_POINT ( 'NONE', #93033 ) ;
#157892=EDGE_CURVE ( 'NONE', #145138, #93015, #114673, .T. ) ;
#157895=CIRCLE ( 'NONE', #74500, 11.80000000000000426 ) ;
#157920=LINE ( 'NONE', #118759, #13733 ) ;
#157942=VERTEX_POINT ( 'NONE', #247812 ) ;
#157945=CARTESIAN_POINT ( 'NONE',  ( 20.94999999999999574, 74.16465844978765176, -124.9679561919613207 ) ) ;
#157956=EDGE_LOOP ( 'NONE', ( #102346, #75354, #141356, #158204 ) ) ;
#157976=TOROIDAL_SURFACE ( 'NONE', #91306, 11.65000000000000036, 0.1000000000000000056 ) ;
#158011=CYLINDRICAL_SURFACE ( 'NONE', #53709, 7.900000000000003908 ) ;
#158022=CARTESIAN_POINT ( 'NONE',  ( 22.46250603428203618, 75.97885582387343106, -148.1729705818643765 ) ) ;
#158036=DIRECTION ( 'NONE',  ( -1.000000000000000000, 0.000000000000000000, -0.000000000000000000 ) ) ;
#158063=CARTESIAN_POINT ( 'NONE',  ( 21.05000000000000071, 76.00000000001190870, -103.0231074845243029 ) ) ;
#158088=CARTESIAN_POINT ( 'NONE',  ( -18.50000972452446035, 65.70673848566977426, -97.56382523348287350 ) ) ;
#158096=DIRECTION ( 'NONE',  ( 1.000000000000000000, 0.000000000000000000, 0.000000000000000000 ) ) ;
#158108=DIRECTION ( 'NONE',  ( 1.000000000000000000, -0.000000000000000000, 0.000000000000000000 ) ) ;
#158128=EDGE_LOOP ( 'NONE', ( #233865, #236477, #235405, #51442 ) ) ;
#158156=ORIENTED_EDGE ( 'NONE', *, *, #214175, .F. ) ;
#158173=CARTESIAN_POINT ( 'NONE',  ( -20.54999999999999716, 66.65000000001198543, -115.2731074845243597 ) ) ;
#158204=ORIENTED_EDGE ( 'NONE', *, *, #189286, .F. ) ;
#158234=TOROIDAL_SURFACE ( 'NONE', #245687, 0.2000000000000000111, 0.1000000000000000056 ) ;
#158251=ORIENTED_EDGE ( 'NONE', *, *, #13130, .T. ) ;
#158259=CIRCLE ( 'NONE', #24969, 0.09999999999998898659 ) ;
#158268=EDGE_LOOP ( 'NONE', ( #175235, #195000, #188581, #80648 ) ) ;
#158269=CARTESIAN_POINT ( 'NONE',  ( 20.12500000000000000, 66.25000000001199396, -115.2731074845243597 ) ) ;
#158273=CARTESIAN_POINT ( 'NONE',  ( -21.05000000000000071, 76.00000000001213607, -136.5231074845242745 ) ) ;
#158277=DIRECTION ( 'NONE',  ( 0.000000000000000000, -1.000000000000000000, -6.982962677686265922E-15 ) ) ;
#158284=ORIENTED_EDGE ( 'NONE', *, *, #68900, .F. ) ;
#158338=ORIENTED_EDGE ( 'NONE', *, *, #231044, .T. ) ;
#158343=DIRECTION ( 'NONE',  ( -0.000000000000000000, -6.982962677686266711E-15, 1.000000000000000000 ) ) ;
#158373=VECTOR ( 'NONE', #38665, 999.9999999999998863 ) ;
#158389=ORIENTED_EDGE ( 'NONE', *, *, #125864, .T. ) ;
#158396=DIRECTION ( 'NONE',  ( 0.000000000000000000, 0.000000000000000000, 1.000000000000000000 ) ) ;
#158409=CIRCLE ( 'NONE', #58386, 0.09999999999999939493 ) ;
#158449=DIRECTION ( 'NONE',  ( 0.000000000000000000, -6.982962677686266711E-15, 1.000000000000000000 ) ) ;
#158476=CYLINDRICAL_SURFACE ( 'NONE', #101442, 0.1000000000000046685 ) ;
#158489=ORIENTED_EDGE ( 'NONE', *, *, #6508, .F. ) ;
#158504=VERTEX_POINT ( 'NONE', #187761 ) ;
#158550=CIRCLE ( 'NONE', #121155, 0.09999999999999520384 ) ;
#158601=CARTESIAN_POINT ( 'NONE',  ( -21.05000000000000071, 76.02110330807134631, -142.8276238137879091 ) ) ;
#158657=ORIENTED_EDGE ( 'NONE', *, *, #60927, .F. ) ;
#158680=DIRECTION ( 'NONE',  ( -0.000000000000000000, -1.000000000000000000, -6.982962677686266711E-15 ) ) ;
#158682=CYLINDRICAL_SURFACE ( 'NONE', #121712, 0.5000000000000004441 ) ;
#158692=DIRECTION ( 'NONE',  ( 0.000000000000000000, -1.411300455031978166E-14, 1.000000000000000000 ) ) ;
#158713=FACE_OUTER_BOUND ( 'NONE', #15073, .T. ) ;
#158717=DIRECTION ( 'NONE',  ( 0.000000000000000000, 0.000000000000000000, -1.000000000000000000 ) ) ;
#158722=DIRECTION ( 'NONE',  ( 0.000000000000000000, -0.7397360091702647189, -0.6728971962616949742 ) ) ;
#158731=CARTESIAN_POINT ( 'NONE',  ( -2.995603634470891112E-16, 87.75000000001196554, -111.7731074845242034 ) ) ;
#158754=CIRCLE ( 'NONE', #67138, 0.09999999999999939493 ) ;
#158770=DIRECTION ( 'NONE',  ( -0.000000000000000000, 1.000000000000000000, 6.982962677686266711E-15 ) ) ;
#158778=VERTEX_POINT ( 'NONE', #12669 ) ;
#158792=EDGE_CURVE ( 'NONE', #162858, #203841, #56552, .T. ) ;
#158797=CIRCLE ( 'NONE', #121397, 0.1000000000000028644 ) ;
#158802=DIRECTION ( 'NONE',  ( 0.000000000000000000, -7.026728003956683390E-15, 1.000000000000000000 ) ) ;
#158805=CYLINDRICAL_SURFACE ( 'NONE', #168423, 0.1000000000000070832 ) ;
#158890=AXIS2_PLACEMENT_3D ( 'NONE', #193991, #216087, #97400 ) ;
#158893=FACE_OUTER_BOUND ( 'NONE', #92078, .T. ) ;
#158898=ORIENTED_EDGE ( 'NONE', *, *, #46501, .T. ) ;
#158920=FACE_OUTER_BOUND ( 'NONE', #113898, .T. ) ;
#158931=AXIS2_PLACEMENT_3D ( 'NONE', #98481, #198911, #159804 ) ;
#158937=AXIS2_PLACEMENT_3D ( 'NONE', #60212, #58906, #241443 ) ;
#158957=LINE ( 'NONE', #178519, #33179 ) ;
#158979=LINE ( 'NONE', #220216, #228273 ) ;
#159008=LINE ( 'NONE', #59847, #141600 ) ;
#159027=ADVANCED_FACE ( 'NONE', ( #45043 ), #164990, .T. ) ;
#159036=DIRECTION ( 'NONE',  ( 0.000000000000000000, 1.000000000000000000, 6.853228547068871147E-15 ) ) ;
#159065=ORIENTED_EDGE ( 'NONE', *, *, #1960, .F. ) ;
#159090=CARTESIAN_POINT ( 'NONE',  ( 18.49999999999999289, 69.55000000001223270, -148.2731074845243597 ) ) ;
#159105=TOROIDAL_SURFACE ( 'NONE', #242452, 0.4000000000000003553, 0.1000000000000000056 ) ;
#159111=CIRCLE ( 'NONE', #84194, 0.1000000000000028644 ) ;
#159121=CARTESIAN_POINT ( 'NONE',  ( 20.21567752745066215, 65.80188589878011385, -128.6404871368697229 ) ) ;
#159137=VERTEX_POINT ( 'NONE', #29378 ) ;
#159142=DIRECTION ( 'NONE',  ( -1.000000000000000000, -0.000000000000000000, -0.000000000000000000 ) ) ;
#159178=DIRECTION ( 'NONE',  ( -4.408576920032447355E-17, -0.1350103645451945777, 0.9908441862701589109 ) ) ;
#159230=EDGE_CURVE ( 'NONE', #63258, #66650, #44318, .T. ) ;
#159240=CARTESIAN_POINT ( 'NONE',  ( 18.49999999999999289, 64.25000000001207923, -128.4231074845243654 ) ) ;
#159268=DIRECTION ( 'NONE',  ( 0.000000000000000000, 0.000000000000000000, 1.000000000000000000 ) ) ;
#159277=ORIENTED_EDGE ( 'NONE', *, *, #186929, .F. ) ;
#159285=DIRECTION ( 'NONE',  ( 0.000000000000000000, 0.9915357197604804940, -0.1298341882520397950 ) ) ;
#159309=ADVANCED_FACE ( 'NONE', ( #220805 ), #42186, .T. ) ;
#159338=AXIS2_PLACEMENT_3D ( 'NONE', #77560, #115425, #136250 ) ;
#159343=CARTESIAN_POINT ( 'NONE',  ( -18.50000000000000000, 65.70711192142367452, -97.56510546851220056 ) ) ;
#159353=DIRECTION ( 'NONE',  ( 0.000000000000000000, -0.1575844902526687130, -0.9875055080513762684 ) ) ;
#159367=DIRECTION ( 'NONE',  ( -0.000000000000000000, -1.000000000000000000, -6.982962677686266711E-15 ) ) ;
#159368=DIRECTION ( 'NONE',  ( 0.000000000000000000, 0.000000000000000000, 1.000000000000000000 ) ) ;
#159385=DIRECTION ( 'NONE',  ( -1.000000000000000000, -0.000000000000000000, -0.000000000000000000 ) ) ;
#159390=CARTESIAN_POINT ( 'NONE',  ( -1.739115166359751801E-14, 64.35000000001200249, -115.1731074845243796 ) ) ;
#159400=CIRCLE ( 'NONE', #5412, 0.1000000000000028644 ) ;
#159425=ADVANCED_FACE ( 'NONE', ( #162142 ), #241656, .F. ) ;
#159491=DIRECTION ( 'NONE',  ( -1.000000000000000000, -0.000000000000000000, -0.000000000000000000 ) ) ;
#159512=CARTESIAN_POINT ( 'NONE',  ( 21.05000000000000071, 69.50331341424531217, -136.5084513660147252 ) ) ;
#159554=LINE ( 'NONE', #61728, #146960 ) ;
#159581=CYLINDRICAL_SURFACE ( 'NONE', #33236, 0.09999999999999939493 ) ;
#159593=CARTESIAN_POINT ( 'NONE',  ( -18.59999999999999787, 85.48068669529084218, -96.08199231576638510 ) ) ;
#159611=CARTESIAN_POINT ( 'NONE',  ( -20.85000000000000142, 68.92903212821303782, -99.27654326265604823 ) ) ;
#159626=CYLINDRICAL_SURFACE ( 'NONE', #83923, 0.1000000000000028644 ) ;
#159670=AXIS2_PLACEMENT_3D ( 'NONE', #28386, #50448, #247379 ) ;
#159675=COLOUR_RGB ( '', 0.72549020, 0.75294118, 0.79215686) ;
#159692=CARTESIAN_POINT ( 'NONE',  ( -20.64999999999999858, 68.85000000001205933, -124.1731074845243370 ) ) ;
#159699=ORIENTED_EDGE ( 'NONE', *, *, #65773, .T. ) ;
#159741=DIRECTION ( 'NONE',  ( 0.000000000000000000, 0.000000000000000000, 1.000000000000000000 ) ) ;
#159746=CIRCLE ( 'NONE', #231074, 11.80000000000000426 ) ;
#159755=ORIENTED_EDGE ( 'NONE', *, *, #164141, .F. ) ;
#159760=EDGE_CURVE ( 'NONE', #17520, #25751, #28123, .T. ) ;
#159804=DIRECTION ( 'NONE',  ( 0.000000000000000000, 0.000000000000000000, 1.000000000000000000 ) ) ;
#159812=CIRCLE ( 'NONE', #188846, 0.1000000000000028644 ) ;
#159854=CYLINDRICAL_SURFACE ( 'NONE', #22908, 0.09999999999999939493 ) ;
#159857=VECTOR ( 'NONE', #143151, 1000.000000000000000 ) ;
#159883=DIRECTION ( 'NONE',  ( 1.000000000000000000, -2.952720810173289112E-16, -2.061873921506763405E-30 ) ) ;
#159893=DIRECTION ( 'NONE',  ( 1.000000000000000000, 7.304098846218163263E-16, -4.217023435051627211E-16 ) ) ;
#159911=LINE ( 'NONE', #63337, #47737 ) ;
#159921=EDGE_CURVE ( 'NONE', #185471, #128716, #248869, .T. ) ;
#159951=TOROIDAL_SURFACE ( 'NONE', #222251, 11.65000000000000036, 0.1000000000000000056 ) ;
#159985=CARTESIAN_POINT ( 'NONE',  ( -21.07928932188134041, 75.90110485435778287, -142.8516241409176075 ) ) ;
#159996=CARTESIAN_POINT ( 'NONE',  ( -20.64999999999999858, 76.00000000001190870, -103.0231074845243029 ) ) ;
#159999=FACE_OUTER_BOUND ( 'NONE', #199015, .T. ) ;
#160008=CARTESIAN_POINT ( 'NONE',  ( -20.64999999999999858, 68.75000000001205080, -124.2731074845243455 ) ) ;
#160038=EDGE_CURVE ( 'NONE', #93827, #29926, #165489, .T. ) ;
#160072=CIRCLE ( 'NONE', #80920, 0.1000000000000017680 ) ;
#160084=CARTESIAN_POINT ( 'NONE',  ( -20.54999999999999361, 64.35000000001198828, -115.1731074845243796 ) ) ;
#160096=CARTESIAN_POINT ( 'NONE',  ( 22.39999999999999503, 68.20922040163875977, -136.6231074845243540 ) ) ;
#160125=DIRECTION ( 'NONE',  ( 0.000000000000000000, 0.9887567792719329507, 0.1495327102803732933 ) ) ;
#160157=ORIENTED_EDGE ( 'NONE', *, *, #205067, .T. ) ;
#160164=ORIENTED_EDGE ( 'NONE', *, *, #103284, .T. ) ;
#160177=FACE_OUTER_BOUND ( 'NONE', #182670, .T. ) ;
#160185=EDGE_LOOP ( 'NONE', ( #237157, #191471, #205637, #78100 ) ) ;
#160203=AXIS2_PLACEMENT_3D ( 'NONE', #223584, #171383, #170102 ) ;
#160205=DIRECTION ( 'NONE',  ( 0.000000000000000000, 6.982962677686267499E-15, -1.000000000000000000 ) ) ;
#160209=CARTESIAN_POINT ( 'NONE',  ( -20.54999999999999716, 85.50000000001207923, -126.6291383618717816 ) ) ;
#160229=VERTEX_POINT ( 'NONE', #11102 ) ;
#160245=AXIS2_PLACEMENT_3D ( 'NONE', #29686, #170505, #212156 ) ;
#160314=ORIENTED_EDGE ( 'NONE', *, *, #99640, .T. ) ;
#160331=CIRCLE ( 'NONE', #131064, 0.1000000000000028644 ) ;
#160387=ORIENTED_EDGE ( 'NONE', *, *, #149237, .T. ) ;
#160407=CARTESIAN_POINT ( 'NONE',  ( 20.74897398619119215, 65.40430697834564455, -128.8437960282674624 ) ) ;
#160411=ORIENTED_EDGE ( 'NONE', *, *, #29664, .F. ) ;
#160413=ORIENTED_EDGE ( 'NONE', *, *, #187727, .T. ) ;
#160416=DIRECTION ( 'NONE',  ( -0.000000000000000000, 1.000000000000000000, 6.982962677686266711E-15 ) ) ;
#160428=CARTESIAN_POINT ( 'NONE',  ( 21.07928932188134397, 69.67148334361883144, -136.6220026301787414 ) ) ;
#160431=DIRECTION ( 'NONE',  ( -1.000000000000000000, 0.000000000000000000, -0.000000000000000000 ) ) ;
#160469=ADVANCED_FACE ( 'NONE', ( #185575 ), #157695, .F. ) ;
#160541=DIRECTION ( 'NONE',  ( 0.000000000000000000, 0.000000000000000000, 1.000000000000000000 ) ) ;
#160542=ORIENTED_EDGE ( 'NONE', *, *, #78547, .F. ) ;
#160553=ORIENTED_EDGE ( 'NONE', *, *, #52774, .F. ) ;
#160611=EDGE_CURVE ( 'NONE', #55329, #103697, #244948, .T. ) ;
#160612=DIRECTION ( 'NONE',  ( 1.000000000000000000, 0.000000000000000000, 0.000000000000000000 ) ) ;
#160630=LINE ( 'NONE', #235010, #8707 ) ;
#160650=ADVANCED_FACE ( 'NONE', ( #234991 ), #194601, .T. ) ;
#160656=CIRCLE ( 'NONE', #48191, 0.09999999999999939493 ) ;
#160668=CARTESIAN_POINT ( 'NONE',  ( -21.07016717457011268, 76.00000000001219291, -142.8440483226251843 ) ) ;
#160681=CARTESIAN_POINT ( 'NONE',  ( -21.05439746398122836, 64.25000000001209344, -129.5331909970393838 ) ) ;
#160715=LINE ( 'NONE', #254617, #237794 ) ;
#160727=ORIENTED_EDGE ( 'NONE', *, *, #193251, .T. ) ;
#160747=ADVANCED_FACE ( 'NONE', ( #183992 ), #82295, .T. ) ;
#160748=EDGE_CURVE ( 'NONE', #144360, #180506, #74295, .T. ) ;
#160756=CIRCLE ( 'NONE', #119217, 0.5000000000000004441 ) ;
#160770=AXIS2_PLACEMENT_3D ( 'NONE', #9462, #88983, #248075 ) ;
#160774=CARTESIAN_POINT ( 'NONE',  ( -18.45037301276613917, 85.49020044755425829, -129.5104333481091601 ) ) ;
#160775=ADVANCED_FACE ( 'NONE', ( #121485 ), #199730, .T. ) ;
#160801=ADVANCED_FACE ( 'NONE', ( #237554 ), #99295, .F. ) ;
#160808=ORIENTED_EDGE ( 'NONE', *, *, #135064, .F. ) ;
#160812=TOROIDAL_SURFACE ( 'NONE', #190002, 11.70000000000000462, 0.1000000000000000056 ) ;
#160823=VERTEX_POINT ( 'NONE', #241413 ) ;
#160824=FACE_OUTER_BOUND ( 'NONE', #125262, .T. ) ;
#160862=ORIENTED_EDGE ( 'NONE', *, *, #207833, .F. ) ;
#160941=EDGE_CURVE ( 'NONE', #147468, #35933, #174453, .T. ) ;
#160960=CARTESIAN_POINT ( 'NONE',  ( -21.07928932188134041, 69.67148334361884565, -136.6220026301787414 ) ) ;
#161014=ORIENTED_EDGE ( 'NONE', *, *, #193251, .F. ) ;
#161018=EDGE_CURVE ( 'NONE', #216543, #176995, #152606, .T. ) ;
#161033=AXIS2_PLACEMENT_3D ( 'NONE', #235044, #43259, #120263 ) ;
#161052=EDGE_CURVE ( 'NONE', #31313, #197247, #215112, .T. ) ;
#161063=VECTOR ( 'NONE', #30390, 1000.000000000000000 ) ;
#161152=CARTESIAN_POINT ( 'NONE',  ( -21.07928932188134397, 75.90110485435778287, -142.8516241409176075 ) ) ;
#161176=EDGE_LOOP ( 'NONE', ( #229531, #27514, #171073 ) ) ;
#161188=DIRECTION ( 'NONE',  ( 0.000000000000000000, -7.147358527629766941E-15, 1.000000000000000000 ) ) ;
#161206=DIRECTION ( 'NONE',  ( -1.000000000000000000, 0.000000000000000000, -0.000000000000000000 ) ) ;
#161208=EDGE_LOOP ( 'NONE', ( #202466, #157327, #237624, #77983 ) ) ;
#161210=ORIENTED_EDGE ( 'NONE', *, *, #80478, .T. ) ;
#161257=DIRECTION ( 'NONE',  ( -1.000000000000000000, -0.000000000000000000, -0.000000000000000000 ) ) ;
#161262=ORIENTED_EDGE ( 'NONE', *, *, #51988, .T. ) ;
#161316=SPHERICAL_SURFACE ( 'NONE', #88080, 0.1000000000000000056 ) ;
#161336=CARTESIAN_POINT ( 'NONE',  ( 23.24999999999999289, 64.25000000001205080, -124.3731074845243825 ) ) ;
#161343=VERTEX_POINT ( 'NONE', #94516 ) ;
#161348=ORIENTED_EDGE ( 'NONE', *, *, #100583, .F. ) ;
#161352=CARTESIAN_POINT ( 'NONE',  ( -23.15000000000000213, 74.00000000001199396, -115.6477294072864055 ) ) ;
#161365=ORIENTED_EDGE ( 'NONE', *, *, #131137, .F. ) ;
#161372=FACE_OUTER_BOUND ( 'NONE', #146895, .T. ) ;
#161375=CARTESIAN_POINT ( 'NONE',  ( 22.39999999999999503, 64.35000000001213039, -136.4231074845243938 ) ) ;
#161389=DIRECTION ( 'NONE',  ( -0.7071067811865127117, -0.7071067811865821007, 0.000000000000000000 ) ) ;
#161400=VERTEX_POINT ( 'NONE', #116658 ) ;
#161404=FACE_OUTER_BOUND ( 'NONE', #48457, .T. ) ;
#161417=AXIS2_PLACEMENT_3D ( 'NONE', #86683, #68444, #91851 ) ;
#161509=VERTEX_POINT ( 'NONE', #253589 ) ;
#161535=AXIS2_PLACEMENT_3D ( 'NONE', #256584, #216215, #255299 ) ;
#161556=ORIENTED_EDGE ( 'NONE', *, *, #220141, .T. ) ;
#161583=DIRECTION ( 'NONE',  ( 1.000000000000000000, 0.000000000000000000, 0.000000000000000000 ) ) ;
#161589=CARTESIAN_POINT ( 'NONE',  ( 21.05000000000000071, 76.00000000001210765, -132.2231074845242631 ) ) ;
#161592=EDGE_CURVE ( 'NONE', #230368, #71963, #58028, .T. ) ;
#161598=EDGE_LOOP ( 'NONE', ( #131522, #22028, #185721, #208348 ) ) ;
#161600=CARTESIAN_POINT ( 'NONE',  ( -18.59999999999999787, 85.50000000001205080, -124.3731074845242262 ) ) ;
#161614=AXIS2_PLACEMENT_3D ( 'NONE', #241328, #43121, #202190 ) ;
#161625=CARTESIAN_POINT ( 'NONE',  ( -22.39999999999999858, 76.00000000001222134, -148.1726782920690937 ) ) ;
#161638=CARTESIAN_POINT ( 'NONE',  ( -18.50000000000000000, 70.65875701002055109, -146.3297576910123610 ) ) ;
#161652=DIRECTION ( 'NONE',  ( 1.000000000000000000, 0.000000000000000000, 0.000000000000000000 ) ) ;
#161683=CARTESIAN_POINT ( 'NONE',  ( 20.50589344625199217, 65.51681206853655226, -128.9501125058533546 ) ) ;
#161689=ORIENTED_EDGE ( 'NONE', *, *, #91321, .T. ) ;
#161701=LINE ( 'NONE', #178711, #48343 ) ;
#161703=CARTESIAN_POINT ( 'NONE',  ( 21.11927991906888025, 69.55150688152073712, -136.5321911639982204 ) ) ;
#161707=ORIENTED_EDGE ( 'NONE', *, *, #203219, .T. ) ;
#161715=EDGE_CURVE ( 'NONE', #254127, #72948, #186690, .T. ) ;
#161741=CYLINDRICAL_SURFACE ( 'NONE', #46039, 0.09999999999999939493 ) ;
#161747=CARTESIAN_POINT ( 'NONE',  ( -18.50000000000000000, 66.65000000001198543, -115.1731074845243654 ) ) ;
#161789=VECTOR ( 'NONE', #208965, 1000.000000000000000 ) ;
#161792=TOROIDAL_SURFACE ( 'NONE', #99199, 11.89999999999999858, 0.1000000000000000056 ) ;
#161796=DIRECTION ( 'NONE',  ( 1.000000000000000000, 0.000000000000000000, 0.000000000000000000 ) ) ;
#161810=TOROIDAL_SURFACE ( 'NONE', #236779, 0.6000000000000009770, 0.1000000000000000056 ) ;
#161811=ORIENTED_EDGE ( 'NONE', *, *, #204653, .F. ) ;
#161865=CARTESIAN_POINT ( 'NONE',  ( -21.12757541349819590, 75.99483878420245730, -142.9964880557758704 ) ) ;
#161879=ORIENTED_EDGE ( 'NONE', *, *, #33281, .F. ) ;
#161881=CARTESIAN_POINT ( 'NONE',  ( 21.05000000000000071, 76.00000000001190870, -103.0231074845243029 ) ) ;
#161889=CARTESIAN_POINT ( 'NONE',  ( 20.94999999999999929, 76.00000000001213607, -136.5231074845242745 ) ) ;
#161890=DIRECTION ( 'NONE',  ( 1.000000000000000000, 0.000000000000000000, 0.000000000000000000 ) ) ;
#161898=ORIENTED_EDGE ( 'NONE', *, *, #62538, .F. ) ;
#161957=LINE ( 'NONE', #121559, #192676 ) ;
#161964=CARTESIAN_POINT ( 'NONE',  ( 21.08489834409762054, 65.37767610527653517, -124.1731074845243512 ) ) ;
#161978=B_SPLINE_CURVE_WITH_KNOTS ( 'NONE', 3,
 ( #136950, #152704, #157848, #251766, #15760, #134365, #213925, #35329, #191828, #97795 ),
 .UNSPECIFIED., .F., .F.,
 ( 4, 3, 3, 4 ),
 ( 3.103167691559091397E-17, 0.0002000000000008536833, 0.001000000000082982687, 0.001967863649483335420 ),
 .UNSPECIFIED. ) ;
#162007=CARTESIAN_POINT ( 'NONE',  ( 23.14999999999999503, 69.45000000001199680, -115.2731074845243455 ) ) ;
#162011=VECTOR ( 'NONE', #187992, 1000.000000000000000 ) ;
#162022=DIRECTION ( 'NONE',  ( 0.000000000000000000, 0.000000000000000000, -1.000000000000000000 ) ) ;
#162070=DIRECTION ( 'NONE',  ( -1.000000000000000000, 2.952720810173289112E-16, 2.061873921506763405E-30 ) ) ;
#162086=CARTESIAN_POINT ( 'NONE',  ( 21.05000000000000071, 69.69548367074810358, -136.5020041764652206 ) ) ;
#162100=ORIENTED_EDGE ( 'NONE', *, *, #45278, .T. ) ;
#162113=ORIENTED_EDGE ( 'NONE', *, *, #215127, .T. ) ;
#162128=EDGE_LOOP ( 'NONE', ( #1109, #83485, #108289, #27686 ) ) ;
#162134=CARTESIAN_POINT ( 'NONE',  ( -21.05000000000000071, 77.26178616857710324, -128.4366085209788366 ) ) ;
#162142=FACE_OUTER_BOUND ( 'NONE', #13284, .T. ) ;
#162191=CARTESIAN_POINT ( 'NONE',  ( -22.50000000000000000, 76.00000000001222134, -148.1726782920690937 ) ) ;
#162215=ORIENTED_EDGE ( 'NONE', *, *, #31554, .T. ) ;
#162230=ORIENTED_EDGE ( 'NONE', *, *, #150311, .T. ) ;
#162252=CARTESIAN_POINT ( 'NONE',  ( 21.05000000000000071, 77.83534155023646406, -124.9679561919612922 ) ) ;
#162265=CARTESIAN_POINT ( 'NONE',  ( -22.50000000000000000, 76.00000000001222134, -148.1726782920690937 ) ) ;
#162288=SPHERICAL_SURFACE ( 'NONE', #169423, 0.1000000000000000056 ) ;
#162298=DIRECTION ( 'NONE',  ( -1.000000000000000000, -0.000000000000000000, -0.000000000000000000 ) ) ;
#162305=CARTESIAN_POINT ( 'NONE',  ( 18.59999999999999787, 77.83534155023646406, -124.9679561919613064 ) ) ;
#162321=VECTOR ( 'NONE', #108319, 1000.000000000000000 ) ;
#162344=CARTESIAN_POINT ( 'NONE',  ( -18.45068461519106151, 85.48650652910120584, -129.4543303156195577 ) ) ;
#162348=CARTESIAN_POINT ( 'NONE',  ( 18.49999999999998934, 65.75000000001196554, -111.7731074845243739 ) ) ;
#162351=ADVANCED_FACE ( 'NONE', ( #244051 ), #249223, .T. ) ;
#162369=CARTESIAN_POINT ( 'NONE',  ( -18.59999999999999787, 74.83729825007408465, -128.4231074845243086 ) ) ;
#162427=CARTESIAN_POINT ( 'NONE',  ( -23.25000000000000000, 77.83585931145546510, -91.51866831572576189 ) ) ;
#162462=ORIENTED_EDGE ( 'NONE', *, *, #135064, .T. ) ;
#162471=AXIS2_PLACEMENT_3D ( 'NONE', #90001, #50857, #32653 ) ;
#162473=CARTESIAN_POINT ( 'NONE',  ( 20.94999999999999929, 65.70729864261004138, -97.56574559737244101 ) ) ;
#162497=ORIENTED_EDGE ( 'NONE', *, *, #159921, .T. ) ;
#162504=EDGE_LOOP ( 'NONE', ( #183924, #129082, #237200, #85620 ) ) ;
#162544=ORIENTED_EDGE ( 'NONE', *, *, #31808, .F. ) ;
#162558=EDGE_CURVE ( 'NONE', #118915, #170795, #216238, .T. ) ;
#162561=ORIENTED_EDGE ( 'NONE', *, *, #157174, .F. ) ;
#162611=AXIS2_PLACEMENT_3D ( 'NONE', #240824, #102548, #182134 ) ;
#162614=CYLINDRICAL_SURFACE ( 'NONE', #183503, 0.09999999999999939493 ) ;
#162629=VERTEX_POINT ( 'NONE', #113539 ) ;
#162638=CARTESIAN_POINT ( 'NONE',  ( -18.59999999999999787, 77.68707439010378835, -149.3376804510659213 ) ) ;
#162663=DIRECTION ( 'NONE',  ( 0.000000000000000000, -6.769652589177772835E-15, 1.000000000000000000 ) ) ;
#162705=DIRECTION ( 'NONE',  ( 6.938893903907030216E-14, 0.000000000000000000, -1.000000000000000000 ) ) ;
#162708=ORIENTED_EDGE ( 'NONE', *, *, #39652, .T. ) ;
#162713=ORIENTED_EDGE ( 'NONE', *, *, #96140, .T. ) ;
#162720=CARTESIAN_POINT ( 'NONE',  ( 20.94999999999999929, 84.73084112150739600, -126.9250327655398962 ) ) ;
#162736=EDGE_LOOP ( 'NONE', ( #212639, #229097, #172147, #93947 ) ) ;
#162758=CARTESIAN_POINT ( 'NONE',  ( 23.15000000000000213, 87.48912529308798014, -106.1231074845242262 ) ) ;
#162766=VERTEX_POINT ( 'NONE', #87228 ) ;
#162769=CARTESIAN_POINT ( 'NONE',  ( -21.09107601085562322, 69.63612202465165524, -136.5624146492413331 ) ) ;
#162777=DIRECTION ( 'NONE',  ( 1.000000000000000000, 0.000000000000000000, 0.000000000000000000 ) ) ;
#162778=ORIENTED_EDGE ( 'NONE', *, *, #221347, .F. ) ;
#162824=VERTEX_POINT ( 'NONE', #63838 ) ;
#162828=VERTEX_POINT ( 'NONE', #122538 ) ;
#162845=CARTESIAN_POINT ( 'NONE',  ( 21.05000000000000071, 69.52293297888738266, -136.4231074845243938 ) ) ;
#162858=VERTEX_POINT ( 'NONE', #144640 ) ;
#162859=DIRECTION ( 'NONE',  ( 0.000000000000000000, 1.000000000000000000, 6.982962677686266711E-15 ) ) ;
#162868=DIRECTION ( 'NONE',  ( 0.000000000000000000, 0.000000000000000000, 1.000000000000000000 ) ) ;
#162916=ORIENTED_EDGE ( 'NONE', *, *, #146571, .T. ) ;
#162926=DIRECTION ( 'NONE',  ( 0.000000000000000000, 0.000000000000000000, 1.000000000000000000 ) ) ;
#162941=ADVANCED_FACE ( 'NONE', ( #42996 ), #224620, .F. ) ;
#162972=CARTESIAN_POINT ( 'NONE',  ( 21.14999999999999503, 87.75000000001210765, -133.6231074845242119 ) ) ;
#162976=ADVANCED_FACE ( 'NONE', ( #111963 ), #216433, .F. ) ;
#163013=ORIENTED_EDGE ( 'NONE', *, *, #136756, .T. ) ;
#163030=TOROIDAL_SURFACE ( 'NONE', #158931, 0.2000000000000000111, 0.1000000000000000056 ) ;
#163038=DIRECTION ( 'NONE',  ( -2.578261006436899437E-14, -0.1350103645451973811, 0.9908441862701586889 ) ) ;
#163062=AXIS2_PLACEMENT_3D ( 'NONE', #137308, #19961, #17381 ) ;
#163064=EDGE_CURVE ( 'NONE', #31427, #134440, #228916, .T. ) ;
#163065=ADVANCED_FACE ( 'NONE', ( #40139 ), #4051, .T. ) ;
#163091=ORIENTED_EDGE ( 'NONE', *, *, #174924, .F. ) ;
#163092=DIRECTION ( 'NONE',  ( -3.265361837132813093E-16, -1.000000000000000000, -6.982962677686266711E-15 ) ) ;
#163117=DIRECTION ( 'NONE',  ( 2.952720810173289112E-16, 1.000000000000000000, -6.088138035986627436E-46 ) ) ;
#163185=CARTESIAN_POINT ( 'NONE',  ( -18.57399277249657032, 65.66887361445333227, -97.43298459182689442 ) ) ;
#163204=VECTOR ( 'NONE', #30111, 1000.000000000000000 ) ;
#163210=DIRECTION ( 'NONE',  ( -2.952720810173289112E-16, -1.000000000000000000, -6.982962677686266711E-15 ) ) ;
#163212=DIRECTION ( 'NONE',  ( 0.000000000000000000, 0.000000000000000000, -1.000000000000000000 ) ) ;
#163228=CARTESIAN_POINT ( 'NONE',  ( -21.12844524849339223, 64.25000000001209344, -129.6186940136819601 ) ) ;
#163243=VERTEX_POINT ( 'NONE', #3536 ) ;
#163272=CARTESIAN_POINT ( 'NONE',  ( 18.49999999999999289, 69.55000000001207638, -126.5060803140843291 ) ) ;
#163296=( BOUNDED_SURFACE ( )  B_SPLINE_SURFACE ( 3, 2, ( 
 ( #55781, #177079, #231913 ),
 ( #75417, #53262, #135339 ),
 ( #58356, #212351, #93663 ),
 ( #132810, #156235, #33743 ),
 ( #72852, #35017, #192774 ),
 ( #175789, #234445, #117086 ) ),
 .UNSPECIFIED., .F., .F., .F. ) 
 B_SPLINE_SURFACE_WITH_KNOTS ( ( 4, 2, 4 ),
 ( 3, 3 ),
 ( 0.0001381104793128061785, 0.0002947094729387726578, 0.0004513084665647390829 ),
 ( 0.000000000000000000, 1.000000000000000000 ),
 .UNSPECIFIED. ) 
 GEOMETRIC_REPRESENTATION_ITEM ( )  RATIONAL_B_SPLINE_SURFACE ( (
 ( 1.000000000000000000, 0.7071067811865494601, 1.000000000000000000),
 ( 1.000000000000000000, 0.6919563088092252068, 1.000000000000000000),
 ( 1.000000000000000000, 0.6959445945726553395, 1.000000000000000000),
 ( 1.000000000000000000, 0.7137882985304006001, 1.000000000000000000),
 ( 1.000000000000000000, 0.7257496306103440320, 1.000000000000000000),
 ( 1.000000000000000000, 0.7250110520819876836, 1.000000000000000000) ) ) 
 REPRESENTATION_ITEM ( '' )  SURFACE ( )  );
#163359=CARTESIAN_POINT ( 'NONE',  ( 21.05000000000000071, 69.58602111852371763, -136.4373083682503704 ) ) ;
#163366=CIRCLE ( 'NONE', #42545, 4.049999999999998046 ) ;
#163375=TOROIDAL_SURFACE ( 'NONE', #200779, 0.2000000000000000111, 0.1000000000000000056 ) ;
#163387=ORIENTED_EDGE ( 'NONE', *, *, #203713, .T. ) ;
#163392=EDGE_LOOP ( 'NONE', ( #195467, #44693, #85143, #167681 ) ) ;
#163401=ORIENTED_EDGE ( 'NONE', *, *, #6508, .T. ) ;
#163405=DIRECTION ( 'NONE',  ( 1.000000000000000000, 0.000000000000000000, 0.000000000000000000 ) ) ;
#163417=LINE ( 'NONE', #143828, #94598 ) ;
#163438=DIRECTION ( 'NONE',  ( 0.000000000000000000, 7.109473446599835262E-15, -1.000000000000000000 ) ) ;
#163487=EDGE_CURVE ( 'NONE', #226829, #47866, #25112, .T. ) ;
#163500=DIRECTION ( 'NONE',  ( 0.000000000000000000, 0.000000000000000000, 1.000000000000000000 ) ) ;
#163533=DIRECTION ( 'NONE',  ( 0.000000000000000000, 1.000000000000000000, 6.982962677686266711E-15 ) ) ;
#163540=CARTESIAN_POINT ( 'NONE',  ( -21.44999999999999929, 68.65000000001199965, -115.3731074845243540 ) ) ;
#163548=EDGE_LOOP ( 'NONE', ( #134875, #51929, #87725, #201010 ) ) ;
#163571=LINE ( 'NONE', #7051, #99827 ) ;
#163587=VERTEX_POINT ( 'NONE', #123194 ) ;
#163591=DIRECTION ( 'NONE',  ( -1.000000000000000000, -0.000000000000000000, -0.000000000000000000 ) ) ;
#163592=VECTOR ( 'NONE', #116782, 1000.000000000000000 ) ;
#163620=CARTESIAN_POINT ( 'NONE',  ( 21.00000000000000000, 66.25000000001199396, -115.3731074845243683 ) ) ;
#163626=AXIS2_PLACEMENT_3D ( 'NONE', #170234, #249718, #172791 ) ;
#163665=CARTESIAN_POINT ( 'NONE',  ( 18.49999999999999645, 76.00000000001190870, -103.0231074845243029 ) ) ;
#163675=DIRECTION ( 'NONE',  ( 0.000000000000000000, 1.000000000000000000, 6.982962677686266711E-15 ) ) ;
#163694=DIRECTION ( 'NONE',  ( 1.000000000000000000, -2.952720810173289112E-16, -2.061873921506763405E-30 ) ) ;
#163698=FACE_OUTER_BOUND ( 'NONE', #154660, .T. ) ;
#163699=AXIS2_PLACEMENT_3D ( 'NONE', #155839, #136218, #176684 ) ;
#163752=CARTESIAN_POINT ( 'NONE',  ( -18.50000000000000000, 76.00000000001213607, -136.5231074845242745 ) ) ;
#163770=VERTEX_POINT ( 'NONE', #192175 ) ;
#163792=EDGE_CURVE ( 'NONE', #95961, #191338, #100066, .T. ) ;
#163800=CARTESIAN_POINT ( 'NONE',  ( 20.94999999999999929, 76.00000000001190870, -103.0231074845243029 ) ) ;
#163807=ORIENTED_EDGE ( 'NONE', *, *, #168544, .T. ) ;
#163841=ORIENTED_EDGE ( 'NONE', *, *, #198714, .T. ) ;
#163844=FACE_OUTER_BOUND ( 'NONE', #174001, .T. ) ;
#163848=CARTESIAN_POINT ( 'NONE',  ( -21.55000000000000071, 68.85000000001200249, -115.2731074845243455 ) ) ;
#163888=FACE_OUTER_BOUND ( 'NONE', #208888, .T. ) ;
#163894=EDGE_CURVE ( 'NONE', #220397, #147164, #241743, .T. ) ;
#163919=CARTESIAN_POINT ( 'NONE',  ( -21.05000000000000071, 76.00000000001213607, -136.5231074845242745 ) ) ;
#163955=CARTESIAN_POINT ( 'NONE',  ( -18.59999999999999787, 74.26374286841466699, -124.9544551555068068 ) ) ;
#163963=FACE_OUTER_BOUND ( 'NONE', #78693, .T. ) ;
#163974=EDGE_CURVE ( 'NONE', #94251, #18434, #129509, .T. ) ;
#163981=CARTESIAN_POINT ( 'NONE',  ( 21.00023020733504708, 76.00000000001219291, -142.9139767297926653 ) ) ;
#164030=DIRECTION ( 'NONE',  ( -0.000000000000000000, 6.982962677686266711E-15, -1.000000000000000000 ) ) ;
#164034=AXIS2_PLACEMENT_3D ( 'NONE', #118472, #153784, #12964 ) ;
#164052=FACE_OUTER_BOUND ( 'NONE', #9399, .T. ) ;
#164060=DIRECTION ( 'NONE',  ( 0.000000000000000000, -6.982962677686266711E-15, 1.000000000000000000 ) ) ;
#164064=CARTESIAN_POINT ( 'NONE',  ( 23.14999999999999503, 69.35000000001200249, -115.1731074845243512 ) ) ;
#164081=ORIENTED_EDGE ( 'NONE', *, *, #45412, .T. ) ;
#164102=DIRECTION ( 'NONE',  ( 1.000000000000000000, 0.000000000000000000, 0.000000000000000000 ) ) ;
#164129=CARTESIAN_POINT ( 'NONE',  ( -21.05000000000000071, 74.83729825007408465, -128.6231074845242972 ) ) ;
#164133=DIRECTION ( 'NONE',  ( -0.000000000000000000, 0.9908441862701591329, 0.1350103645451946055 ) ) ;
#164139=CARTESIAN_POINT ( 'NONE',  ( 21.97500000000000497, 66.25000000001199396, -115.3731074845243683 ) ) ;
#164141=EDGE_CURVE ( 'NONE', #230224, #211628, #87785, .T. ) ;
#164143=AXIS2_PLACEMENT_3D ( 'NONE', #150578, #245824, #108873 ) ;
#164148=ORIENTED_EDGE ( 'NONE', *, *, #242689, .T. ) ;
#164153=VERTEX_POINT ( 'NONE', #119705 ) ;
#164168=ORIENTED_EDGE ( 'NONE', *, *, #184861, .F. ) ;
#164192=EDGE_CURVE ( 'NONE', #164153, #128716, #75368, .T. ) ;
#164199=EDGE_CURVE ( 'NONE', #121611, #2705, #175319, .T. ) ;
#164202=CARTESIAN_POINT ( 'NONE',  ( 20.94999999999999929, 70.60000000001198828, -112.9170766071767815 ) ) ;
#164208=DIRECTION ( 'NONE',  ( -0.000000000000000000, 1.000000000000000000, 6.982962677686266711E-15 ) ) ;
#164218=ORIENTED_EDGE ( 'NONE', *, *, #257197, .T. ) ;
#164242=CARTESIAN_POINT ( 'NONE',  ( -18.59999999999999787, 64.25000000001222134, -148.2731074845243882 ) ) ;
#164254=EDGE_LOOP ( 'NONE', ( #72455, #86635, #63358, #37831 ) ) ;
#164283=ORIENTED_EDGE ( 'NONE', *, *, #60927, .T. ) ;
#164288=VERTEX_POINT ( 'NONE', #85651 ) ;
#164322=EDGE_CURVE ( 'NONE', #240054, #112979, #7432, .T. ) ;
#164329=VERTEX_POINT ( 'NONE', #167832 ) ;
#164333=ORIENTED_EDGE ( 'NONE', *, *, #215239, .T. ) ;
#164354=ORIENTED_EDGE ( 'NONE', *, *, #94076, .T. ) ;
#164374=ORIENTED_EDGE ( 'NONE', *, *, #164768, .F. ) ;
#164380=ORIENTED_EDGE ( 'NONE', *, *, #115968, .F. ) ;
#164405=AXIS2_PLACEMENT_3D ( 'NONE', #103022, #163038, #239993 ) ;
#164421=DIRECTION ( 'NONE',  ( 0.000000000000000000, -1.000000000000000000, -6.982962677686265922E-15 ) ) ;
#164438=CARTESIAN_POINT ( 'NONE',  ( 20.94999999999999929, 70.15000000001198543, -113.1556047088022581 ) ) ;
#164457=CIRCLE ( 'NONE', #176947, 0.1000000000000028644 ) ;
#164463=DIRECTION ( 'NONE',  ( -0.000000000000000000, -1.000000000000000000, -6.982962677686266711E-15 ) ) ;
#164466=EDGE_CURVE ( 'NONE', #255696, #57112, #131236, .T. ) ;
#164485=VECTOR ( 'NONE', #43070, 1000.000000000000000 ) ;
#164487=CARTESIAN_POINT ( 'NONE',  ( 18.49999999999999289, 69.35000000001200249, -115.3731074845243398 ) ) ;
#164509=DIRECTION ( 'NONE',  ( 0.000000000000000000, 1.000000000000000000, 6.982962677686266711E-15 ) ) ;
#164515=CARTESIAN_POINT ( 'NONE',  ( -20.97625342178408658, 64.39999999919190543, -129.5949042547223655 ) ) ;
#164518=CARTESIAN_POINT ( 'NONE',  ( -18.50000000000000000, 64.35000000001222986, -148.2731074845243882 ) ) ;
#164527=ADVANCED_FACE ( 'NONE', ( #135070 ), #163030, .T. ) ;
#164550=CARTESIAN_POINT ( 'NONE',  ( 20.94999999999999574, 76.00000000001213607, -136.5231074845242745 ) ) ;
#164556=AXIS2_PLACEMENT_3D ( 'NONE', #20802, #19510, #98999 ) ;
#164577=( GEOMETRIC_REPRESENTATION_CONTEXT ( 3 ) GLOBAL_UNCERTAINTY_ASSIGNED_CONTEXT ( ( #165191 ) ) GLOBAL_UNIT_ASSIGNED_CONTEXT ( ( #74644, #155466, #36798 ) ) REPRESENTATION_CONTEXT ( 'NONE', 'WORKASPACE' ) );
#164581=CARTESIAN_POINT ( 'NONE',  ( 21.05000000000000071, 85.40000000001198543, -112.9170766071766820 ) ) ;
#164586=ORIENTED_EDGE ( 'NONE', *, *, #220639, .T. ) ;
#164593=CARTESIAN_POINT ( 'NONE',  ( -18.59999999999999787, 74.83729825007408465, -128.4231074845243086 ) ) ;
#164598=ORIENTED_EDGE ( 'NONE', *, *, #201594, .T. ) ;
#164602=TOROIDAL_SURFACE ( 'NONE', #181361, 0.2000000000000000111, 0.1000000000000000056 ) ;
#164606=EDGE_CURVE ( 'NONE', #56789, #234281, #158754, .T. ) ;
#164631=VERTEX_POINT ( 'NONE', #5827 ) ;
#164643=CARTESIAN_POINT ( 'NONE',  ( 21.05000000000000071, 69.45934304831089889, -136.4231074845243654 ) ) ;
#164685=CARTESIAN_POINT ( 'NONE',  ( 21.56666275994540172, 76.00000000001219291, -143.4804758914176261 ) ) ;
#164750=ORIENTED_EDGE ( 'NONE', *, *, #239539, .F. ) ;
#164768=EDGE_CURVE ( 'NONE', #182942, #147024, #188130, .T. ) ;
#164772=ORIENTED_EDGE ( 'NONE', *, *, #100688, .F. ) ;
#164777=CYLINDRICAL_SURFACE ( 'NONE', #23109, 0.5000000000000004441 ) ;
#164786=ADVANCED_FACE ( 'NONE', ( #189635 ), #173566, .F. ) ;
#164793=ORIENTED_EDGE ( 'NONE', *, *, #16092, .F. ) ;
#164799=EDGE_CURVE ( 'NONE', #86933, #213725, #107066, .T. ) ;
#164812=CARTESIAN_POINT ( 'NONE',  ( 23.14999999999999858, 76.00000000001190870, -103.0231074845243029 ) ) ;
#164827=DIRECTION ( 'NONE',  ( 1.000000000000000000, 0.000000000000000000, 0.000000000000000000 ) ) ;
#164829=AXIS2_PLACEMENT_3D ( 'NONE', #206933, #127398, #186087 ) ;
#164830=ADVANCED_FACE ( 'NONE', ( #186628 ), #26267, .T. ) ;
#164837=DIRECTION ( 'NONE',  ( 1.000000000000000000, 0.000000000000000000, 0.000000000000000000 ) ) ;
#164858=DIRECTION ( 'NONE',  ( 0.000000000000000000, 0.000000000000000000, 1.000000000000000000 ) ) ;
#164878=CARTESIAN_POINT ( 'NONE',  ( 20.94999999999999574, 62.00000000001210054, -131.0960149541418502 ) ) ;
#164897=CARTESIAN_POINT ( 'NONE',  ( -18.46856557590793457, 85.47421590779860878, -129.4211212436419487 ) ) ;
#164898=DIRECTION ( 'NONE',  ( 0.000000000000000000, 7.162729191130010591E-15, -1.000000000000000000 ) ) ;
#164922=ORIENTED_EDGE ( 'NONE', *, *, #27489, .T. ) ;
#164979=LINE ( 'NONE', #127139, #63990 ) ;
#164987=CIRCLE ( 'NONE', #127588, 2.100000000000004530 ) ;
#164988=DIRECTION ( 'NONE',  ( 0.7071359030028113724, 0.000000000000000000, -0.7070776581708677622 ) ) ;
#164990=CYLINDRICAL_SURFACE ( 'NONE', #215177, 0.1000000000000028644 ) ;
#164991=CARTESIAN_POINT ( 'NONE',  ( 20.94999999999999574, 74.16465844978765176, -124.8679561919613263 ) ) ;
#164995=DIRECTION ( 'NONE',  ( 0.000000000000000000, 0.000000000000000000, 1.000000000000000000 ) ) ;
#165016=CARTESIAN_POINT ( 'NONE',  ( -18.39999999999999858, 85.51932773110452501, -129.5501311079648872 ) ) ;
#165031=DIRECTION ( 'NONE',  ( -1.000000000000000000, -0.000000000000000000, -0.000000000000000000 ) ) ;
#165074=DIRECTION ( 'NONE',  ( 0.000000000000000000, 0.000000000000000000, -1.000000000000000000 ) ) ;
#165129=CIRCLE ( 'NONE', #23523, 0.1000000000000028644 ) ;
#165147=AXIS2_PLACEMENT_3D ( 'NONE', #51131, #12059, #228528 ) ;
#165161=DIRECTION ( 'NONE',  ( -1.000000000000000000, 0.000000000000000000, 0.000000000000000000 ) ) ;
#165191=UNCERTAINTY_MEASURE_WITH_UNIT (LENGTH_MEASURE( 1.000000000000000082E-05 ), #74644, 'distance_accuracy_value', 'NONE');
#165222=AXIS2_PLACEMENT_3D ( 'NONE', #162348, #241859, #63207 ) ;
#165255=CARTESIAN_POINT ( 'NONE',  ( 21.05000000000000071, 70.50000000001199396, -115.4283735034374274 ) ) ;
#165271=CARTESIAN_POINT ( 'NONE',  ( 23.14999999999999858, 71.00000000001199396, -115.4283735034374274 ) ) ;
#165278=FACE_OUTER_BOUND ( 'NONE', #101800, .T. ) ;
#165320=CARTESIAN_POINT ( 'NONE',  ( -21.11825140030087411, 69.55459243459270624, -136.5303111051574376 ) ) ;
#165375=VECTOR ( 'NONE', #50535, 1000.000000000000000 ) ;
#165388=DIRECTION ( 'NONE',  ( 0.000000000000000000, 6.608470384673558123E-15, -1.000000000000000000 ) ) ;
#165397=ORIENTED_EDGE ( 'NONE', *, *, #126438, .F. ) ;
#165447=ADVANCED_FACE ( 'NONE', ( #86040 ), #228167, .T. ) ;
#165452=ORIENTED_EDGE ( 'NONE', *, *, #172491, .T. ) ;
#165453=VERTEX_POINT ( 'NONE', #242573 ) ;
#165489=CIRCLE ( 'NONE', #53031, 0.1000000000000028644 ) ;
#165534=FACE_OUTER_BOUND ( 'NONE', #232458, .T. ) ;
#165542=ADVANCED_FACE ( 'NONE', ( #92489 ), #191636, .F. ) ;
#165544=CARTESIAN_POINT ( 'NONE',  ( 21.09813707148777340, 69.61493789427564138, -136.5544589840538663 ) ) ;
#165548=AXIS2_PLACEMENT_3D ( 'NONE', #233443, #235971, #138145 ) ;
#165568=DIRECTION ( 'NONE',  ( -0.000000000000000000, -6.982962677686266711E-15, 1.000000000000000000 ) ) ;
#165570=CARTESIAN_POINT ( 'NONE',  ( -20.94999999999999929, 68.97833521811179480, -99.18954208262705663 ) ) ;
#165572=ORIENTED_EDGE ( 'NONE', *, *, #102586, .F. ) ;
#165598=CARTESIAN_POINT ( 'NONE',  ( 20.94999999999999574, 77.83534155023646406, -124.9679561919613064 ) ) ;
#165609=ORIENTED_EDGE ( 'NONE', *, *, #61730, .T. ) ;
#165617=ORIENTED_EDGE ( 'NONE', *, *, #188842, .F. ) ;
#165619=ORIENTED_EDGE ( 'NONE', *, *, #234342, .F. ) ;
#165622=ORIENTED_EDGE ( 'NONE', *, *, #83930, .F. ) ;
#165623=ORIENTED_EDGE ( 'NONE', *, *, #91095, .T. ) ;
#165644=EDGE_CURVE ( 'NONE', #70458, #235860, #96877, .T. ) ;
#165671=CYLINDRICAL_SURFACE ( 'NONE', #36660, 4.049999999999998046 ) ;
#165729=LINE ( 'NONE', #67887, #58169 ) ;
#165762=CARTESIAN_POINT ( 'NONE',  ( -20.64999999999999858, 76.00000000001213607, -136.5231074845242745 ) ) ;
#165796=CARTESIAN_POINT ( 'NONE',  ( -20.54999999999999716, 85.00000000001197975, -112.5170766071766764 ) ) ;
#165797=CARTESIAN_POINT ( 'NONE',  ( -20.94999999999999929, 64.35000000001195986, -109.8069731475024753 ) ) ;
#165824=AXIS2_PLACEMENT_3D ( 'NONE', #67025, #190861, #167435 ) ;
#165843=DIRECTION ( 'NONE',  ( 0.000000000000000000, 0.000000000000000000, 1.000000000000000000 ) ) ;
#165852=LINE ( 'NONE', #244076, #72238 ) ;
#165853=AXIS2_PLACEMENT_3D ( 'NONE', #178980, #177686, #17313 ) ;
#165874=EDGE_CURVE ( 'NONE', #231942, #213725, #255255, .T. ) ;
#165877=DIRECTION ( 'NONE',  ( -1.000000000000000000, 0.000000000000000000, 0.000000000000000000 ) ) ;
#165911=CARTESIAN_POINT ( 'NONE',  ( -20.54999999999999716, 74.00000000001199396, -116.2477294072864140 ) ) ;
#165923=VERTEX_POINT ( 'NONE', #132272 ) ;
#165941=ORIENTED_EDGE ( 'NONE', *, *, #227253, .T. ) ;
#165968=CARTESIAN_POINT ( 'NONE',  ( -22.50000000000000000, 76.00000000001213607, -136.5231074845242745 ) ) ;
#165982=CARTESIAN_POINT ( 'NONE',  ( -21.05000000000000071, 87.41227409416181615, -133.5231074845242176 ) ) ;
#165992=( BOUNDED_CURVE ( )  B_SPLINE_CURVE ( 3, ( #252218, #230097, #112726, #209247 ),
 .UNSPECIFIED., .F., .F. ) 
 B_SPLINE_CURVE_WITH_KNOTS ( ( 4, 4 ),
 ( 1.570796326794901665, 3.141592653589802886 ),
 .UNSPECIFIED. ) 
 CURVE ( )  GEOMETRIC_REPRESENTATION_ITEM ( )  RATIONAL_B_SPLINE_CURVE ( ( 1.000000000000000000, 0.8047378541243639383, 0.8047378541243639383, 1.000000000000000000 ) ) 
 REPRESENTATION_ITEM ( '' )  );
#166066=CIRCLE ( 'NONE', #53614, 0.09999999999999939493 ) ;
#166073=TOROIDAL_SURFACE ( 'NONE', #182825, 11.70000000000000107, 0.1000000000000000056 ) ;
#166074=CYLINDRICAL_SURFACE ( 'NONE', #213153, 0.09999999999999939493 ) ;
#166078=EDGE_CURVE ( 'NONE', #82680, #131402, #159554, .T. ) ;
#166090=DIRECTION ( 'NONE',  ( 0.000000000000000000, -6.982962677686266711E-15, 1.000000000000000000 ) ) ;
#166095=ORIENTED_EDGE ( 'NONE', *, *, #177290, .T. ) ;
#166101=CIRCLE ( 'NONE', #132768, 0.5000000000000004441 ) ;
#166103=CARTESIAN_POINT ( 'NONE',  ( 21.05000000000000071, 71.00000000001199396, -115.4283735034374274 ) ) ;
#166108=ORIENTED_EDGE ( 'NONE', *, *, #24502, .F. ) ;
#166153=EDGE_CURVE ( 'NONE', #98643, #242104, #116577, .T. ) ;
#166198=VECTOR ( 'NONE', #9213, 1000.000000000000000 ) ;
#166235=TOROIDAL_SURFACE ( 'NONE', #232862, 0.2000000000000000111, 0.1000000000000000056 ) ;
#166244=VECTOR ( 'NONE', #219259, 1000.000000000000000 ) ;
#166273=CARTESIAN_POINT ( 'NONE',  ( 20.95483826173899899, 67.12383379524210625, -127.9768319316248437 ) ) ;
#166310=EDGE_CURVE ( 'NONE', #216286, #14895, #215352, .T. ) ;
#166337=ORIENTED_EDGE ( 'NONE', *, *, #28911, .F. ) ;
#166353=ADVANCED_FACE ( 'NONE', ( #31621 ), #88301, .T. ) ;
#166355=CIRCLE ( 'NONE', #28996, 0.09999999999999976963 ) ;
#166358=AXIS2_PLACEMENT_3D ( 'NONE', #156187, #212300, #152340 ) ;
#166361=ADVANCED_FACE ( 'NONE', ( #96657 ), #155009, .T. ) ;
#166367=CARTESIAN_POINT ( 'NONE',  ( 18.59999999999999432, 74.83729825007408465, -128.4231074845243086 ) ) ;
#166388=DIRECTION ( 'NONE',  ( 0.000000000000000000, -1.565658005757035267E-14, 1.000000000000000000 ) ) ;
#166391=CARTESIAN_POINT ( 'NONE',  ( 23.14999999999999503, 64.35000000001221565, -148.2731074845243882 ) ) ;
#166398=CARTESIAN_POINT ( 'NONE',  ( -22.59999999999999787, 64.25043287652275126, -136.6239658536230763 ) ) ;
#166425=EDGE_CURVE ( 'NONE', #156311, #157579, #200933, .T. ) ;
#166440=DIRECTION ( 'NONE',  ( 1.000000000000000000, -0.000000000000000000, 0.000000000000000000 ) ) ;
#166441=CARTESIAN_POINT ( 'NONE',  ( -18.50000000000000000, 66.65000000001205649, -124.3731074845243683 ) ) ;
#166445=CIRCLE ( 'NONE', #108160, 7.720710678118692272 ) ;
#166472=EDGE_LOOP ( 'NONE', ( #198833, #141894, #83968 ) ) ;
#166503=DIRECTION ( 'NONE',  ( 0.000000000000000000, 6.982962677686266711E-15, -1.000000000000000000 ) ) ;
#166505=ADVANCED_FACE ( 'NONE', ( #40618 ), #38451, .T. ) ;
#166533=ORIENTED_EDGE ( 'NONE', *, *, #166631, .T. ) ;
#166534=VECTOR ( 'NONE', #4351, 1000.000000000000000 ) ;
#166569=CARTESIAN_POINT ( 'NONE',  ( -21.05000000000000071, 87.65000000001212754, -133.5231074845242176 ) ) ;
#166586=AXIS2_PLACEMENT_3D ( 'NONE', #65308, #144834, #22360 ) ;
#166631=EDGE_CURVE ( 'NONE', #171429, #121586, #184373, .T. ) ;
#166647=DIRECTION ( 'NONE',  ( -2.952720810173289605E-16, -1.000000000000000000, -7.086529944415894657E-15 ) ) ;
#166649=ORIENTED_EDGE ( 'NONE', *, *, #221347, .T. ) ;
#166684=ORIENTED_EDGE ( 'NONE', *, *, #99129, .F. ) ;
#166709=LINE ( 'NONE', #226633, #151927 ) ;
#166750=EDGE_LOOP ( 'NONE', ( #3816, #160314, #111976, #53985 ) ) ;
#166756=EDGE_CURVE ( 'NONE', #126916, #226829, #48275, .T. ) ;
#166795=CARTESIAN_POINT ( 'NONE',  ( -23.25000000000000000, 76.00000000001190870, -103.0231074845243029 ) ) ;
#166827=DIRECTION ( 'NONE',  ( 0.000000000000000000, 0.000000000000000000, 1.000000000000000000 ) ) ;
#166841=DIRECTION ( 'NONE',  ( 0.000000000000000000, -1.000000000000000000, -6.982962677686265922E-15 ) ) ;
#166847=EDGE_CURVE ( 'NONE', #14291, #16570, #195523, .T. ) ;
#166887=CARTESIAN_POINT ( 'NONE',  ( -18.41418431465367789, 85.50000000001210765, -96.42291809330278340 ) ) ;
#166904=EDGE_CURVE ( 'NONE', #86370, #8189, #117245, .T. ) ;
#166906=DIRECTION ( 'NONE',  ( -0.000000000000000000, 0.8700118002898356018, -0.4930308989875170078 ) ) ;
#166910=VECTOR ( 'NONE', #220260, 1000.000000000000000 ) ;
#166960=ORIENTED_EDGE ( 'NONE', *, *, #66518, .T. ) ;
#166987=LINE ( 'NONE', #89963, #9267 ) ;
#166994=CARTESIAN_POINT ( 'NONE',  ( -21.05000000000000071, 70.10000000001213039, -126.3040077198679398 ) ) ;
#166997=FACE_OUTER_BOUND ( 'NONE', #82760, .T. ) ;
#167006=CIRCLE ( 'NONE', #225197, 0.5000000000000004441 ) ;
#167070=EDGE_LOOP ( 'NONE', ( #32750, #3906, #96409, #112096 ) ) ;
#167089=FACE_OUTER_BOUND ( 'NONE', #174122, .T. ) ;
#167096=CIRCLE ( 'NONE', #17056, 0.1000000000000028644 ) ;
#167136=DIRECTION ( 'NONE',  ( 1.000000000000000000, 0.000000000000000000, 0.000000000000000000 ) ) ;
#167143=EDGE_LOOP ( 'NONE', ( #93886, #166649, #8419, #80263 ) ) ;
#167180=CIRCLE ( 'NONE', #204554, 0.09999999999999939493 ) ;
#167193=ORIENTED_EDGE ( 'NONE', *, *, #233088, .T. ) ;
#167203=ORIENTED_EDGE ( 'NONE', *, *, #142242, .F. ) ;
#167228=VERTEX_POINT ( 'NONE', #32288 ) ;
#167254=DIRECTION ( 'NONE',  ( -0.000000000000000000, 0.9875055080513808203, -0.1575844902526395142 ) ) ;
#167255=AXIS2_PLACEMENT_3D ( 'NONE', #40101, #20526, #98714 ) ;
#167260=DIRECTION ( 'NONE',  ( 0.000000000000000000, 0.000000000000000000, 1.000000000000000000 ) ) ;
#167270=DIRECTION ( 'NONE',  ( 0.000000000000000000, -8.717686153663073805E-15, 1.000000000000000000 ) ) ;
#167323=EDGE_LOOP ( 'NONE', ( #3277, #216613, #15140, #220462 ) ) ;
#167335=DIRECTION ( 'NONE',  ( -0.000000000000000000, 1.000000000000000000, 6.982962677686266711E-15 ) ) ;
#167364=ORIENTED_EDGE ( 'NONE', *, *, #150414, .T. ) ;
#167374=DIRECTION ( 'NONE',  ( 0.000000000000000000, -1.000000000000000000, -6.982962677686265922E-15 ) ) ;
#167382=CARTESIAN_POINT ( 'NONE',  ( -23.25000000000000000, 71.85000000001205933, -124.1731074845243228 ) ) ;
#167435=DIRECTION ( 'NONE',  ( -3.469446951953515108E-14, -1.000000000000000000, 0.000000000000000000 ) ) ;
#167436=ADVANCED_FACE ( 'NONE', ( #106323 ), #184597, .T. ) ;
#167449=FACE_OUTER_BOUND ( 'NONE', #24187, .T. ) ;
#167467=CARTESIAN_POINT ( 'NONE',  ( -21.05000000000000071, 74.14897176987119565, -124.8691942151018139 ) ) ;
#167476=DIRECTION ( 'NONE',  ( 0.000000000000000000, -1.000000000000000000, -6.982962677686266711E-15 ) ) ;
#167490=CARTESIAN_POINT ( 'NONE',  ( 23.24999999999999645, 71.00000000001199396, -115.4283735034374274 ) ) ;
#167514=CIRCLE ( 'NONE', #117612, 0.1000000000000028644 ) ;
#167522=CARTESIAN_POINT ( 'NONE',  ( 21.06089410995835109, 65.27470446788846914, -124.3207267534811677 ) ) ;
#167550=LINE ( 'NONE', #67136, #132767 ) ;
#167551=CARTESIAN_POINT ( 'NONE',  ( -23.15000000000000213, 71.65000000001207070, -124.2731074845243313 ) ) ;
#167560=DIRECTION ( 'NONE',  ( 1.000000000000000000, 0.000000000000000000, 0.000000000000000000 ) ) ;
#167574=EDGE_CURVE ( 'NONE', #47181, #3363, #255141, .T. ) ;
#167578=EDGE_CURVE ( 'NONE', #74752, #188576, #109436, .T. ) ;
#167593=AXIS2_PLACEMENT_3D ( 'NONE', #205924, #160416, #239936 ) ;
#167607=ORIENTED_EDGE ( 'NONE', *, *, #203822, .F. ) ;
#167616=CARTESIAN_POINT ( 'NONE',  ( -20.94999999999999929, 64.35000000001191722, -103.0231074845243882 ) ) ;
#167617=CARTESIAN_POINT ( 'NONE',  ( 21.05000000000000071, 71.00000000001205080, -124.1178414656112352 ) ) ;
#167678=LINE ( 'NONE', #85508, #60995 ) ;
#167681=ORIENTED_EDGE ( 'NONE', *, *, #130757, .T. ) ;
#167696=EDGE_CURVE ( 'NONE', #115956, #144144, #180202, .T. ) ;
#167708=DIRECTION ( 'NONE',  ( 1.000000000000000000, 0.000000000000000000, 0.000000000000000000 ) ) ;
#167758=ADVANCED_FACE ( 'NONE', ( #47015 ), #50861, .F. ) ;
#167774=DIRECTION ( 'NONE',  ( 1.000000000000000000, 0.000000000000000000, 0.000000000000000000 ) ) ;
#167832=CARTESIAN_POINT ( 'NONE',  ( -20.64999999999999858, 85.00000000001197975, -112.4170766071766678 ) ) ;
#167839=CARTESIAN_POINT ( 'NONE',  ( 23.25000000000000000, 87.75000000001222134, -148.2731074845242176 ) ) ;
#167857=AXIS2_PLACEMENT_3D ( 'NONE', #162758, #69757, #149298 ) ;
#167873=CARTESIAN_POINT ( 'NONE',  ( 20.85000000000000142, 76.00000000001190870, -103.0231074845243029 ) ) ;
#167910=ORIENTED_EDGE ( 'NONE', *, *, #168743, .T. ) ;
#167919=CARTESIAN_POINT ( 'NONE',  ( -21.13435531349801266, 69.50627893641960497, -136.5231074845243313 ) ) ;
#167944=ORIENTED_EDGE ( 'NONE', *, *, #50252, .F. ) ;
#167947=CIRCLE ( 'NONE', #147052, 0.09999999999998898659 ) ;
#167978=CARTESIAN_POINT ( 'NONE',  ( 22.49533356619859603, 64.34999999370803891, -136.5882300648470959 ) ) ;
#167993=ORIENTED_EDGE ( 'NONE', *, *, #18461, .F. ) ;
#168035=CARTESIAN_POINT ( 'NONE',  ( -20.64999999999999858, 76.00000000001213607, -136.5231074845242745 ) ) ;
#168042=DIRECTION ( 'NONE',  ( 0.000000000000000000, 0.000000000000000000, 1.000000000000000000 ) ) ;
#168044=AXIS2_PLACEMENT_3D ( 'NONE', #73357, #36805, #14665 ) ;
#168073=ORIENTED_EDGE ( 'NONE', *, *, #86116, .F. ) ;
#168155=AXIS2_PLACEMENT_3D ( 'NONE', #85454, #165031, #145453 ) ;
#168160=EDGE_LOOP ( 'NONE', ( #126561, #67367, #255083, #93237 ) ) ;
#168177=TOROIDAL_SURFACE ( 'NONE', #55650, 11.65000000000000036, 0.1000000000000000056 ) ;
#168227=ORIENTED_EDGE ( 'NONE', *, *, #92732, .T. ) ;
#168262=CARTESIAN_POINT ( 'NONE',  ( 20.94999999999999929, 77.36242903720516040, -95.13422623660308375 ) ) ;
#168273=CIRCLE ( 'NONE', #105656, 12.87499999999999822 ) ;
#168285=DIRECTION ( 'NONE',  ( 0.000000000000000000, 0.8660254037844420383, -0.4999999999999943379 ) ) ;
#168319=AXIS2_PLACEMENT_3D ( 'NONE', #120015, #222917, #83386 ) ;
#168321=ORIENTED_EDGE ( 'NONE', *, *, #99129, .T. ) ;
#168327=DIRECTION ( 'NONE',  ( -1.000000000000000000, -0.000000000000000000, -0.000000000000000000 ) ) ;
#168380=TOROIDAL_SURFACE ( 'NONE', #1717, 0.4000000000000012990, 0.1000000000000000056 ) ;
#168402=CARTESIAN_POINT ( 'NONE',  ( -20.85000000000000142, 77.16412189325305349, -95.10825939895268277 ) ) ;
#168423=AXIS2_PLACEMENT_3D ( 'NONE', #162638, #21839, #100053 ) ;
#168471=CARTESIAN_POINT ( 'NONE',  ( 18.53317502108576775, 65.67736539654941907, -97.46251168765718376 ) ) ;
#168504=ORIENTED_EDGE ( 'NONE', *, *, #207996, .T. ) ;
#168509=EDGE_CURVE ( 'NONE', #28335, #247013, #46880, .T. ) ;
#168544=EDGE_CURVE ( 'NONE', #13761, #197779, #116977, .T. ) ;
#168558=DIRECTION ( 'NONE',  ( 0.000000000000000000, 0.000000000000000000, -1.000000000000000000 ) ) ;
#168566=DIRECTION ( 'NONE',  ( -0.000000000000000000, -6.982962677686266711E-15, 1.000000000000000000 ) ) ;
#168596=DIRECTION ( 'NONE',  ( 0.000000000000000000, 6.982962677686266711E-15, -1.000000000000000000 ) ) ;
#168605=EDGE_LOOP ( 'NONE', ( #149118, #100461, #23817, #76173 ) ) ;
#168615=AXIS2_PLACEMENT_3D ( 'NONE', #70788, #190739, #30365 ) ;
#168653=ORIENTED_EDGE ( 'NONE', *, *, #122032, .F. ) ;
#168665=EDGE_LOOP ( 'NONE', ( #147312, #19391, #134957, #199605 ) ) ;
#168719=DIRECTION ( 'NONE',  ( 0.000000000000000000, 0.000000000000000000, 1.000000000000000000 ) ) ;
#168740=VECTOR ( 'NONE', #132478, 999.9999999999998863 ) ;
#168743=EDGE_CURVE ( 'NONE', #165923, #7536, #30339, .T. ) ;
#168768=ORIENTED_EDGE ( 'NONE', *, *, #205689, .F. ) ;
#168785=AXIS2_PLACEMENT_3D ( 'NONE', #131555, #89848, #251493 ) ;
#168828=DIRECTION ( 'NONE',  ( 0.000000000000000000, 0.000000000000000000, 1.000000000000000000 ) ) ;
#168833=CARTESIAN_POINT ( 'NONE',  ( 18.59999994388910238, 85.36356618708315125, -129.3419902477232029 ) ) ;
#168858=DIRECTION ( 'NONE',  ( -0.000000000000000000, 0.1298341882519953583, 0.9915357197604862671 ) ) ;
#168865=ORIENTED_EDGE ( 'NONE', *, *, #27840, .F. ) ;
#168885=EDGE_LOOP ( 'NONE', ( #202202, #175915, #161707, #236851, #88588, #140665, #250723, #72265, #155044, #5434, #191067, #232451 ) ) ;
#168920=VECTOR ( 'NONE', #60396, 1000.000000000000000 ) ;
#168946=CARTESIAN_POINT ( 'NONE',  ( -23.25000000000000000, 64.25000000001222134, -148.2731074845243882 ) ) ;
#168976=ORIENTED_EDGE ( 'NONE', *, *, #142265, .T. ) ;
#168985=VERTEX_POINT ( 'NONE', #95047 ) ;
#169026=CARTESIAN_POINT ( 'NONE',  ( -20.94999999999999929, 64.35000000001208775, -129.5083017138703667 ) ) ;
#169036=ORIENTED_EDGE ( 'NONE', *, *, #217114, .T. ) ;
#169051=DIRECTION ( 'NONE',  ( 1.000000000000000000, 0.000000000000000000, 0.000000000000000000 ) ) ;
#169055=CARTESIAN_POINT ( 'NONE',  ( 18.43709777086141344, 85.68240343348827537, -96.36626410711144786 ) ) ;
#169067=EDGE_CURVE ( 'NONE', #86736, #161343, #200567, .T. ) ;
#169074=DIRECTION ( 'NONE',  ( 0.000000000000000000, -1.000000000000000000, -6.982962677686265922E-15 ) ) ;
#169101=AXIS2_PLACEMENT_3D ( 'NONE', #117663, #39448, #141090 ) ;
#169102=DIRECTION ( 'NONE',  ( 0.000000000000000000, -1.000000000000000000, 0.000000000000000000 ) ) ;
#169114=CARTESIAN_POINT ( 'NONE',  ( -23.25000000000000000, 76.00000000001213607, -136.5231074845242745 ) ) ;
#169127=CARTESIAN_POINT ( 'NONE',  ( 23.14999999999999858, 76.00000000001213607, -136.5231074845242745 ) ) ;
#169132=ORIENTED_EDGE ( 'NONE', *, *, #180289, .F. ) ;
#169167=DIRECTION ( 'NONE',  ( 0.000000000000000000, 0.000000000000000000, -1.000000000000000000 ) ) ;
#169180=FACE_OUTER_BOUND ( 'NONE', #257659, .T. ) ;
#169196=CARTESIAN_POINT ( 'NONE',  ( -23.15000000000000213, 87.48912529308798014, -106.1231074845242262 ) ) ;
#169250=EDGE_LOOP ( 'NONE', ( #240965, #237919, #100129, #231061 ) ) ;
#169281=EDGE_LOOP ( 'NONE', ( #56432, #233069, #151539, #176647 ) ) ;
#169292=CIRCLE ( 'NONE', #252430, 0.1000000000000028644 ) ;
#169362=LINE ( 'NONE', #248860, #53605 ) ;
#169393=ORIENTED_EDGE ( 'NONE', *, *, #203602, .F. ) ;
#169401=CYLINDRICAL_SURFACE ( 'NONE', #105607, 0.09999999999998898659 ) ;
#169423=AXIS2_PLACEMENT_3D ( 'NONE', #123151, #218368, #243083 ) ;
#169434=CARTESIAN_POINT ( 'NONE',  ( -20.00857864376270001, 66.85000000001205933, -124.1731074845243512 ) ) ;
#169450=AXIS2_PLACEMENT_3D ( 'NONE', #214194, #237609, #137214 ) ;
#169451=ORIENTED_EDGE ( 'NONE', *, *, #257661, .F. ) ;
#169465=CIRCLE ( 'NONE', #223377, 0.6000000000000033085 ) ;
#169489=CYLINDRICAL_SURFACE ( 'NONE', #101432, 0.1000000000000033362 ) ;
#169490=DIRECTION ( 'NONE',  ( -1.000000000000000000, 2.952720810173289112E-16, 2.061873921506763405E-30 ) ) ;
#169607=ORIENTED_EDGE ( 'NONE', *, *, #129068, .T. ) ;
#169616=DIRECTION ( 'NONE',  ( 1.000000000000000000, 0.000000000000000000, 0.000000000000000000 ) ) ;
#169618=DIRECTION ( 'NONE',  ( 0.000000000000000000, 1.000000000000000000, 0.000000000000000000 ) ) ;
#169634=DIRECTION ( 'NONE',  ( 1.000000000000000000, 0.000000000000000000, 0.000000000000000000 ) ) ;
#169638=EDGE_LOOP ( 'NONE', ( #30975, #182536, #250203, #178735 ) ) ;
#169678=CARTESIAN_POINT ( 'NONE',  ( -20.54999999999999716, 87.75000000001205080, -124.1731074845242233 ) ) ;
#169681=ORIENTED_EDGE ( 'NONE', *, *, #248639, .F. ) ;
#169737=ORIENTED_EDGE ( 'NONE', *, *, #181317, .F. ) ;
#169747=EDGE_CURVE ( 'NONE', #88196, #59064, #172391, .T. ) ;
#169757=CIRCLE ( 'NONE', #107166, 0.09999999999999939493 ) ;
#169763=CARTESIAN_POINT ( 'NONE',  ( 20.94999999999999929, 84.66355140188112216, -112.5472086025915388 ) ) ;
#169767=FACE_OUTER_BOUND ( 'NONE', #18067, .T. ) ;
#169775=VECTOR ( 'NONE', #104929, 1000.000000000000000 ) ;
#169783=EDGE_CURVE ( 'NONE', #224224, #107664, #147997, .T. ) ;
#169827=AXIS2_PLACEMENT_3D ( 'NONE', #135409, #115865, #16784 ) ;
#169829=CARTESIAN_POINT ( 'NONE',  ( 18.58143601961975833, 65.56427058491767923, -111.7731074845243597 ) ) ;
#169849=ORIENTED_EDGE ( 'NONE', *, *, #120850, .F. ) ;
#169858=CARTESIAN_POINT ( 'NONE',  ( -20.94999999999999929, 75.74389420791992222, -136.5580039261965908 ) ) ;
#169864=CARTESIAN_POINT ( 'NONE',  ( -18.39999999999999858, 85.51932773110452501, -129.5501311079648872 ) ) ;
#169870=FACE_OUTER_BOUND ( 'NONE', #181130, .T. ) ;
#169902=CYLINDRICAL_SURFACE ( 'NONE', #108122, 0.1000000000000028644 ) ;
#169907=LINE ( 'NONE', #227251, #191433 ) ;
#169935=ORIENTED_EDGE ( 'NONE', *, *, #252306, .T. ) ;
#169939=CIRCLE ( 'NONE', #124121, 0.09999999999999739653 ) ;
#169957=DIRECTION ( 'NONE',  ( 0.000000000000000000, 0.000000000000000000, 1.000000000000000000 ) ) ;
#169984=ORIENTED_EDGE ( 'NONE', *, *, #150823, .T. ) ;
#170028=CIRCLE ( 'NONE', #57527, 4.000000000000003553 ) ;
#170037=DIRECTION ( 'NONE',  ( -1.000000000000000000, 0.000000000000000000, -0.000000000000000000 ) ) ;
#170040=CARTESIAN_POINT ( 'NONE',  ( -20.64999999999999858, 68.75000000001199396, -115.3731074845243540 ) ) ;
#170050=CIRCLE ( 'NONE', #203319, 0.1000000000000043771 ) ;
#170056=DIRECTION ( 'NONE',  ( -1.000000000000000000, 0.000000000000000000, 0.000000000000000000 ) ) ;
#170062=ORIENTED_EDGE ( 'NONE', *, *, #190076, .T. ) ;
#170100=ORIENTED_EDGE ( 'NONE', *, *, #201253, .F. ) ;
#170102=DIRECTION ( 'NONE',  ( 0.000000000000000000, -0.4999999999999689138, -0.8660254037844565822 ) ) ;
#170127=DIRECTION ( 'NONE',  ( 1.000000000000000000, -3.265361837132813093E-16, -2.280189983783949500E-30 ) ) ;
#170145=ORIENTED_EDGE ( 'NONE', *, *, #222706, .T. ) ;
#170151=CARTESIAN_POINT ( 'NONE',  ( 23.14999999999999503, 64.35000000001204512, -124.3731074845243825 ) ) ;
#170158=VERTEX_POINT ( 'NONE', #250627 ) ;
#170162=AXIS2_PLACEMENT_3D ( 'NONE', #26522, #106012, #212857 ) ;
#170215=CARTESIAN_POINT ( 'NONE',  ( 20.94999999999999574, 74.16465844978765176, -124.9679561919613207 ) ) ;
#170234=CARTESIAN_POINT ( 'NONE',  ( 20.85000000000000142, 77.83585931145546510, -91.51866831572576189 ) ) ;
#170257=DIRECTION ( 'NONE',  ( 1.000000000000000000, 0.000000000000000000, 0.000000000000000000 ) ) ;
#170261=EDGE_LOOP ( 'NONE', ( #247325, #179980, #2875, #93362, #116939, #133934, #171215, #117137, #169607, #111446, #99480 ) ) ;
#170263=CARTESIAN_POINT ( 'NONE',  ( -23.15000000000000213, 87.65000000001222702, -148.2731074845242176 ) ) ;
#170265=ORIENTED_EDGE ( 'NONE', *, *, #135274, .T. ) ;
#170295=ADVANCED_FACE ( 'NONE', ( #66870 ), #107271, .T. ) ;
#170304=DIRECTION ( 'NONE',  ( -1.000000000000000000, -0.000000000000000000, -0.000000000000000000 ) ) ;
#170334=EDGE_CURVE ( 'NONE', #158504, #94457, #160072, .T. ) ;
#170376=EDGE_LOOP ( 'NONE', ( #177223, #111040, #188070, #73999 ) ) ;
#170388=CARTESIAN_POINT ( 'NONE',  ( 22.57320508075688537, 64.35000000001214460, -136.5231074845243597 ) ) ;
#170419=CARTESIAN_POINT ( 'NONE',  ( -22.39999999999999858, 75.90000000001219860, -144.3138870828977076 ) ) ;
#170430=DIRECTION ( 'NONE',  ( 0.000000000000000000, 0.4999999999999088507, -0.8660254037844913322 ) ) ;
#170436=VECTOR ( 'NONE', #111033, 1000.000000000000000 ) ;
#170484=ORIENTED_EDGE ( 'NONE', *, *, #241913, .T. ) ;
#170505=DIRECTION ( 'NONE',  ( 0.000000000000000000, -6.982962677686266711E-15, 1.000000000000000000 ) ) ;
#170542=CIRCLE ( 'NONE', #8003, 12.77499999999999503 ) ;
#170569=CARTESIAN_POINT ( 'NONE',  ( -18.59999999999999787, 68.75000000001199396, -115.1731074845243512 ) ) ;
#170634=CARTESIAN_POINT ( 'NONE',  ( 23.24999999999999645, 73.90000000001190017, -103.0231074845243171 ) ) ;
#170653=DIRECTION ( 'NONE',  ( -1.000000000000000000, 3.265361837132813093E-16, 2.280189983783949500E-30 ) ) ;
#170664=CIRCLE ( 'NONE', #179028, 0.2000000000000057288 ) ;
#170666=EDGE_LOOP ( 'NONE', ( #208942, #111687, #223997, #223641 ) ) ;
#170696=CARTESIAN_POINT ( 'NONE',  ( -23.25000000000000000, 76.00000000001188027, -99.12310748452429721 ) ) ;
#170720=VERTEX_POINT ( 'NONE', #79044 ) ;
#170724=VECTOR ( 'NONE', #27602, 1000.000000000000114 ) ;
#170732=DIRECTION ( 'NONE',  ( 1.000000000000000000, 0.000000000000000000, 0.000000000000000000 ) ) ;
#170753=AXIS2_PLACEMENT_3D ( 'NONE', #8363, #128311, #147876 ) ;
#170757=ORIENTED_EDGE ( 'NONE', *, *, #225088, .F. ) ;
#170779=ORIENTED_EDGE ( 'NONE', *, *, #31941, .F. ) ;
#170795=VERTEX_POINT ( 'NONE', #205421 ) ;
#170844=CARTESIAN_POINT ( 'NONE',  ( 18.40916198585733454, 85.50000000001185185, -96.42291785270107596 ) ) ;
#170852=ADVANCED_FACE ( 'NONE', ( #86751 ), #244555, .F. ) ;
#170886=DIRECTION ( 'NONE',  ( -0.000000000000000000, 1.000000000000000000, 8.717686153663073805E-15 ) ) ;
#170896=VERTEX_POINT ( 'NONE', #145451 ) ;
#170965=CARTESIAN_POINT ( 'NONE',  ( -20.64999999999999858, 85.50000000001197975, -112.9170766071766820 ) ) ;
#170974=CARTESIAN_POINT ( 'NONE',  ( 18.49999999999999645, 77.86671491006937629, -124.7704322382422788 ) ) ;
#170978=CARTESIAN_POINT ( 'NONE',  ( 20.00000000000000355, 64.25000000001196554, -111.8731074845243825 ) ) ;
#171003=DIRECTION ( 'NONE',  ( -3.265361837132813093E-16, -1.000000000000000000, -7.086529944415894657E-15 ) ) ;
#171036=CARTESIAN_POINT ( 'NONE',  ( 18.58222699835054570, 65.66799936921529479, -97.42993998886008455 ) ) ;
#171043=ADVANCED_FACE ( 'NONE', ( #193585 ), #202117, .F. ) ;
#171049=EDGE_LOOP ( 'NONE', ( #92368, #186829, #179865, #59103, #73718, #91424, #67443, #188741 ) ) ;
#171062=TOROIDAL_SURFACE ( 'NONE', #100239, 0.4000000000000015210, 0.1000000000000000056 ) ;
#171073=ORIENTED_EDGE ( 'NONE', *, *, #167696, .T. ) ;
#171094=EDGE_CURVE ( 'NONE', #14889, #127805, #235409, .T. ) ;
#171097=ORIENTED_EDGE ( 'NONE', *, *, #26286, .T. ) ;
#171112=LINE ( 'NONE', #73280, #224537 ) ;
#171121=CIRCLE ( 'NONE', #87839, 0.09999999999998898659 ) ;
#171130=DIRECTION ( 'NONE',  ( 0.000000000000000000, 0.1455152366551500653, 0.9893560106964507384 ) ) ;
#171135=CARTESIAN_POINT ( 'NONE',  ( -20.94999999999999929, 87.65000000001212754, -133.4231074845242233 ) ) ;
#171152=ADVANCED_FACE ( 'NONE', ( #196144 ), #228359, .T. ) ;
#171159=FACE_OUTER_BOUND ( 'NONE', #149895, .T. ) ;
#171165=EDGE_CURVE ( 'NONE', #35302, #56619, #206394, .T. ) ;
#171177=DIRECTION ( 'NONE',  ( -1.000000000000000000, -0.000000000000000000, -0.000000000000000000 ) ) ;
#171207=CIRCLE ( 'NONE', #112896, 0.1000000000000026007 ) ;
#171208=CARTESIAN_POINT ( 'NONE',  ( -23.15000000000000213, 76.00000000001213607, -136.5231074845242745 ) ) ;
#171215=ORIENTED_EDGE ( 'NONE', *, *, #148288, .T. ) ;
#171221=CIRCLE ( 'NONE', #225311, 11.89999999999999325 ) ;
#171240=AXIS2_PLACEMENT_3D ( 'NONE', #105458, #224150, #242429 ) ;
#171253=CARTESIAN_POINT ( 'NONE',  ( -18.59999999999999787, 66.85000000001221565, -148.2731074845243597 ) ) ;
#171292=ORIENTED_EDGE ( 'NONE', *, *, #58095, .F. ) ;
#171327=CARTESIAN_POINT ( 'NONE',  ( -20.00857864376270001, 66.65000000001198543, -115.3731074845243683 ) ) ;
#171360=DIRECTION ( 'NONE',  ( 0.000000000000000000, -6.938893903907222067E-15, 1.000000000000000000 ) ) ;
#171370=ORIENTED_EDGE ( 'NONE', *, *, #168544, .F. ) ;
#171381=VECTOR ( 'NONE', #157451, 1000.000000000000000 ) ;
#171383=DIRECTION ( 'NONE',  ( 0.000000000000000000, -0.8660254037844387076, 0.4999999999999998335 ) ) ;
#171386=DIRECTION ( 'NONE',  ( 1.000000000000000000, 0.000000000000000000, 0.000000000000000000 ) ) ;
#171389=CARTESIAN_POINT ( 'NONE',  ( 22.00411653889219465, 75.90096189422516204, -143.7765503521648043 ) ) ;
#171402=DIRECTION ( 'NONE',  ( 1.000000000000000000, 0.000000000000000000, 0.000000000000000000 ) ) ;
#171426=LINE ( 'NONE', #21007, #43928 ) ;
#171429=VERTEX_POINT ( 'NONE', #126887 ) ;
#171438=EDGE_CURVE ( 'NONE', #61324, #149131, #2359, .T. ) ;
#171456=DIRECTION ( 'NONE',  ( -0.000000000000000000, 0.2605042016806385363, 0.9654727137038795481 ) ) ;
#171467=FACE_OUTER_BOUND ( 'NONE', #5559, .T. ) ;
#171519=CARTESIAN_POINT ( 'NONE',  ( -23.15000000000000213, 64.35000000001205933, -124.3731074845243825 ) ) ;
#171538=DIRECTION ( 'NONE',  ( 0.000000000000000000, 0.4999999999999088507, -0.8660254037844913322 ) ) ;
#171550=AXIS2_PLACEMENT_3D ( 'NONE', #152734, #210124, #52292 ) ;
#171596=ORIENTED_EDGE ( 'NONE', *, *, #95569, .T. ) ;
#171615=LINE ( 'NONE', #192432, #256015 ) ;
#171618=CARTESIAN_POINT ( 'NONE',  ( 18.58719872626880587, 85.56664439761047447, -96.20062928812723158 ) ) ;
#171634=EDGE_CURVE ( 'NONE', #56953, #164631, #202483, .T. ) ;
#171636=VECTOR ( 'NONE', #188862, 1000.000000000000000 ) ;
#171651=DIRECTION ( 'NONE',  ( 1.000000000000000000, 0.000000000000000000, 0.000000000000000000 ) ) ;
#171656=CARTESIAN_POINT ( 'NONE',  ( 21.05000000000000071, 70.15000000001211333, -126.3906102602463619 ) ) ;
#171686=SHAPE_REPRESENTATION ( 'Injection Molded Chain Links 13', ( #2425 ), #164577 ) ;
#171712=ORIENTED_EDGE ( 'NONE', *, *, #157105, .T. ) ;
#171715=CARTESIAN_POINT ( 'NONE',  ( -21.04386569057497525, 64.25000000001236344, -109.8802701327446130 ) ) ;
#171733=ORIENTED_EDGE ( 'NONE', *, *, #243030, .T. ) ;
#171735=DIRECTION ( 'NONE',  ( 0.000000000000000000, -0.9908441862701605762, -0.1350103645451835310 ) ) ;
#171736=DIRECTION ( 'NONE',  ( -1.000000000000000000, 0.000000000000000000, -0.000000000000000000 ) ) ;
#171770=AXIS2_PLACEMENT_3D ( 'NONE', #108957, #146792, #223768 ) ;
#171800=AXIS2_PLACEMENT_3D ( 'NONE', #7101, #61960, #86620 ) ;
#171835=CARTESIAN_POINT ( 'NONE',  ( 23.24999999999999289, 69.45000000001199680, -115.1731074845243512 ) ) ;
#171837=CARTESIAN_POINT ( 'NONE',  ( 21.14999999999999858, 76.00000000001219291, -143.0637644362255401 ) ) ;
#171859=CARTESIAN_POINT ( 'NONE',  ( -18.59999999999999787, 77.26327546522911405, -95.12124281777788326 ) ) ;
#171876=EDGE_LOOP ( 'NONE', ( #231558, #80512, #201802, #144101, #190798, #230891, #88849 ) ) ;
#171928=DIRECTION ( 'NONE',  ( 0.000000000000000000, 0.1350103645451807555, 0.9908441862701609093 ) ) ;
#171980=EDGE_LOOP ( 'NONE', ( #107869, #18740, #71786, #96250 ) ) ;
#171999=LINE ( 'NONE', #228090, #38424 ) ;
#172010=ORIENTED_EDGE ( 'NONE', *, *, #75132, .T. ) ;
#172044=ORIENTED_EDGE ( 'NONE', *, *, #248985, .F. ) ;
#172047=ADVANCED_FACE ( 'NONE', ( #218947 ), #121181, .T. ) ;
#172048=VERTEX_POINT ( 'NONE', #203243 ) ;
#172082=DIRECTION ( 'NONE',  ( 0.000000000000000000, 1.000000000000000000, 6.853228547068871147E-15 ) ) ;
#172099=EDGE_CURVE ( 'NONE', #243260, #86736, #94317, .T. ) ;
#172117=CARTESIAN_POINT ( 'NONE',  ( 18.58725287972292506, 85.56662691070332016, -96.20060267875838633 ) ) ;
#172130=ORIENTED_EDGE ( 'NONE', *, *, #69153, .F. ) ;
#172131=CARTESIAN_POINT ( 'NONE',  ( -20.85000000000000142, 77.73670573947940454, -91.50568489690056140 ) ) ;
#172132=ORIENTED_EDGE ( 'NONE', *, *, #221548, .T. ) ;
#172147=ORIENTED_EDGE ( 'NONE', *, *, #42418, .F. ) ;
#172160=ORIENTED_EDGE ( 'NONE', *, *, #70962, .T. ) ;
#172163=VECTOR ( 'NONE', #129667, 1000.000000000000000 ) ;
#172192=AXIS2_PLACEMENT_3D ( 'NONE', #216599, #37993, #21000 ) ;
#172299=CARTESIAN_POINT ( 'NONE',  ( 21.05000000000000071, 65.39167043205810614, -128.9314224712280179 ) ) ;
#172315=VERTEX_POINT ( 'NONE', #96114 ) ;
#172374=DIRECTION ( 'NONE',  ( 1.000000000000000000, 0.000000000000000000, 0.000000000000000000 ) ) ;
#172382=ADVANCED_FACE ( 'NONE', ( #16616 ), #256954, .T. ) ;
#172384=DIRECTION ( 'NONE',  ( 0.7071067811865475727, -0.7071067811865475727, -5.142139384388981164E-15 ) ) ;
#172391=CIRCLE ( 'NONE', #93216, 4.000000000000003553 ) ;
#172425=ORIENTED_EDGE ( 'NONE', *, *, #62259, .T. ) ;
#172460=ORIENTED_EDGE ( 'NONE', *, *, #12626, .F. ) ;
#172472=LINE ( 'NONE', #94158, #146604 ) ;
#172490=CIRCLE ( 'NONE', #18316, 3.900000000000000799 ) ;
#172491=EDGE_CURVE ( 'NONE', #147024, #220397, #190399, .T. ) ;
#172498=CARTESIAN_POINT ( 'NONE',  ( -21.09610168723073542, 69.62104428478737361, -136.5566969914158051 ) ) ;
#172533=DIRECTION ( 'NONE',  ( 1.000000000000000000, 0.000000000000000000, 0.000000000000000000 ) ) ;
#172579=FACE_OUTER_BOUND ( 'NONE', #60487, .T. ) ;
#172624=VECTOR ( 'NONE', #22045, 1000.000000000000000 ) ;
#172626=DIRECTION ( 'NONE',  ( 1.836970198721029934E-16, 1.000000000000000000, 6.982962677686266711E-15 ) ) ;
#172630=DIRECTION ( 'NONE',  ( -1.000000000000000000, 0.000000000000000000, -0.000000000000000000 ) ) ;
#172650=LINE ( 'NONE', #34396, #119982 ) ;
#172651=CARTESIAN_POINT ( 'NONE',  ( -18.59999999999999787, 77.83585931145546510, -91.41866831572575336 ) ) ;
#172678=CARTESIAN_POINT ( 'NONE',  ( 21.04999999999999716, 65.37127968600771055, -124.3731074845243540 ) ) ;
#172701=SPHERICAL_SURFACE ( 'NONE', #63779, 0.1000000000000000056 ) ;
#172720=EDGE_CURVE ( 'NONE', #112369, #156851, #202462, .T. ) ;
#172733=CIRCLE ( 'NONE', #135254, 0.1000000000000028644 ) ;
#172734=ORIENTED_EDGE ( 'NONE', *, *, #150642, .T. ) ;
#172754=EDGE_CURVE ( 'NONE', #224952, #14895, #219969, .T. ) ;
#172791=DIRECTION ( 'NONE',  ( 0.000000000000000000, 0.000000000000000000, 1.000000000000000000 ) ) ;
#172797=ORIENTED_EDGE ( 'NONE', *, *, #250955, .F. ) ;
#172806=EDGE_CURVE ( 'NONE', #18434, #94251, #64892, .T. ) ;
#172821=DIRECTION ( 'NONE',  ( -1.000000000000000000, 0.000000000000000000, 0.000000000000000000 ) ) ;
#172832=PLANE ( 'NONE',  #39685 ) ;
#172850=CIRCLE ( 'NONE', #35467, 0.09999999999999939493 ) ;
#172858=( BOUNDED_SURFACE ( )  B_SPLINE_SURFACE ( 3, 2, ( 
 ( #126174, #203156, #84444 ),
 ( #167919, #64922, #207015 ),
 ( #165320, #244841, #87035 ),
 ( #162769, #246144, #147020 ),
 ( #66222, #204429, #23271 ),
 ( #45368, #63644, #67493 ) ),
 .UNSPECIFIED., .F., .F., .F. ) 
 B_SPLINE_SURFACE_WITH_KNOTS ( ( 4, 2, 4 ),
 ( 3, 3 ),
 ( 0.0001300404313046710908, 0.0003183318589266637198, 0.0005066232865486563217 ),
 ( 0.000000000000000000, 1.000000000000000000 ),
 .UNSPECIFIED. ) 
 GEOMETRIC_REPRESENTATION_ITEM ( )  RATIONAL_B_SPLINE_SURFACE ( (
 ( 1.000000000000000000, 0.7071067811865475727, 1.000000000000000000),
 ( 1.000000000000000000, 0.7625113560541042501, 1.000000000000000000),
 ( 1.000000000000000000, 0.8126073484687571513, 1.000000000000000000),
 ( 1.000000000000000000, 0.8923049332733655747, 1.000000000000000000),
 ( 1.000000000000000000, 0.9231914937768425089, 1.000000000000000000),
 ( 1.000000000000000000, 0.9238795325112945100, 1.000000000000000000) ) ) 
 REPRESENTATION_ITEM ( '' )  SURFACE ( )  );
#172923=CARTESIAN_POINT ( 'NONE',  ( -18.59999999999999787, 66.75000000001199396, -115.2731074845243597 ) ) ;
#172943=CARTESIAN_POINT ( 'NONE',  ( -18.50000000000000000, 64.35000000001205933, -124.3731074845243825 ) ) ;
#172956=TOROIDAL_SURFACE ( 'NONE', #231371, 12.97499999999999787, 0.1000000000000000056 ) ;
#172966=AXIS2_PLACEMENT_3D ( 'NONE', #83482, #23589, #6542 ) ;
#172986=VERTEX_POINT ( 'NONE', #141947 ) ;
#172999=EDGE_LOOP ( 'NONE', ( #216380, #179486, #88087, #70998 ) ) ;
#173003=CARTESIAN_POINT ( 'NONE',  ( -23.15000000000000213, 73.50000000001205080, -123.2984855617622202 ) ) ;
#173012=CARTESIAN_POINT ( 'NONE',  ( -20.96077737575320654, 64.37609936600745186, -109.8823155274178163 ) ) ;
#173057=CIRCLE ( 'NONE', #131497, 4.000000000000003553 ) ;
#173073=DIRECTION ( 'NONE',  ( 0.000000000000000000, 0.000000000000000000, -1.000000000000000000 ) ) ;
#173098=CARTESIAN_POINT ( 'NONE',  ( 21.14999999999999858, 69.74218538953603286, -136.6208977758331287 ) ) ;
#173105=CIRCLE ( 'NONE', #60607, 0.1000000000000028644 ) ;
#173122=ADVANCED_FACE ( 'NONE', ( #212215 ), #113099, .T. ) ;
#173126=EDGE_LOOP ( 'NONE', ( #247707, #77624, #253819, #55798 ) ) ;
#173128=CARTESIAN_POINT ( 'NONE',  ( -21.05000000000000071, 74.75000000001207923, -128.5231074845243029 ) ) ;
#173193=AXIS2_PLACEMENT_3D ( 'NONE', #50698, #89842, #128995 ) ;
#173199=( NAMED_UNIT ( * ) PLANE_ANGLE_UNIT ( ) SI_UNIT ( $, .RADIAN. ) );
#173211=AXIS2_PLACEMENT_3D ( 'NONE', #66685, #212303, #207495 ) ;
#173219=DIRECTION ( 'NONE',  ( 1.000000000000000000, 0.000000000000000000, 0.000000000000000000 ) ) ;
#173227=DIRECTION ( 'NONE',  ( 0.000000000000000000, -0.01562499999996560217, -0.9998779222360102414 ) ) ;
#173248=EDGE_CURVE ( 'NONE', #196564, #87303, #81768, .T. ) ;
#173289=AXIS2_PLACEMENT_3D ( 'NONE', #251656, #11794, #233405 ) ;
#173290=AXIS2_PLACEMENT_3D ( 'NONE', #46678, #221454, #81928 ) ;
#173298=CARTESIAN_POINT ( 'NONE',  ( -20.85000000000000142, 87.65000000001192859, -105.9231074845242091 ) ) ;
#173331=CYLINDRICAL_SURFACE ( 'NONE', #215939, 0.1000000000000046685 ) ;
#173377=CARTESIAN_POINT ( 'NONE',  ( 23.14999999999998437, 76.00000000001213607, -136.5231074845242745 ) ) ;
#173410=CARTESIAN_POINT ( 'NONE',  ( 18.54271179734060127, 85.62408429011072997, -96.28214263182411514 ) ) ;
#173423=ORIENTED_EDGE ( 'NONE', *, *, #71642, .T. ) ;
#173438=AXIS2_PLACEMENT_3D ( 'NONE', #209620, #28458, #8855 ) ;
#173456=DIRECTION ( 'NONE',  ( 0.000000000000000000, 6.982962677686266711E-15, -1.000000000000000000 ) ) ;
#173489=AXIS2_PLACEMENT_3D ( 'NONE', #196164, #18806, #157058 ) ;
#173491=AXIS2_PLACEMENT_3D ( 'NONE', #37903, #133133, #193116 ) ;
#173514=EDGE_LOOP ( 'NONE', ( #46876, #78406, #23867, #114357, #232195 ) ) ;
#173544=DIRECTION ( 'NONE',  ( 0.000000000000000000, -0.9274965247785504907, -0.3738317757009320674 ) ) ;
#173557=EDGE_CURVE ( 'NONE', #213725, #152168, #48690, .T. ) ;
#173558=DIRECTION ( 'NONE',  ( 0.000000000000000000, 1.000000000000000000, 7.116814260417668513E-15 ) ) ;
#173566=( BOUNDED_SURFACE ( )  B_SPLINE_SURFACE ( 3, 2, ( 
 ( #130933, #172678, #188340 ),
 ( #52667, #132218, #112662 ),
 ( #192211, #87927, #167522 ),
 ( #27582, #125363, #147489 ),
 ( #88773, #182779, #206180 ),
 ( #244005, #7991, #65379 ) ),
 .UNSPECIFIED., .F., .F., .F. ) 
 B_SPLINE_SURFACE_WITH_KNOTS ( ( 4, 2, 4 ),
 ( 3, 3 ),
 ( 0.0001342700090130014186, 0.0002909192928057377698, 0.0004475685765984741210 ),
 ( 0.000000000000000000, 1.000000000000000000 ),
 .UNSPECIFIED. ) 
 GEOMETRIC_REPRESENTATION_ITEM ( )  RATIONAL_B_SPLINE_SURFACE ( (
 ( 1.000000000000000000, 0.7250110520819876836, 1.000000000000000000),
 ( 1.000000000000000000, 0.7257599279135071857, 1.000000000000000000),
 ( 1.000000000000000000, 0.7137594617282845277, 1.000000000000000000),
 ( 1.000000000000000000, 0.6959270178810901264, 1.000000000000000000),
 ( 1.000000000000000000, 0.6919879549338453506, 1.000000000000000000),
 ( 1.000000000000000000, 0.7071067811865494601, 1.000000000000000000) ) ) 
 REPRESENTATION_ITEM ( '' )  SURFACE ( )  );
#173573=FACE_OUTER_BOUND ( 'NONE', #110471, .T. ) ;
#173592=ORIENTED_EDGE ( 'NONE', *, *, #99609, .T. ) ;
#173597=CYLINDRICAL_SURFACE ( 'NONE', #15034, 0.1000000000000028644 ) ;
#173599=CIRCLE ( 'NONE', #148432, 0.1000000000000028644 ) ;
#173653=ADVANCED_FACE ( 'NONE', ( #44507 ), #122769, .F. ) ;
#173656=ORIENTED_EDGE ( 'NONE', *, *, #44114, .F. ) ;
#173714=FACE_OUTER_BOUND ( 'NONE', #89447, .T. ) ;
#173730=CARTESIAN_POINT ( 'NONE',  ( 20.95325940946048249, 65.47660992931579926, -128.9586453552842897 ) ) ;
#173744=VECTOR ( 'NONE', #72065, 1000.000000000000000 ) ;
#173751=AXIS2_PLACEMENT_3D ( 'NONE', #12942, #11650, #209837 ) ;
#173761=DIRECTION ( 'NONE',  ( 0.000000000000000000, 0.000000000000000000, -1.000000000000000000 ) ) ;
#173766=CIRCLE ( 'NONE', #23896, 0.09999999999998898659 ) ;
#173769=DIRECTION ( 'NONE',  ( 0.000000000000000000, 0.000000000000000000, 1.000000000000000000 ) ) ;
#173780=DIRECTION ( 'NONE',  ( 0.000000000000000000, 0.000000000000000000, 1.000000000000000000 ) ) ;
#173792=CARTESIAN_POINT ( 'NONE',  ( -21.95218792049438861, 75.90097156021228386, -143.7246150457709746 ) ) ;
#173810=CARTESIAN_POINT ( 'NONE',  ( 18.42555734704284731, 85.49715836194880580, -129.4832769867893205 ) ) ;
#173860=PLANE ( 'NONE',  #88803 ) ;
#173866=EDGE_LOOP ( 'NONE', ( #55649, #118988, #173656, #111205 ) ) ;
#173871=DIRECTION ( 'NONE',  ( 0.000000000000000000, 0.8660254037844419273, -0.4999999999999942824 ) ) ;
#173878=DIRECTION ( 'NONE',  ( 1.000000000000000000, 0.000000000000000000, 0.000000000000000000 ) ) ;
#173897=VERTEX_POINT ( 'NONE', #233424 ) ;
#173935=FACE_OUTER_BOUND ( 'NONE', #69132, .T. ) ;
#173980=VERTEX_POINT ( 'NONE', #161589 ) ;
#173988=ORIENTED_EDGE ( 'NONE', *, *, #2031, .T. ) ;
#174001=EDGE_LOOP ( 'NONE', ( #95795, #179935, #11327, #19216 ) ) ;
#174003=ORIENTED_EDGE ( 'NONE', *, *, #43926, .F. ) ;
#174004=ORIENTED_EDGE ( 'NONE', *, *, #20214, .F. ) ;
#174048=CARTESIAN_POINT ( 'NONE',  ( -23.25000000000000000, 64.25000000001206502, -124.3731074845243825 ) ) ;
#174057=VECTOR ( 'NONE', #188231, 1000.000000000000000 ) ;
#174059=CARTESIAN_POINT ( 'NONE',  ( -18.36527282681991124, 85.50000060000968460, -96.10095852002184813 ) ) ;
#174077=VERTEX_POINT ( 'NONE', #222803 ) ;
#174089=EDGE_CURVE ( 'NONE', #15679, #107177, #95069, .T. ) ;
#174101=AXIS2_PLACEMENT_3D ( 'NONE', #122272, #218783, #118432 ) ;
#174120=AXIS2_PLACEMENT_3D ( 'NONE', #90371, #70852, #51223 ) ;
#174122=EDGE_LOOP ( 'NONE', ( #105888, #154114, #1403, #149712 ) ) ;
#174123=FACE_OUTER_BOUND ( 'NONE', #214127, .T. ) ;
#174134=CIRCLE ( 'NONE', #99240, 0.1000000000000028644 ) ;
#174181=DIRECTION ( 'NONE',  ( -0.000000000000000000, 1.000000000000000000, 6.982962677686266711E-15 ) ) ;
#174195=CIRCLE ( 'NONE', #49245, 0.1000000000000028644 ) ;
#174205=CARTESIAN_POINT ( 'NONE',  ( 20.85000000000000142, 77.73670573947940454, -91.50568489690056140 ) ) ;
#174206=ADVANCED_FACE ( 'NONE', ( #132719 ), #229255, .T. ) ;
#174255=ORIENTED_EDGE ( 'NONE', *, *, #138600, .F. ) ;
#174265=ORIENTED_EDGE ( 'NONE', *, *, #164322, .F. ) ;
#174269=ORIENTED_EDGE ( 'NONE', *, *, #243030, .F. ) ;
#174284=ORIENTED_EDGE ( 'NONE', *, *, #124699, .T. ) ;
#174322=AXIS2_PLACEMENT_3D ( 'NONE', #65092, #164208, #222873 ) ;
#174349=SPHERICAL_SURFACE ( 'NONE', #208560, 0.1000000000000000056 ) ;
#174359=ORIENTED_EDGE ( 'NONE', *, *, #20520, .F. ) ;
#174367=DIRECTION ( 'NONE',  ( 0.000000000000000000, -6.982962677686266711E-15, 1.000000000000000000 ) ) ;
#174398=VERTEX_POINT ( 'NONE', #863 ) ;
#174402=EDGE_CURVE ( 'NONE', #127492, #140147, #194842, .T. ) ;
#174408=CARTESIAN_POINT ( 'NONE',  ( 21.05000000000000071, 67.12338541492499644, -128.1380270056797031 ) ) ;
#174420=DIRECTION ( 'NONE',  ( 0.000000000000000000, -6.982962677686266711E-15, 1.000000000000000000 ) ) ;
#174445=CARTESIAN_POINT ( 'NONE',  ( 21.05000000000000071, 87.48912529308798014, -106.1231074845242262 ) ) ;
#174453=CIRCLE ( 'NONE', #49500, 0.1000000000000028644 ) ;
#174455=EDGE_CURVE ( 'NONE', #56953, #194835, #202940, .T. ) ;
#174457=AXIS2_PLACEMENT_3D ( 'NONE', #128916, #209734, #132782 ) ;
#174498=VECTOR ( 'NONE', #71189, 1000.000000000000000 ) ;
#174510=CYLINDRICAL_SURFACE ( 'NONE', #223615, 0.1000000000000028644 ) ;
#174511=CIRCLE ( 'NONE', #37100, 0.1000000000000028644 ) ;
#174542=ORIENTED_EDGE ( 'NONE', *, *, #101475, .F. ) ;
#174558=ORIENTED_EDGE ( 'NONE', *, *, #12864, .T. ) ;
#174578=EDGE_CURVE ( 'NONE', #80026, #216286, #195019, .T. ) ;
#174594=DIRECTION ( 'NONE',  ( 0.000000000000000000, -0.4930308989875575865, -0.8700118002898125091 ) ) ;
#174657=DIRECTION ( 'NONE',  ( 0.000000000000000000, 0.000000000000000000, 1.000000000000000000 ) ) ;
#174739=DIRECTION ( 'NONE',  ( 0.000000000000000000, -6.982962677686266711E-15, 1.000000000000000000 ) ) ;
#174743=EDGE_LOOP ( 'NONE', ( #156654, #172132, #113469, #55961 ) ) ;
#174765=DIRECTION ( 'NONE',  ( 0.000000000000000000, 0.000000000000000000, 1.000000000000000000 ) ) ;
#174777=AXIS2_PLACEMENT_3D ( 'NONE', #166391, #25574, #201626 ) ;
#174818=VERTEX_POINT ( 'NONE', #155828 ) ;
#174853=CARTESIAN_POINT ( 'NONE',  ( -23.25000000000000000, 76.00000000001210765, -132.4731074845242915 ) ) ;
#174898=VECTOR ( 'NONE', #11699, 1000.000000000000000 ) ;
#174924=EDGE_CURVE ( 'NONE', #15448, #105294, #143936, .T. ) ;
#174927=CIRCLE ( 'NONE', #41622, 12.97499999999999964 ) ;
#175020=LINE ( 'NONE', #233670, #18181 ) ;
#175041=EDGE_CURVE ( 'NONE', #18414, #221149, #48683, .T. ) ;
#175051=DIRECTION ( 'NONE',  ( 0.000000000000000000, -0.6728971962617102953, -0.7397360091702507301 ) ) ;
#175057=AXIS2_PLACEMENT_3D ( 'NONE', #53651, #229720, #112354 ) ;
#175061=DIRECTION ( 'NONE',  ( 1.000000000000000000, 0.000000000000000000, 0.000000000000000000 ) ) ;
#175079=ORIENTED_EDGE ( 'NONE', *, *, #121669, .F. ) ;
#175093=CARTESIAN_POINT ( 'NONE',  ( 20.94999999999999574, 64.37928932189329601, -109.8915241368653284 ) ) ;
#175099=CARTESIAN_POINT ( 'NONE',  ( -18.59999999999999787, 77.85161776048073534, -91.41991776492061206 ) ) ;
#175168=ORIENTED_EDGE ( 'NONE', *, *, #123858, .F. ) ;
#175172=DIRECTION ( 'NONE',  ( -1.000000000000000000, -0.000000000000000000, -0.000000000000000000 ) ) ;
#175176=ADVANCED_FACE ( 'NONE', ( #77230 ), #24512, .F. ) ;
#175178=CARTESIAN_POINT ( 'NONE',  ( 23.14999999999999858, 76.00000000001190870, -103.0231074845243029 ) ) ;
#175183=CARTESIAN_POINT ( 'NONE',  ( 20.30531438145591139, 65.90309893892202808, -128.7270896772505466 ) ) ;
#175191=CARTESIAN_POINT ( 'NONE',  ( 21.04999999999999716, 64.25000000001195133, -109.8647081744214375 ) ) ;
#175235=ORIENTED_EDGE ( 'NONE', *, *, #171094, .T. ) ;
#175253=CARTESIAN_POINT ( 'NONE',  ( 18.42595409746874680, 85.49999981257707304, -129.5237451327773215 ) ) ;
#175259=CARTESIAN_POINT ( 'NONE',  ( -20.94999999999999929, 87.48912529308798014, -106.1231074845242262 ) ) ;
#175262=EDGE_LOOP ( 'NONE', ( #182006, #252472, #219665, #25709, #52380, #180021 ) ) ;
#175286=VECTOR ( 'NONE', #233415, 1000.000000000000000 ) ;
#175313=EDGE_CURVE ( 'NONE', #38011, #226695, #45526, .T. ) ;
#175319=CIRCLE ( 'NONE', #62864, 0.09999999999999939493 ) ;
#175323=CARTESIAN_POINT ( 'NONE',  ( 20.94999999999999574, 87.41227409416181615, -133.6231074845242119 ) ) ;
#175329=CARTESIAN_POINT ( 'NONE',  ( -18.43459694179558639, 85.49421012500988581, -96.40610228186316988 ) ) ;
#175370=DIRECTION ( 'NONE',  ( 0.000000000000000000, 0.000000000000000000, -1.000000000000000000 ) ) ;
#175371=CARTESIAN_POINT ( 'NONE',  ( 21.04999999999999361, 76.01759718702061264, -142.9638783781856830 ) ) ;
#175381=DIRECTION ( 'NONE',  ( 0.000000000000000000, -0.1575844902526687130, -0.9875055080513762684 ) ) ;
#175482=DIRECTION ( 'NONE',  ( -3.469446951953995998E-14, 0.000000000000000000, -1.000000000000000000 ) ) ;
#175486=AXIS2_PLACEMENT_3D ( 'NONE', #5697, #27896, #44855 ) ;
#175521=FACE_OUTER_BOUND ( 'NONE', #121436, .T. ) ;
#175558=EDGE_LOOP ( 'NONE', ( #175733, #188284, #243265, #143527 ) ) ;
#175566=VECTOR ( 'NONE', #248661, 1000.000000000000114 ) ;
#175570=FACE_OUTER_BOUND ( 'NONE', #37691, .T. ) ;
#175608=VERTEX_POINT ( 'NONE', #92017 ) ;
#175657=CARTESIAN_POINT ( 'NONE',  ( -23.15000000000000213, 76.00000000001190870, -103.0231074845243029 ) ) ;
#175699=TOROIDAL_SURFACE ( 'NONE', #238391, 0.2000000000000000111, 0.1000000000000000056 ) ;
#175708=EDGE_CURVE ( 'NONE', #70203, #197443, #112357, .T. ) ;
#175724=CARTESIAN_POINT ( 'NONE',  ( 21.04999999999908411, 67.22371710472138773, -124.3651984818718574 ) ) ;
#175733=ORIENTED_EDGE ( 'NONE', *, *, #186952, .F. ) ;
#175738=CARTESIAN_POINT ( 'NONE',  ( 18.59999999999999076, 65.79142135624930177, -115.1731074845243796 ) ) ;
#175745=CYLINDRICAL_SURFACE ( 'NONE', #242075, 0.09999999999999939493 ) ;
#175758=FACE_OUTER_BOUND ( 'NONE', #167323, .T. ) ;
#175789=CARTESIAN_POINT ( 'NONE',  ( 20.95512820512820440, 67.12384868372393498, -124.3731074845243683 ) ) ;
#175813=DIRECTION ( 'NONE',  ( -1.000000000000000000, 0.000000000000000000, -0.000000000000000000 ) ) ;
#175838=CYLINDRICAL_SURFACE ( 'NONE', #238033, 0.09999999999999976963 ) ;
#175860=DIRECTION ( 'NONE',  ( 0.000000000000000000, 0.9893560106964510714, -0.1455152366551481502 ) ) ;
#175879=AXIS2_PLACEMENT_3D ( 'NONE', #74696, #233739, #134599 ) ;
#175895=ORIENTED_EDGE ( 'NONE', *, *, #230443, .F. ) ;
#175910=CIRCLE ( 'NONE', #121913, 11.70000000000000284 ) ;
#175915=ORIENTED_EDGE ( 'NONE', *, *, #63221, .T. ) ;
#175951=CARTESIAN_POINT ( 'NONE',  ( 18.33683296300528198, 85.51114997114476068, -96.11740007181523993 ) ) ;
#175966=ORIENTED_EDGE ( 'NONE', *, *, #103332, .T. ) ;
#175998=CARTESIAN_POINT ( 'NONE',  ( 23.25000000000000000, 87.65000000001221281, -148.2731074845242176 ) ) ;
#176012=CIRCLE ( 'NONE', #146911, 0.09999999999999939493 ) ;
#176033=CARTESIAN_POINT ( 'NONE',  ( -23.15000000000000213, 64.35000000001198828, -115.2731074845243739 ) ) ;
#176066=ORIENTED_EDGE ( 'NONE', *, *, #206427, .F. ) ;
#176071=CIRCLE ( 'NONE', #134325, 0.1000000000000028644 ) ;
#176084=PLANE ( 'NONE',  #97816 ) ;
#176156=AXIS2_PLACEMENT_3D ( 'NONE', #251466, #166841, #147235 ) ;
#176166=CARTESIAN_POINT ( 'NONE',  ( -21.05000000000000071, 64.37928932189343811, -129.6546908321833484 ) ) ;
#176178=DIRECTION ( 'NONE',  ( 1.000000000000000000, -3.265361837132813093E-16, -2.280189983783949500E-30 ) ) ;
#176186=EDGE_LOOP ( 'NONE', ( #29316, #186077, #34219, #26101 ) ) ;
#176228=AXIS2_PLACEMENT_3D ( 'NONE', #110099, #28033, #184491 ) ;
#176256=AXIS2_PLACEMENT_3D ( 'NONE', #71345, #191307, #150858 ) ;
#176263=VERTEX_POINT ( 'NONE', #56906 ) ;
#176274=CARTESIAN_POINT ( 'NONE',  ( -20.64999999999999858, 84.66355140188112216, -112.5472086025915388 ) ) ;
#176279=CARTESIAN_POINT ( 'NONE',  ( 21.04999999999999716, 76.08561306081617204, -142.9368672183345552 ) ) ;
#176281=AXIS2_PLACEMENT_3D ( 'NONE', #85327, #141472, #164898 ) ;
#176293=( NAMED_UNIT ( * ) SI_UNIT ( $, .STERADIAN. ) SOLID_ANGLE_UNIT ( ) );
#176312=ORIENTED_EDGE ( 'NONE', *, *, #189619, .F. ) ;
#176326=EDGE_CURVE ( 'NONE', #58209, #66400, #16685, .T. ) ;
#176329=ORIENTED_EDGE ( 'NONE', *, *, #237813, .F. ) ;
#176343=ORIENTED_EDGE ( 'NONE', *, *, #207996, .F. ) ;
#176363=EDGE_CURVE ( 'NONE', #152762, #74814, #88026, .T. ) ;
#176367=AXIS2_PLACEMENT_3D ( 'NONE', #238695, #237417, #138287 ) ;
#176381=CYLINDRICAL_SURFACE ( 'NONE', #227319, 0.09999999999999939493 ) ;
#176389=ORIENTED_EDGE ( 'NONE', *, *, #167578, .F. ) ;
#176390=CARTESIAN_POINT ( 'NONE',  ( 23.14999999999999503, 64.25000000001195133, -110.0379132551783243 ) ) ;
#176439=EDGE_CURVE ( 'NONE', #127497, #148843, #208215, .T. ) ;
#176447=CARTESIAN_POINT ( 'NONE',  ( 21.05000000000000071, 64.25000000001195133, -110.0379132551783243 ) ) ;
#176474=SPHERICAL_SURFACE ( 'NONE', #43351, 0.1000000000000000056 ) ;
#176478=EDGE_CURVE ( 'NONE', #22276, #193833, #8525, .T. ) ;
#176490=FACE_OUTER_BOUND ( 'NONE', #19370, .T. ) ;
#176522=LINE ( 'NONE', #158269, #168920 ) ;
#176523=ORIENTED_EDGE ( 'NONE', *, *, #44465, .T. ) ;
#176524=CARTESIAN_POINT ( 'NONE',  ( -21.14999999999999858, 64.25000000001210765, -129.7392418215462158 ) ) ;
#176530=VECTOR ( 'NONE', #164030, 1000.000000000000000 ) ;
#176538=EDGE_LOOP ( 'NONE', ( #37605, #139368, #189757, #41247 ) ) ;
#176543=EDGE_LOOP ( 'NONE', ( #198959, #43863, #47338, #116108 ) ) ;
#176548=ORIENTED_EDGE ( 'NONE', *, *, #189692, .F. ) ;
#176564=CARTESIAN_POINT ( 'NONE',  ( -23.15000000000000213, 64.25000000001195133, -109.8647081744214375 ) ) ;
#176574=CIRCLE ( 'NONE', #9956, 0.1000000000000028644 ) ;
#176597=( BOUNDED_CURVE ( )  B_SPLINE_CURVE ( 3, ( #176524, #72282, #151833, #52691 ),
 .UNSPECIFIED., .F., .F. ) 
 B_SPLINE_CURVE_WITH_KNOTS ( ( 4, 4 ),
 ( 1.570796326794895448, 3.141592653589791784 ),
 .UNSPECIFIED. ) 
 CURVE ( )  GEOMETRIC_REPRESENTATION_ITEM ( )  RATIONAL_B_SPLINE_CURVE ( ( 1.000000000000000000, 0.8047378541243650485, 0.8047378541243650485, 1.000000000000000000 ) ) 
 REPRESENTATION_ITEM ( '' )  );
#176603=CARTESIAN_POINT ( 'NONE',  ( -18.37151313414566545, 85.57101412579110900, -96.20644457528561588 ) ) ;
#176622=DIRECTION ( 'NONE',  ( -1.000000000000000000, 0.000000000000000000, 0.000000000000000000 ) ) ;
#176624=ADVANCED_FACE ( 'NONE', ( #117577 ), #188199, .F. ) ;
#176647=ORIENTED_EDGE ( 'NONE', *, *, #175708, .T. ) ;
#176648=CARTESIAN_POINT ( 'NONE',  ( 20.85000000000000142, 77.75000000001182343, -91.40415744590204383 ) ) ;
#176655=EDGE_CURVE ( 'NONE', #242065, #239290, #134018, .T. ) ;
#176657=DIRECTION ( 'NONE',  ( -0.000000000000000000, 0.1350103645451835865, 0.9908441862701605762 ) ) ;
#176676=DIRECTION ( 'NONE',  ( -1.000000000000000000, 0.000000000000000000, 0.000000000000000000 ) ) ;
#176684=DIRECTION ( 'NONE',  ( 0.000000000000000000, 0.000000000000000000, -1.000000000000000000 ) ) ;
#176698=DIRECTION ( 'NONE',  ( 0.000000000000000000, -6.982962677686266711E-15, 1.000000000000000000 ) ) ;
#176702=AXIS2_PLACEMENT_3D ( 'NONE', #105264, #68756, #86995 ) ;
#176707=ORIENTED_EDGE ( 'NONE', *, *, #68793, .F. ) ;
#176761=PLANE ( 'NONE',  #57485 ) ;
#176782=CARTESIAN_POINT ( 'NONE',  ( -20.94999999999999929, 74.16465844978765176, -124.9679561919613207 ) ) ;
#176789=EDGE_CURVE ( 'NONE', #122058, #206647, #125290, .T. ) ;
#176795=ORIENTED_EDGE ( 'NONE', *, *, #87811, .F. ) ;
#176802=CARTESIAN_POINT ( 'NONE',  ( -18.59999999999999787, 77.16412189325305349, -95.10825939895268277 ) ) ;
#176814=ORIENTED_EDGE ( 'NONE', *, *, #6391, .F. ) ;
#176815=FACE_OUTER_BOUND ( 'NONE', #21915, .T. ) ;
#176827=DIRECTION ( 'NONE',  ( 0.000000000000000000, -6.982962677686266711E-15, 1.000000000000000000 ) ) ;
#176848=ORIENTED_EDGE ( 'NONE', *, *, #98695, .F. ) ;
#176889=DIRECTION ( 'NONE',  ( -0.000000000000000000, 6.982962677686266711E-15, -1.000000000000000000 ) ) ;
#176893=ORIENTED_EDGE ( 'NONE', *, *, #42483, .T. ) ;
#176914=DIRECTION ( 'NONE',  ( 0.000000000000000000, 0.000000000000000000, 1.000000000000000000 ) ) ;
#176947=AXIS2_PLACEMENT_3D ( 'NONE', #156301, #18033, #98816 ) ;
#176981=EDGE_CURVE ( 'NONE', #22494, #164329, #55074, .T. ) ;
#176995=VERTEX_POINT ( 'NONE', #20763 ) ;
#177047=DIRECTION ( 'NONE',  ( -1.000000000000000000, 0.000000000000000000, -0.000000000000000000 ) ) ;
#177075=DIRECTION ( 'NONE',  ( 1.000000000000000000, 7.304098846218105085E-16, 4.217023435051677501E-16 ) ) ;
#177079=CARTESIAN_POINT ( 'NONE',  ( 21.13461538461538325, 67.11458296203758778, -124.2731074845243597 ) ) ;
#177154=CIRCLE ( 'NONE', #222896, 0.09999999999998708533 ) ;
#177223=ORIENTED_EDGE ( 'NONE', *, *, #197709, .F. ) ;
#177224=ORIENTED_EDGE ( 'NONE', *, *, #6391, .T. ) ;
#177257=FACE_OUTER_BOUND ( 'NONE', #100758, .T. ) ;
#177282=CIRCLE ( 'NONE', #214641, 0.1000000000000028644 ) ;
#177290=EDGE_CURVE ( 'NONE', #34419, #82189, #28137, .T. ) ;
#177320=ORIENTED_EDGE ( 'NONE', *, *, #189619, .T. ) ;
#177356=CIRCLE ( 'NONE', #152220, 4.299999999999970512 ) ;
#177372=EDGE_LOOP ( 'NONE', ( #4437, #51714, #138998, #193244 ) ) ;
#177386=EDGE_CURVE ( 'NONE', #165923, #220397, #94733, .T. ) ;
#177389=AXIS2_PLACEMENT_3D ( 'NONE', #83854, #81296, #121768 ) ;
#177401=FACE_OUTER_BOUND ( 'NONE', #240362, .T. ) ;
#177416=VERTEX_POINT ( 'NONE', #182082 ) ;
#177458=DIRECTION ( 'NONE',  ( 0.000000000000000000, 0.000000000000000000, 1.000000000000000000 ) ) ;
#177503=EDGE_CURVE ( 'NONE', #241360, #57517, #219631, .T. ) ;
#177518=VERTEX_POINT ( 'NONE', #205474 ) ;
#177519=FACE_OUTER_BOUND ( 'NONE', #244042, .T. ) ;
#177561=DIRECTION ( 'NONE',  ( -1.000000000000000000, 2.952720810173289112E-16, 2.061873921506763405E-30 ) ) ;
#177587=CYLINDRICAL_SURFACE ( 'NONE', #82110, 0.09999999999999939493 ) ;
#177593=PRESENTATION_STYLE_ASSIGNMENT (( #38066 ) ) ;
#177645=DIRECTION ( 'NONE',  ( -3.265361837132813093E-16, -1.000000000000000000, -6.982962677686266711E-15 ) ) ;
#177657=AXIS2_PLACEMENT_3D ( 'NONE', #118332, #197845, #137860 ) ;
#177686=DIRECTION ( 'NONE',  ( -1.000000000000000000, 0.000000000000000000, -0.000000000000000000 ) ) ;
#177730=DIRECTION ( 'NONE',  ( 1.000000000000000000, -2.952720810173289112E-16, -2.061873921506763405E-30 ) ) ;
#177763=CARTESIAN_POINT ( 'NONE',  ( -18.49719636458551264, 85.44636535924043130, -129.4514936146411799 ) ) ;
#177766=ADVANCED_FACE ( 'NONE', ( #18831 ), #140131, .T. ) ;
#177767=AXIS2_PLACEMENT_3D ( 'NONE', #200615, #203172, #61097 ) ;
#177795=ORIENTED_EDGE ( 'NONE', *, *, #210680, .T. ) ;
#177803=EDGE_CURVE ( 'NONE', #247369, #129910, #52649, .T. ) ;
#177821=EDGE_CURVE ( 'NONE', #140961, #102291, #224726, .T. ) ;
#177829=ORIENTED_EDGE ( 'NONE', *, *, #246622, .T. ) ;
#177840=DIRECTION ( 'NONE',  ( 0.000000000000000000, 0.000000000000000000, 1.000000000000000000 ) ) ;
#177880=CARTESIAN_POINT ( 'NONE',  ( -20.99142135623731065, 64.40000000001194280, -109.9513107147998880 ) ) ;
#177882=CARTESIAN_POINT ( 'NONE',  ( -18.52309608778508832, 85.64247632006711797, -96.30851114335470697 ) ) ;
#177907=ORIENTED_EDGE ( 'NONE', *, *, #121669, .T. ) ;
#177923=CARTESIAN_POINT ( 'NONE',  ( 21.05000000000000071, 76.09999993531927487, -143.0011857056192639 ) ) ;
#177966=ORIENTED_EDGE ( 'NONE', *, *, #233088, .F. ) ;
#178059=EDGE_LOOP ( 'NONE', ( #175079, #122822, #112624, #123884 ) ) ;
#178067=CIRCLE ( 'NONE', #111413, 0.1000000000000028644 ) ;
#178106=EDGE_CURVE ( 'NONE', #230546, #254598, #140309, .T. ) ;
#178123=ORIENTED_EDGE ( 'NONE', *, *, #220577, .F. ) ;
#178155=AXIS2_PLACEMENT_3D ( 'NONE', #39715, #119235, #21435 ) ;
#178188=AXIS2_PLACEMENT_3D ( 'NONE', #189797, #75009, #133665 ) ;
#178197=DIRECTION ( 'NONE',  ( 1.000000000000000000, 0.000000000000000000, 0.000000000000000000 ) ) ;
#178206=DIRECTION ( 'NONE',  ( 0.000000000000000000, -0.9998779222360104635, -0.01562499999996343723 ) ) ;
#178219=ORIENTED_EDGE ( 'NONE', *, *, #154906, .F. ) ;
#178231=ORIENTED_EDGE ( 'NONE', *, *, #30374, .T. ) ;
#178244=CARTESIAN_POINT ( 'NONE',  ( -20.54999999999999716, 68.85000000001205933, -124.1731074845243370 ) ) ;
#178247=FACE_OUTER_BOUND ( 'NONE', #188410, .T. ) ;
#178286=CARTESIAN_POINT ( 'NONE',  ( 20.95512820512820440, 67.12384868372393498, -124.3229346253956038 ) ) ;
#178289=DIRECTION ( 'NONE',  ( 0.000000000000000000, -0.9654727137038715545, 0.2605042016806676242 ) ) ;
#178332=CARTESIAN_POINT ( 'NONE',  ( 23.14999999999999858, 71.00000000001205080, -124.1178414656112352 ) ) ;
#178339=EDGE_CURVE ( 'NONE', #220552, #136488, #15454, .T. ) ;
#178348=ORIENTED_EDGE ( 'NONE', *, *, #149847, .T. ) ;
#178352=AXIS2_PLACEMENT_3D ( 'NONE', #232363, #195806, #231079 ) ;
#178384=CARTESIAN_POINT ( 'NONE',  ( -18.59999999999999787, 74.16465844978765176, -124.9679561919613207 ) ) ;
#178390=EDGE_CURVE ( 'NONE', #86933, #162629, #2764, .T. ) ;
#178401=FACE_OUTER_BOUND ( 'NONE', #141205, .T. ) ;
#178402=AXIS2_PLACEMENT_3D ( 'NONE', #87702, #224653, #8200 ) ;
#178459=DIRECTION ( 'NONE',  ( 0.000000000000000000, 0.9915357197604862671, -0.1298341882519953583 ) ) ;
#178486=CARTESIAN_POINT ( 'NONE',  ( 18.49999999999999645, 76.00000000001190870, -103.0231074845243029 ) ) ;
#178519=CARTESIAN_POINT ( 'NONE',  ( -18.50000000000000000, 64.35000000001205933, -124.2731074845243882 ) ) ;
#178522=AXIS2_PLACEMENT_3D ( 'NONE', #238702, #202149, #100444 ) ;
#178552=EDGE_CURVE ( 'NONE', #105294, #192091, #90438, .T. ) ;
#178556=ADVANCED_FACE ( 'NONE', ( #120886 ), #202951, .T. ) ;
#178587=FACE_OUTER_BOUND ( 'NONE', #168160, .T. ) ;
#178588=CARTESIAN_POINT ( 'NONE',  ( 20.94999999999999929, 76.00000000001213607, -136.5231074845242745 ) ) ;
#178603=ORIENTED_EDGE ( 'NONE', *, *, #5338, .T. ) ;
#178623=CARTESIAN_POINT ( 'NONE',  ( -22.44366136229477249, 75.99065843052615321, -148.1728260419982064 ) ) ;
#178640=CARTESIAN_POINT ( 'NONE',  ( -22.50000000000000000, 64.25000000001215028, -136.5231074845243597 ) ) ;
#178650=ADVANCED_FACE ( 'NONE', ( #247211 ), #69891, .T. ) ;
#178653=AXIS2_PLACEMENT_3D ( 'NONE', #22979, #199021, #179476 ) ;
#178711=CARTESIAN_POINT ( 'NONE',  ( -20.94999999999999929, 77.25000000001209344, -128.5231074845242745 ) ) ;
#178725=EDGE_CURVE ( 'NONE', #145261, #217224, #111567, .T. ) ;
#178730=TOROIDAL_SURFACE ( 'NONE', #62171, 11.70000000000000107, 0.1000000000000000056 ) ;
#178735=ORIENTED_EDGE ( 'NONE', *, *, #148218, .F. ) ;
#178747=ADVANCED_FACE ( 'NONE', ( #51551 ), #251057, .T. ) ;
#178751=CARTESIAN_POINT ( 'NONE',  ( 21.05000000000000071, 77.16270174995010223, -128.4231074845242802 ) ) ;
#178773=VERTEX_POINT ( 'NONE', #214503 ) ;
#178790=ORIENTED_EDGE ( 'NONE', *, *, #160611, .T. ) ;
#178804=VERTEX_POINT ( 'NONE', #232817 ) ;
#178855=AXIS2_PLACEMENT_3D ( 'NONE', #30954, #70074, #53044 ) ;
#178862=CARTESIAN_POINT ( 'NONE',  ( 21.05000000000000426, 75.93429838969011314, -142.7814235418563271 ) ) ;
#178902=ADVANCED_FACE ( 'NONE', ( #236631 ), #140701, .F. ) ;
#178908=CIRCLE ( 'NONE', #95639, 0.09999999999999939493 ) ;
#178916=ORIENTED_EDGE ( 'NONE', *, *, #76235, .F. ) ;
#178922=CARTESIAN_POINT ( 'NONE',  ( -18.53317502108577131, 65.67736539654943329, -97.46251168765716955 ) ) ;
#178927=ORIENTED_EDGE ( 'NONE', *, *, #256871, .T. ) ;
#178945=EDGE_CURVE ( 'NONE', #76954, #43436, #3148, .T. ) ;
#178967=FACE_OUTER_BOUND ( 'NONE', #251215, .T. ) ;
#178972=PLANE ( 'NONE',  #132453 ) ;
#178980=CARTESIAN_POINT ( 'NONE',  ( -20.54999999999999716, 76.00000000001190870, -103.0231074845243029 ) ) ;
#178987=EDGE_CURVE ( 'NONE', #172986, #14889, #85238, .T. ) ;
#179006=ORIENTED_EDGE ( 'NONE', *, *, #64611, .F. ) ;
#179021=ORIENTED_EDGE ( 'NONE', *, *, #14881, .T. ) ;
#179028=AXIS2_PLACEMENT_3D ( 'NONE', #20760, #179832, #35209 ) ;
#179029=EDGE_LOOP ( 'NONE', ( #242881, #26485, #2755, #169737, #54858 ) ) ;
#179036=EDGE_CURVE ( 'NONE', #219596, #19771, #86528, .T. ) ;
#179045=ADVANCED_BREP_SHAPE_REPRESENTATION ( '', ( #26097, #2425 ), #164577 ) ;
#179053=CARTESIAN_POINT ( 'NONE',  ( -22.50000000000000000, 64.35000000001214460, -136.5231074845243597 ) ) ;
#179093=ORIENTED_EDGE ( 'NONE', *, *, #125702, .T. ) ;
#179114=CARTESIAN_POINT ( 'NONE',  ( 21.05000000000000071, 76.00000000001189449, -101.0231074845243029 ) ) ;
#179148=EDGE_CURVE ( 'NONE', #8640, #199333, #249053, .T. ) ;
#179171=ORIENTED_EDGE ( 'NONE', *, *, #23764, .F. ) ;
#179185=CARTESIAN_POINT ( 'NONE',  ( -23.25000000000000000, 64.35000000001198828, -115.1731074845243938 ) ) ;
#179212=ORIENTED_EDGE ( 'NONE', *, *, #92427, .T. ) ;
#179219=DIRECTION ( 'NONE',  ( 0.000000000000000000, -6.454785026890406770E-15, 1.000000000000000000 ) ) ;
#179232=CARTESIAN_POINT ( 'NONE',  ( 21.07928932188134397, 75.90110485435778287, -142.8516241409176075 ) ) ;
#179252=ADVANCED_FACE ( 'NONE', ( #98080 ), #57688, .T. ) ;
#179271=ADVANCED_FACE ( 'NONE', ( #181526 ), #190806, .F. ) ;
#179274=DIRECTION ( 'NONE',  ( 0.000000000000000000, 6.982962677686266711E-15, -1.000000000000000000 ) ) ;
#179282=CIRCLE ( 'NONE', #37625, 0.1000000000000026007 ) ;
#179294=CARTESIAN_POINT ( 'NONE',  ( 21.05000000000000071, 76.00000000001188027, -99.02310748452428868 ) ) ;
#179330=ORIENTED_EDGE ( 'NONE', *, *, #247066, .F. ) ;
#179377=CIRCLE ( 'NONE', #212694, 0.2000000000000057288 ) ;
#179391=AXIS2_PLACEMENT_3D ( 'NONE', #180538, #241779, #81388 ) ;
#179393=DIRECTION ( 'NONE',  ( 0.000000000000000000, 0.000000000000000000, -1.000000000000000000 ) ) ;
#179420=DIRECTION ( 'NONE',  ( 0.000000000000000000, 0.000000000000000000, 1.000000000000000000 ) ) ;
#179448=AXIS2_PLACEMENT_3D ( 'NONE', #136509, #80376, #75307 ) ;
#179450=ORIENTED_EDGE ( 'NONE', *, *, #194553, .F. ) ;
#179473=CARTESIAN_POINT ( 'NONE',  ( -20.54999999999999716, 68.75000000001199396, -115.3731074845243540 ) ) ;
#179476=DIRECTION ( 'NONE',  ( 0.000000000000000000, 0.000000000000000000, 1.000000000000000000 ) ) ;
#179480=AXIS2_PLACEMENT_3D ( 'NONE', #187420, #145695, #205669 ) ;
#179482=ORIENTED_EDGE ( 'NONE', *, *, #15983, .T. ) ;
#179486=ORIENTED_EDGE ( 'NONE', *, *, #132277, .T. ) ;
#179496=EDGE_LOOP ( 'NONE', ( #135193, #214504, #99577, #18248 ) ) ;
#179544=CARTESIAN_POINT ( 'NONE',  ( 19.97071067811865319, 64.27928932189330169, -111.8145288407616817 ) ) ;
#179551=CYLINDRICAL_SURFACE ( 'NONE', #21065, 11.80000000000000426 ) ;
#179572=ADVANCED_FACE ( 'NONE', ( #92666 ), #73146, .F. ) ;
#179580=DIRECTION ( 'NONE',  ( -0.7071067811865475727, 0.7071067811865475727, 4.937700262164531476E-15 ) ) ;
#179594=DIRECTION ( 'NONE',  ( 0.000000000000000000, -7.056502275159890832E-15, 1.000000000000000000 ) ) ;
#179611=CIRCLE ( 'NONE', #33713, 11.80000000000000426 ) ;
#179667=DIRECTION ( 'NONE',  ( -1.000000000000000000, -0.000000000000000000, -0.000000000000000000 ) ) ;
#179668=ORIENTED_EDGE ( 'NONE', *, *, #80030, .F. ) ;
#179728=CARTESIAN_POINT ( 'NONE',  ( 21.05000000000000071, 85.00000000001197975, -112.9170766071766820 ) ) ;
#179738=ORIENTED_EDGE ( 'NONE', *, *, #154906, .T. ) ;
#179740=CYLINDRICAL_SURFACE ( 'NONE', #202386, 0.09999999999999939493 ) ;
#179801=CARTESIAN_POINT ( 'NONE',  ( -18.59999999999999787, 66.65000000001198543, -115.1731074845243654 ) ) ;
#179832=DIRECTION ( 'NONE',  ( 1.000000000000000000, 0.000000000000000000, 0.000000000000000000 ) ) ;
#179836=ORIENTED_EDGE ( 'NONE', *, *, #47655, .T. ) ;
#179851=LINE ( 'NONE', #256748, #166910 ) ;
#179865=ORIENTED_EDGE ( 'NONE', *, *, #192850, .T. ) ;
#179866=EDGE_CURVE ( 'NONE', #69624, #60014, #91184, .T. ) ;
#179869=CARTESIAN_POINT ( 'NONE',  ( 18.39999999999999858, 85.50000000001209344, -129.4910380878245633 ) ) ;
#179880=EDGE_CURVE ( 'NONE', #121418, #194615, #132889, .T. ) ;
#179893=CARTESIAN_POINT ( 'NONE',  ( -22.49756042579671700, 75.92195366299505110, -148.1729724456266410 ) ) ;
#179909=PLANE ( 'NONE',  #23769 ) ;
#179935=ORIENTED_EDGE ( 'NONE', *, *, #101725, .T. ) ;
#179970=AXIS2_PLACEMENT_3D ( 'NONE', #107975, #164102, #6286 ) ;
#179974=CARTESIAN_POINT ( 'NONE',  ( 21.08035267497491105, 69.66829316022912622, -136.6057961093004849 ) ) ;
#179980=ORIENTED_EDGE ( 'NONE', *, *, #41723, .T. ) ;
#179991=EDGE_CURVE ( 'NONE', #122858, #60637, #69787, .T. ) ;
#179997=CARTESIAN_POINT ( 'NONE',  ( 22.49436431346199683, 64.35004905235869899, -136.5900110142466417 ) ) ;
#180002=FACE_OUTER_BOUND ( 'NONE', #52283, .T. ) ;
#180021=ORIENTED_EDGE ( 'NONE', *, *, #67663, .F. ) ;
#180035=AXIS2_PLACEMENT_3D ( 'NONE', #191137, #252350, #128572 ) ;
#180068=EDGE_CURVE ( 'NONE', #196564, #159137, #103809, .T. ) ;
#180077=EDGE_LOOP ( 'NONE', ( #208894, #236057, #96940, #251039 ) ) ;
#180082=EDGE_CURVE ( 'NONE', #22794, #7849, #241228, .T. ) ;
#180103=ORIENTED_EDGE ( 'NONE', *, *, #242615, .F. ) ;
#180136=SURFACE_STYLE_FILL_AREA ( #60158 ) ;
#180153=ORIENTED_EDGE ( 'NONE', *, *, #176478, .F. ) ;
#180159=DIRECTION ( 'NONE',  ( -0.7071067811865475727, 0.7071067811865475727, 4.937700262164531476E-15 ) ) ;
#180164=DIRECTION ( 'NONE',  ( 0.000000000000000000, -7.056502275159890832E-15, 1.000000000000000000 ) ) ;
#180192=CARTESIAN_POINT ( 'NONE',  ( -20.94999999999999929, 64.35000000001191722, -103.0231074845243882 ) ) ;
#180202=CIRCLE ( 'NONE', #38729, 0.1000000000000064587 ) ;
#180221=CARTESIAN_POINT ( 'NONE',  ( 22.49999999999999645, 75.89914163091350474, -148.2726746080136877 ) ) ;
#180289=EDGE_CURVE ( 'NONE', #25668, #221833, #41496, .T. ) ;
#180356=ADVANCED_FACE ( 'NONE', ( #130717 ), #169902, .F. ) ;
#180360=CARTESIAN_POINT ( 'NONE',  ( 18.59999999999999076, 65.79142135624930177, -115.1731074845243796 ) ) ;
#180368=DIRECTION ( 'NONE',  ( 0.000000000000000000, 0.000000000000000000, 1.000000000000000000 ) ) ;
#180370=CARTESIAN_POINT ( 'NONE',  ( -21.05000000000000071, 74.16465844978765176, -124.9679561919613207 ) ) ;
#180372=CARTESIAN_POINT ( 'NONE',  ( 23.14999999999999858, 76.00000000001213607, -136.5231074845242745 ) ) ;
#180386=CARTESIAN_POINT ( 'NONE',  ( -23.25000000000000000, 76.00000000001190870, -103.0231074845243029 ) ) ;
#180387=ORIENTED_EDGE ( 'NONE', *, *, #172099, .T. ) ;
#180394=ORIENTED_EDGE ( 'NONE', *, *, #231951, .T. ) ;
#180403=EDGE_CURVE ( 'NONE', #47601, #228369, #183143, .T. ) ;
#180431=DIRECTION ( 'NONE',  ( 1.000000000000000000, 0.000000000000000000, 0.000000000000000000 ) ) ;
#180506=VERTEX_POINT ( 'NONE', #82274 ) ;
#180522=MECHANICAL_DESIGN_GEOMETRIC_PRESENTATION_REPRESENTATION('',(#184605),#43153);
#180523=DIRECTION ( 'NONE',  ( 0.000000000000000000, 0.000000000000000000, -1.000000000000000000 ) ) ;
#180530=EDGE_LOOP ( 'NONE', ( #231692, #105840, #222113, #233636, #46350, #237044, #160157, #239306 ) ) ;
#180538=CARTESIAN_POINT ( 'NONE',  ( -23.15000000000000213, 71.65000000001199965, -115.3731074845243256 ) ) ;
#180568=CARTESIAN_POINT ( 'NONE',  ( -23.25000000000000000, 87.65000000001192859, -106.0231074845242176 ) ) ;
#180573=ORIENTED_EDGE ( 'NONE', *, *, #198084, .F. ) ;
#180575=DIRECTION ( 'NONE',  ( 0.000000000000000000, -7.086529944415894657E-15, 1.000000000000000000 ) ) ;
#180602=CARTESIAN_POINT ( 'NONE',  ( 21.14999999999999858, 64.35000000001214460, -136.4231074845243938 ) ) ;
#180607=CARTESIAN_POINT ( 'NONE',  ( 21.05000000000000071, 74.63912941282003999, -128.4501095574333647 ) ) ;
#180622=EDGE_CURVE ( 'NONE', #255696, #207631, #112408, .T. ) ;
#180647=LINE ( 'NONE', #231344, #51306 ) ;
#180682=EDGE_CURVE ( 'NONE', #177416, #250872, #211246, .T. ) ;
#180694=VECTOR ( 'NONE', #221399, 1000.000000000000000 ) ;
#180695=EDGE_CURVE ( 'NONE', #61013, #237888, #224808, .T. ) ;
#180717=CARTESIAN_POINT ( 'NONE',  ( -21.15000000000000213, 76.00000000001219291, -143.0637644362255401 ) ) ;
#180737=ORIENTED_EDGE ( 'NONE', *, *, #37713, .T. ) ;
#180745=CARTESIAN_POINT ( 'NONE',  ( 23.14999999999999503, 69.55000000001199112, -115.3731074845243398 ) ) ;
#180761=EDGE_CURVE ( 'NONE', #6106, #86933, #78136, .T. ) ;
#180837=CARTESIAN_POINT ( 'NONE',  ( -18.59999999999999787, 68.97833521811179480, -99.18954208262705663 ) ) ;
#180840=SPHERICAL_SURFACE ( 'NONE', #225799, 0.1000000000000000056 ) ;
#180843=CARTESIAN_POINT ( 'NONE',  ( -21.05000000000000071, 76.00000000001216449, -140.8231074845242574 ) ) ;
#180848=ORIENTED_EDGE ( 'NONE', *, *, #190693, .T. ) ;
#180854=AXIS2_PLACEMENT_3D ( 'NONE', #168946, #30703, #8547 ) ;
#180878=CARTESIAN_POINT ( 'NONE',  ( -18.59999999999999787, 64.35000000001205933, -124.3731074845243825 ) ) ;
#180881=CARTESIAN_POINT ( 'NONE',  ( -23.25000000000000000, 87.75000000001212186, -133.4231074845242233 ) ) ;
#180899=CARTESIAN_POINT ( 'NONE',  ( 20.94999999999999574, 87.39257802171779588, -133.4491579046922709 ) ) ;
#180907=DIRECTION ( 'NONE',  ( 0.7071359030027593029, -0.7070776581709197206, 0.000000000000000000 ) ) ;
#180914=DIRECTION ( 'NONE',  ( 0.000000000000000000, -6.982962677686266711E-15, 1.000000000000000000 ) ) ;
#180936=ORIENTED_EDGE ( 'NONE', *, *, #202981, .F. ) ;
#180946=EDGE_CURVE ( 'NONE', #155807, #225917, #159008, .T. ) ;
#180969=AXIS2_PLACEMENT_3D ( 'NONE', #165911, #68069, #146309 ) ;
#181002=CIRCLE ( 'NONE', #139266, 0.09999999999999938105 ) ;
#181014=EDGE_CURVE ( 'NONE', #57631, #7849, #95984, .T. ) ;
#181019=ORIENTED_EDGE ( 'NONE', *, *, #72754, .F. ) ;
#181049=CARTESIAN_POINT ( 'NONE',  ( 22.39999999999999503, 76.10000000001222986, -148.1726782920690937 ) ) ;
#181050=ADVANCED_FACE ( 'NONE', ( #130107 ), #49290, .T. ) ;
#181130=EDGE_LOOP ( 'NONE', ( #77096, #142105, #208773, #113595, #110477 ) ) ;
#181139=DIRECTION ( 'NONE',  ( -0.000000000000000000, 1.000000000000000000, 7.172728831056617961E-15 ) ) ;
#181152=ORIENTED_EDGE ( 'NONE', *, *, #66914, .T. ) ;
#181155=FACE_OUTER_BOUND ( 'NONE', #217573, .T. ) ;
#181200=DIRECTION ( 'NONE',  ( -2.812466655313719426E-14, -0.1350103645451835865, -0.9908441862701605762 ) ) ;
#181206=VERTEX_POINT ( 'NONE', #14038 ) ;
#181211=( BOUNDED_SURFACE ( )  B_SPLINE_SURFACE ( 3, 2, ( 
 ( #247925, #112291, #8053 ),
 ( #246640, #191845, #69315 ),
 ( #30193, #172299, #210110 ),
 ( #28938, #13187, #31488 ),
 ( #87557, #251783, #73184 ),
 ( #152723, #232246, #53589 ) ),
 .UNSPECIFIED., .F., .F., .F. ) 
 B_SPLINE_SURFACE_WITH_KNOTS ( ( 4, 2, 4 ),
 ( 3, 3 ),
 ( 6.719893378900957922E-05, 0.0002757154632485724760, 0.0004842319927081353728 ),
 ( 0.000000000000000000, 1.000000000000000000 ),
 .UNSPECIFIED. ) 
 GEOMETRIC_REPRESENTATION_ITEM ( )  RATIONAL_B_SPLINE_SURFACE ( (
 ( 1.000000000000000000, 0.7250110520819756932, 1.000000000000000000),
 ( 1.000000000000000000, 0.7277932058358959067, 1.000000000000000000),
 ( 1.000000000000000000, 0.7278452872617939828, 1.000000000000000000),
 ( 1.000000000000000000, 0.7221445671548865075, 1.000000000000000000),
 ( 1.000000000000000000, 0.7163662143779842006, 1.000000000000000000),
 ( 1.000000000000000000, 0.7071067811865475727, 1.000000000000000000) ) ) 
 REPRESENTATION_ITEM ( '' )  SURFACE ( )  );
#181214=CARTESIAN_POINT ( 'NONE',  ( 21.14999999999999858, 64.35000000001214460, -136.4231074845243938 ) ) ;
#181225=CARTESIAN_POINT ( 'NONE',  ( -23.15000000000000213, 76.00000000001190870, -103.0231074845243029 ) ) ;
#181227=EDGE_CURVE ( 'NONE', #178773, #27724, #154328, .T. ) ;
#181245=CARTESIAN_POINT ( 'NONE',  ( 20.22483756094572271, 66.49809532114170452, -128.3835683558091603 ) ) ;
#181257=VERTEX_POINT ( 'NONE', #107340 ) ;
#181317=EDGE_CURVE ( 'NONE', #121092, #226829, #250134, .T. ) ;
#181323=EDGE_CURVE ( 'NONE', #71756, #60014, #201308, .T. ) ;
#181325=LINE ( 'NONE', #2654, #223078 ) ;
#181332=EDGE_CURVE ( 'NONE', #155848, #2636, #126917, .T. ) ;
#181350=VECTOR ( 'NONE', #918, 1000.000000000000000 ) ;
#181361=AXIS2_PLACEMENT_3D ( 'NONE', #57730, #135980, #99420 ) ;
#181363=VECTOR ( 'NONE', #121711, 1000.000000000000000 ) ;
#181367=ORIENTED_EDGE ( 'NONE', *, *, #155392, .T. ) ;
#181372=ORIENTED_EDGE ( 'NONE', *, *, #12265, .T. ) ;
#181379=DIRECTION ( 'NONE',  ( 0.000000000000000000, 0.000000000000000000, 1.000000000000000000 ) ) ;
#181477=DIRECTION ( 'NONE',  ( 0.000000000000000000, -6.608470384673536824E-15, 1.000000000000000000 ) ) ;
#181488=CIRCLE ( 'NONE', #64928, 0.3999999999999975797 ) ;
#181490=FILL_AREA_STYLE_COLOUR ( '', #159675 ) ;
#181496=ORIENTED_EDGE ( 'NONE', *, *, #67663, .T. ) ;
#181515=CARTESIAN_POINT ( 'NONE',  ( -21.05000000000000071, 64.35000000001208775, -129.7392418215462158 ) ) ;
#181526=FACE_OUTER_BOUND ( 'NONE', #87306, .T. ) ;
#181535=EDGE_CURVE ( 'NONE', #51816, #187259, #160630, .T. ) ;
#181557=FACE_OUTER_BOUND ( 'NONE', #11379, .T. ) ;
#181621=CIRCLE ( 'NONE', #73312, 0.1000000000000028644 ) ;
#181667=ORIENTED_EDGE ( 'NONE', *, *, #153553, .F. ) ;
#181671=ORIENTED_EDGE ( 'NONE', *, *, #112625, .F. ) ;
#181703=VECTOR ( 'NONE', #117404, 1000.000000000000000 ) ;
#181718=CIRCLE ( 'NONE', #52525, 11.80000000000000426 ) ;
#181722=VECTOR ( 'NONE', #37828, 1000.000000000000000 ) ;
#181753=VERTEX_POINT ( 'NONE', #208730 ) ;
#181780=ORIENTED_EDGE ( 'NONE', *, *, #235997, .F. ) ;
#181782=DIRECTION ( 'NONE',  ( 0.000000000000000000, 6.938893903907222067E-15, -1.000000000000000000 ) ) ;
#181803=DIRECTION ( 'NONE',  ( -1.000000000000000000, -0.000000000000000000, -0.000000000000000000 ) ) ;
#181822=AXIS2_PLACEMENT_3D ( 'NONE', #108110, #51957, #225460 ) ;
#181869=DIRECTION ( 'NONE',  ( 0.000000000000000000, 0.8660254037844378194, 0.5000000000000016653 ) ) ;
#181870=ORIENTED_EDGE ( 'NONE', *, *, #209439, .T. ) ;
#181893=CARTESIAN_POINT ( 'NONE',  ( -18.39999999999999858, 85.50000000001209344, -129.4910380878245633 ) ) ;
#181902=DIRECTION ( 'NONE',  ( 0.000000000000000000, 6.982962677686266711E-15, -1.000000000000000000 ) ) ;
#181905=FACE_OUTER_BOUND ( 'NONE', #230431, .T. ) ;
#181921=EDGE_LOOP ( 'NONE', ( #42331, #131388, #76377, #259, #224315, #93379, #137385, #70744, #139234, #92163, #164333, #186725 ) ) ;
#181977=LINE ( 'NONE', #81552, #230874 ) ;
#181982=TOROIDAL_SURFACE ( 'NONE', #11287, 0.2000000000000000111, 0.1000000000000000056 ) ;
#181992=DIRECTION ( 'NONE',  ( 1.000000000000000000, 0.000000000000000000, 0.000000000000000000 ) ) ;
#181995=EDGE_CURVE ( 'NONE', #231430, #130380, #144568, .T. ) ;
#182006=ORIENTED_EDGE ( 'NONE', *, *, #218988, .T. ) ;
#182015=ORIENTED_EDGE ( 'NONE', *, *, #134138, .T. ) ;
#182024=CARTESIAN_POINT ( 'NONE',  ( 20.93975676684922504, 65.68895814178239334, -97.50265578621379348 ) ) ;
#182028=ORIENTED_EDGE ( 'NONE', *, *, #42057, .T. ) ;
#182061=ORIENTED_EDGE ( 'NONE', *, *, #193925, .F. ) ;
#182068=CARTESIAN_POINT ( 'NONE',  ( 21.05000000000000071, 85.40000000001198543, -112.9170766071766820 ) ) ;
#182082=CARTESIAN_POINT ( 'NONE',  ( -23.25000000000000000, 87.65000000001192859, -106.1231074845242262 ) ) ;
#182088=VERTEX_POINT ( 'NONE', #210985 ) ;
#182092=AXIS2_PLACEMENT_3D ( 'NONE', #65015, #24646, #8903 ) ;
#182134=DIRECTION ( 'NONE',  ( 2.715809747126117987E-16, 1.000000000000000000, 8.690591190803577558E-15 ) ) ;
#182194=ORIENTED_EDGE ( 'NONE', *, *, #192322, .F. ) ;
#182207=FACE_OUTER_BOUND ( 'NONE', #184802, .T. ) ;
#182227=AXIS2_PLACEMENT_3D ( 'NONE', #46665, #205748, #104064 ) ;
#182317=CARTESIAN_POINT ( 'NONE',  ( 21.14999999999999503, 64.25000000001215028, -136.5231074845243597 ) ) ;
#182350=DIRECTION ( 'NONE',  ( 0.000000000000000000, 1.000000000000000000, 6.982962677686266711E-15 ) ) ;
#182413=ADVANCED_FACE ( 'NONE', ( #163844 ), #21555, .T. ) ;
#182414=ORIENTED_EDGE ( 'NONE', *, *, #180695, .F. ) ;
#182449=VECTOR ( 'NONE', #122671, 1000.000000000000000 ) ;
#182451=CARTESIAN_POINT ( 'NONE',  ( 22.16821283564876666, 68.44102665923138318, -136.5231074845243313 ) ) ;
#182465=VERTEX_POINT ( 'NONE', #102541 ) ;
#182470=AXIS2_PLACEMENT_3D ( 'NONE', #137208, #158108, #120260 ) ;
#182517=ORIENTED_EDGE ( 'NONE', *, *, #57423, .F. ) ;
#182532=CARTESIAN_POINT ( 'NONE',  ( 18.59999999999999787, 77.83534155023646406, -124.8679561919613121 ) ) ;
#182534=CARTESIAN_POINT ( 'NONE',  ( -21.05000000000000071, 77.16270174995010223, -128.5231074845242745 ) ) ;
#182536=ORIENTED_EDGE ( 'NONE', *, *, #78547, .T. ) ;
#182546=DIRECTION ( 'NONE',  ( -1.000000000000000000, 0.000000000000000000, 0.000000000000000000 ) ) ;
#182563=CARTESIAN_POINT ( 'NONE',  ( 18.49999999999999645, 77.36242903720516040, -95.13422623660308375 ) ) ;
#182575=DIRECTION ( 'NONE',  ( 0.000000000000000000, -1.000000000000000000, -6.982962677686265922E-15 ) ) ;
#182581=FACE_OUTER_BOUND ( 'NONE', #145431, .T. ) ;
#182592=CARTESIAN_POINT ( 'NONE',  ( 21.05000000000000071, 76.10000000001214460, -136.5231074845242745 ) ) ;
#182604=ADVANCED_FACE ( 'NONE', ( #26925 ), #171062, .F. ) ;
#182606=AXIS2_PLACEMENT_3D ( 'NONE', #225951, #30376, #8238 ) ;
#182611=CIRCLE ( 'NONE', #174457, 0.1000000000000028644 ) ;
#182615=VERTEX_POINT ( 'NONE', #166441 ) ;
#182616=LINE ( 'NONE', #120092, #26232 ) ;
#182662=EDGE_LOOP ( 'NONE', ( #238274, #92056, #150056, #9298 ) ) ;
#182665=VERTEX_POINT ( 'NONE', #217063 ) ;
#182670=EDGE_LOOP ( 'NONE', ( #158338, #98274, #64491, #182028 ) ) ;
#182705=CARTESIAN_POINT ( 'NONE',  ( -21.14250536705909411, 76.00000000001219291, -143.0412796614050706 ) ) ;
#182710=EDGE_CURVE ( 'NONE', #12190, #100578, #125221, .T. ) ;
#182717=DIRECTION ( 'NONE',  ( -3.890533409366484652E-14, 0.1298341882520054891, 0.9915357197604850459 ) ) ;
#182735=CARTESIAN_POINT ( 'NONE',  ( -23.15000000000000213, 76.00000000001190870, -103.0231074845243029 ) ) ;
#182746=EDGE_CURVE ( 'NONE', #153892, #145261, #158550, .T. ) ;
#182753=CARTESIAN_POINT ( 'NONE',  ( -21.14999999999999858, 64.25000000001215028, -136.4231074845243938 ) ) ;
#182755=ORIENTED_EDGE ( 'NONE', *, *, #180068, .T. ) ;
#182779=CARTESIAN_POINT ( 'NONE',  ( 21.11344571971299544, 65.38212097649356735, -124.2770865921250447 ) ) ;
#182793=VECTOR ( 'NONE', #144685, 1000.000000000000000 ) ;
#182802=EDGE_CURVE ( 'NONE', #45647, #255801, #154467, .T. ) ;
#182803=DIRECTION ( 'NONE',  ( 0.000000000000000000, 4.163336342344217877E-13, -1.000000000000000000 ) ) ;
#182824=ORIENTED_EDGE ( 'NONE', *, *, #84100, .T. ) ;
#182825=AXIS2_PLACEMENT_3D ( 'NONE', #138390, #158036, #18476 ) ;
#182831=ADVANCED_FACE ( 'NONE', ( #21476 ), #146050, .T. ) ;
#182850=ORIENTED_EDGE ( 'NONE', *, *, #164799, .T. ) ;
#182914=DIRECTION ( 'NONE',  ( 2.952720810173289112E-16, 1.000000000000000000, 7.086529944415894657E-15 ) ) ;
#182916=ADVANCED_FACE ( 'NONE', ( #7023 ), #29562, .F. ) ;
#182917=FACE_OUTER_BOUND ( 'NONE', #83287, .T. ) ;
#182931=CARTESIAN_POINT ( 'NONE',  ( 21.05000000000000071, 69.74218538953601865, -136.6208977758331287 ) ) ;
#182942=VERTEX_POINT ( 'NONE', #53533 ) ;
#182962=VECTOR ( 'NONE', #149327, 1000.000000000000000 ) ;
#183002=ORIENTED_EDGE ( 'NONE', *, *, #52299, .T. ) ;
#183006=CYLINDRICAL_SURFACE ( 'NONE', #87341, 0.09999999999999939493 ) ;
#183035=CARTESIAN_POINT ( 'NONE',  ( 23.14999999999998437, 76.00000000001216449, -140.5731074845242858 ) ) ;
#183054=DIRECTION ( 'NONE',  ( 1.000000000000000000, 0.000000000000000000, 0.000000000000000000 ) ) ;
#183055=CARTESIAN_POINT ( 'NONE',  ( -20.94999999999999929, 87.29603075034721371, -106.0710066441880883 ) ) ;
#183065=DIRECTION ( 'NONE',  ( 0.000000000000000000, 0.4930308989875575865, 0.8700118002898125091 ) ) ;
#183074=CARTESIAN_POINT ( 'NONE',  ( -20.94999999999999929, 77.16412189325305349, -95.30825939895268561 ) ) ;
#183075=CYLINDRICAL_SURFACE ( 'NONE', #186777, 0.1000000000000028644 ) ;
#183122=EDGE_CURVE ( 'NONE', #30882, #2981, #187949, .T. ) ;
#183138=CARTESIAN_POINT ( 'NONE',  ( 18.49999999999998934, 65.75000000001196554, -111.8731074845243683 ) ) ;
#183143=CIRCLE ( 'NONE', #66427, 0.1000000000000028644 ) ;
#183149=CARTESIAN_POINT ( 'NONE',  ( 23.24999999999999645, 71.22429906543254674, -114.8718755885703047 ) ) ;
#183185=DIRECTION ( 'NONE',  ( -1.000000000000000000, 1.836970198721029934E-16, 1.282749433769087582E-30 ) ) ;
#183189=ORIENTED_EDGE ( 'NONE', *, *, #79671, .T. ) ;
#183193=ORIENTED_EDGE ( 'NONE', *, *, #57608, .F. ) ;
#183199=VECTOR ( 'NONE', #154992, 1000.000000000000000 ) ;
#183204=CIRCLE ( 'NONE', #75079, 0.09999999999998898659 ) ;
#183207=LINE ( 'NONE', #144049, #1927 ) ;
#183245=CARTESIAN_POINT ( 'NONE',  ( 20.94999999999999929, 76.00000000001190870, -103.0231074845243029 ) ) ;
#183267=VERTEX_POINT ( 'NONE', #130181 ) ;
#183307=CARTESIAN_POINT ( 'NONE',  ( 20.87600722750343252, 65.66887361445333227, -97.43298459182690863 ) ) ;
#183321=CARTESIAN_POINT ( 'NONE',  ( 23.14999999999999858, 72.00000000001190870, -103.0231074845243313 ) ) ;
#183381=CARTESIAN_POINT ( 'NONE',  ( -23.25000000000000000, 77.85161776048073534, -91.41991776492061206 ) ) ;
#183502=CARTESIAN_POINT ( 'NONE',  ( 20.94999999999999929, 76.00000000001190870, -103.0231074845243029 ) ) ;
#183503=AXIS2_PLACEMENT_3D ( 'NONE', #186016, #200450, #102591 ) ;
#183507=ORIENTED_EDGE ( 'NONE', *, *, #117599, .T. ) ;
#183509=AXIS2_PLACEMENT_3D ( 'NONE', #72210, #172630, #93037 ) ;
#183510=AXIS2_PLACEMENT_3D ( 'NONE', #28859, #110909, #208745 ) ;
#183538=CIRCLE ( 'NONE', #100303, 0.1000000000000028644 ) ;
#183546=DIRECTION ( 'NONE',  ( -1.000000000000000000, -9.012599976027990443E-15, -6.882867235861669241E-14 ) ) ;
#183621=ORIENTED_EDGE ( 'NONE', *, *, #39573, .T. ) ;
#183639=EDGE_CURVE ( 'NONE', #130380, #170720, #250471, .T. ) ;
#183645=ORIENTED_EDGE ( 'NONE', *, *, #230443, .T. ) ;
#183705=CARTESIAN_POINT ( 'NONE',  ( 19.75857864376268935, 64.25000000001196554, -111.6731074845243796 ) ) ;
#183722=DIRECTION ( 'NONE',  ( 1.000000000000000000, 0.000000000000000000, 0.000000000000000000 ) ) ;
#183744=DIRECTION ( 'NONE',  ( 1.000000000000000000, 0.000000000000000000, 0.000000000000000000 ) ) ;
#183745=DIRECTION ( 'NONE',  ( 1.000000000000000000, 0.000000000000000000, 0.000000000000000000 ) ) ;
#183747=CIRCLE ( 'NONE', #179480, 0.09999999999999939493 ) ;
#183759=ORIENTED_EDGE ( 'NONE', *, *, #76039, .F. ) ;
#183768=CARTESIAN_POINT ( 'NONE',  ( -22.47071067811865319, 68.27992525551407255, -136.6221999392269595 ) ) ;
#183792=CARTESIAN_POINT ( 'NONE',  ( 20.97438252431638972, 67.07457649393607824, -128.0507367955135578 ) ) ;
#183807=AXIS2_PLACEMENT_3D ( 'NONE', #111859, #113135, #132710 ) ;
#183851=EDGE_LOOP ( 'NONE', ( #189409, #62618, #119375 ) ) ;
#183866=EDGE_CURVE ( 'NONE', #61549, #154428, #163366, .T. ) ;
#183885=CARTESIAN_POINT ( 'NONE',  ( 23.14999999999999858, 76.00000000001190870, -103.0231074845243029 ) ) ;
#183893=AXIS2_PLACEMENT_3D ( 'NONE', #27571, #187900, #87485 ) ;
#183924=ORIENTED_EDGE ( 'NONE', *, *, #102042, .T. ) ;
#183928=AXIS2_PLACEMENT_3D ( 'NONE', #202805, #141543, #64574 ) ;
#183952=CARTESIAN_POINT ( 'NONE',  ( -21.14999999999999858, 87.75000000001212186, -133.6231074845242119 ) ) ;
#183966=ADVANCED_FACE ( 'NONE', ( #158920 ), #159105, .F. ) ;
#183970=CARTESIAN_POINT ( 'NONE',  ( -21.14999999999999858, 76.00000000001219291, -143.0637644362255401 ) ) ;
#183983=B_SPLINE_CURVE_WITH_KNOTS ( 'NONE', 3,
 ( #96935, #40886, #22591, #215625, #37028, #425 ),
 .UNSPECIFIED., .F., .F.,
 ( 4, 2, 4 ),
 ( 0.000000000000000000, 0.0002113392456166052918, 0.0004226784912332105836 ),
 .UNSPECIFIED. ) ;
#183992=FACE_OUTER_BOUND ( 'NONE', #39780, .T. ) ;
#183999=FACE_OUTER_BOUND ( 'NONE', #140698, .T. ) ;
#184026=CARTESIAN_POINT ( 'NONE',  ( 20.95429402530550433, 67.12380584890989610, -128.0000207865865320 ) ) ;
#184070=ORIENTED_EDGE ( 'NONE', *, *, #34408, .F. ) ;
#184090=FACE_OUTER_BOUND ( 'NONE', #146007, .T. ) ;
#184105=DIRECTION ( 'NONE',  ( 1.000000000000000000, 0.000000000000000000, 0.000000000000000000 ) ) ;
#184132=FACE_OUTER_BOUND ( 'NONE', #30901, .T. ) ;
#184135=DIRECTION ( 'NONE',  ( 0.000000000000000000, -6.688090509790120484E-15, 1.000000000000000000 ) ) ;
#184137=EDGE_CURVE ( 'NONE', #25096, #226829, #196731, .T. ) ;
#184159=AXIS2_PLACEMENT_3D ( 'NONE', #255598, #215245, #195707 ) ;
#184164=CARTESIAN_POINT ( 'NONE',  ( -21.05000000000000071, 87.65000000001214175, -136.5231074845242176 ) ) ;
#184190=CARTESIAN_POINT ( 'NONE',  ( -20.94999999999999929, 87.48912529308798014, -106.1231074845242262 ) ) ;
#184209=CIRCLE ( 'NONE', #255067, 12.87499999999999822 ) ;
#184287=FACE_OUTER_BOUND ( 'NONE', #130750, .T. ) ;
#184298=CARTESIAN_POINT ( 'NONE',  ( -20.85000000000000142, 77.16412189325305349, -95.10825939895268277 ) ) ;
#184300=ORIENTED_EDGE ( 'NONE', *, *, #140285, .F. ) ;
#184308=FACE_OUTER_BOUND ( 'NONE', #28670, .T. ) ;
#184349=CARTESIAN_POINT ( 'NONE',  ( -20.92356734117541706, 65.68026841930900162, -97.47257401318893244 ) ) ;
#184358=DIRECTION ( 'NONE',  ( 0.000000000000000000, -6.982962677686266711E-15, 1.000000000000000000 ) ) ;
#184371=EDGE_CURVE ( 'NONE', #54998, #57631, #115278, .T. ) ;
#184373=CIRCLE ( 'NONE', #5288, 0.1000000000000033362 ) ;
#184408=ORIENTED_EDGE ( 'NONE', *, *, #21277, .F. ) ;
#184446=LINE ( 'NONE', #146584, #67171 ) ;
#184450=EDGE_CURVE ( 'NONE', #111084, #214648, #217682, .T. ) ;
#184456=DIRECTION ( 'NONE',  ( -1.000000000000000000, 0.000000000000000000, 0.000000000000000000 ) ) ;
#184460=AXIS2_PLACEMENT_3D ( 'NONE', #38487, #138824, #21508 ) ;
#184491=DIRECTION ( 'NONE',  ( 0.000000000000000000, 0.000000000000000000, 1.000000000000000000 ) ) ;
#184496=AXIS2_PLACEMENT_3D ( 'NONE', #110812, #25205, #103410 ) ;
#184523=CIRCLE ( 'NONE', #238709, 0.5999999999999894307 ) ;
#184530=ORIENTED_EDGE ( 'NONE', *, *, #162558, .T. ) ;
#184533=ADVANCED_FACE ( 'NONE', ( #25194 ), #246921, .F. ) ;
#184553=ADVANCED_FACE ( 'NONE', ( #169870 ), #5579, .F. ) ;
#184560=EDGE_LOOP ( 'NONE', ( #151720, #84351, #220722, #211870 ) ) ;
#184591=AXIS2_PLACEMENT_3D ( 'NONE', #89913, #52064, #228164 ) ;
#184597=CYLINDRICAL_SURFACE ( 'NONE', #217571, 12.87499999999999822 ) ;
#184605=STYLED_ITEM ( 'NONE', ( #6679 ), #26097 ) ;
#184629=DIRECTION ( 'NONE',  ( 0.000000000000000000, -7.116814260417668513E-15, 1.000000000000000000 ) ) ;
#184634=LINE ( 'NONE', #145503, #54247 ) ;
#184648=CARTESIAN_POINT ( 'NONE',  ( -18.59999999999999787, 85.48068669529084218, -96.08199231576638510 ) ) ;
#184651=DIRECTION ( 'NONE',  ( 0.000000000000000000, -7.304098846218139203E-15, 1.000000000000000000 ) ) ;
#184669=DIRECTION ( 'NONE',  ( 0.000000000000000000, -1.000000000000000000, 0.000000000000000000 ) ) ;
#184686=CARTESIAN_POINT ( 'NONE',  ( -18.39999999999999858, 85.50000000001209344, -129.5238218066853904 ) ) ;
#184690=CIRCLE ( 'NONE', #226166, 0.1000000000000045158 ) ;
#184697=DIRECTION ( 'NONE',  ( 0.000000000000000000, -6.769652589177772835E-15, 1.000000000000000000 ) ) ;
#184751=DIRECTION ( 'NONE',  ( -0.4999999999999799050, -6.047423072554995242E-15, 0.8660254037844502539 ) ) ;
#184755=CARTESIAN_POINT ( 'NONE',  ( -20.94999999999999929, 64.30000000001196270, -109.7781056340430013 ) ) ;
#184802=EDGE_LOOP ( 'NONE', ( #111491, #151486, #9617, #17136 ) ) ;
#184850=CARTESIAN_POINT ( 'NONE',  ( -23.25000000000000000, 76.00000000001192291, -105.1231074845242972 ) ) ;
#184857=VECTOR ( 'NONE', #53173, 1000.000000000000000 ) ;
#184861=EDGE_CURVE ( 'NONE', #165453, #49989, #63955, .T. ) ;
#184888=AXIS2_PLACEMENT_3D ( 'NONE', #80891, #221682, #41812 ) ;
#184908=ORIENTED_EDGE ( 'NONE', *, *, #207833, .T. ) ;
#184933=EDGE_LOOP ( 'NONE', ( #140909, #20916, #150439, #207411 ) ) ;
#184951=CARTESIAN_POINT ( 'NONE',  ( -23.15000000000000213, 71.65000000001199965, -115.2731074845243171 ) ) ;
#184953=DIRECTION ( 'NONE',  ( 0.000000000000000000, -6.982962677686266711E-15, 1.000000000000000000 ) ) ;
#184965=CARTESIAN_POINT ( 'NONE',  ( -21.65000000000000213, 68.29142135624930177, -115.3731074845243540 ) ) ;
#185053=ADVANCED_FACE ( 'NONE', ( #88667 ), #59632, .T. ) ;
#185076=ORIENTED_EDGE ( 'NONE', *, *, #217061, .F. ) ;
#185095=DIRECTION ( 'NONE',  ( 0.000000000000000000, -6.982962677686266711E-15, 1.000000000000000000 ) ) ;
#185096=VERTEX_POINT ( 'NONE', #172131 ) ;
#185127=AXIS2_PLACEMENT_3D ( 'NONE', #162369, #77652, #120684 ) ;
#185130=EDGE_LOOP ( 'NONE', ( #204039, #251259, #148959, #51296 ) ) ;
#185133=AXIS2_PLACEMENT_3D ( 'NONE', #250780, #209092, #115132 ) ;
#185156=ADVANCED_FACE ( 'NONE', ( #109528 ), #113400, .T. ) ;
#185158=B_SPLINE_CURVE_WITH_KNOTS ( 'NONE', 3,
 ( #1174, #59859, #62463, #83269, #141981, #173792, #42897, #238519, #253258, #39063 ),
 .UNSPECIFIED., .F., .F.,
 ( 4, 3, 3, 4 ),
 ( 0.000000000000000000, 0.0002000000000002785953, 0.001000000000045107602, 0.001967863649472123035 ),
 .UNSPECIFIED. ) ;
#185168=VERTEX_POINT ( 'NONE', #89966 ) ;
#185219=AXIS2_PLACEMENT_3D ( 'NONE', #19028, #13908, #97240 ) ;
#185224=AXIS2_PLACEMENT_3D ( 'NONE', #189579, #34376, #10944 ) ;
#185257=EDGE_LOOP ( 'NONE', ( #160387, #106551, #253066 ) ) ;
#185281=ORIENTED_EDGE ( 'NONE', *, *, #166756, .F. ) ;
#185304=CARTESIAN_POINT ( 'NONE',  ( 20.94999999999999929, 65.27628289530453287, -124.3731074845243825 ) ) ;
#185347=CIRCLE ( 'NONE', #152045, 3.900000000000000799 ) ;
#185361=CYLINDRICAL_SURFACE ( 'NONE', #34531, 0.1000000000000028644 ) ;
#185379=CARTESIAN_POINT ( 'NONE',  ( -20.54999999999999716, 68.75000000001199396, -115.2731074845243455 ) ) ;
#185431=LINE ( 'NONE', #245414, #230482 ) ;
#185471=VERTEX_POINT ( 'NONE', #29735 ) ;
#185513=B_SPLINE_CURVE_WITH_KNOTS ( 'NONE', 3,
 ( #69514, #206431, #26528, #244255, #47336, #189448, #8245, #246832 ),
 .UNSPECIFIED., .F., .F.,
 ( 4, 2, 2, 4 ),
 ( 0.000000000000000000, 0.0002114466876442005951, 0.0003171700314663121684, 0.0004228933752884237417 ),
 .UNSPECIFIED. ) ;
#185523=ORIENTED_EDGE ( 'NONE', *, *, #106508, .F. ) ;
#185538=LINE ( 'NONE', #66873, #197954 ) ;
#185562=CIRCLE ( 'NONE', #102137, 0.2000000000000057288 ) ;
#185567=ORIENTED_EDGE ( 'NONE', *, *, #217231, .T. ) ;
#185569=CARTESIAN_POINT ( 'NONE',  ( -18.41809261886928084, 85.68240331476862082, -96.36626393443329164 ) ) ;
#185575=FACE_OUTER_BOUND ( 'NONE', #189074, .T. ) ;
#185601=CARTESIAN_POINT ( 'NONE',  ( 20.94999999999999574, 87.41227409416181615, -133.5231074845242176 ) ) ;
#185610=DIRECTION ( 'NONE',  ( 0.000000000000000000, -1.000000000000000000, -6.352154140967427193E-15 ) ) ;
#185679=CARTESIAN_POINT ( 'NONE',  ( 23.24999999999999289, 64.35000000001197407, -115.1731074845243796 ) ) ;
#185706=DIRECTION ( 'NONE',  ( -1.000000000000000000, 1.836970198721029934E-16, 1.282749433769087582E-30 ) ) ;
#185721=ORIENTED_EDGE ( 'NONE', *, *, #211331, .F. ) ;
#185725=ORIENTED_EDGE ( 'NONE', *, *, #246642, .F. ) ;
#185744=EDGE_CURVE ( 'NONE', #139626, #118915, #19119, .T. ) ;
#185775=CARTESIAN_POINT ( 'NONE',  ( -23.15000000000000213, 85.00000000001197975, -112.9170766071766820 ) ) ;
#185778=ORIENTED_EDGE ( 'NONE', *, *, #147521, .T. ) ;
#185799=CARTESIAN_POINT ( 'NONE',  ( 20.94999999999999574, 67.07338541492499928, -128.0514244653012383 ) ) ;
#185804=TOROIDAL_SURFACE ( 'NONE', #56777, 3.899999999999999467, 0.1000000000000000056 ) ;
#185817=DIRECTION ( 'NONE',  ( 0.000000000000000000, -6.853228547068871147E-15, 1.000000000000000000 ) ) ;
#185846=CARTESIAN_POINT ( 'NONE',  ( 20.95576188350343116, 65.39101945504869207, -128.9118737617700674 ) ) ;
#185852=VERTEX_POINT ( 'NONE', #103760 ) ;
#185864=CARTESIAN_POINT ( 'NONE',  ( 20.91682497891422798, 65.67736539654943329, -97.46251168765718376 ) ) ;
#185890=ORIENTED_EDGE ( 'NONE', *, *, #119424, .T. ) ;
#185896=ORIENTED_EDGE ( 'NONE', *, *, #157892, .F. ) ;
#185904=ORIENTED_EDGE ( 'NONE', *, *, #48804, .F. ) ;
#185941=ADVANCED_FACE ( 'NONE', ( #77173, #230154 ), #250982, .F. ) ;
#185977=CIRCLE ( 'NONE', #106858, 0.1000000000000072220 ) ;
#186016=CARTESIAN_POINT ( 'NONE',  ( -21.65000000000000213, 68.25000000001205080, -124.1731074845243512 ) ) ;
#186027=AXIS2_PLACEMENT_3D ( 'NONE', #141214, #42131, #38267 ) ;
#186048=CARTESIAN_POINT ( 'NONE',  ( -21.05000000000000071, 76.00000000001190870, -103.0231074845243029 ) ) ;
#186077=ORIENTED_EDGE ( 'NONE', *, *, #134902, .T. ) ;
#186078=DIRECTION ( 'NONE',  ( 0.000000000000000000, -7.086529944415894657E-15, 1.000000000000000000 ) ) ;
#186087=DIRECTION ( 'NONE',  ( 0.000000000000000000, 0.000000000000000000, -1.000000000000000000 ) ) ;
#186097=DIRECTION ( 'NONE',  ( 0.000000000000000000, -6.467318590049456648E-15, 1.000000000000000000 ) ) ;
#186103=ORIENTED_EDGE ( 'NONE', *, *, #245809, .F. ) ;
#186127=CIRCLE ( 'NONE', #198591, 0.1000000000000028644 ) ;
#186131=CARTESIAN_POINT ( 'NONE',  ( 18.59999999999999432, 77.73625713160946304, -124.9544551555067926 ) ) ;
#186154=LINE ( 'NONE', #225251, #180694 ) ;
#186156=LINE ( 'NONE', #204418, #176530 ) ;
#186173=VERTEX_POINT ( 'NONE', #103145 ) ;
#186179=ORIENTED_EDGE ( 'NONE', *, *, #191429, .F. ) ;
#186184=ORIENTED_EDGE ( 'NONE', *, *, #253079, .T. ) ;
#186191=CARTESIAN_POINT ( 'NONE',  ( -18.59999999999999787, 64.25000000001190870, -103.0231074845243882 ) ) ;
#186225=AXIS2_PLACEMENT_3D ( 'NONE', #13963, #93475, #11391 ) ;
#186227=VERTEX_POINT ( 'NONE', #26213 ) ;
#186278=EDGE_CURVE ( 'NONE', #30941, #119976, #210262, .T. ) ;
#186279=VERTEX_POINT ( 'NONE', #164438 ) ;
#186286=DIRECTION ( 'NONE',  ( 1.000000000000000000, 0.000000000000000000, 0.000000000000000000 ) ) ;
#186320=EDGE_CURVE ( 'NONE', #135040, #249019, #139500, .T. ) ;
#186330=LINE ( 'NONE', #164202, #86467 ) ;
#186341=VECTOR ( 'NONE', #57216, 1000.000000000000000 ) ;
#186344=DIRECTION ( 'NONE',  ( -1.000000000000000000, 0.000000000000000000, 0.000000000000000000 ) ) ;
#186346=CARTESIAN_POINT ( 'NONE',  ( -20.85000000000000142, 76.00000000001190870, -103.0231074845243029 ) ) ;
#186377=DIRECTION ( 'NONE',  ( 0.000000000000000000, 1.000000000000000000, 0.000000000000000000 ) ) ;
#186382=VECTOR ( 'NONE', #203622, 1000.000000000000000 ) ;
#186394=FACE_OUTER_BOUND ( 'NONE', #200154, .T. ) ;
#186435=ORIENTED_EDGE ( 'NONE', *, *, #250201, .F. ) ;
#186449=CIRCLE ( 'NONE', #144725, 0.2000000000000057288 ) ;
#186469=CIRCLE ( 'NONE', #144936, 0.5000000000000004441 ) ;
#186470=CARTESIAN_POINT ( 'NONE',  ( 20.94999999999999929, 76.00000000001213607, -136.5231074845242745 ) ) ;
#186494=CARTESIAN_POINT ( 'NONE',  ( 23.14999999999999858, 78.00000000001190870, -103.0231074845242887 ) ) ;
#186528=LINE ( 'NONE', #166994, #236864 ) ;
#186537=EDGE_CURVE ( 'NONE', #188655, #156311, #97977, .T. ) ;
#186552=CARTESIAN_POINT ( 'NONE',  ( 21.05000000000000071, 84.73084112150739600, -126.9250327655398962 ) ) ;
#186554=CARTESIAN_POINT ( 'NONE',  ( -20.94999999999999929, 87.41227409416181615, -133.5231074845242176 ) ) ;
#186622=DIRECTION ( 'NONE',  ( 1.000000000000000000, -0.000000000000000000, 0.000000000000000000 ) ) ;
#186628=FACE_OUTER_BOUND ( 'NONE', #216906, .T. ) ;
#186631=EDGE_CURVE ( 'NONE', #88161, #132227, #156304, .T. ) ;
#186679=CARTESIAN_POINT ( 'NONE',  ( 20.94999999999999929, 67.22371710471958295, -124.3731074845243683 ) ) ;
#186684=CARTESIAN_POINT ( 'NONE',  ( -18.50000000000000000, 74.16465844978765176, -124.9679561919613207 ) ) ;
#186690=CIRCLE ( 'NONE', #236533, 0.09999999999998898659 ) ;
#186725=ORIENTED_EDGE ( 'NONE', *, *, #181535, .T. ) ;
#186762=CARTESIAN_POINT ( 'NONE',  ( -18.59999999999999787, 76.00000000001190870, -103.0231074845243029 ) ) ;
#186777=AXIS2_PLACEMENT_3D ( 'NONE', #119250, #198762, #163500 ) ;
#186784=CYLINDRICAL_SURFACE ( 'NONE', #190520, 0.09999999999999939493 ) ;
#186785=TOROIDAL_SURFACE ( 'NONE', #74378, 11.65000000000000036, 0.1000000000000000056 ) ;
#186829=ORIENTED_EDGE ( 'NONE', *, *, #24502, .T. ) ;
#186830=DIRECTION ( 'NONE',  ( 0.000000000000000000, -6.938893903907222067E-15, 1.000000000000000000 ) ) ;
#186897=VERTEX_POINT ( 'NONE', #159985 ) ;
#186913=DIRECTION ( 'NONE',  ( 1.000000000000000000, 0.000000000000000000, 0.000000000000000000 ) ) ;
#186926=EDGE_LOOP ( 'NONE', ( #154985, #85025, #67757, #124620 ) ) ;
#186929=EDGE_CURVE ( 'NONE', #99499, #54789, #205466, .T. ) ;
#186945=CARTESIAN_POINT ( 'NONE',  ( 20.94999999999999574, 76.00000000001213607, -136.5231074845242745 ) ) ;
#186947=EDGE_LOOP ( 'NONE', ( #155304, #132630, #2502, #67615 ) ) ;
#186952=EDGE_CURVE ( 'NONE', #87569, #201070, #231958, .T. ) ;
#186975=CARTESIAN_POINT ( 'NONE',  ( 18.49999999999996803, 68.92903212821303782, -99.27654326265604823 ) ) ;
#187017=EDGE_CURVE ( 'NONE', #127664, #37720, #244619, .T. ) ;
#187020=AXIS2_PLACEMENT_3D ( 'NONE', #56278, #36775, #255734 ) ;
#187061=CARTESIAN_POINT ( 'NONE',  ( 18.49999999999999289, 68.87972903831429505, -99.36354444268502561 ) ) ;
#187063=AXIS2_PLACEMENT_3D ( 'NONE', #231745, #115635, #248734 ) ;
#187069=ORIENTED_EDGE ( 'NONE', *, *, #256992, .F. ) ;
#187082=EDGE_CURVE ( 'NONE', #93827, #197206, #176522, .T. ) ;
#187098=DIRECTION ( 'NONE',  ( 1.000000000000000000, 0.000000000000000000, 0.000000000000000000 ) ) ;
#187106=ORIENTED_EDGE ( 'NONE', *, *, #238272, .F. ) ;
#187177=CARTESIAN_POINT ( 'NONE',  ( -18.39999999999999858, 85.50000000001186606, -96.42291809330220076 ) ) ;
#187207=EDGE_CURVE ( 'NONE', #47181, #24834, #235500, .T. ) ;
#187235=LINE ( 'NONE', #111528, #41518 ) ;
#187248=ORIENTED_EDGE ( 'NONE', *, *, #116698, .T. ) ;
#187256=AXIS2_PLACEMENT_3D ( 'NONE', #185379, #246625, #167136 ) ;
#187259=VERTEX_POINT ( 'NONE', #223316 ) ;
#187278=CIRCLE ( 'NONE', #120638, 0.09999999999999939493 ) ;
#187320=CARTESIAN_POINT ( 'NONE',  ( 18.59999999999996945, 65.66751761918668251, -97.42826094061121012 ) ) ;
#187355=DIRECTION ( 'NONE',  ( 0.000000000000000000, -7.429790795770644761E-15, 1.000000000000000000 ) ) ;
#187362=AXIS2_PLACEMENT_3D ( 'NONE', #36938, #35651, #236377 ) ;
#187367=VECTOR ( 'NONE', #4646, 1000.000000000000000 ) ;
#187375=DIRECTION ( 'NONE',  ( 1.000000000000000000, 0.000000000000000000, 0.000000000000000000 ) ) ;
#187401=EDGE_CURVE ( 'NONE', #231809, #17154, #118828, .T. ) ;
#187420=CARTESIAN_POINT ( 'NONE',  ( -20.64999999999999858, 85.40000000001207070, -126.6291383618717816 ) ) ;
#187438=AXIS2_PLACEMENT_3D ( 'NONE', #104129, #101547, #241118 ) ;
#187481=DIRECTION ( 'NONE',  ( 0.000000000000000000, 0.000000000000000000, -1.000000000000000000 ) ) ;
#187489=EDGE_LOOP ( 'NONE', ( #143193, #220780, #225119, #43787, #14896 ) ) ;
#187507=ADVANCED_FACE ( 'NONE', ( #113812 ), #176381, .T. ) ;
#187529=EDGE_CURVE ( 'NONE', #93827, #58001, #35802, .T. ) ;
#187546=CARTESIAN_POINT ( 'NONE',  ( 21.05000000000000071, 64.25000000001195133, -110.0379132551783243 ) ) ;
#187556=VERTEX_POINT ( 'NONE', #142356 ) ;
#187595=DIRECTION ( 'NONE',  ( 0.000000000000000000, 0.000000000000000000, 1.000000000000000000 ) ) ;
#187648=CIRCLE ( 'NONE', #179448, 11.74999999999999645 ) ;
#187663=CARTESIAN_POINT ( 'NONE',  ( -22.57320508075687115, 64.35000000001214460, -136.5231074845243313 ) ) ;
#187665=CARTESIAN_POINT ( 'NONE',  ( 20.96937028524355284, 65.37553062838541962, -129.0316813833547656 ) ) ;
#187686=ORIENTED_EDGE ( 'NONE', *, *, #149795, .T. ) ;
#187696=FACE_OUTER_BOUND ( 'NONE', #102967, .T. ) ;
#187727=EDGE_CURVE ( 'NONE', #94457, #13684, #10852, .T. ) ;
#187761=CARTESIAN_POINT ( 'NONE',  ( -20.94999999999999929, 77.13501884592203339, -95.30613060109196510 ) ) ;
#187830=ORIENTED_EDGE ( 'NONE', *, *, #211313, .T. ) ;
#187841=EDGE_CURVE ( 'NONE', #250872, #160823, #119179, .T. ) ;
#187845=DIRECTION ( 'NONE',  ( 0.000000000000000000, 6.982962677686266711E-15, -1.000000000000000000 ) ) ;
#187849=AXIS2_PLACEMENT_3D ( 'NONE', #250298, #71684, #151211 ) ;
#187857=ORIENTED_EDGE ( 'NONE', *, *, #83693, .F. ) ;
#187859=DIRECTION ( 'NONE',  ( 0.000000000000000000, 1.000000000000000000, 7.272083257015735086E-15 ) ) ;
#187900=DIRECTION ( 'NONE',  ( 1.000000000000000000, 0.000000000000000000, 0.000000000000000000 ) ) ;
#187922=CARTESIAN_POINT ( 'NONE',  ( -22.48660254037843131, 64.35000000001213039, -136.5731074845243711 ) ) ;
#187945=EDGE_CURVE ( 'NONE', #188576, #192766, #190106, .T. ) ;
#187947=EDGE_CURVE ( 'NONE', #147639, #118755, #244237, .T. ) ;
#187949=CIRCLE ( 'NONE', #171240, 0.1000000000000028644 ) ;
#187953=DIRECTION ( 'NONE',  ( 0.000000000000000000, -7.487053152578127080E-15, 1.000000000000000000 ) ) ;
#187983=DIRECTION ( 'NONE',  ( 0.000000000000000000, 0.000000000000000000, -1.000000000000000000 ) ) ;
#187986=FACE_OUTER_BOUND ( 'NONE', #167143, .T. ) ;
#187992=DIRECTION ( 'NONE',  ( -0.000000000000000000, 7.172728831056617961E-15, -1.000000000000000000 ) ) ;
#187998=DIRECTION ( 'NONE',  ( -1.000000000000000000, -0.000000000000000000, -0.000000000000000000 ) ) ;
#188029=EDGE_CURVE ( 'NONE', #199333, #236302, #169292, .T. ) ;
#188039=EDGE_CURVE ( 'NONE', #112979, #13011, #181718, .T. ) ;
#188070=ORIENTED_EDGE ( 'NONE', *, *, #4367, .T. ) ;
#188130=CIRCLE ( 'NONE', #96523, 0.1000000000000028644 ) ;
#188137=CARTESIAN_POINT ( 'NONE',  ( 20.04142135623730070, 64.35000000001198828, -115.1731074845243796 ) ) ;
#188199=TOROIDAL_SURFACE ( 'NONE', #246453, 0.2000000000000000111, 0.1000000000000000056 ) ;
#188206=ORIENTED_EDGE ( 'NONE', *, *, #172754, .T. ) ;
#188231=DIRECTION ( 'NONE',  ( -1.000000000000000000, 0.000000000000000000, -0.000000000000000000 ) ) ;
#188247=DIRECTION ( 'NONE',  ( 0.000000000000000000, -0.1568667991644355497, 0.9876197685951332295 ) ) ;
#188255=ORIENTED_EDGE ( 'NONE', *, *, #12791, .T. ) ;
#188263=DIRECTION ( 'NONE',  ( 0.000000000000000000, 6.467318590049456648E-15, -1.000000000000000000 ) ) ;
#188284=ORIENTED_EDGE ( 'NONE', *, *, #44245, .T. ) ;
#188340=CARTESIAN_POINT ( 'NONE',  ( 21.05000000000000071, 65.27628289530454708, -124.3731074845243825 ) ) ;
#188342=ORIENTED_EDGE ( 'NONE', *, *, #201660, .F. ) ;
#188369=CARTESIAN_POINT ( 'NONE',  ( 20.95224633520496127, 67.09947783345485561, -128.0298310366030989 ) ) ;
#188382=CARTESIAN_POINT ( 'NONE',  ( -20.00857864376270001, 66.85000000001200249, -115.2731074845243597 ) ) ;
#188410=EDGE_LOOP ( 'NONE', ( #18602, #44426, #197453, #152016, #118678, #184530, #247399, #75415 ) ) ;
#188465=DIRECTION ( 'NONE',  ( 2.915501640297156255E-16, 1.000000000000000000, 6.997203936713175802E-15 ) ) ;
#188466=VECTOR ( 'NONE', #159893, 1000.000000000000000 ) ;
#188484=FACE_OUTER_BOUND ( 'NONE', #116978, .T. ) ;
#188502=AXIS2_PLACEMENT_3D ( 'NONE', #173298, #212385, #170732 ) ;
#188576=VERTEX_POINT ( 'NONE', #248235 ) ;
#188581=ORIENTED_EDGE ( 'NONE', *, *, #200054, .F. ) ;
#188590=CARTESIAN_POINT ( 'NONE',  ( 21.07946286933444568, 75.92331615675576018, -142.8521448035320986 ) ) ;
#188602=DIRECTION ( 'NONE',  ( 0.000000000000000000, 6.938893903907222067E-15, -1.000000000000000000 ) ) ;
#188645=CARTESIAN_POINT ( 'NONE',  ( 20.46382478191414833, 67.09862044130947822, -127.9773793896412712 ) ) ;
#188655=VERTEX_POINT ( 'NONE', #38194 ) ;
#188696=ORIENTED_EDGE ( 'NONE', *, *, #105586, .F. ) ;
#188716=AXIS2_PLACEMENT_3D ( 'NONE', #143094, #996, #44013 ) ;
#188741=ORIENTED_EDGE ( 'NONE', *, *, #194042, .T. ) ;
#188744=CARTESIAN_POINT ( 'NONE',  ( 23.14999999999999858, 70.50000000001199396, -115.4283735034374274 ) ) ;
#188783=CARTESIAN_POINT ( 'NONE',  ( 22.48660254037844197, 64.35000000001213039, -136.5731074845243995 ) ) ;
#188788=ADVANCED_FACE ( 'NONE', ( #181557 ), #43318, .F. ) ;
#188797=VERTEX_POINT ( 'NONE', #163272 ) ;
#188808=AXIS2_PLACEMENT_3D ( 'NONE', #215706, #56609, #176622 ) ;
#188832=CARTESIAN_POINT ( 'NONE',  ( -22.47071067811865319, 68.27992525551407255, -136.6221999392269595 ) ) ;
#188842=EDGE_CURVE ( 'NONE', #58209, #230546, #223214, .T. ) ;
#188846=AXIS2_PLACEMENT_3D ( 'NONE', #81007, #99284, #101847 ) ;
#188849=ORIENTED_EDGE ( 'NONE', *, *, #142265, .F. ) ;
#188862=DIRECTION ( 'NONE',  ( 0.7071067811865487940, -4.937700262164522799E-15, 0.7071067811865463515 ) ) ;
#188902=CARTESIAN_POINT ( 'NONE',  ( 23.25000000000000000, 85.00000000001197975, -112.9170766071766820 ) ) ;
#188914=VERTEX_POINT ( 'NONE', #10609 ) ;
#188938=DIRECTION ( 'NONE',  ( 0.000000000000000000, 1.000000000000000000, 0.000000000000000000 ) ) ;
#188970=EDGE_CURVE ( 'NONE', #82680, #174398, #35959, .T. ) ;
#188995=VECTOR ( 'NONE', #107131, 1000.000000000000000 ) ;
#188997=CARTESIAN_POINT ( 'NONE',  ( -18.59999999999999787, 70.65875701002055109, -146.3297576910123610 ) ) ;
#189074=EDGE_LOOP ( 'NONE', ( #15557, #74510, #88443, #221533 ) ) ;
#189113=EDGE_LOOP ( 'NONE', ( #239173, #60960, #127206, #200796 ) ) ;
#189137=CARTESIAN_POINT ( 'NONE',  ( -20.54999999999999716, 74.07476635515223506, -123.7928639513981892 ) ) ;
#189160=AXIS2_PLACEMENT_3D ( 'NONE', #246111, #11345, #27088 ) ;
#189188=ORIENTED_EDGE ( 'NONE', *, *, #252959, .F. ) ;
#189202=FACE_OUTER_BOUND ( 'NONE', #239031, .T. ) ;
#189221=EDGE_CURVE ( 'NONE', #55329, #182665, #2574, .T. ) ;
#189231=CARTESIAN_POINT ( 'NONE',  ( 21.14999999999999858, 65.28660755661216797, -124.1731074845243654 ) ) ;
#189236=AXIS2_PLACEMENT_3D ( 'NONE', #240714, #178197, #176914 ) ;
#189249=VECTOR ( 'NONE', #127428, 1000.000000000000000 ) ;
#189267=CARTESIAN_POINT ( 'NONE',  ( -20.54999999999999716, 85.00000000001197975, -112.9170766071766820 ) ) ;
#189286=EDGE_CURVE ( 'NONE', #199333, #216543, #44298, .T. ) ;
#189309=VERTEX_POINT ( 'NONE', #9009 ) ;
#189313=ADVANCED_FACE ( 'NONE', ( #26017 ), #84648, .T. ) ;
#189324=ORIENTED_EDGE ( 'NONE', *, *, #5024, .T. ) ;
#189325=ORIENTED_EDGE ( 'NONE', *, *, #105832, .F. ) ;
#189331=ORIENTED_EDGE ( 'NONE', *, *, #56557, .T. ) ;
#189363=PLANE ( 'NONE',  #18104 ) ;
#189369=ORIENTED_EDGE ( 'NONE', *, *, #232459, .F. ) ;
#189370=ORIENTED_EDGE ( 'NONE', *, *, #146188, .T. ) ;
#189399=CIRCLE ( 'NONE', #101878, 0.5000000000000004441 ) ;
#189409=ORIENTED_EDGE ( 'NONE', *, *, #84100, .F. ) ;
#189431=VERTEX_POINT ( 'NONE', #54548 ) ;
#189448=CARTESIAN_POINT ( 'NONE',  ( 18.46921299892754931, 85.50937817783589878, -129.5365287751537835 ) ) ;
#189471=DIRECTION ( 'NONE',  ( 0.000000000000000000, -1.000000000000000000, -6.982962677686265922E-15 ) ) ;
#189483=EDGE_CURVE ( 'NONE', #205485, #25805, #48597, .T. ) ;
#189485=EDGE_CURVE ( 'NONE', #66400, #151038, #85995, .T. ) ;
#189493=CYLINDRICAL_SURFACE ( 'NONE', #248596, 0.1000000000000028644 ) ;
#189501=CARTESIAN_POINT ( 'NONE',  ( 22.59999999999999432, 75.90000000001222702, -148.1726782920690937 ) ) ;
#189525=LINE ( 'NONE', #250764, #41335 ) ;
#189537=CIRCLE ( 'NONE', #256081, 12.87499999999999822 ) ;
#189541=AXIS2_PLACEMENT_3D ( 'NONE', #3512, #118355, #23115 ) ;
#189546=CIRCLE ( 'NONE', #152136, 0.5000000000000004441 ) ;
#189555=ORIENTED_EDGE ( 'NONE', *, *, #106949, .F. ) ;
#189579=CARTESIAN_POINT ( 'NONE',  ( -21.05000000000000071, 87.65000000001192859, -105.9231074845242091 ) ) ;
#189590=AXIS2_PLACEMENT_3D ( 'NONE', #18993, #80221, #256257 ) ;
#189591=AXIS2_PLACEMENT_3D ( 'NONE', #53307, #51997, #149856 ) ;
#189595=DIRECTION ( 'NONE',  ( -1.000000000000000000, 2.952720810173289112E-16, 2.061873921506763405E-30 ) ) ;
#189598=ORIENTED_EDGE ( 'NONE', *, *, #161052, .T. ) ;
#189619=EDGE_CURVE ( 'NONE', #134440, #195402, #223373, .T. ) ;
#189621=ORIENTED_EDGE ( 'NONE', *, *, #72661, .F. ) ;
#189628=DIRECTION ( 'NONE',  ( -4.336808689941751890E-15, -0.8660254037844445918, -0.4999999999999897304 ) ) ;
#189632=DIRECTION ( 'NONE',  ( 0.000000000000000000, 0.000000000000000000, 1.000000000000000000 ) ) ;
#189635=FACE_OUTER_BOUND ( 'NONE', #85827, .T. ) ;
#189643=CARTESIAN_POINT ( 'NONE',  ( 18.46082813848004278, 85.48074965091954880, -129.4387373818085791 ) ) ;
#189646=AXIS2_PLACEMENT_3D ( 'NONE', #230592, #33711, #154924 ) ;
#189660=ORIENTED_EDGE ( 'NONE', *, *, #175313, .T. ) ;
#189673=EDGE_LOOP ( 'NONE', ( #202428, #168865, #34668, #244849 ) ) ;
#189682=AXIS2_PLACEMENT_3D ( 'NONE', #18542, #177645, #257094 ) ;
#189692=EDGE_CURVE ( 'NONE', #129910, #158778, #252788, .T. ) ;
#189716=DIRECTION ( 'NONE',  ( 1.000000000000000000, 0.000000000000000000, 0.000000000000000000 ) ) ;
#189732=DIRECTION ( 'NONE',  ( 1.000000000000000000, 0.000000000000000000, 0.000000000000000000 ) ) ;
#189757=ORIENTED_EDGE ( 'NONE', *, *, #88278, .F. ) ;
#189766=DIRECTION ( 'NONE',  ( 0.000000000000000000, -1.000000000000000000, 0.000000000000000000 ) ) ;
#189771=ORIENTED_EDGE ( 'NONE', *, *, #149237, .F. ) ;
#189794=CARTESIAN_POINT ( 'NONE',  ( -20.64999999999999858, 71.65000000001207070, -124.2731074845243313 ) ) ;
#189797=CARTESIAN_POINT ( 'NONE',  ( -18.59999999999999787, 74.65925378207852248, -146.7959699899454904 ) ) ;
#189833=CARTESIAN_POINT ( 'NONE',  ( -20.54999999999999716, 87.75000000001202238, -119.7731074845242176 ) ) ;
#189840=DIRECTION ( 'NONE',  ( 1.000000000000000000, 0.000000000000000000, 0.000000000000000000 ) ) ;
#189863=CARTESIAN_POINT ( 'NONE',  ( 18.59999999999999432, 85.48068669529082797, -96.08199231576637089 ) ) ;
#189872=EDGE_LOOP ( 'NONE', ( #133236, #153150, #151741, #142263 ) ) ;
#189890=PLANE ( 'NONE',  #240663 ) ;
#189897=CARTESIAN_POINT ( 'NONE',  ( -20.54999999999999716, 76.00000000001213607, -136.5231074845242745 ) ) ;
#189907=ADVANCED_FACE ( 'NONE', ( #218110 ), #119042, .T. ) ;
#189909=DIRECTION ( 'NONE',  ( -0.000000000000000000, -6.982962677686266711E-15, 1.000000000000000000 ) ) ;
#189916=DIRECTION ( 'NONE',  ( 1.000000000000000000, 0.000000000000000000, 0.000000000000000000 ) ) ;
#189919=CARTESIAN_POINT ( 'NONE',  ( 20.94999999999999574, 69.60000000001207354, -126.5926828544627654 ) ) ;
#189939=CIRCLE ( 'NONE', #244096, 0.1000000000000028644 ) ;
#189942=AXIS2_PLACEMENT_3D ( 'NONE', #179801, #1120, #80660 ) ;
#189948=CARTESIAN_POINT ( 'NONE',  ( 20.94999999999999929, 76.00000000001190870, -103.0231074845243029 ) ) ;
#190002=AXIS2_PLACEMENT_3D ( 'NONE', #112192, #191739, #133028 ) ;
#190007=AXIS2_PLACEMENT_3D ( 'NONE', #22369, #100561, #144848 ) ;
#190009=CARTESIAN_POINT ( 'NONE',  ( -21.93642651522410247, 68.67283376068633061, -136.5231074845243313 ) ) ;
#190022=FACE_OUTER_BOUND ( 'NONE', #30396, .T. ) ;
#190076=EDGE_CURVE ( 'NONE', #112033, #143411, #229694, .T. ) ;
#190104=VERTEX_POINT ( 'NONE', #18343 ) ;
#190106=CIRCLE ( 'NONE', #77635, 4.100000000000006750 ) ;
#190111=DIRECTION ( 'NONE',  ( 0.000000000000000000, 0.000000000000000000, 1.000000000000000000 ) ) ;
#190184=CIRCLE ( 'NONE', #65266, 0.09999999999999939493 ) ;
#190203=ADVANCED_FACE ( 'NONE', ( #137002 ), #144635, .F. ) ;
#190277=CARTESIAN_POINT ( 'NONE',  ( -18.44448725179913495, 85.49008171549517954, -96.39414719046173730 ) ) ;
#190340=ORIENTED_EDGE ( 'NONE', *, *, #205067, .F. ) ;
#190344=EDGE_CURVE ( 'NONE', #76136, #148869, #119724, .T. ) ;
#190359=EDGE_CURVE ( 'NONE', #17539, #156363, #153073, .T. ) ;
#190366=CARTESIAN_POINT ( 'NONE',  ( 21.05000000000000071, 76.00000000001190870, -103.0231074845243029 ) ) ;
#190375=CIRCLE ( 'NONE', #11286, 0.09999999999999939493 ) ;
#190399=CIRCLE ( 'NONE', #148700, 0.1000000000000028644 ) ;
#190483=CARTESIAN_POINT ( 'NONE',  ( -21.05000000000000071, 69.69257478044671927, -136.5062876161386498 ) ) ;
#190490=CIRCLE ( 'NONE', #182092, 0.1000000000000028644 ) ;
#190496=LINE ( 'NONE', #130484, #119413 ) ;
#190498=DIRECTION ( 'NONE',  ( -1.836970198721029934E-16, -1.000000000000000000, -6.982962677686266711E-15 ) ) ;
#190520=AXIS2_PLACEMENT_3D ( 'NONE', #8137, #49818, #15532 ) ;
#190526=VECTOR ( 'NONE', #77613, 1000.000000000000000 ) ;
#190557=FACE_OUTER_BOUND ( 'NONE', #101264, .T. ) ;
#190563=CARTESIAN_POINT ( 'NONE',  ( -21.05000000000000071, 87.48912529308817909, -133.4231074845242233 ) ) ;
#190621=VERTEX_POINT ( 'NONE', #255304 ) ;
#190626=CARTESIAN_POINT ( 'NONE',  ( 23.15000000000000213, 87.48912529308798014, -106.1231074845242262 ) ) ;
#190675=DIRECTION ( 'NONE',  ( 0.000000000000000000, -1.000000000000000000, -6.982962677686265922E-15 ) ) ;
#190693=EDGE_CURVE ( 'NONE', #162766, #231702, #140738, .T. ) ;
#190698=ORIENTED_EDGE ( 'NONE', *, *, #108553, .T. ) ;
#190702=CARTESIAN_POINT ( 'NONE',  ( 20.95545211741311320, 65.41358668846814339, -128.9369606249360629 ) ) ;
#190705=DIRECTION ( 'NONE',  ( 0.000000000000000000, 0.000000000000000000, 1.000000000000000000 ) ) ;
#190725=EDGE_CURVE ( 'NONE', #126029, #64409, #19317, .T. ) ;
#190739=DIRECTION ( 'NONE',  ( -0.000000000000000000, 1.000000000000000000, 6.982962677686266711E-15 ) ) ;
#190784=EDGE_LOOP ( 'NONE', ( #80431, #246140 ) ) ;
#190795=DIRECTION ( 'NONE',  ( -1.000000000000000000, 0.000000000000000000, -0.000000000000000000 ) ) ;
#190798=ORIENTED_EDGE ( 'NONE', *, *, #222663, .T. ) ;
#190801=FACE_OUTER_BOUND ( 'NONE', #201552, .T. ) ;
#190802=DIRECTION ( 'NONE',  ( 1.000000000000000000, 0.000000000000000000, 0.000000000000000000 ) ) ;
#190806=TOROIDAL_SURFACE ( 'NONE', #236542, 7.791421356237335338, 0.1000000000000000056 ) ;
#190825=AXIS2_PLACEMENT_3D ( 'NONE', #11860, #93933, #249172 ) ;
#190836=DIRECTION ( 'NONE',  ( 1.000000000000000000, 0.000000000000000000, -0.000000000000000000 ) ) ;
#190853=ORIENTED_EDGE ( 'NONE', *, *, #209246, .T. ) ;
#190861=DIRECTION ( 'NONE',  ( 1.000000000000000000, -3.469446951953718318E-14, 2.003086131649645455E-14 ) ) ;
#190862=TOROIDAL_SURFACE ( 'NONE', #145020, 11.70000000000000639, 0.1000000000000000056 ) ;
#190945=CARTESIAN_POINT ( 'NONE',  ( 18.47073956224740954, 85.47172941248408051, -129.4144217317060566 ) ) ;
#190963=ORIENTED_EDGE ( 'NONE', *, *, #97709, .F. ) ;
#190966=DIRECTION ( 'NONE',  ( -0.000000000000000000, -0.1350103645451835865, -0.9908441862701606873 ) ) ;
#190979=ORIENTED_EDGE ( 'NONE', *, *, #72754, .T. ) ;
#190993=EDGE_CURVE ( 'NONE', #117705, #174077, #34512, .T. ) ;
#190995=CARTESIAN_POINT ( 'NONE',  ( -21.05000000000000071, 74.83729825007408465, -128.5231074845243029 ) ) ;
#191005=EDGE_CURVE ( 'NONE', #254127, #131694, #209064, .T. ) ;
#191035=ORIENTED_EDGE ( 'NONE', *, *, #66914, .F. ) ;
#191067=ORIENTED_EDGE ( 'NONE', *, *, #171634, .F. ) ;
#191085=( BOUNDED_SURFACE ( )  B_SPLINE_SURFACE ( 3, 2, ( 
 ( #131943, #211488, #112395 ),
 ( #191955, #92807, #244832 ),
 ( #241001, #205704, #45359 ),
 ( #24538, #44079, #225254 ) ),
 .UNSPECIFIED., .F., .F., .F. ) 
 B_SPLINE_SURFACE_WITH_KNOTS ( ( 4, 4 ),
 ( 3, 3 ),
 ( -5.692061405548898279E-19, 0.0003124336117481333599 ),
 ( 0.000000000000000000, 1.000000000000000000 ),
 .UNSPECIFIED. ) 
 GEOMETRIC_REPRESENTATION_ITEM ( )  RATIONAL_B_SPLINE_SURFACE ( (
 ( 1.000000000000000000, 0.7040654476015839602, 1.000000000000000000),
 ( 1.000000000000000000, 0.7039193538781748360, 1.000000000000000000),
 ( 1.000000000000000000, 0.7089171279145581872, 1.000000000000000000),
 ( 1.000000000000000000, 0.7071067811865509034, 1.000000000000000000) ) ) 
 REPRESENTATION_ITEM ( '' )  SURFACE ( )  );
#191089=CARTESIAN_POINT ( 'NONE',  ( -22.50000000000000000, 76.00000000001217870, -142.7731074845243029 ) ) ;
#191113=CARTESIAN_POINT ( 'NONE',  ( -23.15000000000000213, 73.50000000001199396, -116.2477294072864140 ) ) ;
#191129=CARTESIAN_POINT ( 'NONE',  ( -23.25000000000000000, 85.60000000001208775, -126.6291383618717816 ) ) ;
#191137=CARTESIAN_POINT ( 'NONE',  ( -20.94999999999999929, 77.83534155023646406, -124.9679561919612922 ) ) ;
#191222=LINE ( 'NONE', #127369, #43049 ) ;
#191307=DIRECTION ( 'NONE',  ( -1.000000000000000000, -0.000000000000000000, -0.000000000000000000 ) ) ;
#191338=VERTEX_POINT ( 'NONE', #88658 ) ;
#191379=AXIS2_PLACEMENT_3D ( 'NONE', #218688, #40108, #119626 ) ;
#191404=EDGE_LOOP ( 'NONE', ( #197634, #70282, #158284, #190853 ) ) ;
#191411=AXIS2_PLACEMENT_3D ( 'NONE', #246488, #67850, #6589 ) ;
#191426=FACE_OUTER_BOUND ( 'NONE', #166472, .T. ) ;
#191427=DIRECTION ( 'NONE',  ( 1.000000000000000000, 0.000000000000000000, 0.000000000000000000 ) ) ;
#191429=EDGE_CURVE ( 'NONE', #181753, #61045, #232066, .T. ) ;
#191433=VECTOR ( 'NONE', #130722, 1000.000000000000000 ) ;
#191460=DIRECTION ( 'NONE',  ( 0.000000000000000000, 0.000000000000000000, 1.000000000000000000 ) ) ;
#191471=ORIENTED_EDGE ( 'NONE', *, *, #21277, .T. ) ;
#191481=DIRECTION ( 'NONE',  ( 0.000000000000000000, 1.000000000000000000, 0.000000000000000000 ) ) ;
#191504=EDGE_CURVE ( 'NONE', #182088, #49212, #158957, .T. ) ;
#191507=ORIENTED_EDGE ( 'NONE', *, *, #183639, .T. ) ;
#191519=CARTESIAN_POINT ( 'NONE',  ( -20.94999999999999929, 76.00000000001210765, -133.6231074845243256 ) ) ;
#191527=VERTEX_POINT ( 'NONE', #195517 ) ;
#191584=ADVANCED_FACE ( 'NONE', ( #35172 ), #217590, .T. ) ;
#191600=DIRECTION ( 'NONE',  ( 0.000000000000000000, 1.000000000000000000, 6.352154140967427193E-15 ) ) ;
#191636=CYLINDRICAL_SURFACE ( 'NONE', #100953, 0.5000000000000004441 ) ;
#191640=CARTESIAN_POINT ( 'NONE',  ( 18.59999999999999076, 69.55000000001199112, -115.2731074845243455 ) ) ;
#191659=ORIENTED_EDGE ( 'NONE', *, *, #44114, .T. ) ;
#191667=EDGE_LOOP ( 'NONE', ( #90124, #13440, #158156, #202050 ) ) ;
#191669=CARTESIAN_POINT ( 'NONE',  ( 18.46163235739473407, 85.48015080693014056, -96.36549694464677884 ) ) ;
#191714=DIRECTION ( 'NONE',  ( 0.000000000000000000, -0.1495327102803078179, -0.9887567792719429427 ) ) ;
#191739=DIRECTION ( 'NONE',  ( 1.000000000000000000, 0.000000000000000000, 0.000000000000000000 ) ) ;
#191745=CIRCLE ( 'NONE', #224992, 0.09999999999999489853 ) ;
#191748=AXIS2_PLACEMENT_3D ( 'NONE', #104466, #221844, #62802 ) ;
#191781=ORIENTED_EDGE ( 'NONE', *, *, #67408, .T. ) ;
#191788=CARTESIAN_POINT ( 'NONE',  ( 21.97500000000000497, 66.25000000001199396, -115.2731074845243597 ) ) ;
#191800=DIRECTION ( 'NONE',  ( 1.000000000000000000, -0.000000000000000000, 0.000000000000000000 ) ) ;
#191801=AXIS2_PLACEMENT_3D ( 'NONE', #170569, #248774, #46696 ) ;
#191802=ORIENTED_EDGE ( 'NONE', *, *, #120611, .T. ) ;
#191826=DIRECTION ( 'NONE',  ( 0.000000000000000000, -8.267618268485210697E-15, 1.000000000000000000 ) ) ;
#191828=CARTESIAN_POINT ( 'NONE',  ( 22.24259225415828922, 75.90093411655936961, -144.0150453550897112 ) ) ;
#191845=CARTESIAN_POINT ( 'NONE',  ( 21.05000000000000071, 65.37049252075115646, -128.8951280845284941 ) ) ;
#191852=ORIENTED_EDGE ( 'NONE', *, *, #178106, .F. ) ;
#191860=CARTESIAN_POINT ( 'NONE',  ( -20.54999999999999716, 73.50000000001199396, -116.2477294072864140 ) ) ;
#191863=CARTESIAN_POINT ( 'NONE',  ( 18.51024323315077069, 65.68895814178237913, -97.50265578621377927 ) ) ;
#191870=EDGE_CURVE ( 'NONE', #66650, #442, #91585, .T. ) ;
#191894=ORIENTED_EDGE ( 'NONE', *, *, #220625, .F. ) ;
#191930=VERTEX_POINT ( 'NONE', #62085 ) ;
#191952=CARTESIAN_POINT ( 'NONE',  ( -1.820710678118657944, 85.92928932189330737, -111.7731074845242176 ) ) ;
#191955=CARTESIAN_POINT ( 'NONE',  ( -22.45437739390954590, 76.00000000001222134, -148.1726782961185052 ) ) ;
#191956=EDGE_LOOP ( 'NONE', ( #140844, #225516, #152141, #244141 ) ) ;
#191957=DIRECTION ( 'NONE',  ( 1.000000000000000000, 0.000000000000000000, 0.000000000000000000 ) ) ;
#191966=DIRECTION ( 'NONE',  ( 1.000000000000000000, 0.000000000000000000, 0.000000000000000000 ) ) ;
#191968=ORIENTED_EDGE ( 'NONE', *, *, #226588, .T. ) ;
#191982=CARTESIAN_POINT ( 'NONE',  ( 20.94999999999999574, 65.52661458509918191, -128.9444530202758301 ) ) ;
#191983=CYLINDRICAL_SURFACE ( 'NONE', #57965, 0.1000000000000026007 ) ;
#192005=DIRECTION ( 'NONE',  ( -0.000000000000000000, 1.000000000000000000, 7.272083257015735086E-15 ) ) ;
#192019=EDGE_LOOP ( 'NONE', ( #236797, #164380, #150417, #124017 ) ) ;
#192051=DIRECTION ( 'NONE',  ( -7.304098846218134667E-16, 1.000000000000000000, 6.982962677686266711E-15 ) ) ;
#192091=VERTEX_POINT ( 'NONE', #30685 ) ;
#192105=CARTESIAN_POINT ( 'NONE',  ( -18.43707690579160641, 85.68240343348828958, -96.36626410711146207 ) ) ;
#192119=FACE_OUTER_BOUND ( 'NONE', #46916, .T. ) ;
#192136=ADVANCED_FACE ( 'NONE', ( #95740 ), #17500, .F. ) ;
#192142=CARTESIAN_POINT ( 'NONE',  ( -20.54999999999999716, 76.00000000001190870, -103.0231074845243029 ) ) ;
#192147=DIRECTION ( 'NONE',  ( 0.000000000000000000, 0.000000000000000000, -1.000000000000000000 ) ) ;
#192175=CARTESIAN_POINT ( 'NONE',  ( -23.25000000000000000, 71.85000000001198828, -115.3731074845243256 ) ) ;
#192183=CARTESIAN_POINT ( 'NONE',  ( -18.50000000000000000, 85.50000000001209344, -128.4231074845242233 ) ) ;
#192187=AXIS2_PLACEMENT_3D ( 'NONE', #190626, #133202, #172374 ) ;
#192211=CARTESIAN_POINT ( 'NONE',  ( 20.97468175916167255, 65.37473483564103560, -124.2683460491115852 ) ) ;
#192229=DIRECTION ( 'NONE',  ( 1.000000000000000000, 0.000000000000000000, 0.000000000000000000 ) ) ;
#192322=EDGE_CURVE ( 'NONE', #73777, #206383, #25152, .T. ) ;
#192323=DIRECTION ( 'NONE',  ( -0.000000000000000000, 0.1350103645451807555, 0.9908441862701610203 ) ) ;
#192361=DIRECTION ( 'NONE',  ( 1.000000000000000000, 0.000000000000000000, 0.000000000000000000 ) ) ;
#192381=CARTESIAN_POINT ( 'NONE',  ( -21.14999999999999858, 69.45934304831089889, -136.4231074845243654 ) ) ;
#192432=CARTESIAN_POINT ( 'NONE',  ( 20.94999999999999929, 70.50000000001205080, -124.1178414656112352 ) ) ;
#192438=CARTESIAN_POINT ( 'NONE',  ( -22.57848426163147693, 76.00426432929532439, -148.2731657914146126 ) ) ;
#192475=VERTEX_POINT ( 'NONE', #52461 ) ;
#192479=DIRECTION ( 'NONE',  ( 1.000000000000000000, -3.265361837132813093E-16, -2.280189983783949500E-30 ) ) ;
#192546=EDGE_CURVE ( 'NONE', #170720, #235551, #167006, .T. ) ;
#192572=CARTESIAN_POINT ( 'NONE',  ( -23.15000000000000213, 71.65000000001207070, -124.1731074845243228 ) ) ;
#192580=CARTESIAN_POINT ( 'NONE',  ( -20.94999999999999929, 76.00000000001199396, -114.7231074845243057 ) ) ;
#192601=FACE_OUTER_BOUND ( 'NONE', #67006, .T. ) ;
#192664=VERTEX_POINT ( 'NONE', #147095 ) ;
#192676=VECTOR ( 'NONE', #65397, 1000.000000000000000 ) ;
#192740=CARTESIAN_POINT ( 'NONE',  ( 21.05000000000000071, 76.00000000001190870, -103.0231074845243029 ) ) ;
#192750=CARTESIAN_POINT ( 'NONE',  ( -20.64999999999999858, 76.00000000001189449, -101.1231074845242972 ) ) ;
#192766=VERTEX_POINT ( 'NONE', #253900 ) ;
#192774=CARTESIAN_POINT ( 'NONE',  ( 21.05000000000000071, 67.22371711014432094, -124.3468923434561617 ) ) ;
#192776=VECTOR ( 'NONE', #236605, 1000.000000000000000 ) ;
#192783=CARTESIAN_POINT ( 'NONE',  ( -23.15000000000000213, 85.50000000001197975, -112.9170766071766820 ) ) ;
#192789=EDGE_LOOP ( 'NONE', ( #57996, #161348, #130243, #105303 ) ) ;
#192822=CARTESIAN_POINT ( 'NONE',  ( -21.05000000000000071, 64.40000000001195701, -109.9513107147998880 ) ) ;
#192840=DIRECTION ( 'NONE',  ( 0.000000000000000000, -0.008583690987162452199, -0.9999631594459053030 ) ) ;
#192850=EDGE_CURVE ( 'NONE', #76825, #110925, #187648, .T. ) ;
#192890=CARTESIAN_POINT ( 'NONE',  ( 20.94999999999999929, 71.00000000001199396, -115.4283735034374274 ) ) ;
#192903=TOROIDAL_SURFACE ( 'NONE', #213736, 12.77499999999999858, 0.1000000000000000056 ) ;
#192953=AXIS2_PLACEMENT_3D ( 'NONE', #83847, #200000, #163438 ) ;
#192970=DIRECTION ( 'NONE',  ( 1.000000000000000000, 0.000000000000000000, 0.000000000000000000 ) ) ;
#192974=CIRCLE ( 'NONE', #51449, 0.1000000000000028644 ) ;
#193014=VECTOR ( 'NONE', #34694, 1000.000000000000000 ) ;
#193019=LINE ( 'NONE', #33982, #232069 ) ;
#193026=CARTESIAN_POINT ( 'NONE',  ( 21.14999999999999858, 69.35000000001205933, -124.2731074845243455 ) ) ;
#193027=CARTESIAN_POINT ( 'NONE',  ( -23.15000000000000213, 64.40000000001195701, -109.9513107147998880 ) ) ;
#193045=ORIENTED_EDGE ( 'NONE', *, *, #188039, .F. ) ;
#193094=TOROIDAL_SURFACE ( 'NONE', #80624, 4.149999999999999467, 0.1000000000000000056 ) ;
#193116=DIRECTION ( 'NONE',  ( 0.000000000000000000, 6.982962677686266711E-15, -1.000000000000000000 ) ) ;
#193121=EDGE_CURVE ( 'NONE', #182942, #14587, #187235, .T. ) ;
#193123=ORIENTED_EDGE ( 'NONE', *, *, #202981, .T. ) ;
#193224=ORIENTED_EDGE ( 'NONE', *, *, #209757, .T. ) ;
#193238=DIRECTION ( 'NONE',  ( 2.952720810173289112E-16, 1.000000000000000000, 6.467318590049456648E-15 ) ) ;
#193244=ORIENTED_EDGE ( 'NONE', *, *, #177821, .F. ) ;
#193247=DIRECTION ( 'NONE',  ( 1.000000000000000000, 0.000000000000000000, 0.000000000000000000 ) ) ;
#193251=EDGE_CURVE ( 'NONE', #127664, #4373, #8186, .T. ) ;
#193269=DIRECTION ( 'NONE',  ( 1.000000000000000000, 0.000000000000000000, -0.000000000000000000 ) ) ;
#193273=CIRCLE ( 'NONE', #80807, 0.09999999999999939493 ) ;
#193279=ORIENTED_EDGE ( 'NONE', *, *, #116425, .T. ) ;
#193281=FACE_OUTER_BOUND ( 'NONE', #89640, .T. ) ;
#193285=CARTESIAN_POINT ( 'NONE',  ( 20.94999999999999574, 87.48912529308817909, -133.4231074845242233 ) ) ;
#193286=FACE_OUTER_BOUND ( 'NONE', #128694, .T. ) ;
#193298=AXIS2_PLACEMENT_3D ( 'NONE', #200426, #41378, #21800 ) ;
#193321=LINE ( 'NONE', #253271, #144339 ) ;
#193326=DIRECTION ( 'NONE',  ( 1.000000000000000000, -0.000000000000000000, 0.000000000000000000 ) ) ;
#193363=DIRECTION ( 'NONE',  ( 0.000000000000000000, -0.008583690987162452199, -0.9999631594459053030 ) ) ;
#193372=CARTESIAN_POINT ( 'NONE',  ( 21.14999999999999858, 64.35000000001221565, -148.2731074845243882 ) ) ;
#193374=AXIS2_PLACEMENT_3D ( 'NONE', #257946, #217564, #97607 ) ;
#193382=EDGE_CURVE ( 'NONE', #244668, #19771, #229118, .T. ) ;
#193383=CARTESIAN_POINT ( 'NONE',  ( 22.47007471830798409, 68.27928934808569750, -136.5231074845243597 ) ) ;
#193388=CARTESIAN_POINT ( 'NONE',  ( -23.15000000000000213, 64.35000000001195986, -110.0379132551783243 ) ) ;
#193454=CARTESIAN_POINT ( 'NONE',  ( -23.15000000000000213, 84.59626168225506149, -127.0729799673739677 ) ) ;
#193494=DIRECTION ( 'NONE',  ( 1.000000000000000000, 0.000000000000000000, 0.000000000000000000 ) ) ;
#193496=CIRCLE ( 'NONE', #197757, 0.1000000000000052097 ) ;
#193524=CARTESIAN_POINT ( 'NONE',  ( -23.25000000000000000, 76.00000000001216449, -140.5731074845242858 ) ) ;
#193536=ORIENTED_EDGE ( 'NONE', *, *, #185744, .F. ) ;
#193567=DIRECTION ( 'NONE',  ( 0.000000000000000000, -0.9908441862701420355, -0.1350103645453197554 ) ) ;
#193568=EDGE_CURVE ( 'NONE', #102067, #89168, #141629, .T. ) ;
#193585=FACE_OUTER_BOUND ( 'NONE', #35974, .T. ) ;
#193636=AXIS2_PLACEMENT_3D ( 'NONE', #193454, #194748, #361 ) ;
#193663=CARTESIAN_POINT ( 'NONE',  ( -23.15000000000000213, 64.35000000001198828, -115.1731074845243796 ) ) ;
#193669=DIRECTION ( 'NONE',  ( -1.000000000000000000, 2.952720810173289112E-16, 2.061873921506763405E-30 ) ) ;
#193677=DIRECTION ( 'NONE',  ( 1.000000000000000000, 0.000000000000000000, 0.000000000000000000 ) ) ;
#193712=CARTESIAN_POINT ( 'NONE',  ( -23.15000000000000213, 85.00000000001197975, -112.3170766071766735 ) ) ;
#193721=AXIS2_PLACEMENT_3D ( 'NONE', #137121, #77136, #159268 ) ;
#193725=CYLINDRICAL_SURFACE ( 'NONE', #25481, 0.1000000000000028644 ) ;
#193727=ORIENTED_EDGE ( 'NONE', *, *, #195361, .T. ) ;
#193755=CARTESIAN_POINT ( 'NONE',  ( -20.94999999999999929, 76.00000000001199396, -114.8231074845243000 ) ) ;
#193821=ORIENTED_EDGE ( 'NONE', *, *, #165644, .F. ) ;
#193833=VERTEX_POINT ( 'NONE', #180192 ) ;
#193840=DIRECTION ( 'NONE',  ( 1.000000000000000000, 0.000000000000000000, 0.000000000000000000 ) ) ;
#193863=DIRECTION ( 'NONE',  ( 1.000000000000000000, 0.000000000000000000, 0.000000000000000000 ) ) ;
#193885=ORIENTED_EDGE ( 'NONE', *, *, #116787, .F. ) ;
#193896=EDGE_CURVE ( 'NONE', #140147, #219486, #21040, .T. ) ;
#193905=VERTEX_POINT ( 'NONE', #210027 ) ;
#193925=EDGE_CURVE ( 'NONE', #69086, #23447, #191745, .T. ) ;
#193930=CARTESIAN_POINT ( 'NONE',  ( 21.05000000000000071, 67.18454772081454962, -128.1027149319100999 ) ) ;
#193943=PLANE ( 'NONE',  #257326 ) ;
#193945=ORIENTED_EDGE ( 'NONE', *, *, #25797, .F. ) ;
#193951=LINE ( 'NONE', #152271, #150468 ) ;
#193956=ADVANCED_FACE ( 'NONE', ( #31412 ), #100087, .F. ) ;
#193958=VECTOR ( 'NONE', #235659, 1000.000000000000000 ) ;
#193964=ORIENTED_EDGE ( 'NONE', *, *, #140522, .T. ) ;
#193991=CARTESIAN_POINT ( 'NONE',  ( -21.05000000000000071, 74.16465844978765176, -124.9679561919613207 ) ) ;
#194042=EDGE_CURVE ( 'NONE', #157579, #199005, #66987, .T. ) ;
#194050=ORIENTED_EDGE ( 'NONE', *, *, #231410, .F. ) ;
#194098=ADVANCED_FACE ( 'NONE', ( #211299 ), #251704, .F. ) ;
#194143=CARTESIAN_POINT ( 'NONE',  ( 20.02499999999999858, 66.25000000001199396, -115.2731074845243597 ) ) ;
#194196=ORIENTED_EDGE ( 'NONE', *, *, #4336, .T. ) ;
#194210=EDGE_LOOP ( 'NONE', ( #150351, #21043, #75502, #121858, #88515 ) ) ;
#194224=CARTESIAN_POINT ( 'NONE',  ( -21.14999999999999858, 76.10000000001222986, -148.1726782920690937 ) ) ;
#194225=DIRECTION ( 'NONE',  ( -0.000000000000000000, 1.000000000000000000, 6.352154140967427193E-15 ) ) ;
#194234=AXIS2_PLACEMENT_3D ( 'NONE', #107580, #142832, #222365 ) ;
#194248=EDGE_LOOP ( 'NONE', ( #47292, #79107, #2382, #225045, #116516 ) ) ;
#194249=ADVANCED_FACE ( 'NONE', ( #108985 ), #90708, .T. ) ;
#194269=AXIS2_PLACEMENT_3D ( 'NONE', #71726, #52128, #9169 ) ;
#194277=ORIENTED_EDGE ( 'NONE', *, *, #55144, .F. ) ;
#194308=ADVANCED_FACE ( 'NONE', ( #128565 ), #196335, .F. ) ;
#194321=EDGE_CURVE ( 'NONE', #89168, #239754, #71177, .T. ) ;
#194324=VECTOR ( 'NONE', #111313, 1000.000000000000000 ) ;
#194335=EDGE_CURVE ( 'NONE', #58001, #190621, #236635, .T. ) ;
#194372=DIRECTION ( 'NONE',  ( -1.000000000000000000, 0.000000000000000000, -0.000000000000000000 ) ) ;
#194428=AXIS2_PLACEMENT_3D ( 'NONE', #228794, #190966, #68428 ) ;
#194520=FACE_OUTER_BOUND ( 'NONE', #231313, .T. ) ;
#194530=ADVANCED_FACE ( 'NONE', ( #173714 ), #73309, .F. ) ;
#194536=VERTEX_POINT ( 'NONE', #113684 ) ;
#194553=EDGE_CURVE ( 'NONE', #147707, #175608, #14614, .T. ) ;
#194561=CARTESIAN_POINT ( 'NONE',  ( 22.49999999999999645, 75.91119002362528079, -148.1728704025562138 ) ) ;
#194575=CARTESIAN_POINT ( 'NONE',  ( 23.15000000000000213, 87.48912529308798014, -106.0231074845242176 ) ) ;
#194592=DIRECTION ( 'NONE',  ( 0.000000000000000000, -0.7397360091702802620, 0.6728971962616779878 ) ) ;
#194599=CIRCLE ( 'NONE', #195154, 0.1000000000000045158 ) ;
#194600=EDGE_CURVE ( 'NONE', #151185, #29926, #254742, .T. ) ;
#194601=CYLINDRICAL_SURFACE ( 'NONE', #45211, 0.1000000000000028644 ) ;
#194615=VERTEX_POINT ( 'NONE', #251374 ) ;
#194687=CARTESIAN_POINT ( 'NONE',  ( -18.59999999999999787, 85.52395432076465909, -96.14109042769693758 ) ) ;
#194692=CIRCLE ( 'NONE', #28081, 0.09999999999999939493 ) ;
#194748=DIRECTION ( 'NONE',  ( 0.000000000000000000, 0.7397360091702792628, -0.6728971962616790981 ) ) ;
#194835=VERTEX_POINT ( 'NONE', #41345 ) ;
#194842=CIRCLE ( 'NONE', #136535, 12.87499999999999822 ) ;
#194868=EDGE_LOOP ( 'NONE', ( #209841, #166108, #150338, #230657 ) ) ;
#194882=CARTESIAN_POINT ( 'NONE',  ( -18.50000000000000000, 85.40000000001187175, -96.14106563635156988 ) ) ;
#194886=CARTESIAN_POINT ( 'NONE',  ( 18.59999999999999787, 74.14897176987119565, -124.8691942151018139 ) ) ;
#194896=EDGE_CURVE ( 'NONE', #92332, #162858, #79972, .T. ) ;
#194924=CARTESIAN_POINT ( 'NONE',  ( 21.04999999999999361, 75.90156250001187743, -142.8223383946165370 ) ) ;
#194990=EDGE_CURVE ( 'NONE', #249019, #155941, #167514, .T. ) ;
#195000=ORIENTED_EDGE ( 'NONE', *, *, #31392, .F. ) ;
#195019=CIRCLE ( 'NONE', #232445, 11.80000000000000426 ) ;
#195080=AXIS2_PLACEMENT_3D ( 'NONE', #202280, #101863, #2771 ) ;
#195100=CIRCLE ( 'NONE', #61990, 0.09999999999999938105 ) ;
#195109=VECTOR ( 'NONE', #66980, 1000.000000000000000 ) ;
#195114=CIRCLE ( 'NONE', #7667, 0.09999999999998898659 ) ;
#195121=CARTESIAN_POINT ( 'NONE',  ( -20.99749315643148151, 64.25000000001195133, -110.0379132532841453 ) ) ;
#195140=CARTESIAN_POINT ( 'NONE',  ( 19.97071067811864609, 64.27928932189333011, -115.1731074845243796 ) ) ;
#195154=AXIS2_PLACEMENT_3D ( 'NONE', #89000, #66886, #48599 ) ;
#195159=CARTESIAN_POINT ( 'NONE',  ( 23.14999999999999858, 76.00000000001190870, -103.0231074845243029 ) ) ;
#195183=ORIENTED_EDGE ( 'NONE', *, *, #178552, .T. ) ;
#195220=AXIS2_PLACEMENT_3D ( 'NONE', #120530, #74985, #154532 ) ;
#195245=ORIENTED_EDGE ( 'NONE', *, *, #166425, .F. ) ;
#195250=ORIENTED_EDGE ( 'NONE', *, *, #44465, .F. ) ;
#195251=FACE_OUTER_BOUND ( 'NONE', #14354, .T. ) ;
#195287=DIRECTION ( 'NONE',  ( -3.469446951953515108E-14, 1.000000000000000000, 0.000000000000000000 ) ) ;
#195295=ADVANCED_FACE ( 'NONE', ( #38441 ), #117980, .F. ) ;
#195316=AXIS2_PLACEMENT_3D ( 'NONE', #133705, #15061, #115421 ) ;
#195357=ORIENTED_EDGE ( 'NONE', *, *, #85253, .F. ) ;
#195361=EDGE_CURVE ( 'NONE', #2705, #105079, #234066, .T. ) ;
#195363=DIRECTION ( 'NONE',  ( 1.000000000000000000, 0.000000000000000000, 0.000000000000000000 ) ) ;
#195402=VERTEX_POINT ( 'NONE', #41036 ) ;
#195467=ORIENTED_EDGE ( 'NONE', *, *, #193382, .T. ) ;
#195517=CARTESIAN_POINT ( 'NONE',  ( 23.24999999999999645, 71.22429906543263201, -124.6743393804783722 ) ) ;
#195523=LINE ( 'NONE', #53415, #155198 ) ;
#195540=DIRECTION ( 'NONE',  ( 1.000000000000000000, 0.000000000000000000, 0.000000000000000000 ) ) ;
#195572=DIRECTION ( 'NONE',  ( 0.000000000000000000, -1.000000000000000000, -6.982962677686265922E-15 ) ) ;
#195574=EDGE_CURVE ( 'NONE', #197779, #115956, #84411, .T. ) ;
#195623=DIRECTION ( 'NONE',  ( 0.000000000000000000, 0.8068669527896844551, 0.5907332058517525963 ) ) ;
#195686=ORIENTED_EDGE ( 'NONE', *, *, #223575, .T. ) ;
#195691=EDGE_CURVE ( 'NONE', #8870, #102921, #236340, .T. ) ;
#195701=LINE ( 'NONE', #256875, #43257 ) ;
#195707=DIRECTION ( 'NONE',  ( 0.000000000000000000, 0.9908441862701420355, 0.1350103645453197554 ) ) ;
#195724=CARTESIAN_POINT ( 'NONE',  ( 22.49999999999999645, 64.35023708198022518, -136.6119174609113145 ) ) ;
#195770=EDGE_LOOP ( 'NONE', ( #71909, #13258, #212304, #137634 ) ) ;
#195787=EDGE_CURVE ( 'NONE', #224814, #221149, #32868, .T. ) ;
#195806=DIRECTION ( 'NONE',  ( 1.000000000000000000, 0.000000000000000000, 0.000000000000000000 ) ) ;
#195807=ORIENTED_EDGE ( 'NONE', *, *, #207806, .T. ) ;
#195817=ORIENTED_EDGE ( 'NONE', *, *, #40915, .F. ) ;
#195823=DIRECTION ( 'NONE',  ( -0.000000000000000000, -0.8660254037844420383, 0.4999999999999943379 ) ) ;
#195846=VECTOR ( 'NONE', #104131, 1000.000000000000000 ) ;
#195852=DIRECTION ( 'NONE',  ( 0.000000000000000000, -6.982962677686266711E-15, 1.000000000000000000 ) ) ;
#195855=CARTESIAN_POINT ( 'NONE',  ( -20.54999999999999716, 85.40000000001207070, -126.6291383618717816 ) ) ;
#195889=CIRCLE ( 'NONE', #254108, 0.3999999999999975797 ) ;
#195926=ORIENTED_EDGE ( 'NONE', *, *, #90457, .F. ) ;
#195934=CARTESIAN_POINT ( 'NONE',  ( -21.07094088545368749, 75.90110629745997528, -142.8432747064414343 ) ) ;
#195957=CARTESIAN_POINT ( 'NONE',  ( 23.14999999999999503, 69.55000000001223270, -148.2731074845243597 ) ) ;
#195972=CARTESIAN_POINT ( 'NONE',  ( 21.14999999999999503, 87.75000000001222134, -148.2731074845242176 ) ) ;
#195995=DIRECTION ( 'NONE',  ( -1.000000000000000000, -0.000000000000000000, -0.000000000000000000 ) ) ;
#196006=LINE ( 'NONE', #30833, #168740 ) ;
#196030=CARTESIAN_POINT ( 'NONE',  ( -20.94999999999999929, 76.00000000001190870, -103.0231074845243029 ) ) ;
#196031=CARTESIAN_POINT ( 'NONE',  ( -18.40000000000000213, 85.51932773110452501, -129.5501311079649156 ) ) ;
#196063=CARTESIAN_POINT ( 'NONE',  ( 18.43579564894469414, 85.51932753530462605, -129.5501308406639112 ) ) ;
#196077=CARTESIAN_POINT ( 'NONE',  ( -20.64999999999999858, 74.07476635515223506, -123.7928639513981892 ) ) ;
#196083=DIRECTION ( 'NONE',  ( 1.000000000000000000, 0.000000000000000000, 0.000000000000000000 ) ) ;
#196125=LINE ( 'NONE', #199983, #151031 ) ;
#196128=ORIENTED_EDGE ( 'NONE', *, *, #194321, .T. ) ;
#196133=CIRCLE ( 'NONE', #116838, 0.1000000000000067224 ) ;
#196144=FACE_OUTER_BOUND ( 'NONE', #40413, .T. ) ;
#196164=CARTESIAN_POINT ( 'NONE',  ( -21.05000000000000071, 74.83729825007408465, -128.4231074845243086 ) ) ;
#196283=CARTESIAN_POINT ( 'NONE',  ( 18.59999999999999432, 70.30054753569064019, -149.0653814410941607 ) ) ;
#196287=DIRECTION ( 'NONE',  ( -1.000000000000000000, 0.000000000000000000, 0.000000000000000000 ) ) ;
#196335=TOROIDAL_SURFACE ( 'NONE', #83873, 0.4000000000000003553, 0.1000000000000000056 ) ;
#196341=ORIENTED_EDGE ( 'NONE', *, *, #123775, .T. ) ;
#196368=FACE_OUTER_BOUND ( 'NONE', #22487, .T. ) ;
#196377=DIRECTION ( 'NONE',  ( 0.000000000000000000, -6.982962677686266711E-15, 1.000000000000000000 ) ) ;
#196403=DIRECTION ( 'NONE',  ( -1.000000000000000000, 2.952720810173289112E-16, 2.061873921506763405E-30 ) ) ;
#196405=EDGE_CURVE ( 'NONE', #4010, #73777, #246997, .T. ) ;
#196408=CARTESIAN_POINT ( 'NONE',  ( -21.05000000000000071, 76.01465611852459858, -143.0197940702917094 ) ) ;
#196435=FACE_OUTER_BOUND ( 'NONE', #135386, .T. ) ;
#196440=ORIENTED_EDGE ( 'NONE', *, *, #53510, .T. ) ;
#196460=CARTESIAN_POINT ( 'NONE',  ( -20.54999999999999716, 85.00000000001207923, -126.6291383618717816 ) ) ;
#196481=EDGE_CURVE ( 'NONE', #63725, #181753, #609, .T. ) ;
#196499=CARTESIAN_POINT ( 'NONE',  ( -23.25000000000000000, 77.83585931145546510, -91.41866831572575336 ) ) ;
#196516=CIRCLE ( 'NONE', #109019, 0.1000000000000021427 ) ;
#196528=AXIS2_PLACEMENT_3D ( 'NONE', #220078, #3584, #199241 ) ;
#196545=CARTESIAN_POINT ( 'NONE',  ( 18.39999999999999858, 85.60000000001186038, -96.42291809330220076 ) ) ;
#196551=ORIENTED_EDGE ( 'NONE', *, *, #176363, .F. ) ;
#196561=EDGE_CURVE ( 'NONE', #13684, #139774, #47077, .T. ) ;
#196564=VERTEX_POINT ( 'NONE', #24084 ) ;
#196604=DIRECTION ( 'NONE',  ( 1.000000000000000000, -3.265361837132813093E-16, -2.280189983783949500E-30 ) ) ;
#196642=CARTESIAN_POINT ( 'NONE',  ( -22.49806830649814415, 64.35011034517307849, -136.6005718008498775 ) ) ;
#196665=ORIENTED_EDGE ( 'NONE', *, *, #83875, .F. ) ;
#196680=VERTEX_POINT ( 'NONE', #170040 ) ;
#196690=ADVANCED_FACE ( 'NONE', ( #248246 ), #147031, .T. ) ;
#196720=CARTESIAN_POINT ( 'NONE',  ( -23.15000000000000213, 74.07476635515219243, -115.7533510176504450 ) ) ;
#196728=CARTESIAN_POINT ( 'NONE',  ( -21.44999999999999929, 68.65000000001199965, -115.3731074845243540 ) ) ;
#196731=LINE ( 'NONE', #160209, #142493 ) ;
#196759=ORIENTED_EDGE ( 'NONE', *, *, #157174, .T. ) ;
#196798=CARTESIAN_POINT ( 'NONE',  ( -20.64999999999999858, 85.00000000001197975, -112.9170766071766820 ) ) ;
#196846=ORIENTED_EDGE ( 'NONE', *, *, #190993, .F. ) ;
#196870=EDGE_CURVE ( 'NONE', #201070, #87569, #251269, .T. ) ;
#196883=FACE_OUTER_BOUND ( 'NONE', #134500, .T. ) ;
#196900=DIRECTION ( 'NONE',  ( 1.000000000000000000, -0.000000000000000000, 0.000000000000000000 ) ) ;
#196902=CARTESIAN_POINT ( 'NONE',  ( 21.05000000000000071, 74.83729825007408465, -128.6231074845242972 ) ) ;
#196912=VECTOR ( 'NONE', #57180, 1000.000000000000000 ) ;
#196919=ADVANCED_FACE ( 'NONE', ( #143694 ), #88955, .F. ) ;
#196921=DIRECTION ( 'NONE',  ( 1.000000000000000000, 0.000000000000000000, 0.000000000000000000 ) ) ;
#196943=PLANE ( 'NONE',  #173491 ) ;
#196959=CARTESIAN_POINT ( 'NONE',  ( -20.64999999999999858, 74.07476635515219243, -115.7533510176504450 ) ) ;
#196967=CARTESIAN_POINT ( 'NONE',  ( -18.50000000000000000, 77.16270174995010223, -128.4231074845242802 ) ) ;
#196985=LINE ( 'NONE', #117475, #122188 ) ;
#196998=EDGE_CURVE ( 'NONE', #234281, #212214, #165852, .T. ) ;
#197013=ORIENTED_EDGE ( 'NONE', *, *, #241188, .T. ) ;
#197020=CARTESIAN_POINT ( 'NONE',  ( -20.94999999999999929, 76.00000000001207923, -128.6231074845242972 ) ) ;
#197039=DIRECTION ( 'NONE',  ( 0.000000000000000000, 0.000000000000000000, 1.000000000000000000 ) ) ;
#197068=VERTEX_POINT ( 'NONE', #249233 ) ;
#197072=CARTESIAN_POINT ( 'NONE',  ( 21.05000000000000071, 87.65000000001192859, -106.1231074845242262 ) ) ;
#197073=DIRECTION ( 'NONE',  ( 0.000000000000000000, -1.000000000000000000, 0.000000000000000000 ) ) ;
#197082=CYLINDRICAL_SURFACE ( 'NONE', #3383, 0.1000000000000028644 ) ;
#197134=CIRCLE ( 'NONE', #138835, 0.1000000000000064587 ) ;
#197151=CARTESIAN_POINT ( 'NONE',  ( -18.50596464788227635, 65.69367753730655579, -97.51892380663478832 ) ) ;
#197154=DIRECTION ( 'NONE',  ( 0.000000000000000000, -7.109473446599835262E-15, 1.000000000000000000 ) ) ;
#197157=CYLINDRICAL_SURFACE ( 'NONE', #67099, 0.09999999999999520384 ) ;
#197160=FACE_OUTER_BOUND ( 'NONE', #176543, .T. ) ;
#197170=DIRECTION ( 'NONE',  ( 0.000000000000000000, -1.000000000000000000, -6.982962677686266711E-15 ) ) ;
#197193=CARTESIAN_POINT ( 'NONE',  ( 22.59999954896768770, 76.00882823225471441, -148.2736161585922616 ) ) ;
#197206=VERTEX_POINT ( 'NONE', #105512 ) ;
#197210=DIRECTION ( 'NONE',  ( -0.000000000000000000, -6.982962677686266711E-15, 1.000000000000000000 ) ) ;
#197231=ADVANCED_FACE ( 'NONE', ( #84659 ), #125129, .T. ) ;
#197239=AXIS2_PLACEMENT_3D ( 'NONE', #121080, #221400, #58476 ) ;
#197247=VERTEX_POINT ( 'NONE', #3882 ) ;
#197251=DIRECTION ( 'NONE',  ( 0.000000000000000000, -1.000000000000000000, -6.982962677686265922E-15 ) ) ;
#197266=CIRCLE ( 'NONE', #84796, 0.1000000000000028644 ) ;
#197269=CARTESIAN_POINT ( 'NONE',  ( 20.96428641294180650, 64.25000000001195133, -109.8482143065826051 ) ) ;
#197273=CARTESIAN_POINT ( 'NONE',  ( 20.94999999999999929, 74.16465844978765176, -124.9679561919613207 ) ) ;
#197293=CARTESIAN_POINT ( 'NONE',  ( -18.49999999999999289, 85.32100840337339775, -129.2871692354463562 ) ) ;
#197297=ORIENTED_EDGE ( 'NONE', *, *, #241626, .F. ) ;
#197323=ORIENTED_EDGE ( 'NONE', *, *, #85939, .T. ) ;
#197343=DIRECTION ( 'NONE',  ( -1.000000000000000000, -0.000000000000000000, -0.000000000000000000 ) ) ;
#197362=DIRECTION ( 'NONE',  ( -0.000000000000000000, 0.4791956752371485107, 0.8777080977375185666 ) ) ;
#197413=FACE_OUTER_BOUND ( 'NONE', #118006, .T. ) ;
#197443=VERTEX_POINT ( 'NONE', #9016 ) ;
#197444=APPLICATION_CONTEXT ( 'automotive_design' ) ;
#197453=ORIENTED_EDGE ( 'NONE', *, *, #22397, .F. ) ;
#197465=DIRECTION ( 'NONE',  ( 1.000000000000000000, 0.000000000000000000, 0.000000000000000000 ) ) ;
#197478=LINE ( 'NONE', #99641, #78277 ) ;
#197505=DIRECTION ( 'NONE',  ( 0.000000000000000000, -0.8660254037844377084, -0.5000000000000016653 ) ) ;
#197519=AXIS2_PLACEMENT_3D ( 'NONE', #47884, #28378, #106566 ) ;
#197571=ORIENTED_EDGE ( 'NONE', *, *, #20263, .F. ) ;
#197585=AXIS2_PLACEMENT_3D ( 'NONE', #170215, #235257, #154486 ) ;
#197634=ORIENTED_EDGE ( 'NONE', *, *, #85910, .F. ) ;
#197637=CARTESIAN_POINT ( 'NONE',  ( -21.14999999999999858, 69.74218538953603286, -136.6208977758331287 ) ) ;
#197642=CARTESIAN_POINT ( 'NONE',  ( -18.59999999999999787, 66.85000000001205933, -124.1731074845243512 ) ) ;
#197669=FACE_OUTER_BOUND ( 'NONE', #213088, .T. ) ;
#197685=CARTESIAN_POINT ( 'NONE',  ( -1.739115166359751801E-14, 64.35000000001197407, -111.6731074845243796 ) ) ;
#197709=EDGE_CURVE ( 'NONE', #216286, #217224, #129622, .T. ) ;
#197728=DIRECTION ( 'NONE',  ( 0.000000000000000000, -1.000000000000000000, 0.000000000000000000 ) ) ;
#197757=AXIS2_PLACEMENT_3D ( 'NONE', #243768, #204624, #26015 ) ;
#197779=VERTEX_POINT ( 'NONE', #172651 ) ;
#197817=LINE ( 'NONE', #160008, #146686 ) ;
#197827=CARTESIAN_POINT ( 'NONE',  ( -20.85000000000001208, 64.25000000001196554, -109.9422547304830999 ) ) ;
#197845=DIRECTION ( 'NONE',  ( -1.000000000000000000, -0.000000000000000000, -0.000000000000000000 ) ) ;
#197847=DIRECTION ( 'NONE',  ( 0.000000000000000000, 1.000000000000000000, 7.116814260417668513E-15 ) ) ;
#197876=EDGE_LOOP ( 'NONE', ( #10578, #178916, #132914, #17345 ) ) ;
#197882=CIRCLE ( 'NONE', #189541, 0.1000000000000072220 ) ;
#197887=FACE_OUTER_BOUND ( 'NONE', #155713, .T. ) ;
#197897=ORIENTED_EDGE ( 'NONE', *, *, #212652, .F. ) ;
#197898=ORIENTED_EDGE ( 'NONE', *, *, #65669, .F. ) ;
#197954=VECTOR ( 'NONE', #43456, 1000.000000000000227 ) ;
#197962=DIRECTION ( 'NONE',  ( 0.000000000000000000, 0.9654727137038715545, -0.2605042016806676242 ) ) ;
#197991=ORIENTED_EDGE ( 'NONE', *, *, #194896, .F. ) ;
#198057=EDGE_CURVE ( 'NONE', #226700, #61549, #106061, .T. ) ;
#198082=VECTOR ( 'NONE', #78574, 1000.000000000000000 ) ;
#198084=EDGE_CURVE ( 'NONE', #82189, #20391, #60293, .T. ) ;
#198139=CIRCLE ( 'NONE', #148249, 12.97499999999999964 ) ;
#198169=EDGE_CURVE ( 'NONE', #16840, #178804, #239366, .T. ) ;
#198201=DIRECTION ( 'NONE',  ( -0.000000000000000000, -1.000000000000000000, -6.982962677686266711E-15 ) ) ;
#198202=ADVANCED_FACE ( 'NONE', ( #66332 ), #60461, .F. ) ;
#198209=DIRECTION ( 'NONE',  ( 0.000000000000000000, 0.000000000000000000, -1.000000000000000000 ) ) ;
#198268=EDGE_CURVE ( 'NONE', #64409, #129910, #39847, .T. ) ;
#198291=AXIS2_PLACEMENT_3D ( 'NONE', #146663, #163694, #8476 ) ;
#198296=VERTEX_POINT ( 'NONE', #78172 ) ;
#198320=CARTESIAN_POINT ( 'NONE',  ( 20.94999999999999929, 87.48912529308798014, -105.9231074845242091 ) ) ;
#198327=EDGE_CURVE ( 'NONE', #25668, #158504, #185562, .T. ) ;
#198331=AXIS2_PLACEMENT_3D ( 'NONE', #28877, #107068, #227019 ) ;
#198339=ORIENTED_EDGE ( 'NONE', *, *, #118034, .T. ) ;
#198348=DIRECTION ( 'NONE',  ( 1.000000000000000000, -3.265361837132813093E-16, -2.280189983783949500E-30 ) ) ;
#198372=CARTESIAN_POINT ( 'NONE',  ( 23.15000000000000213, 85.50000000001197975, -112.9170766071766820 ) ) ;
#198382=AXIS2_PLACEMENT_3D ( 'NONE', #52823, #211929, #154544 ) ;
#198398=CARTESIAN_POINT ( 'NONE',  ( -21.08134388332232589, 75.92418108250521414, -142.8577880650422571 ) ) ;
#198401=( LENGTH_UNIT ( ) NAMED_UNIT ( * ) SI_UNIT ( .MILLI., .METRE. ) );
#198408=DIRECTION ( 'NONE',  ( 0.000000000000000000, -0.9915357197604804940, 0.1298341882520397950 ) ) ;
#198417=LINE ( 'NONE', #4066, #146404 ) ;
#198440=CIRCLE ( 'NONE', #65167, 0.6000000000000033085 ) ;
#198442=CARTESIAN_POINT ( 'NONE',  ( -18.50211644919735576, 65.69792220476320210, -97.53355541284614105 ) ) ;
#198450=DIRECTION ( 'NONE',  ( 0.000000000000000000, -0.6728971962616412394, 0.7397360091703134577 ) ) ;
#198474=EDGE_CURVE ( 'NONE', #137392, #47866, #127594, .T. ) ;
#198502=ORIENTED_EDGE ( 'NONE', *, *, #119340, .F. ) ;
#198539=EDGE_CURVE ( 'NONE', #249019, #172315, #48005, .T. ) ;
#198560=AXIS2_PLACEMENT_3D ( 'NONE', #170388, #184751, #107787 ) ;
#198570=FACE_OUTER_BOUND ( 'NONE', #42709, .T. ) ;
#198591=AXIS2_PLACEMENT_3D ( 'NONE', #45523, #69920, #162926 ) ;
#198604=VECTOR ( 'NONE', #63411, 1000.000000000000000 ) ;
#198614=CARTESIAN_POINT ( 'NONE',  ( 21.05000000000000426, 69.69981666374590645, -136.5744349168656697 ) ) ;
#198670=CIRCLE ( 'NONE', #240213, 0.1000000000000028644 ) ;
#198686=ORIENTED_EDGE ( 'NONE', *, *, #112625, .T. ) ;
#198708=ORIENTED_EDGE ( 'NONE', *, *, #133257, .F. ) ;
#198711=CARTESIAN_POINT ( 'NONE',  ( -21.05000000000000071, 87.48912529308817909, -133.5231074845242176 ) ) ;
#198714=EDGE_CURVE ( 'NONE', #88928, #238533, #238230, .T. ) ;
#198746=CARTESIAN_POINT ( 'NONE',  ( 21.05000000000000071, 76.00000000001213607, -136.5231074845242745 ) ) ;
#198762=DIRECTION ( 'NONE',  ( 1.000000000000000000, 0.000000000000000000, 0.000000000000000000 ) ) ;
#198767=VECTOR ( 'NONE', #13748, 999.9999999999998863 ) ;
#198810=FACE_OUTER_BOUND ( 'NONE', #139848, .T. ) ;
#198833=ORIENTED_EDGE ( 'NONE', *, *, #137034, .T. ) ;
#198911=DIRECTION ( 'NONE',  ( 1.000000000000000000, 0.000000000000000000, 0.000000000000000000 ) ) ;
#198929=CARTESIAN_POINT ( 'NONE',  ( -18.59999999999999787, 64.35000000001208775, -129.5083017138703667 ) ) ;
#198950=VECTOR ( 'NONE', #64435, 1000.000000000000000 ) ;
#198956=DIRECTION ( 'NONE',  ( 1.000000000000000000, -3.265361837132813093E-16, -2.280189983783949500E-30 ) ) ;
#198959=ORIENTED_EDGE ( 'NONE', *, *, #238546, .T. ) ;
#198978=DIRECTION ( 'NONE',  ( -2.978066053179066272E-16, -1.000000000000000000, -8.338584948901384773E-15 ) ) ;
#198990=AXIS2_PLACEMENT_3D ( 'NONE', #194224, #237179, #61096 ) ;
#199000=AXIS2_PLACEMENT_3D ( 'NONE', #197637, #3276, #142782 ) ;
#199002=VERTEX_POINT ( 'NONE', #104488 ) ;
#199005=VERTEX_POINT ( 'NONE', #244017 ) ;
#199015=EDGE_LOOP ( 'NONE', ( #207370, #211422, #130344, #23013 ) ) ;
#199021=DIRECTION ( 'NONE',  ( 1.000000000000000000, 0.000000000000000000, 0.000000000000000000 ) ) ;
#199104=CARTESIAN_POINT ( 'NONE',  ( 21.03675099975491136, 67.12481996722722499, -124.1975653477462913 ) ) ;
#199108=DIRECTION ( 'NONE',  ( 0.000000000000000000, 6.982962677686266711E-15, -1.000000000000000000 ) ) ;
#199125=EDGE_CURVE ( 'NONE', #86736, #1482, #147778, .T. ) ;
#199166=ORIENTED_EDGE ( 'NONE', *, *, #132277, .F. ) ;
#199177=VECTOR ( 'NONE', #171177, 1000.000000000000000 ) ;
#199218=AXIS2_PLACEMENT_3D ( 'NONE', #56943, #136492, #239476 ) ;
#199241=DIRECTION ( 'NONE',  ( 1.000000000000000000, 0.000000000000000000, 0.000000000000000000 ) ) ;
#199292=ORIENTED_EDGE ( 'NONE', *, *, #52774, .T. ) ;
#199333=VERTEX_POINT ( 'NONE', #219013 ) ;
#199349=ORIENTED_EDGE ( 'NONE', *, *, #34489, .T. ) ;
#199429=EDGE_CURVE ( 'NONE', #200753, #213781, #47986, .T. ) ;
#199447=DIRECTION ( 'NONE',  ( -1.000000000000000000, 0.000000000000000000, -0.000000000000000000 ) ) ;
#199488=CIRCLE ( 'NONE', #87000, 0.09999999999999939493 ) ;
#199496=CIRCLE ( 'NONE', #128739, 0.2000000000000057288 ) ;
#199501=EDGE_LOOP ( 'NONE', ( #178231, #195250, #148344, #160411 ) ) ;
#199525=CARTESIAN_POINT ( 'NONE',  ( 20.30466543256828160, 66.69576306075789773, -128.2694448331316153 ) ) ;
#199605=ORIENTED_EDGE ( 'NONE', *, *, #142114, .F. ) ;
#199617=ADVANCED_FACE ( 'NONE', ( #93635 ), #153673, .F. ) ;
#199680=EDGE_CURVE ( 'NONE', #111107, #220201, #113199, .T. ) ;
#199682=ORIENTED_EDGE ( 'NONE', *, *, #140659, .T. ) ;
#199712=CARTESIAN_POINT ( 'NONE',  ( 22.39999999999999858, 68.20922040163875977, -136.6231074845243540 ) ) ;
#199728=CARTESIAN_POINT ( 'NONE',  ( 21.30000000000002558, 76.00000000001213607, -136.5231074845242745 ) ) ;
#199730=CYLINDRICAL_SURFACE ( 'NONE', #128422, 0.1000000000000026007 ) ;
#199739=AXIS2_PLACEMENT_3D ( 'NONE', #134367, #213927, #108415 ) ;
#199745=CIRCLE ( 'NONE', #91401, 0.1000000000000028644 ) ;
#199756=FACE_OUTER_BOUND ( 'NONE', #34055, .T. ) ;
#199760=CARTESIAN_POINT ( 'NONE',  ( -20.64999999999999858, 85.40000000001198543, -112.9170766071766820 ) ) ;
#199779=EDGE_CURVE ( 'NONE', #208687, #93015, #200439, .T. ) ;
#199787=DIRECTION ( 'NONE',  ( 0.000000000000000000, -6.982962677686266711E-15, 1.000000000000000000 ) ) ;
#199793=CARTESIAN_POINT ( 'NONE',  ( 22.49999999999999645, 75.90000000001222702, -148.1726782920690937 ) ) ;
#199801=CARTESIAN_POINT ( 'NONE',  ( -21.55000000000000071, 68.75000000001205080, -124.1731074845243370 ) ) ;
#199861=CARTESIAN_POINT ( 'NONE',  ( 20.99551997958429794, 64.25000000001158185, -109.8714483468354928 ) ) ;
#199872=EDGE_CURVE ( 'NONE', #70203, #8870, #26964, .T. ) ;
#199885=CARTESIAN_POINT ( 'NONE',  ( -23.15000000000000213, 74.00000000001205080, -123.2984855617622060 ) ) ;
#199887=CARTESIAN_POINT ( 'NONE',  ( -18.59999999999999787, 66.75000000001205080, -124.1731074845243654 ) ) ;
#199891=AXIS2_PLACEMENT_3D ( 'NONE', #119344, #80171, #60626 ) ;
#199895=VECTOR ( 'NONE', #174739, 1000.000000000000000 ) ;
#199929=ORIENTED_EDGE ( 'NONE', *, *, #176981, .T. ) ;
#199983=CARTESIAN_POINT ( 'NONE',  ( -23.25000000000000000, 65.66751761918668251, -97.42826094061121012 ) ) ;
#199995=AXIS2_PLACEMENT_3D ( 'NONE', #90160, #128035, #148887 ) ;
#199996=DIRECTION ( 'NONE',  ( -0.000000000000000000, 6.982962677686266711E-15, -1.000000000000000000 ) ) ;
#200000=DIRECTION ( 'NONE',  ( 0.000000000000000000, -1.000000000000000000, -7.109473446599835262E-15 ) ) ;
#200006=CARTESIAN_POINT ( 'NONE',  ( -18.50000000000000000, 76.00000000001190870, -103.0231074845243029 ) ) ;
#200037=CARTESIAN_POINT ( 'NONE',  ( -21.05000000000000071, 87.75000000001192291, -105.9231074845242091 ) ) ;
#200054=EDGE_CURVE ( 'NONE', #235865, #188797, #223136, .T. ) ;
#200152=DIRECTION ( 'NONE',  ( 1.000000000000000000, 0.000000000000000000, 0.000000000000000000 ) ) ;
#200154=EDGE_LOOP ( 'NONE', ( #66354, #254284, #114746, #221957 ) ) ;
#200167=EDGE_CURVE ( 'NONE', #163243, #80026, #52439, .T. ) ;
#200175=CARTESIAN_POINT ( 'NONE',  ( 23.14999999999998437, 76.00000000001213607, -136.5231074845242745 ) ) ;
#200231=AXIS2_PLACEMENT_3D ( 'NONE', #2926, #201139, #184135 ) ;
#200268=FACE_BOUND ( 'NONE', #170261, .T. ) ;
#200285=ORIENTED_EDGE ( 'NONE', *, *, #157153, .T. ) ;
#200301=CARTESIAN_POINT ( 'NONE',  ( 20.89192007715127986, 65.67101464000501210, -97.44043916224792667 ) ) ;
#200326=CIRCLE ( 'NONE', #388, 0.09999999999999939493 ) ;
#200360=CARTESIAN_POINT ( 'NONE',  ( -18.59999999999999787, 77.73625713160946304, -124.9544551555067926 ) ) ;
#200381=AXIS2_PLACEMENT_3D ( 'NONE', #174445, #90998, #233108 ) ;
#200391=DIRECTION ( 'NONE',  ( 1.000000000000000000, 0.000000000000000000, -0.000000000000000000 ) ) ;
#200410=CARTESIAN_POINT ( 'NONE',  ( 23.25000000000000000, 85.00000000001207923, -126.6291383618717816 ) ) ;
#200426=CARTESIAN_POINT ( 'NONE',  ( 20.04142135623730070, 64.35000000001198828, -115.1731074845243796 ) ) ;
#200439=LINE ( 'NONE', #180881, #248082 ) ;
#200450=DIRECTION ( 'NONE',  ( -6.938893903907222856E-15, -1.000000000000000000, -7.272083257015735086E-15 ) ) ;
#200495=DIRECTION ( 'NONE',  ( 0.000000000000000000, 0.000000000000000000, 1.000000000000000000 ) ) ;
#200554=DIRECTION ( 'NONE',  ( 0.000000000000000000, 0.000000000000000000, 1.000000000000000000 ) ) ;
#200566=EDGE_CURVE ( 'NONE', #14889, #235865, #31806, .T. ) ;
#200567=LINE ( 'NONE', #20670, #196912 ) ;
#200587=EDGE_LOOP ( 'NONE', ( #235847, #112677, #147988, #251784 ) ) ;
#200597=EDGE_CURVE ( 'NONE', #176995, #2636, #83373, .T. ) ;
#200608=ORIENTED_EDGE ( 'NONE', *, *, #218988, .F. ) ;
#200613=ADVANCED_FACE ( 'NONE', ( #125118 ), #240514, .T. ) ;
#200615=CARTESIAN_POINT ( 'NONE',  ( 20.85000000000000142, 77.83585931145546510, -91.51866831572576189 ) ) ;
#200652=EDGE_CURVE ( 'NONE', #246496, #25668, #69409, .T. ) ;
#200675=ADVANCED_FACE ( 'NONE', ( #147226 ), #145934, .T. ) ;
#200695=DIRECTION ( 'NONE',  ( 1.000000000000000000, -3.265361837132813093E-16, -2.280189983783949500E-30 ) ) ;
#200708=CARTESIAN_POINT ( 'NONE',  ( 21.14999999999999858, 76.00000000001213607, -136.4231074845243086 ) ) ;
#200718=VERTEX_POINT ( 'NONE', #237037 ) ;
#200739=LINE ( 'NONE', #101595, #2869 ) ;
#200753=VERTEX_POINT ( 'NONE', #36288 ) ;
#200779=AXIS2_PLACEMENT_3D ( 'NONE', #121184, #19489, #256749 ) ;
#200796=ORIENTED_EDGE ( 'NONE', *, *, #217708, .F. ) ;
#200802=ORIENTED_EDGE ( 'NONE', *, *, #213846, .F. ) ;
#200811=CARTESIAN_POINT ( 'NONE',  ( 21.08198257630413508, 69.66340326599708987, -136.5957508083089351 ) ) ;
#200836=CARTESIAN_POINT ( 'NONE',  ( 22.48970261584622321, 64.35000000001214460, -136.5784769727417824 ) ) ;
#200863=ORIENTED_EDGE ( 'NONE', *, *, #224641, .F. ) ;
#200867=CIRCLE ( 'NONE', #100864, 0.09999999999999939493 ) ;
#200916=DIRECTION ( 'NONE',  ( 1.000000000000000000, 0.000000000000000000, 0.000000000000000000 ) ) ;
#200933=LINE ( 'NONE', #39318, #5098 ) ;
#200953=ORIENTED_EDGE ( 'NONE', *, *, #111945, .F. ) ;
#200956=EDGE_CURVE ( 'NONE', #112369, #24275, #227784, .T. ) ;
#200989=TOROIDAL_SURFACE ( 'NONE', #80135, 2.100000000000002309, 0.1000000000000000056 ) ;
#201010=ORIENTED_EDGE ( 'NONE', *, *, #96499, .F. ) ;
#201059=DIRECTION ( 'NONE',  ( -1.000000000000000000, 0.000000000000000000, -0.000000000000000000 ) ) ;
#201070=VERTEX_POINT ( 'NONE', #152078 ) ;
#201086=CIRCLE ( 'NONE', #184496, 0.09999999999999939493 ) ;
#201092=EDGE_CURVE ( 'NONE', #116058, #148174, #71257, .T. ) ;
#201115=CARTESIAN_POINT ( 'NONE',  ( 18.49999999999999645, 74.26374286841466699, -124.9544551555068068 ) ) ;
#201123=DIRECTION ( 'NONE',  ( 0.000000000000000000, -1.000000000000000000, 0.000000000000000000 ) ) ;
#201139=DIRECTION ( 'NONE',  ( 1.000000000000000000, 0.000000000000000000, 0.000000000000000000 ) ) ;
#201184=EDGE_CURVE ( 'NONE', #241341, #226700, #94501, .T. ) ;
#201191=EDGE_LOOP ( 'NONE', ( #70688, #241045, #107171, #158251 ) ) ;
#201240=TOROIDAL_SURFACE ( 'NONE', #84685, 0.6000000000000015321, 0.1000000000000000056 ) ;
#201253=EDGE_CURVE ( 'NONE', #121611, #23447, #140471, .T. ) ;
#201262=ADVANCED_FACE ( 'NONE', ( #224855 ), #64512, .F. ) ;
#201265=EDGE_CURVE ( 'NONE', #185168, #102921, #169757, .T. ) ;
#201276=DIRECTION ( 'NONE',  ( 0.000000000000000000, 7.116814260417668513E-15, -1.000000000000000000 ) ) ;
#201282=CIRCLE ( 'NONE', #163699, 0.09999999999998898659 ) ;
#201308=LINE ( 'NONE', #185601, #141784 ) ;
#201372=CARTESIAN_POINT ( 'NONE',  ( 20.94999999999999929, 84.66355140188123585, -126.9990063664569391 ) ) ;
#201377=ORIENTED_EDGE ( 'NONE', *, *, #168743, .F. ) ;
#201380=DIRECTION ( 'NONE',  ( 1.000000000000000000, 0.000000000000000000, 0.000000000000000000 ) ) ;
#201389=CARTESIAN_POINT ( 'NONE',  ( -20.85000000000000142, 77.83585931145546510, -91.51866831572576189 ) ) ;
#201398=CARTESIAN_POINT ( 'NONE',  ( -21.05000000000000071, 74.16465844978765176, -124.8679561919613263 ) ) ;
#201401=CARTESIAN_POINT ( 'NONE',  ( -20.85000000000000142, 76.00000000001190870, -103.0231074845243029 ) ) ;
#201431=ORIENTED_EDGE ( 'NONE', *, *, #236806, .T. ) ;
#201452=TOROIDAL_SURFACE ( 'NONE', #43250, 0.2000000000000000111, 0.1000000000000000056 ) ;
#201459=DIRECTION ( 'NONE',  ( -0.000000000000000000, -6.982962677686266711E-15, 1.000000000000000000 ) ) ;
#201478=VECTOR ( 'NONE', #56775, 1000.000000000000000 ) ;
#201494=ADVANCED_FACE ( 'NONE', ( #219410 ), #140742, .T. ) ;
#201537=VERTEX_POINT ( 'NONE', #176033 ) ;
#201541=EDGE_CURVE ( 'NONE', #214613, #24834, #32381, .T. ) ;
#201544=CARTESIAN_POINT ( 'NONE',  ( -21.04999999999999716, 75.90156250001219007, -142.8223383946111937 ) ) ;
#201552=EDGE_LOOP ( 'NONE', ( #244183, #157428, #200802, #189369 ) ) ;
#201584=EDGE_LOOP ( 'NONE', ( #43319, #89982, #206814, #144211 ) ) ;
#201594=EDGE_CURVE ( 'NONE', #230546, #154466, #186469, .T. ) ;
#201607=ADVANCED_FACE ( 'NONE', ( #7877 ), #165671, .F. ) ;
#201618=CARTESIAN_POINT ( 'NONE',  ( -20.64999999999999858, 71.75000000001205080, -124.2731074845243313 ) ) ;
#201626=DIRECTION ( 'NONE',  ( -1.000000000000000000, 0.000000000000000000, 0.000000000000000000 ) ) ;
#201652=ORIENTED_EDGE ( 'NONE', *, *, #101499, .F. ) ;
#201657=CARTESIAN_POINT ( 'NONE',  ( -20.94999999999999929, 77.36242903720516040, -95.13422623660308375 ) ) ;
#201660=EDGE_CURVE ( 'NONE', #195402, #71875, #88649, .T. ) ;
#201684=CIRCLE ( 'NONE', #205777, 0.09999999999999939493 ) ;
#201724=DIRECTION ( 'NONE',  ( -0.000000000000000000, -0.01283462868040327436, 0.9999176327611370985 ) ) ;
#201732=ORIENTED_EDGE ( 'NONE', *, *, #153553, .T. ) ;
#201733=CARTESIAN_POINT ( 'NONE',  ( -23.25000000000000000, 76.00000000001190870, -103.0231074845243029 ) ) ;
#201746=DIRECTION ( 'NONE',  ( 1.000000000000000000, 7.304098846218133681E-16, 5.100424963727255128E-30 ) ) ;
#201766=ORIENTED_EDGE ( 'NONE', *, *, #242190, .F. ) ;
#201802=ORIENTED_EDGE ( 'NONE', *, *, #85294, .T. ) ;
#201809=AXIS2_PLACEMENT_3D ( 'NONE', #251439, #136605, #37538 ) ;
#201832=DIRECTION ( 'NONE',  ( 0.000000000000000000, 1.000000000000000000, 0.000000000000000000 ) ) ;
#201871=DIRECTION ( 'NONE',  ( -4.448008912761042820E-16, -1.000000000000000000, -7.116814260417668513E-15 ) ) ;
#201876=FACE_OUTER_BOUND ( 'NONE', #100792, .T. ) ;
#201879=AXIS2_PLACEMENT_3D ( 'NONE', #234774, #156557, #217752 ) ;
#201880=ORIENTED_EDGE ( 'NONE', *, *, #123122, .F. ) ;
#201900=FACE_OUTER_BOUND ( 'NONE', #73435, .T. ) ;
#201958=CARTESIAN_POINT ( 'NONE',  ( 21.05000000000000071, 69.45934304831089889, -136.4231074845243654 ) ) ;
#201967=CARTESIAN_POINT ( 'NONE',  ( 21.14999999999999858, 69.45934304831089889, -136.4231074845243654 ) ) ;
#201989=CARTESIAN_POINT ( 'NONE',  ( 23.14999999999999858, 76.00000000001190870, -103.0231074845243029 ) ) ;
#202024=AXIS2_PLACEMENT_3D ( 'NONE', #63268, #241903, #257565 ) ;
#202040=DIRECTION ( 'NONE',  ( 1.000000000000000000, 0.000000000000000000, 0.000000000000000000 ) ) ;
#202050=ORIENTED_EDGE ( 'NONE', *, *, #17351, .F. ) ;
#202052=AXIS2_PLACEMENT_3D ( 'NONE', #66098, #223870, #204312 ) ;
#202056=DIRECTION ( 'NONE',  ( 1.000000000000000000, 0.000000000000000000, 0.000000000000000000 ) ) ;
#202117=TOROIDAL_SURFACE ( 'NONE', #147947, 0.4000000000000012990, 0.1000000000000000056 ) ;
#202149=DIRECTION ( 'NONE',  ( 1.000000000000000000, -7.304098846218133681E-16, -4.639676173203992654E-30 ) ) ;
#202190=DIRECTION ( 'NONE',  ( 0.7071067811865127117, 0.7071067811865821007, 0.000000000000000000 ) ) ;
#202194=CARTESIAN_POINT ( 'NONE',  ( 23.14999999999999147, 71.85000000001214460, -136.5231074845243029 ) ) ;
#202202=ORIENTED_EDGE ( 'NONE', *, *, #95562, .F. ) ;
#202225=ORIENTED_EDGE ( 'NONE', *, *, #92766, .T. ) ;
#202239=DIRECTION ( 'NONE',  ( 0.000000000000000000, -1.000000000000000000, -6.860497997771531562E-15 ) ) ;
#202244=EDGE_CURVE ( 'NONE', #257983, #196680, #255079, .T. ) ;
#202280=CARTESIAN_POINT ( 'NONE',  ( -20.64999999999999858, 68.85000000001200249, -115.3731074845243540 ) ) ;
#202288=CARTESIAN_POINT ( 'NONE',  ( -1.820710678118658388, 85.92928932189330737, -111.8731074845242262 ) ) ;
#202313=CARTESIAN_POINT ( 'NONE',  ( 21.05000000000000071, 67.12791932463434819, -128.0020600656931720 ) ) ;
#202335=AXIS2_PLACEMENT_3D ( 'NONE', #74066, #12803, #253936 ) ;
#202373=CARTESIAN_POINT ( 'NONE',  ( 22.37643362114956247, 68.37421000605377230, -136.6221888582057318 ) ) ;
#202374=CARTESIAN_POINT ( 'NONE',  ( 18.59999999999999787, 77.85102823015292017, -124.8691942151017855 ) ) ;
#202385=ORIENTED_EDGE ( 'NONE', *, *, #180289, .T. ) ;
#202386=AXIS2_PLACEMENT_3D ( 'NONE', #121073, #58468, #78048 ) ;
#202421=EDGE_CURVE ( 'NONE', #246341, #6807, #27010, .T. ) ;
#202428=ORIENTED_EDGE ( 'NONE', *, *, #59638, .T. ) ;
#202451=ORIENTED_EDGE ( 'NONE', *, *, #231621, .F. ) ;
#202462=CIRCLE ( 'NONE', #52415, 0.09999999999999939493 ) ;
#202466=ORIENTED_EDGE ( 'NONE', *, *, #108175, .F. ) ;
#202480=CARTESIAN_POINT ( 'NONE',  ( 21.05000000000000071, 69.74115287693305731, -136.5548658375798254 ) ) ;
#202483=CIRCLE ( 'NONE', #190007, 0.2000000000000057288 ) ;
#202490=ORIENTED_EDGE ( 'NONE', *, *, #226869, .T. ) ;
#202497=DIRECTION ( 'NONE',  ( 0.000000000000000000, 0.000000000000000000, -1.000000000000000000 ) ) ;
#202540=VERTEX_POINT ( 'NONE', #488 ) ;
#202563=AXIS2_PLACEMENT_3D ( 'NONE', #167873, #28372, #246107 ) ;
#202592=VECTOR ( 'NONE', #243730, 1000.000000000000000 ) ;
#202595=CIRCLE ( 'NONE', #119393, 0.09999999999998712696 ) ;
#202598=DIRECTION ( 'NONE',  ( 0.000000000000000000, -1.000000000000000000, -8.717686153663073805E-15 ) ) ;
#202614=DIRECTION ( 'NONE',  ( -1.000000000000000000, 0.000000000000000000, -0.000000000000000000 ) ) ;
#202625=FACE_OUTER_BOUND ( 'NONE', #205486, .T. ) ;
#202673=CIRCLE ( 'NONE', #177767, 0.09999999999999459321 ) ;
#202677=ORIENTED_EDGE ( 'NONE', *, *, #94979, .T. ) ;
#202693=EDGE_LOOP ( 'NONE', ( #104375, #113201, #210864, #28738 ) ) ;
#202709=AXIS2_PLACEMENT_3D ( 'NONE', #203909, #85213, #146489 ) ;
#202715=ORIENTED_EDGE ( 'NONE', *, *, #118159, .T. ) ;
#202723=AXIS2_PLACEMENT_3D ( 'NONE', #31845, #238685, #77035 ) ;
#202728=PLANE ( 'NONE',  #118685 ) ;
#202781=DIRECTION ( 'NONE',  ( -2.978066053179066272E-16, -1.000000000000000000, -7.147358527629759053E-15 ) ) ;
#202784=CARTESIAN_POINT ( 'NONE',  ( -20.64999999999999858, 68.85000000001200249, -115.3731074845243540 ) ) ;
#202805=CARTESIAN_POINT ( 'NONE',  ( -20.85000000000000142, 76.00000000001190870, -103.0231074845243029 ) ) ;
#202849=ORIENTED_EDGE ( 'NONE', *, *, #2341, .T. ) ;
#202855=CARTESIAN_POINT ( 'NONE',  ( 20.84999999999998721, 65.66751761918668251, -97.42826094061121012 ) ) ;
#202938=LINE ( 'NONE', #245928, #70887 ) ;
#202940=LINE ( 'NONE', #82957, #57432 ) ;
#202951=PLANE ( 'NONE',  #19730 ) ;
#202953=ORIENTED_EDGE ( 'NONE', *, *, #228094, .F. ) ;
#202981=EDGE_CURVE ( 'NONE', #63725, #122081, #141226, .T. ) ;
#203012=CARTESIAN_POINT ( 'NONE',  ( -18.59999999999999787, 77.36242903720516040, -95.13422623660308375 ) ) ;
#203024=ADVANCED_FACE ( 'NONE', ( #152900 ), #49638, .F. ) ;
#203037=AXIS2_PLACEMENT_3D ( 'NONE', #19779, #21076, #138391 ) ;
#203045=DIRECTION ( 'NONE',  ( -1.000000000000000000, 0.000000000000000000, -0.000000000000000000 ) ) ;
#203046=AXIS2_PLACEMENT_3D ( 'NONE', #142657, #141387, #117981 ) ;
#203081=ORIENTED_EDGE ( 'NONE', *, *, #79613, .F. ) ;
#203150=CARTESIAN_POINT ( 'NONE',  ( 21.13461538461538325, 65.38541703798651383, -124.1731074845243654 ) ) ;
#203156=CARTESIAN_POINT ( 'NONE',  ( -21.05000000000000071, 69.45934304831089889, -136.5231074845243313 ) ) ;
#203172=DIRECTION ( 'NONE',  ( 0.000000000000000000, -0.9875055080513754913, 0.1575844902526733482 ) ) ;
#203200=CARTESIAN_POINT ( 'NONE',  ( -23.15000000000000213, 64.25000000001206502, -124.2731074845243882 ) ) ;
#203219=EDGE_CURVE ( 'NONE', #29923, #8334, #165729, .T. ) ;
#203240=DIRECTION ( 'NONE',  ( 0.000000000000000000, 0.000000000000000000, 1.000000000000000000 ) ) ;
#203243=CARTESIAN_POINT ( 'NONE',  ( -21.05000000000000071, 64.35000000001208775, -129.7392418215462158 ) ) ;
#203248=DIRECTION ( 'NONE',  ( 0.000000000000000000, 0.000000000000000000, -1.000000000000000000 ) ) ;
#203290=CARTESIAN_POINT ( 'NONE',  ( -22.46246831459151494, 75.97808783307279157, -148.1729720457342694 ) ) ;
#203299=AXIS2_PLACEMENT_3D ( 'NONE', #246881, #27879, #66967 ) ;
#203319=AXIS2_PLACEMENT_3D ( 'NONE', #139783, #58945, #219328 ) ;
#203325=FACE_OUTER_BOUND ( 'NONE', #255556, .T. ) ;
#203338=AXIS2_PLACEMENT_3D ( 'NONE', #182753, #204846, #220584 ) ;
#203378=CARTESIAN_POINT ( 'NONE',  ( 21.11101077988997332, 69.57631526528609811, -136.5383927534386430 ) ) ;
#203390=ADVANCED_FACE ( 'NONE', ( #178247 ), #119546, .T. ) ;
#203430=AXIS2_PLACEMENT_3D ( 'NONE', #107113, #65420, #27623 ) ;
#203444=AXIS2_PLACEMENT_3D ( 'NONE', #116478, #73526, #171360 ) ;
#203509=ADVANCED_FACE ( 'NONE', ( #146759 ), #47669, .T. ) ;
#203525=CARTESIAN_POINT ( 'NONE',  ( 21.05000000000000426, 76.01681986839787442, -142.8305327040896771 ) ) ;
#203552=CARTESIAN_POINT ( 'NONE',  ( -18.59999999999999787, 68.97833521811179480, -99.18954208262705663 ) ) ;
#203557=DIRECTION ( 'NONE',  ( 1.000000000000000000, 0.000000000000000000, 0.000000000000000000 ) ) ;
#203564=VECTOR ( 'NONE', #191800, 1000.000000000000000 ) ;
#203594=CYLINDRICAL_SURFACE ( 'NONE', #191748, 0.1000000000000028644 ) ;
#203602=EDGE_CURVE ( 'NONE', #23492, #245468, #7759, .T. ) ;
#203615=CIRCLE ( 'NONE', #53207, 0.1000000000000028644 ) ;
#203619=CARTESIAN_POINT ( 'NONE',  ( -22.48660254037843131, 64.25000000001212186, -136.5731074845243711 ) ) ;
#203622=DIRECTION ( 'NONE',  ( -1.000000000000000000, 0.000000000000000000, -0.000000000000000000 ) ) ;
#203628=FACE_OUTER_BOUND ( 'NONE', #114763, .T. ) ;
#203635=CARTESIAN_POINT ( 'NONE',  ( -21.05000000000000071, 87.65000000001192859, -106.0231074845242176 ) ) ;
#203677=EDGE_CURVE ( 'NONE', #4373, #93991, #16149, .T. ) ;
#203692=ORIENTED_EDGE ( 'NONE', *, *, #145336, .T. ) ;
#203707=ADVANCED_FACE ( 'NONE', ( #217016 ), #69181, .T. ) ;
#203713=EDGE_CURVE ( 'NONE', #173980, #19723, #149420, .T. ) ;
#203721=CYLINDRICAL_SURFACE ( 'NONE', #168785, 0.8750000000000007772 ) ;
#203724=FACE_OUTER_BOUND ( 'NONE', #78079, .T. ) ;
#203736=LINE ( 'NONE', #26399, #57526 ) ;
#203742=DIRECTION ( 'NONE',  ( 0.000000000000000000, 7.086529944415894657E-15, -1.000000000000000000 ) ) ;
#203759=ORIENTED_EDGE ( 'NONE', *, *, #151545, .F. ) ;
#203785=ORIENTED_EDGE ( 'NONE', *, *, #30368, .F. ) ;
#203803=DIRECTION ( 'NONE',  ( 1.000000000000000000, 0.000000000000000000, 0.000000000000000000 ) ) ;
#203809=CARTESIAN_POINT ( 'NONE',  ( 20.94999999999999929, 70.60000000001205933, -124.1178414656112352 ) ) ;
#203820=CARTESIAN_POINT ( 'NONE',  ( 18.49999999999999645, 70.30054753569064019, -149.0653814410941607 ) ) ;
#203822=EDGE_CURVE ( 'NONE', #111919, #121611, #42257, .T. ) ;
#203841=VERTEX_POINT ( 'NONE', #23993 ) ;
#203863=DIRECTION ( 'NONE',  ( 0.000000000000000000, 0.9908441862701791170, -0.1350103645450472789 ) ) ;
#203882=LINE ( 'NONE', #83896, #154860 ) ;
#203903=DIRECTION ( 'NONE',  ( 0.000000000000000000, 0.000000000000000000, 1.000000000000000000 ) ) ;
#203909=CARTESIAN_POINT ( 'NONE',  ( 23.14999999999999503, 64.35000000001204512, -124.3731074845243825 ) ) ;
#203912=CARTESIAN_POINT ( 'NONE',  ( 22.50000000000000000, 75.90000000001222702, -148.2731074845243029 ) ) ;
#203913=AXIS2_PLACEMENT_3D ( 'NONE', #126547, #125265, #26173 ) ;
#203916=AXIS2_PLACEMENT_3D ( 'NONE', #251647, #173456, #70484 ) ;
#203944=DIRECTION ( 'NONE',  ( 1.000000000000000000, 0.000000000000000000, 0.000000000000000000 ) ) ;
#203979=DIRECTION ( 'NONE',  ( 0.000000000000000000, 0.000000000000000000, 1.000000000000000000 ) ) ;
#204014=DIRECTION ( 'NONE',  ( 0.000000000000000000, 1.000000000000000000, 0.000000000000000000 ) ) ;
#204026=DIRECTION ( 'NONE',  ( 0.000000000000000000, 0.000000000000000000, 1.000000000000000000 ) ) ;
#204038=CARTESIAN_POINT ( 'NONE',  ( 21.05000000000000071, 69.35000000001207354, -126.6792853948412159 ) ) ;
#204039=ORIENTED_EDGE ( 'NONE', *, *, #36737, .T. ) ;
#204097=DIRECTION ( 'NONE',  ( 0.000000000000000000, 0.000000000000000000, 1.000000000000000000 ) ) ;
#204107=DIRECTION ( 'NONE',  ( 0.000000000000000000, 0.000000000000000000, -1.000000000000000000 ) ) ;
#204143=EDGE_CURVE ( 'NONE', #182615, #144364, #199496, .T. ) ;
#204146=CARTESIAN_POINT ( 'NONE',  ( 18.57071067811864040, 65.82071067813065213, -115.2731074845243597 ) ) ;
#204249=CARTESIAN_POINT ( 'NONE',  ( 18.39999999999999858, 85.68240343348826116, -96.36626410711143365 ) ) ;
#204292=ADVANCED_FACE ( 'NONE', ( #240153 ), #224423, .F. ) ;
#204309=ORIENTED_EDGE ( 'NONE', *, *, #178987, .T. ) ;
#204312=DIRECTION ( 'NONE',  ( 1.000000000000000000, 0.000000000000000000, 0.000000000000000000 ) ) ;
#204314=EDGE_LOOP ( 'NONE', ( #108642, #183507, #181152, #133836 ) ) ;
#204319=DIRECTION ( 'NONE',  ( 0.000000000000000000, -0.9915357197604982575, 0.1298341882519033486 ) ) ;
#204323=CARTESIAN_POINT ( 'NONE',  ( 21.07928932188134397, 69.67148334361883144, -136.6220026301787414 ) ) ;
#204375=CARTESIAN_POINT ( 'NONE',  ( -23.15000000000000213, 76.00000000001189449, -100.9231074845242944 ) ) ;
#204418=CARTESIAN_POINT ( 'NONE',  ( -18.50000000000000000, 64.35000000001222986, -148.2731074845243882 ) ) ;
#204429=CARTESIAN_POINT ( 'NONE',  ( -21.04999999999999716, 69.69982018209529429, -136.5745903664069090 ) ) ;
#204438=ORIENTED_EDGE ( 'NONE', *, *, #187017, .T. ) ;
#204446=CARTESIAN_POINT ( 'NONE',  ( -18.50000000000000000, 85.40000000001187175, -96.10844914155457275 ) ) ;
#204469=FACE_OUTER_BOUND ( 'NONE', #59947, .T. ) ;
#204530=AXIS2_PLACEMENT_3D ( 'NONE', #42353, #104849, #120625 ) ;
#204547=ORIENTED_EDGE ( 'NONE', *, *, #129068, .F. ) ;
#204554=AXIS2_PLACEMENT_3D ( 'NONE', #15492, #55845, #156299 ) ;
#204598=DIRECTION ( 'NONE',  ( -1.000000000000000000, 2.952720810173289112E-16, 2.061873921506763405E-30 ) ) ;
#204621=CARTESIAN_POINT ( 'NONE',  ( 20.58091095332318332, 66.98152984665834708, -128.1044573023665691 ) ) ;
#204624=DIRECTION ( 'NONE',  ( 2.342056488767301376E-15, 0.1350103645451835865, 0.9908441862701605762 ) ) ;
#204651=LINE ( 'NONE', #61308, #234547 ) ;
#204653=EDGE_CURVE ( 'NONE', #60670, #237888, #41245, .T. ) ;
#204658=CARTESIAN_POINT ( 'NONE',  ( 21.05000000000000071, 69.35000000001205933, -124.3731074845243540 ) ) ;
#204661=CARTESIAN_POINT ( 'NONE',  ( -20.85000000000000142, 64.35000000001195986, -109.8069731475024753 ) ) ;
#204683=VECTOR ( 'NONE', #111675, 1000.000000000000000 ) ;
#204701=AXIS2_PLACEMENT_3D ( 'NONE', #33786, #230671, #113279 ) ;
#204707=DIRECTION ( 'NONE',  ( 0.000000000000000000, -1.000000000000000000, -6.982962677686265922E-15 ) ) ;
#204708=ORIENTED_EDGE ( 'NONE', *, *, #96506, .F. ) ;
#204760=CARTESIAN_POINT ( 'NONE',  ( -23.25000000000000000, 76.00000000001213607, -136.5231074845242745 ) ) ;
#204840=EDGE_CURVE ( 'NONE', #234233, #231766, #46760, .T. ) ;
#204846=DIRECTION ( 'NONE',  ( 0.000000000000000000, 1.000000000000000000, 6.352154140967427193E-15 ) ) ;
#204847=DIRECTION ( 'NONE',  ( 1.000000000000000000, 0.000000000000000000, 0.000000000000000000 ) ) ;
#204886=DIRECTION ( 'NONE',  ( 0.000000000000000000, 0.000000000000000000, 1.000000000000000000 ) ) ;
#204892=CARTESIAN_POINT ( 'NONE',  ( -20.94999999999999929, 64.25000000001209344, -129.6815067946272677 ) ) ;
#204913=ORIENTED_EDGE ( 'NONE', *, *, #67489, .T. ) ;
#204930=CARTESIAN_POINT ( 'NONE',  ( -18.50000000000000000, 68.97833521811179480, -99.18954208262705663 ) ) ;
#204961=DIRECTION ( 'NONE',  ( -0.000000000000000000, 6.982962677686266711E-15, -1.000000000000000000 ) ) ;
#204979=ORIENTED_EDGE ( 'NONE', *, *, #4526, .T. ) ;
#204998=EDGE_CURVE ( 'NONE', #100578, #226855, #99837, .T. ) ;
#205003=CARTESIAN_POINT ( 'NONE',  ( 20.94999999999999574, 77.34908441863910866, -128.5366085209788025 ) ) ;
#205061=ORIENTED_EDGE ( 'NONE', *, *, #198084, .T. ) ;
#205067=EDGE_CURVE ( 'NONE', #76136, #191527, #212686, .T. ) ;
#205072=DIRECTION ( 'NONE',  ( 0.000000000000000000, 0.000000000000000000, 1.000000000000000000 ) ) ;
#205088=DIRECTION ( 'NONE',  ( 3.469446951953728416E-14, 0.8660254037844343777, -0.5000000000000074385 ) ) ;
#205118=FACE_OUTER_BOUND ( 'NONE', #136622, .T. ) ;
#205128=EDGE_CURVE ( 'NONE', #10477, #217558, #115607, .T. ) ;
#205155=DIRECTION ( 'NONE',  ( 1.040834085586049673E-13, 0.7899159663865300551, 0.6132151058540831201 ) ) ;
#205191=CARTESIAN_POINT ( 'NONE',  ( -20.93975676684922504, 65.68895814178239334, -97.50265578621379348 ) ) ;
#205226=AXIS2_PLACEMENT_3D ( 'NONE', #79330, #121081, #138019 ) ;
#205239=CARTESIAN_POINT ( 'NONE',  ( 21.05933563467872105, 65.27547528793073184, -124.3294597355684346 ) ) ;
#205241=ORIENTED_EDGE ( 'NONE', *, *, #181535, .F. ) ;
#205253=CARTESIAN_POINT ( 'NONE',  ( -20.64999999999999858, 74.00000000001205080, -123.2984855617622060 ) ) ;
#205333=DIRECTION ( 'NONE',  ( 1.000000000000000000, 0.000000000000000000, 0.000000000000000000 ) ) ;
#205347=DIRECTION ( 'NONE',  ( -0.000000000000000000, 0.9887567792719327286, 0.1495327102803745423 ) ) ;
#205366=AXIS2_PLACEMENT_3D ( 'NONE', #224763, #220906, #46134 ) ;
#205396=ORIENTED_EDGE ( 'NONE', *, *, #23485, .T. ) ;
#205421=CARTESIAN_POINT ( 'NONE',  ( -21.14999999999999858, 76.10085836911093793, -148.2726746080136877 ) ) ;
#205466=( BOUNDED_CURVE ( )  B_SPLINE_CURVE ( 3, ( #118271, #179544, #115701, #236924 ),
 .UNSPECIFIED., .F., .F. ) 
 B_SPLINE_CURVE_WITH_KNOTS ( ( 4, 4 ),
 ( 4.937700262165045813E-15, 1.570796326794912323 ),
 .UNSPECIFIED. ) 
 CURVE ( )  GEOMETRIC_REPRESENTATION_ITEM ( )  RATIONAL_B_SPLINE_CURVE ( ( 1.000000000000000000, 0.8047378541243623840, 0.8047378541243623840, 1.000000000000000000 ) ) 
 REPRESENTATION_ITEM ( '' )  );
#205474=CARTESIAN_POINT ( 'NONE',  ( -23.15000000000000213, 74.00000000001205080, -123.7984855617622060 ) ) ;
#205485=VERTEX_POINT ( 'NONE', #102218 ) ;
#205486=EDGE_LOOP ( 'NONE', ( #127755, #232055, #242940, #56392, #252048, #142735, #256350, #219761, #77917, #76202, #46334, #39904, #112427, #137565, #224712, #244049, #227731, #66007, #91038, #189598, #185904, #159699, #113367, #151712, #17137, #119480, #53943 ) ) ;
#205510=EDGE_CURVE ( 'NONE', #238533, #188914, #83635, .T. ) ;
#205559=CARTESIAN_POINT ( 'NONE',  ( -21.05000000000000071, 76.00000000001213607, -136.5231074845242745 ) ) ;
#205594=DIRECTION ( 'NONE',  ( 0.000000000000000000, -1.000000000000000000, -6.982962677686266711E-15 ) ) ;
#205609=CARTESIAN_POINT ( 'NONE',  ( -21.56666275994540172, 76.00000000001219291, -143.4804758914176261 ) ) ;
#205637=ORIENTED_EDGE ( 'NONE', *, *, #180068, .F. ) ;
#205646=DIRECTION ( 'NONE',  ( 1.000000000000000000, 0.000000000000000000, 0.000000000000000000 ) ) ;
#205669=DIRECTION ( 'NONE',  ( 1.000000000000000000, 0.000000000000000000, 0.000000000000000000 ) ) ;
#205689=EDGE_CURVE ( 'NONE', #207616, #188655, #73441, .T. ) ;
#205704=CARTESIAN_POINT ( 'NONE',  ( -22.50047199487877947, 75.95509394809208459, -148.2731549034355112 ) ) ;
#205748=DIRECTION ( 'NONE',  ( 0.000000000000000000, -1.000000000000000000, -6.982962677686266711E-15 ) ) ;
#205777=AXIS2_PLACEMENT_3D ( 'NONE', #204661, #165568, #2611 ) ;
#205783=CARTESIAN_POINT ( 'NONE',  ( 20.94999999999999574, 74.73821383144705521, -128.4366085209788366 ) ) ;
#205829=CARTESIAN_POINT ( 'NONE',  ( -21.46681500593010838, 69.14248884062493516, -136.5231074845243597 ) ) ;
#205844=DIRECTION ( 'NONE',  ( 1.000000000000000000, 0.000000000000000000, 0.000000000000000000 ) ) ;
#205916=DIRECTION ( 'NONE',  ( 0.000000000000000000, -6.982962677686266711E-15, 1.000000000000000000 ) ) ;
#205924=CARTESIAN_POINT ( 'NONE',  ( -20.64999999999999858, 85.00000000001197975, -112.5170766071766764 ) ) ;
#205976=EDGE_CURVE ( 'NONE', #242949, #213781, #161957, .T. ) ;
#206000=DIRECTION ( 'NONE',  ( -1.000000000000000000, 0.000000000000000000, -0.000000000000000000 ) ) ;
#206031=ORIENTED_EDGE ( 'NONE', *, *, #243413, .F. ) ;
#206066=AXIS2_PLACEMENT_3D ( 'NONE', #116850, #196377, #93422 ) ;
#206067=VERTEX_POINT ( 'NONE', #170974 ) ;
#206092=VECTOR ( 'NONE', #62084, 1000.000000000000000 ) ;
#206144=VECTOR ( 'NONE', #230303, 1000.000000000000114 ) ;
#206146=CARTESIAN_POINT ( 'NONE',  ( 20.85000000000000142, 87.65000000001190017, -103.0231074845242176 ) ) ;
#206154=AXIS2_PLACEMENT_3D ( 'NONE', #257238, #159491, #219428 ) ;
#206162=EDGE_CURVE ( 'NONE', #168985, #82680, #142752, .T. ) ;
#206175=FILL_AREA_STYLE ('',( #181490 ) ) ;
#206180=CARTESIAN_POINT ( 'NONE',  ( 21.12400247839514122, 65.27851195598167067, -124.2731074845243739 ) ) ;
#206201=CARTESIAN_POINT ( 'NONE',  ( 23.25000000000000000, 84.59626168225496201, -112.4732350016745244 ) ) ;
#206250=FACE_OUTER_BOUND ( 'NONE', #117097, .T. ) ;
#206259=AXIS2_PLACEMENT_3D ( 'NONE', #10842, #52511, #49951 ) ;
#206291=LINE ( 'NONE', #10660, #5337 ) ;
#206358=CARTESIAN_POINT ( 'NONE',  ( -18.59999999999999787, 77.83585931145546510, -91.51866831572576189 ) ) ;
#206361=DIRECTION ( 'NONE',  ( 0.000000000000000000, -6.982962677686266711E-15, 1.000000000000000000 ) ) ;
#206383=VERTEX_POINT ( 'NONE', #82054 ) ;
#206394=CIRCLE ( 'NONE', #177389, 2.000000000000001776 ) ;
#206427=EDGE_CURVE ( 'NONE', #9803, #257751, #50657, .T. ) ;
#206431=CARTESIAN_POINT ( 'NONE',  ( 18.60000000000001563, 85.36423601037887465, -129.3428530837995822 ) ) ;
#206445=ADVANCED_FACE ( 'NONE', ( #253653 ), #145900, .T. ) ;
#206447=CARTESIAN_POINT ( 'NONE',  ( -23.25000000000000000, 64.25000000001190870, -103.0231074845243882 ) ) ;
#206455=DIRECTION ( 'NONE',  ( 0.000000000000000000, 7.116814260417668513E-15, -1.000000000000000000 ) ) ;
#206495=CARTESIAN_POINT ( 'NONE',  ( 21.05000000000000071, 76.00000000001216449, -140.8231074845243143 ) ) ;
#206502=ORIENTED_EDGE ( 'NONE', *, *, #180946, .T. ) ;
#206523=CARTESIAN_POINT ( 'NONE',  ( 20.94999999999999929, 85.00000000001197975, -112.9170766071766820 ) ) ;
#206536=VERTEX_POINT ( 'NONE', #102263 ) ;
#206542=CARTESIAN_POINT ( 'NONE',  ( 21.12769345151713196, 65.28071232307149785, -124.2756271383268967 ) ) ;
#206593=ORIENTED_EDGE ( 'NONE', *, *, #83693, .T. ) ;
#206601=DIRECTION ( 'NONE',  ( -1.000000000000000000, 7.304098846218164250E-16, -4.217023435051628197E-16 ) ) ;
#206605=FACE_OUTER_BOUND ( 'NONE', #119743, .T. ) ;
#206610=DIRECTION ( 'NONE',  ( -5.603264701231743991E-32, -7.172728831056617961E-15, 1.000000000000000000 ) ) ;
#206625=CARTESIAN_POINT ( 'NONE',  ( 18.54147908293604985, 85.46326165794013718, -129.4741585877683292 ) ) ;
#206645=EDGE_CURVE ( 'NONE', #18233, #153656, #74757, .T. ) ;
#206647=VERTEX_POINT ( 'NONE', #87851 ) ;
#206678=EDGE_CURVE ( 'NONE', #146024, #185168, #104812, .T. ) ;
#206682=DIRECTION ( 'NONE',  ( 1.000000000000000000, 0.000000000000000000, 0.000000000000000000 ) ) ;
#206688=CARTESIAN_POINT ( 'NONE',  ( -21.45000000000000284, 68.29142135624935861, -124.1731074845243512 ) ) ;
#206692=CIRCLE ( 'NONE', #189942, 0.1000000000000028644 ) ;
#206718=ORIENTED_EDGE ( 'NONE', *, *, #132986, .F. ) ;
#206749=AXIS2_PLACEMENT_3D ( 'NONE', #256105, #20144, #158396 ) ;
#206752=AXIS2_PLACEMENT_3D ( 'NONE', #178751, #224242, #123882 ) ;
#206766=CARTESIAN_POINT ( 'NONE',  ( -22.47071067811865319, 76.00000000001213607, -136.5231074845242745 ) ) ;
#206780=EDGE_CURVE ( 'NONE', #197206, #18414, #85872, .T. ) ;
#206797=AXIS2_PLACEMENT_3D ( 'NONE', #116719, #55427, #33375 ) ;
#206814=ORIENTED_EDGE ( 'NONE', *, *, #43737, .F. ) ;
#206828=EDGE_CURVE ( 'NONE', #197443, #132227, #58993, .T. ) ;
#206856=DIRECTION ( 'NONE',  ( -1.000000000000000000, 0.000000000000000000, 0.000000000000000000 ) ) ;
#206897=DIRECTION ( 'NONE',  ( 0.000000000000000000, 0.000000000000000000, -1.000000000000000000 ) ) ;
#206920=AXIS2_PLACEMENT_3D ( 'NONE', #202288, #103162, #242681 ) ;
#206933=CARTESIAN_POINT ( 'NONE',  ( -20.85000000000000142, 77.83585931145546510, -91.51866831572576189 ) ) ;
#206937=AXIS2_PLACEMENT_3D ( 'NONE', #253909, #75318, #234351 ) ;
#207001=CARTESIAN_POINT ( 'NONE',  ( -20.94999999999999929, 68.97833521811179480, -99.38954208262707368 ) ) ;
#207015=CARTESIAN_POINT ( 'NONE',  ( -21.05000000000000071, 69.52192177891714664, -136.4231075492198784 ) ) ;
#207037=ORIENTED_EDGE ( 'NONE', *, *, #145410, .T. ) ;
#207077=LINE ( 'NONE', #29752, #207239 ) ;
#207095=FACE_OUTER_BOUND ( 'NONE', #95130, .T. ) ;
#207160=EDGE_CURVE ( 'NONE', #187556, #206536, #142602, .T. ) ;
#207167=AXIS2_PLACEMENT_3D ( 'NONE', #41346, #98677, #257739 ) ;
#207172=DIRECTION ( 'NONE',  ( 1.000000000000000000, 0.000000000000000000, 0.000000000000000000 ) ) ;
#207183=EDGE_LOOP ( 'NONE', ( #58387, #72078, #157549, #59731 ) ) ;
#207192=DIRECTION ( 'NONE',  ( 0.000000000000000000, 6.938893903907222067E-15, -1.000000000000000000 ) ) ;
#207198=ORIENTED_EDGE ( 'NONE', *, *, #71790, .F. ) ;
#207210=LINE ( 'NONE', #92369, #68558 ) ;
#207217=DIRECTION ( 'NONE',  ( 0.000000000000000000, -1.000000000000000000, -8.717686153663073805E-15 ) ) ;
#207239=VECTOR ( 'NONE', #149689, 1000.000000000000000 ) ;
#207297=CARTESIAN_POINT ( 'NONE',  ( 18.49999999999999289, 64.35000000001197407, -111.6731074845243796 ) ) ;
#207299=DIRECTION ( 'NONE',  ( 1.000000000000000000, 0.000000000000000000, 0.000000000000000000 ) ) ;
#207317=VERTEX_POINT ( 'NONE', #126389 ) ;
#207360=VERTEX_POINT ( 'NONE', #2579 ) ;
#207370=ORIENTED_EDGE ( 'NONE', *, *, #154504, .T. ) ;
#207385=EDGE_CURVE ( 'NONE', #164329, #151038, #933, .T. ) ;
#207390=CIRCLE ( 'NONE', #94924, 2.100000000000004530 ) ;
#207393=AXIS2_PLACEMENT_3D ( 'NONE', #135483, #1097, #215040 ) ;
#207395=ORIENTED_EDGE ( 'NONE', *, *, #55144, .T. ) ;
#207411=ORIENTED_EDGE ( 'NONE', *, *, #37662, .F. ) ;
#207421=CARTESIAN_POINT ( 'NONE',  ( -21.05000000000000071, 70.15000000001211333, -126.3906102602463619 ) ) ;
#207452=ADVANCED_FACE ( 'NONE', ( #246343 ), #212368, .T. ) ;
#207459=EDGE_CURVE ( 'NONE', #229115, #89242, #159400, .T. ) ;
#207473=EDGE_CURVE ( 'NONE', #211151, #147787, #209787, .T. ) ;
#207493=CARTESIAN_POINT ( 'NONE',  ( -22.49533356619861735, 64.34999999370803891, -136.5882300648471244 ) ) ;
#207495=DIRECTION ( 'NONE',  ( 0.000000000000000000, 7.026728003956683390E-15, -1.000000000000000000 ) ) ;
#207530=ORIENTED_EDGE ( 'NONE', *, *, #19975, .T. ) ;
#207534=ORIENTED_EDGE ( 'NONE', *, *, #22397, .T. ) ;
#207556=CARTESIAN_POINT ( 'NONE',  ( 18.56579813702275317, 65.66974365629664590, -97.43601455626048846 ) ) ;
#207616=VERTEX_POINT ( 'NONE', #2261 ) ;
#207622=EDGE_CURVE ( 'NONE', #152046, #70458, #34505, .T. ) ;
#207631=VERTEX_POINT ( 'NONE', #119678 ) ;
#207643=VERTEX_POINT ( 'NONE', #124806 ) ;
#207645=EDGE_LOOP ( 'NONE', ( #91844, #54647, #162544, #29540 ) ) ;
#207649=ORIENTED_EDGE ( 'NONE', *, *, #77470, .F. ) ;
#207665=ORIENTED_EDGE ( 'NONE', *, *, #19151, .F. ) ;
#207696=DIRECTION ( 'NONE',  ( 0.000000000000000000, -0.4999999999999689138, -0.8660254037844565822 ) ) ;
#207709=VERTEX_POINT ( 'NONE', #3556 ) ;
#207718=DIRECTION ( 'NONE',  ( -0.000000000000000000, -0.8700118002898356018, 0.4930308989875170078 ) ) ;
#207728=DIRECTION ( 'NONE',  ( 0.7071067811865474617, -0.7071067811865474617, -4.937700262164531476E-15 ) ) ;
#207732=CYLINDRICAL_SURFACE ( 'NONE', #149734, 11.74999999999999645 ) ;
#207757=CARTESIAN_POINT ( 'NONE',  ( -23.15000000000000213, 64.35000000001222986, -148.2731074845243882 ) ) ;
#207806=EDGE_CURVE ( 'NONE', #255801, #211746, #251140, .T. ) ;
#207815=LINE ( 'NONE', #253321, #232376 ) ;
#207818=EDGE_CURVE ( 'NONE', #16570, #221411, #191222, .T. ) ;
#207833=EDGE_CURVE ( 'NONE', #151026, #87941, #130515, .T. ) ;
#207841=DIRECTION ( 'NONE',  ( 0.000000000000000000, 0.1298341882519953583, 0.9915357197604861561 ) ) ;
#207855=VERTEX_POINT ( 'NONE', #132504 ) ;
#207870=EDGE_CURVE ( 'NONE', #67694, #1155, #101245, .T. ) ;
#207884=EDGE_LOOP ( 'NONE', ( #97265, #68356, #219698, #112464 ) ) ;
#207890=DIRECTION ( 'NONE',  ( 0.000000000000000000, 0.000000000000000000, -1.000000000000000000 ) ) ;
#207996=EDGE_CURVE ( 'NONE', #182942, #147164, #142965, .T. ) ;
#208002=VERTEX_POINT ( 'NONE', #77632 ) ;
#208019=EDGE_CURVE ( 'NONE', #132343, #1155, #185431, .T. ) ;
#208025=DIRECTION ( 'NONE',  ( 1.000000000000000000, 0.000000000000000000, 0.000000000000000000 ) ) ;
#208052=CIRCLE ( 'NONE', #95607, 0.2000000000000057288 ) ;
#208070=DIRECTION ( 'NONE',  ( 0.000000000000000000, -6.853228547068871147E-15, 1.000000000000000000 ) ) ;
#208076=EDGE_LOOP ( 'NONE', ( #111119, #117084, #219050 ) ) ;
#208094=CARTESIAN_POINT ( 'NONE',  ( 20.85000000000000142, 64.35000000001195986, -109.8069731475024753 ) ) ;
#208107=CARTESIAN_POINT ( 'NONE',  ( -23.25000000000000000, 77.73670573947940454, -91.50568489690056140 ) ) ;
#208209=ADVANCED_FACE ( 'NONE', ( #31529 ), #72463, .T. ) ;
#208215=CIRCLE ( 'NONE', #95750, 11.89999999999999325 ) ;
#208218=DIRECTION ( 'NONE',  ( 0.000000000000000000, -6.853228547068871147E-15, 1.000000000000000000 ) ) ;
#208233=CARTESIAN_POINT ( 'NONE',  ( 20.12500000000000000, 66.25000000001209344, -128.4113362024100979 ) ) ;
#208246=EDGE_LOOP ( 'NONE', ( #74216, #35032, #154846 ) ) ;
#208348=ORIENTED_EDGE ( 'NONE', *, *, #152137, .T. ) ;
#208365=AXIS2_PLACEMENT_3D ( 'NONE', #199728, #41937, #21097 ) ;
#208370=CARTESIAN_POINT ( 'NONE',  ( 23.15000000000000213, 88.41227409416161720, -106.1231074845242262 ) ) ;
#208396=EDGE_CURVE ( 'NONE', #155941, #87320, #229261, .T. ) ;
#208405=CARTESIAN_POINT ( 'NONE',  ( -20.64999999999999858, 74.00000000001199396, -115.8477294072864083 ) ) ;
#208417=ADVANCED_FACE ( 'NONE', ( #11501, #92293 ), #91018, .T. ) ;
#208419=CARTESIAN_POINT ( 'NONE',  ( 20.04142135623731136, 64.25000000001196554, -111.7559501969989952 ) ) ;
#208431=ORIENTED_EDGE ( 'NONE', *, *, #109677, .T. ) ;
#208466=DIRECTION ( 'NONE',  ( 0.000000000000000000, 0.000000000000000000, 1.000000000000000000 ) ) ;
#208483=DIRECTION ( 'NONE',  ( 1.000000000000000000, 0.000000000000000000, 0.000000000000000000 ) ) ;
#208510=CARTESIAN_POINT ( 'NONE',  ( -20.94999999999999929, 77.16412189325305349, -95.10825939895268277 ) ) ;
#208550=ORIENTED_EDGE ( 'NONE', *, *, #164606, .F. ) ;
#208554=EDGE_CURVE ( 'NONE', #3601, #154962, #80162, .T. ) ;
#208555=ORIENTED_EDGE ( 'NONE', *, *, #212527, .T. ) ;
#208560=AXIS2_PLACEMENT_3D ( 'NONE', #169196, #253817, #248703 ) ;
#208682=AXIS2_PLACEMENT_3D ( 'NONE', #238206, #218637, #119577 ) ;
#208687=VERTEX_POINT ( 'NONE', #28204 ) ;
#208711=CARTESIAN_POINT ( 'NONE',  ( -21.14999999999999858, 64.25000000001215028, -136.4231074845243938 ) ) ;
#208726=CIRCLE ( 'NONE', #33778, 0.1000000000000028644 ) ;
#208727=EDGE_CURVE ( 'NONE', #111851, #199002, #86165, .T. ) ;
#208730=CARTESIAN_POINT ( 'NONE',  ( 23.24999999999999289, 64.35000000001204512, -124.3731074845243825 ) ) ;
#208745=DIRECTION ( 'NONE',  ( 0.000000000000000000, -7.056502275159890043E-15, 1.000000000000000000 ) ) ;
#208761=CARTESIAN_POINT ( 'NONE',  ( 18.45139536634708577, 85.48608172029307184, -96.38259586671357226 ) ) ;
#208762=AXIS2_PLACEMENT_3D ( 'NONE', #12774, #92276, #53158 ) ;
#208773=ORIENTED_EDGE ( 'NONE', *, *, #122032, .T. ) ;
#208824=FACE_OUTER_BOUND ( 'NONE', #149585, .T. ) ;
#208845=AXIS2_PLACEMENT_3D ( 'NONE', #221260, #218692, #165161 ) ;
#208861=ORIENTED_EDGE ( 'NONE', *, *, #186320, .T. ) ;
#208888=EDGE_LOOP ( 'NONE', ( #202490, #41559, #187857, #86009 ) ) ;
#208889=ORIENTED_EDGE ( 'NONE', *, *, #126277, .F. ) ;
#208892=CARTESIAN_POINT ( 'NONE',  ( -21.05000000000000071, 76.00000000001213607, -136.5231074845242745 ) ) ;
#208894=ORIENTED_EDGE ( 'NONE', *, *, #127346, .F. ) ;
#208906=FACE_OUTER_BOUND ( 'NONE', #228151, .T. ) ;
#208928=DIRECTION ( 'NONE',  ( 1.000000000000000000, -0.000000000000000000, 0.000000000000000000 ) ) ;
#208929=CARTESIAN_POINT ( 'NONE',  ( -20.64999999999999858, 68.85000000001200249, -115.3731074845243540 ) ) ;
#208942=ORIENTED_EDGE ( 'NONE', *, *, #69183, .T. ) ;
#208959=DIRECTION ( 'NONE',  ( 0.000000000000000000, 0.000000000000000000, -1.000000000000000000 ) ) ;
#208965=DIRECTION ( 'NONE',  ( 1.000000000000000000, 0.000000000000000000, 0.000000000000000000 ) ) ;
#209038=ORIENTED_EDGE ( 'NONE', *, *, #163487, .T. ) ;
#209045=DIRECTION ( 'NONE',  ( -1.000000000000000000, -0.000000000000000000, -0.000000000000000000 ) ) ;
#209055=DIRECTION ( 'NONE',  ( -0.000000000000000000, -6.982962677686266711E-15, 1.000000000000000000 ) ) ;
#209064=LINE ( 'NONE', #5694, #195109 ) ;
#209092=DIRECTION ( 'NONE',  ( -0.000000000000000000, -6.982962677686266711E-15, 1.000000000000000000 ) ) ;
#209095=CARTESIAN_POINT ( 'NONE',  ( 23.24999999999999645, 76.00000000001190870, -103.0231074845243029 ) ) ;
#209105=ORIENTED_EDGE ( 'NONE', *, *, #174402, .F. ) ;
#209115=TOROIDAL_SURFACE ( 'NONE', #966, 7.800000000000000711, 0.1000000000000000056 ) ;
#209190=CARTESIAN_POINT ( 'NONE',  ( 18.51997666896875572, 85.39233213153090674, -129.3797012970411231 ) ) ;
#209202=EDGE_CURVE ( 'NONE', #71875, #154018, #255914, .T. ) ;
#209224=EDGE_LOOP ( 'NONE', ( #105596, #163013, #44407, #221917 ) ) ;
#209227=EDGE_CURVE ( 'NONE', #14872, #257751, #58206, .T. ) ;
#209242=EDGE_LOOP ( 'NONE', ( #246976, #193821, #101988, #25031 ) ) ;
#209246=EDGE_CURVE ( 'NONE', #61013, #48194, #130678, .T. ) ;
#209247=CARTESIAN_POINT ( 'NONE',  ( 18.49999999999999289, 65.79142135624927334, -111.8731074845243683 ) ) ;
#209268=B_SPLINE_CURVE_WITH_KNOTS ( 'NONE', 3,
 ( #40177, #156277, #117122, #18004, #196642, #59678, #139216 ),
 .UNSPECIFIED., .F., .F.,
 ( 4, 3, 4 ),
 ( 0.000000000000000000, 1.860045280646152724E-05, 5.251155757305309607E-05 ),
 .UNSPECIFIED. ) ;
#209304=LINE ( 'NONE', #110200, #94222 ) ;
#209306=CARTESIAN_POINT ( 'NONE',  ( 23.24999999999999645, 76.00000000001190870, -103.0231074845243029 ) ) ;
#209315=CARTESIAN_POINT ( 'NONE',  ( 18.59999999999999787, 70.10000000001213039, -126.3040077198679398 ) ) ;
#209351=CARTESIAN_POINT ( 'NONE',  ( 20.94999999999999929, 76.00000000001190870, -103.0231074845243029 ) ) ;
#209355=CARTESIAN_POINT ( 'NONE',  ( 18.59999999999999076, 77.16412189325305349, -95.10825939895268277 ) ) ;
#209415=CARTESIAN_POINT ( 'NONE',  ( 18.54286124688534798, 85.62391757880969578, -96.28190515266155103 ) ) ;
#209433=ORIENTED_EDGE ( 'NONE', *, *, #243122, .T. ) ;
#209439=EDGE_CURVE ( 'NONE', #238178, #70035, #101408, .T. ) ;
#209464=CARTESIAN_POINT ( 'NONE',  ( 18.59999999999999432, 74.36282728704168221, -124.9409541190522930 ) ) ;
#209580=ORIENTED_EDGE ( 'NONE', *, *, #204653, .T. ) ;
#209620=CARTESIAN_POINT ( 'NONE',  ( 18.59999999999999076, 69.55000000001207638, -126.5060803140843291 ) ) ;
#209624=DIRECTION ( 'NONE',  ( 0.000000000000000000, -1.000000000000000000, 0.000000000000000000 ) ) ;
#209656=CARTESIAN_POINT ( 'NONE',  ( 18.49999999999998934, 69.55000000001207638, -126.5060803140843291 ) ) ;
#209673=AXIS2_PLACEMENT_3D ( 'NONE', #114793, #229611, #70563 ) ;
#209702=EDGE_LOOP ( 'NONE', ( #245066, #165622, #39840, #236770 ) ) ;
#209734=DIRECTION ( 'NONE',  ( -1.000000000000000000, 0.000000000000000000, -0.000000000000000000 ) ) ;
#209748=ADVANCED_FACE ( 'NONE', ( #41925 ), #1671, .T. ) ;
#209757=EDGE_CURVE ( 'NONE', #54789, #107177, #22550, .T. ) ;
#209787=LINE ( 'NONE', #33760, #130324 ) ;
#209803=ORIENTED_EDGE ( 'NONE', *, *, #37965, .T. ) ;
#209829=EDGE_LOOP ( 'NONE', ( #19893, #108555, #45325, #58260 ) ) ;
#209837=DIRECTION ( 'NONE',  ( 0.000000000000000000, 0.000000000000000000, 1.000000000000000000 ) ) ;
#209841=ORIENTED_EDGE ( 'NONE', *, *, #152175, .T. ) ;
#209858=DIRECTION ( 'NONE',  ( 1.000000000000000000, -3.265361837132813093E-16, -2.280189983783949500E-30 ) ) ;
#209962=VECTOR ( 'NONE', #112722, 1000.000000000000000 ) ;
#209987=ORIENTED_EDGE ( 'NONE', *, *, #67122, .F. ) ;
#209991=CARTESIAN_POINT ( 'NONE',  ( -23.15000000000000213, 76.00000000001213607, -136.5231074845242745 ) ) ;
#210027=CARTESIAN_POINT ( 'NONE',  ( 21.05000000000000071, 87.29603075034741266, -133.4752083248603469 ) ) ;
#210051=DIRECTION ( 'NONE',  ( 1.000000000000000000, -1.836970198721029934E-16, -1.282749433769087582E-30 ) ) ;
#210064=EDGE_CURVE ( 'NONE', #182665, #170158, #41619, .T. ) ;
#210101=CARTESIAN_POINT ( 'NONE',  ( 21.14999999999999858, 69.45000000001205365, -124.1731074845243370 ) ) ;
#210110=CARTESIAN_POINT ( 'NONE',  ( 20.95595012432474391, 65.39582078693574374, -128.9273381543061134 ) ) ;
#210120=CARTESIAN_POINT ( 'NONE',  ( -23.25000000000000000, 64.25000000001199396, -115.1731074845243938 ) ) ;
#210124=DIRECTION ( 'NONE',  ( 1.000000000000000000, 0.000000000000000000, 0.000000000000000000 ) ) ;
#210186=ORIENTED_EDGE ( 'NONE', *, *, #106408, .T. ) ;
#210232=EDGE_CURVE ( 'NONE', #207855, #121700, #166709, .T. ) ;
#210244=ADVANCED_FACE ( 'NONE', ( #207095 ), #239198, .T. ) ;
#210257=DIRECTION ( 'NONE',  ( 4.026293107431335996E-15, 0.8700118002898393765, -0.4930308989875104575 ) ) ;
#210262=CIRCLE ( 'NONE', #118688, 11.74999999999999645 ) ;
#210275=DIRECTION ( 'NONE',  ( 0.000000000000000000, 0.000000000000000000, 1.000000000000000000 ) ) ;
#210321=VECTOR ( 'NONE', #152358, 1000.000000000000000 ) ;
#210368=FACE_OUTER_BOUND ( 'NONE', #250793, .T. ) ;
#210414=AXIS2_PLACEMENT_3D ( 'NONE', #146348, #128092, #107235 ) ;
#210448=VERTEX_POINT ( 'NONE', #200360 ) ;
#210457=CARTESIAN_POINT ( 'NONE',  ( -23.25000000000000000, 64.35000000001205933, -124.3731074845243825 ) ) ;
#210480=ORIENTED_EDGE ( 'NONE', *, *, #41995, .F. ) ;
#210490=CARTESIAN_POINT ( 'NONE',  ( 18.59999999999999787, 85.32100840337339775, -129.2871692354463562 ) ) ;
#210594=LINE ( 'NONE', #230157, #135988 ) ;
#210646=CIRCLE ( 'NONE', #119074, 0.1000000000000028644 ) ;
#210656=CARTESIAN_POINT ( 'NONE',  ( -23.24999999999999645, 85.60000000001186038, -96.42291809330220076 ) ) ;
#210665=CARTESIAN_POINT ( 'NONE',  ( -18.50000000000000000, 64.35000000001205933, -124.3731074845243825 ) ) ;
#210680=EDGE_CURVE ( 'NONE', #224814, #190621, #89525, .T. ) ;
#210682=FACE_OUTER_BOUND ( 'NONE', #7864, .T. ) ;
#210684=ADVANCED_FACE ( 'NONE', ( #134905 ), #172832, .F. ) ;
#210740=DIRECTION ( 'NONE',  ( 0.000000000000000000, 0.000000000000000000, 1.000000000000000000 ) ) ;
#210744=ORIENTED_EDGE ( 'NONE', *, *, #132986, .T. ) ;
#210827=CARTESIAN_POINT ( 'NONE',  ( -18.59999999999999787, 74.36282728704168221, -124.9409541190522930 ) ) ;
#210847=ADVANCED_FACE ( 'NONE', ( #106054 ), #164777, .F. ) ;
#210864=ORIENTED_EDGE ( 'NONE', *, *, #20650, .T. ) ;
#210902=DIRECTION ( 'NONE',  ( 0.000000000000000000, 0.000000000000000000, -1.000000000000000000 ) ) ;
#210924=AXIS2_PLACEMENT_3D ( 'NONE', #24754, #106810, #186377 ) ;
#210941=DIRECTION ( 'NONE',  ( 0.000000000000000000, 0.000000000000000000, 1.000000000000000000 ) ) ;
#210948=ADVANCED_FACE ( 'NONE', ( #94210 ), #53812, .T. ) ;
#210955=EDGE_CURVE ( 'NONE', #37312, #192475, #227087, .T. ) ;
#210982=CARTESIAN_POINT ( 'NONE',  ( 21.13920837816993270, 67.21675294989213967, -124.2731074845243597 ) ) ;
#210985=CARTESIAN_POINT ( 'NONE',  ( -23.15000000000000213, 64.35000000001205933, -124.2731074845243882 ) ) ;
#210997=ORIENTED_EDGE ( 'NONE', *, *, #62259, .F. ) ;
#211016=CARTESIAN_POINT ( 'NONE',  ( 21.05000000000000071, 87.75000000001192291, -106.1231074845242262 ) ) ;
#211052=CARTESIAN_POINT ( 'NONE',  ( -21.44999999999999929, 68.65000000001205649, -124.1731074845243512 ) ) ;
#211120=CARTESIAN_POINT ( 'NONE',  ( -20.64999999999999858, 68.85000000001205933, -124.2731074845243455 ) ) ;
#211130=CARTESIAN_POINT ( 'NONE',  ( -21.14999999999999858, 64.35000000001214460, -136.4231074845243938 ) ) ;
#211145=ORIENTED_EDGE ( 'NONE', *, *, #222663, .F. ) ;
#211146=ADVANCED_FACE ( 'NONE', ( #197160 ), #118938, .T. ) ;
#211150=ORIENTED_EDGE ( 'NONE', *, *, #217480, .T. ) ;
#211151=VERTEX_POINT ( 'NONE', #138453 ) ;
#211196=FACE_OUTER_BOUND ( 'NONE', #49366, .T. ) ;
#211229=ORIENTED_EDGE ( 'NONE', *, *, #43894, .T. ) ;
#211246=LINE ( 'NONE', #112169, #8357 ) ;
#211248=CIRCLE ( 'NONE', #153023, 11.74999999999999645 ) ;
#211265=CARTESIAN_POINT ( 'NONE',  ( 18.49999999999999645, 77.13501884592203339, -95.30613060109196510 ) ) ;
#211292=AXIS2_PLACEMENT_3D ( 'NONE', #134205, #71701, #112113 ) ;
#211299=FACE_OUTER_BOUND ( 'NONE', #246060, .T. ) ;
#211310=AXIS2_PLACEMENT_3D ( 'NONE', #213784, #233379, #55969 ) ;
#211313=EDGE_CURVE ( 'NONE', #155989, #24275, #106632, .T. ) ;
#211318=ADVANCED_FACE ( 'NONE', ( #57002 ), #93994, .T. ) ;
#211320=CARTESIAN_POINT ( 'NONE',  ( 18.47688499308724985, 85.46485595029596993, -96.32175973138681968 ) ) ;
#211330=EDGE_LOOP ( 'NONE', ( #209433, #116969, #220566, #103417 ) ) ;
#211331=EDGE_CURVE ( 'NONE', #7658, #102511, #122448, .T. ) ;
#211422=ORIENTED_EDGE ( 'NONE', *, *, #56454, .T. ) ;
#211471=AXIS2_PLACEMENT_3D ( 'NONE', #122971, #44717, #202497 ) ;
#211483=ORIENTED_EDGE ( 'NONE', *, *, #76039, .T. ) ;
#211488=CARTESIAN_POINT ( 'NONE',  ( -22.40000000000000213, 76.00000000001222134, -148.2735403769829077 ) ) ;
#211490=SPHERICAL_SURFACE ( 'NONE', #106726, 0.1000000000000000056 ) ;
#211541=DIRECTION ( 'NONE',  ( -1.000000000000000000, 0.000000000000000000, 0.000000000000000000 ) ) ;
#211589=EDGE_CURVE ( 'NONE', #119534, #25751, #30771, .T. ) ;
#211595=EDGE_LOOP ( 'NONE', ( #188255, #100518, #65712, #55024 ) ) ;
#211611=CARTESIAN_POINT ( 'NONE',  ( -20.94999999999999929, 77.83534155023646406, -124.9679561919612922 ) ) ;
#211628=VERTEX_POINT ( 'NONE', #146822 ) ;
#211638=CARTESIAN_POINT ( 'NONE',  ( 21.05000000000000071, 69.35000000001207354, -126.5060803140843291 ) ) ;
#211667=CARTESIAN_POINT ( 'NONE',  ( -23.25000000000000000, 69.01799029515544248, -99.32695536626806643 ) ) ;
#211676=EDGE_LOOP ( 'NONE', ( #194196, #27151, #216887, #236565 ) ) ;
#211677=CARTESIAN_POINT ( 'NONE',  ( -21.05000000000000071, 87.48912529308798014, -106.0231074845242176 ) ) ;
#211727=AXIS2_PLACEMENT_3D ( 'NONE', #239183, #81357, #181782 ) ;
#211729=AXIS2_PLACEMENT_3D ( 'NONE', #163665, #241899, #202781 ) ;
#211737=EDGE_LOOP ( 'NONE', ( #66856, #251831, #129129, #99985 ) ) ;
#211746=VERTEX_POINT ( 'NONE', #213217 ) ;
#211778=CARTESIAN_POINT ( 'NONE',  ( 18.50000000000000000, 85.40000000001207070, -129.2258477248609552 ) ) ;
#211786=ORIENTED_EDGE ( 'NONE', *, *, #65669, .T. ) ;
#211790=ORIENTED_EDGE ( 'NONE', *, *, #76738, .T. ) ;
#211791=EDGE_CURVE ( 'NONE', #162828, #39149, #235350, .T. ) ;
#211824=ORIENTED_EDGE ( 'NONE', *, *, #96388, .F. ) ;
#211835=CARTESIAN_POINT ( 'NONE',  ( 21.05000000000000071, 76.00000000001213607, -136.5231074845242745 ) ) ;
#211838=CARTESIAN_POINT ( 'NONE',  ( -23.15000000000000213, 87.48912529308798014, -106.1231074845242262 ) ) ;
#211865=AXIS2_PLACEMENT_3D ( 'NONE', #18247, #138167, #195623 ) ;
#211870=ORIENTED_EDGE ( 'NONE', *, *, #257197, .F. ) ;
#211879=CARTESIAN_POINT ( 'NONE',  ( 20.94999999999999929, 67.22371710471952611, -115.2731074845243597 ) ) ;
#211900=ADVANCED_FACE ( 'NONE', ( #146516 ), #145236, .T. ) ;
#211920=CARTESIAN_POINT ( 'NONE',  ( 22.60000000000000142, 75.89914163091351895, -148.2726746080136877 ) ) ;
#211921=CARTESIAN_POINT ( 'NONE',  ( -21.14999999999999858, 76.00000000001222134, -148.1726782920690937 ) ) ;
#211929=DIRECTION ( 'NONE',  ( -1.000000000000000000, -0.000000000000000000, -0.000000000000000000 ) ) ;
#211968=CIRCLE ( 'NONE', #107885, 0.09999999999999489853 ) ;
#211978=DIRECTION ( 'NONE',  ( 1.000000000000000000, 0.000000000000000000, 0.000000000000000000 ) ) ;
#212021=CIRCLE ( 'NONE', #257740, 0.1000000000000028644 ) ;
#212057=DIRECTION ( 'NONE',  ( 0.000000000000000000, 0.000000000000000000, 1.000000000000000000 ) ) ;
#212071=DIRECTION ( 'NONE',  ( 1.000000000000000000, 0.000000000000000000, 0.000000000000000000 ) ) ;
#212124=DIRECTION ( 'NONE',  ( 0.000000000000000000, 0.000000000000000000, 1.000000000000000000 ) ) ;
#212139=AXIS2_PLACEMENT_3D ( 'NONE', #42906, #200695, #157766 ) ;
#212156=DIRECTION ( 'NONE',  ( -1.000000000000000000, 0.000000000000000000, 0.000000000000000000 ) ) ;
#212200=ORIENTED_EDGE ( 'NONE', *, *, #3119, .F. ) ;
#212204=DIRECTION ( 'NONE',  ( -1.000000000000000000, -0.000000000000000000, 0.000000000000000000 ) ) ;
#212211=AXIS2_PLACEMENT_3D ( 'NONE', #209991, #52175, #50876 ) ;
#212214=VERTEX_POINT ( 'NONE', #136650 ) ;
#212215=FACE_OUTER_BOUND ( 'NONE', #106698, .T. ) ;
#212216=AXIS2_PLACEMENT_3D ( 'NONE', #59197, #537, #175370 ) ;
#212225=CARTESIAN_POINT ( 'NONE',  ( 22.39999999999999503, 64.35000000001213039, -136.6231074845243825 ) ) ;
#212236=EDGE_LOOP ( 'NONE', ( #131586, #39006, #26100, #58366 ) ) ;
#212265=ADVANCED_FACE ( 'NONE', ( #55808 ), #114544, .T. ) ;
#212300=DIRECTION ( 'NONE',  ( 1.000000000000000000, -2.952720810173289112E-16, -2.061873921506763405E-30 ) ) ;
#212303=DIRECTION ( 'NONE',  ( 1.000000000000000000, -0.000000000000000000, 0.000000000000000000 ) ) ;
#212304=ORIENTED_EDGE ( 'NONE', *, *, #163064, .F. ) ;
#212314=ADVANCED_FACE ( 'NONE', ( #94966 ), #256554, .F. ) ;
#212317=AXIS2_PLACEMENT_3D ( 'NONE', #44909, #162298, #164858 ) ;
#212326=ORIENTED_EDGE ( 'NONE', *, *, #82200, .T. ) ;
#212351=CARTESIAN_POINT ( 'NONE',  ( 21.09546886439513713, 67.12144688699748940, -124.2860136339693611 ) ) ;
#212368=SPHERICAL_SURFACE ( 'NONE', #176156, 0.1000000000000000056 ) ;
#212385=DIRECTION ( 'NONE',  ( -0.000000000000000000, -6.982962677686266711E-15, 1.000000000000000000 ) ) ;
#212469=EDGE_LOOP ( 'NONE', ( #54906, #14325, #143776 ) ) ;
#212492=DIRECTION ( 'NONE',  ( 0.000000000000000000, -6.467318590049456648E-15, 1.000000000000000000 ) ) ;
#212498=CARTESIAN_POINT ( 'NONE',  ( -21.04999999999999716, 76.08574093704558550, -142.9369337733372447 ) ) ;
#212525=CARTESIAN_POINT ( 'NONE',  ( 18.59999999999998721, 69.15387683765929694, -99.28538121767448388 ) ) ;
#212527=EDGE_CURVE ( 'NONE', #14594, #161400, #219269, .T. ) ;
#212540=CARTESIAN_POINT ( 'NONE',  ( 21.05000000000000071, 76.00000000001213607, -136.5231074845242745 ) ) ;
#212546=DIRECTION ( 'NONE',  ( 0.000000000000000000, -0.9887567792719351711, 0.1495327102803594987 ) ) ;
#212568=CARTESIAN_POINT ( 'NONE',  ( -21.05000000000000071, 87.48912529308798014, -106.1231074845242262 ) ) ;
#212579=ADVANCED_FACE ( 'NONE', ( #244731 ), #223710, .F. ) ;
#212617=DIRECTION ( 'NONE',  ( 1.000000000000000000, 0.000000000000000000, 0.000000000000000000 ) ) ;
#212639=ORIENTED_EDGE ( 'NONE', *, *, #57423, .T. ) ;
#212643=EDGE_LOOP ( 'NONE', ( #131315, #146310, #218581, #26168 ) ) ;
#212652=EDGE_CURVE ( 'NONE', #170896, #59827, #247306, .T. ) ;
#212686=CIRCLE ( 'NONE', #162611, 12.77499999999999503 ) ;
#212694=AXIS2_PLACEMENT_3D ( 'NONE', #164487, #24988, #104471 ) ;
#212738=CARTESIAN_POINT ( 'NONE',  ( 23.25000000000000000, 85.60000000001197407, -112.9170766071766820 ) ) ;
#212742=ORIENTED_EDGE ( 'NONE', *, *, #244529, .T. ) ;
#212782=CARTESIAN_POINT ( 'NONE',  ( 20.94999999999999574, 67.07338541492499928, -128.0514244653012383 ) ) ;
#212813=CARTESIAN_POINT ( 'NONE',  ( 20.95556889135987788, 65.37805641227699027, -128.8807132626668306 ) ) ;
#212834=CARTESIAN_POINT ( 'NONE',  ( -21.05000000000000071, 77.26178616857710324, -128.4366085209788366 ) ) ;
#212835=DIRECTION ( 'NONE',  ( 0.000000000000000000, 0.000000000000000000, 1.000000000000000000 ) ) ;
#212837=ORIENTED_EDGE ( 'NONE', *, *, #236451, .T. ) ;
#212839=CARTESIAN_POINT ( 'NONE',  ( -21.14999999999999858, 87.75000000001213607, -136.5231074845242176 ) ) ;
#212857=DIRECTION ( 'NONE',  ( 1.000000000000000000, 0.000000000000000000, 0.000000000000000000 ) ) ;
#212859=LINE ( 'NONE', #18510, #37236 ) ;
#212882=FACE_OUTER_BOUND ( 'NONE', #143203, .T. ) ;
#212888=PLANE ( 'NONE',  #216928 ) ;
#212918=ORIENTED_EDGE ( 'NONE', *, *, #120850, .T. ) ;
#212960=ORIENTED_EDGE ( 'NONE', *, *, #4507, .T. ) ;
#212969=DIRECTION ( 'NONE',  ( -1.000000000000000000, 2.952720810173289112E-16, 2.061873921506763405E-30 ) ) ;
#212980=DIRECTION ( 'NONE',  ( -1.000000000000000000, 0.000000000000000000, 0.000000000000000000 ) ) ;
#213006=DIRECTION ( 'NONE',  ( -1.000000000000000000, 0.000000000000000000, 0.000000000000000000 ) ) ;
#213028=ORIENTED_EDGE ( 'NONE', *, *, #70820, .F. ) ;
#213049=DIRECTION ( 'NONE',  ( 0.000000000000000000, 0.000000000000000000, -1.000000000000000000 ) ) ;
#213059=ORIENTED_EDGE ( 'NONE', *, *, #180946, .F. ) ;
#213077=ORIENTED_EDGE ( 'NONE', *, *, #7653, .F. ) ;
#213080=CIRCLE ( 'NONE', #142170, 0.09999999999999971412 ) ;
#213088=EDGE_LOOP ( 'NONE', ( #89175, #109853, #248452, #135488, #108627 ) ) ;
#213153=AXIS2_PLACEMENT_3D ( 'NONE', #207757, #104744, #242999 ) ;
#213174=DIRECTION ( 'NONE',  ( 0.000000000000000000, -6.982962677686267499E-15, 1.000000000000000000 ) ) ;
#213217=CARTESIAN_POINT ( 'NONE',  ( -20.54999999999999716, 68.85000000001200249, -115.3731074845243540 ) ) ;
#213284=CARTESIAN_POINT ( 'NONE',  ( -23.15000000000000213, 85.00000000001207923, -127.1291383618717816 ) ) ;
#213287=ORIENTED_EDGE ( 'NONE', *, *, #4532, .F. ) ;
#213308=DIRECTION ( 'NONE',  ( 0.000000000000000000, 0.000000000000000000, -1.000000000000000000 ) ) ;
#213312=CARTESIAN_POINT ( 'NONE',  ( -21.05000000000000071, 76.25610579210437834, -136.5580039261965908 ) ) ;
#213344=VERTEX_POINT ( 'NONE', #150194 ) ;
#213358=CARTESIAN_POINT ( 'NONE',  ( -21.04999999999999716, 64.25000000001195133, -109.8647081744214375 ) ) ;
#213373=ORIENTED_EDGE ( 'NONE', *, *, #251258, .T. ) ;
#213393=CARTESIAN_POINT ( 'NONE',  ( -2.995603634470891112E-16, 69.35000000001200249, -115.2731074845243455 ) ) ;
#213398=CARTESIAN_POINT ( 'NONE',  ( -18.50000000000000000, 77.83585931145546510, -91.51866831572576189 ) ) ;
#213411=ORIENTED_EDGE ( 'NONE', *, *, #75351, .F. ) ;
#213424=ORIENTED_EDGE ( 'NONE', *, *, #87523, .F. ) ;
#213471=ORIENTED_EDGE ( 'NONE', *, *, #32895, .F. ) ;
#213472=CARTESIAN_POINT ( 'NONE',  ( 21.05000000000000071, 67.22371710471961137, -128.0351067629399893 ) ) ;
#213475=ORIENTED_EDGE ( 'NONE', *, *, #85587, .T. ) ;
#213479=DIRECTION ( 'NONE',  ( -0.000000000000000000, -6.982962677686266711E-15, 1.000000000000000000 ) ) ;
#213481=DIRECTION ( 'NONE',  ( 7.304098846218134667E-16, 1.000000000000000000, 6.982962677686267499E-15 ) ) ;
#213493=DIRECTION ( 'NONE',  ( 0.000000000000000000, 0.5000000000000209832, 0.8660254037844264952 ) ) ;
#213515=CARTESIAN_POINT ( 'NONE',  ( -23.15000000000000213, 71.85000000001222986, -148.2731074845243313 ) ) ;
#213545=VERTEX_POINT ( 'NONE', #43077 ) ;
#213555=ADVANCED_FACE ( 'NONE', ( #237423 ), #118771, .T. ) ;
#213575=DIRECTION ( 'NONE',  ( 0.000000000000000000, 0.000000000000000000, -1.000000000000000000 ) ) ;
#213594=ORIENTED_EDGE ( 'NONE', *, *, #111144, .F. ) ;
#213619=CARTESIAN_POINT ( 'NONE',  ( 18.59999999999999432, 74.83729825007408465, -128.4231074845243086 ) ) ;
#213669=VERTEX_POINT ( 'NONE', #23550 ) ;
#213671=LINE ( 'NONE', #97535, #26427 ) ;
#213693=CARTESIAN_POINT ( 'NONE',  ( 23.25000000000000000, 84.59626168225506149, -127.0729799673739677 ) ) ;
#213725=VERTEX_POINT ( 'NONE', #59385 ) ;
#213736=AXIS2_PLACEMENT_3D ( 'NONE', #98218, #113964, #74883 ) ;
#213753=CARTESIAN_POINT ( 'NONE',  ( -23.15000000000000213, 87.65000000001192859, -106.0231074845242176 ) ) ;
#213781=VERTEX_POINT ( 'NONE', #173003 ) ;
#213784=CARTESIAN_POINT ( 'NONE',  ( -23.25000000000000000, 71.65000000001207070, -124.1731074845243228 ) ) ;
#213792=AXIS2_PLACEMENT_3D ( 'NONE', #50971, #87541, #251767 ) ;
#213822=DIRECTION ( 'NONE',  ( 1.000000000000000000, -3.265361837132813093E-16, -2.280189983783949500E-30 ) ) ;
#213835=LINE ( 'NONE', #229560, #52433 ) ;
#213846=EDGE_CURVE ( 'NONE', #144364, #62401, #86880, .T. ) ;
#213875=EDGE_CURVE ( 'NONE', #196680, #228703, #203615, .T. ) ;
#213877=EDGE_CURVE ( 'NONE', #39149, #54998, #243187, .T. ) ;
#213901=FACE_OUTER_BOUND ( 'NONE', #136420, .T. ) ;
#213925=CARTESIAN_POINT ( 'NONE',  ( 21.78635804494511419, 75.90099493450451007, -143.5587689696774873 ) ) ;
#213927=DIRECTION ( 'NONE',  ( 0.000000000000000000, 6.982962677686266711E-15, -1.000000000000000000 ) ) ;
#213928=CIRCLE ( 'NONE', #72291, 0.2000000000000057288 ) ;
#213951=CIRCLE ( 'NONE', #134809, 11.64999999999999325 ) ;
#213957=ORIENTED_EDGE ( 'NONE', *, *, #184137, .F. ) ;
#213961=VERTEX_POINT ( 'NONE', #239351 ) ;
#213982=CARTESIAN_POINT ( 'NONE',  ( 21.05000000000000071, 85.00000000001197975, -112.9170766071766820 ) ) ;
#214013=CIRCLE ( 'NONE', #47389, 0.1000000000000028644 ) ;
#214027=ORIENTED_EDGE ( 'NONE', *, *, #175313, .F. ) ;
#214070=DIRECTION ( 'NONE',  ( 0.000000000000000000, -0.9908441862701420355, -0.1350103645453197554 ) ) ;
#214095=CARTESIAN_POINT ( 'NONE',  ( 22.44352723754029810, 75.99072290496894766, -148.1728288298729979 ) ) ;
#214110=CARTESIAN_POINT ( 'NONE',  ( 23.14999999999999147, 76.00000000001213607, -136.5231074845242745 ) ) ;
#214127=EDGE_LOOP ( 'NONE', ( #174004, #180848, #127216, #197013 ) ) ;
#214142=DIRECTION ( 'NONE',  ( -0.7071067811865127117, -0.7071067811865821007, 0.000000000000000000 ) ) ;
#214163=AXIS2_PLACEMENT_3D ( 'NONE', #254962, #109413, #226802 ) ;
#214175=EDGE_CURVE ( 'NONE', #19089, #153900, #123953, .T. ) ;
#214180=VECTOR ( 'NONE', #92220, 1000.000000000000000 ) ;
#214194=CARTESIAN_POINT ( 'NONE',  ( 21.14999999999999858, 67.21339244341194785, -124.1731074845243512 ) ) ;
#214207=DIRECTION ( 'NONE',  ( -1.000000000000000000, 0.000000000000000000, 0.000000000000000000 ) ) ;
#214216=CARTESIAN_POINT ( 'NONE',  ( 21.07016717456945187, 69.67905916191187998, -136.5231074845243597 ) ) ;
#214222=DIRECTION ( 'NONE',  ( 0.000000000000000000, 0.000000000000000000, -1.000000000000000000 ) ) ;
#214224=ORIENTED_EDGE ( 'NONE', *, *, #149449, .F. ) ;
#214262=CARTESIAN_POINT ( 'NONE',  ( 21.05000000000000071, 87.48912529308798014, -106.0231074845242176 ) ) ;
#214428=ORIENTED_EDGE ( 'NONE', *, *, #72207, .T. ) ;
#214435=CYLINDRICAL_SURFACE ( 'NONE', #173489, 0.09999999999998898659 ) ;
#214452=CARTESIAN_POINT ( 'NONE',  ( 21.05000000000000071, 75.90220970870296924, -142.7809220950058204 ) ) ;
#214478=DIRECTION ( 'NONE',  ( 0.000000000000000000, -1.000000000000000000, -6.982962677686265922E-15 ) ) ;
#214503=CARTESIAN_POINT ( 'NONE',  ( -20.85000000000000142, 87.75000000001192291, -105.9231074845242091 ) ) ;
#214504=ORIENTED_EDGE ( 'NONE', *, *, #218127, .F. ) ;
#214518=CARTESIAN_POINT ( 'NONE',  ( -22.39999999999999858, 64.25000000001215028, -136.5231074845243597 ) ) ;
#214519=CARTESIAN_POINT ( 'NONE',  ( -20.85000000000000142, 76.00000000001190870, -103.0231074845243029 ) ) ;
#214589=ORIENTED_EDGE ( 'NONE', *, *, #180622, .T. ) ;
#214613=VERTEX_POINT ( 'NONE', #95378 ) ;
#214641=AXIS2_PLACEMENT_3D ( 'NONE', #82427, #19941, #162022 ) ;
#214648=VERTEX_POINT ( 'NONE', #56227 ) ;
#214681=DIRECTION ( 'NONE',  ( 1.000000000000000000, 0.000000000000000000, 0.000000000000000000 ) ) ;
#214690=ADVANCED_FACE ( 'NONE', ( #13281 ), #66035, .T. ) ;
#214694=AXIS2_PLACEMENT_3D ( 'NONE', #65202, #62652, #86019 ) ;
#214774=CARTESIAN_POINT ( 'NONE',  ( 21.05000000000000071, 71.00000000001199396, -115.0283735034374359 ) ) ;
#214787=ORIENTED_EDGE ( 'NONE', *, *, #198539, .F. ) ;
#214800=AXIS2_PLACEMENT_3D ( 'NONE', #127792, #9124, #249031 ) ;
#214817=CARTESIAN_POINT ( 'NONE',  ( 21.05995757104869526, 67.22461075529079721, -124.3282023615331440 ) ) ;
#214825=CARTESIAN_POINT ( 'NONE',  ( -18.39999999999999858, 85.50000000001209344, -129.4910380878245633 ) ) ;
#214831=ORIENTED_EDGE ( 'NONE', *, *, #92233, .T. ) ;
#214848=VECTOR ( 'NONE', #118676, 1000.000000000000000 ) ;
#214864=ORIENTED_EDGE ( 'NONE', *, *, #24580, .T. ) ;
#214878=ORIENTED_EDGE ( 'NONE', *, *, #116698, .F. ) ;
#214887=CARTESIAN_POINT ( 'NONE',  ( 18.55857864376268296, 65.63284271248657831, -111.7731074845243597 ) ) ;
#214893=DIRECTION ( 'NONE',  ( 0.000000000000000000, 5.551115123126393596E-13, -1.000000000000000000 ) ) ;
#214898=AXIS2_PLACEMENT_3D ( 'NONE', #36873, #17287, #96773 ) ;
#214944=CARTESIAN_POINT ( 'NONE',  ( -18.50000000000000000, 64.25000000001206502, -124.3731074845243825 ) ) ;
#214949=ORIENTED_EDGE ( 'NONE', *, *, #210955, .T. ) ;
#214961=ORIENTED_EDGE ( 'NONE', *, *, #201660, .T. ) ;
#214988=CARTESIAN_POINT ( 'NONE',  ( -20.85000000000000142, 77.25000000001185185, -95.22262673010919798 ) ) ;
#215003=AXIS2_PLACEMENT_3D ( 'NONE', #170419, #109092, #249906 ) ;
#215040=DIRECTION ( 'NONE',  ( 0.000000000000000000, 6.982962677686266711E-15, -1.000000000000000000 ) ) ;
#215044=CARTESIAN_POINT ( 'NONE',  ( -20.54999999999999716, 68.75000000001205080, -124.2731074845243455 ) ) ;
#215048=CARTESIAN_POINT ( 'NONE',  ( 18.60000000000000142, 85.48068669529082797, -96.08199231576635668 ) ) ;
#215049=CARTESIAN_POINT ( 'NONE',  ( -21.05000000000000426, 76.10000000001218723, -143.0001745056490847 ) ) ;
#215054=CARTESIAN_POINT ( 'NONE',  ( -20.64999999999999858, 84.66355140188123585, -126.9990063664569391 ) ) ;
#215067=AXIS2_PLACEMENT_3D ( 'NONE', #49135, #33475, #170430 ) ;
#215082=EDGE_CURVE ( 'NONE', #122058, #75479, #82754, .T. ) ;
#215101=ORIENTED_EDGE ( 'NONE', *, *, #112491, .T. ) ;
#215105=AXIS2_PLACEMENT_3D ( 'NONE', #101105, #238094, #198978 ) ;
#215106=DIRECTION ( 'NONE',  ( -2.915501640297152804E-16, -1.000000000000000000, -6.997203936713167125E-15 ) ) ;
#215112=LINE ( 'NONE', #35228, #128609 ) ;
#215127=EDGE_CURVE ( 'NONE', #40198, #59439, #78679, .T. ) ;
#215177=AXIS2_PLACEMENT_3D ( 'NONE', #243230, #64596, #204107 ) ;
#215179=FACE_OUTER_BOUND ( 'NONE', #19506, .T. ) ;
#215194=CIRCLE ( 'NONE', #169450, 0.1000000000000011990 ) ;
#215239=EDGE_CURVE ( 'NONE', #160823, #51816, #226540, .T. ) ;
#215245=DIRECTION ( 'NONE',  ( 0.000000000000000000, 0.1350103645451974088, -0.9908441862701587999 ) ) ;
#215279=CIRCLE ( 'NONE', #128365, 0.1000000000000028644 ) ;
#215340=CARTESIAN_POINT ( 'NONE',  ( 18.59999999999997655, 76.00000000001190870, -103.0231074845243029 ) ) ;
#215352=LINE ( 'NONE', #233651, #84173 ) ;
#215387=VERTEX_POINT ( 'NONE', #192580 ) ;
#215396=AXIS2_PLACEMENT_3D ( 'NONE', #138484, #38149, #19870 ) ;
#215433=ADVANCED_FACE ( 'NONE', ( #152196 ), #174349, .T. ) ;
#215444=DIRECTION ( 'NONE',  ( 0.000000000000000000, 0.000000000000000000, -1.000000000000000000 ) ) ;
#215469=VECTOR ( 'NONE', #56980, 1000.000000000000000 ) ;
#215521=ORIENTED_EDGE ( 'NONE', *, *, #118034, .F. ) ;
#215531=EDGE_CURVE ( 'NONE', #155848, #217558, #38640, .T. ) ;
#215534=ORIENTED_EDGE ( 'NONE', *, *, #253950, .T. ) ;
#215542=CARTESIAN_POINT ( 'NONE',  ( 20.99780126800921209, 64.39461131213536760, -109.9357549128188936 ) ) ;
#215553=VERTEX_POINT ( 'NONE', #156045 ) ;
#215555=TOROIDAL_SURFACE ( 'NONE', #119719, 4.099999999999999645, 0.1000000000000000056 ) ;
#215570=CARTESIAN_POINT ( 'NONE',  ( -18.48550754432078236, 85.46339977857184067, -129.4743177321095970 ) ) ;
#215625=CARTESIAN_POINT ( 'NONE',  ( 21.04999999999999716, 65.31569084252699042, -128.9964106941975501 ) ) ;
#215657=DIRECTION ( 'NONE',  ( -3.469446951953515108E-14, -1.000000000000000000, 0.000000000000000000 ) ) ;
#215696=CARTESIAN_POINT ( 'NONE',  ( -18.50000000000000000, 77.63717271298244782, -124.9409541190522788 ) ) ;
#215706=CARTESIAN_POINT ( 'NONE',  ( 21.05000000000000071, 87.65000000001192859, -105.9231074845242091 ) ) ;
#215738=DIRECTION ( 'NONE',  ( 0.000000000000000000, -6.661338147750933721E-15, 1.000000000000000000 ) ) ;
#215756=ORIENTED_EDGE ( 'NONE', *, *, #106508, .T. ) ;
#215772=CARTESIAN_POINT ( 'NONE',  ( 23.24999999999999645, 76.00000000001213607, -136.5231074845242745 ) ) ;
#215782=CIRCLE ( 'NONE', #86778, 0.1000000000000028644 ) ;
#215783=CARTESIAN_POINT ( 'NONE',  ( 23.14999999999999503, 64.35000000001195986, -110.0379132551783243 ) ) ;
#215795=ORIENTED_EDGE ( 'NONE', *, *, #230374, .F. ) ;
#215876=ORIENTED_EDGE ( 'NONE', *, *, #206828, .F. ) ;
#215890=CARTESIAN_POINT ( 'NONE',  ( -22.39999999999999858, 76.10085836911093793, -148.2726746080136877 ) ) ;
#215908=CARTESIAN_POINT ( 'NONE',  ( 21.05000000000000071, 76.00000000001205080, -123.6481074845242887 ) ) ;
#215917=CARTESIAN_POINT ( 'NONE',  ( -20.94999999999999929, 64.25000000001195133, -109.8069731475024753 ) ) ;
#215928=DIRECTION ( 'NONE',  ( -0.000000000000000000, -6.982962677686266711E-15, 1.000000000000000000 ) ) ;
#215936=CARTESIAN_POINT ( 'NONE',  ( 20.94999999999999574, 74.14897176987119565, -124.8691942151018139 ) ) ;
#215939=AXIS2_PLACEMENT_3D ( 'NONE', #188997, #252798, #53329 ) ;
#215955=CARTESIAN_POINT ( 'NONE',  ( -20.64999999999999858, 68.85000000001200249, -115.2731074845243455 ) ) ;
#215966=ORIENTED_EDGE ( 'NONE', *, *, #248543, .T. ) ;
#215978=EDGE_LOOP ( 'NONE', ( #238134, #179006, #48066, #106871 ) ) ;
#216016=ORIENTED_EDGE ( 'NONE', *, *, #187529, .F. ) ;
#216087=DIRECTION ( 'NONE',  ( 1.000000000000000000, 0.000000000000000000, 0.000000000000000000 ) ) ;
#216095=CARTESIAN_POINT ( 'NONE',  ( 21.11747605621531321, 67.22129199451916293, -124.2785443147345745 ) ) ;
#216148=ORIENTED_EDGE ( 'NONE', *, *, #31968, .T. ) ;
#216166=CARTESIAN_POINT ( 'NONE',  ( -21.05000000000000071, 70.15000000001198543, -113.1556047088022581 ) ) ;
#216197=DIRECTION ( 'NONE',  ( 0.000000000000000000, 0.000000000000000000, 1.000000000000000000 ) ) ;
#216215=DIRECTION ( 'NONE',  ( -1.000000000000000000, 0.000000000000000000, -0.000000000000000000 ) ) ;
#216238=CIRCLE ( 'NONE', #157862, 11.74999999999999645 ) ;
#216249=CARTESIAN_POINT ( 'NONE',  ( -20.94999999999999929, 76.00000000001190870, -103.0231074845243029 ) ) ;
#216286=VERTEX_POINT ( 'NONE', #65846 ) ;
#216328=CIRCLE ( 'NONE', #3949, 0.09999999999999939493 ) ;
#216337=DIRECTION ( 'NONE',  ( -1.000000000000000000, 3.265361837132813093E-16, 2.280189983783949500E-30 ) ) ;
#216369=VERTEX_POINT ( 'NONE', #167551 ) ;
#216380=ORIENTED_EDGE ( 'NONE', *, *, #119574, .T. ) ;
#216433=TOROIDAL_SURFACE ( 'NONE', #45572, 0.2000000000000000111, 0.1000000000000000056 ) ;
#216438=DIRECTION ( 'NONE',  ( 0.000000000000000000, 1.000000000000000000, 6.352154140967427193E-15 ) ) ;
#216457=LINE ( 'NONE', #250453, #203564 ) ;
#216460=DIRECTION ( 'NONE',  ( 0.000000000000000000, 6.769652589177772835E-15, -1.000000000000000000 ) ) ;
#216487=CARTESIAN_POINT ( 'NONE',  ( -20.85000000000000142, 77.16412189325305349, -95.20825939895267709 ) ) ;
#216518=CARTESIAN_POINT ( 'NONE',  ( -22.50000000000000000, 75.90000000001219860, -144.3138870828977076 ) ) ;
#216522=ORIENTED_EDGE ( 'NONE', *, *, #25606, .F. ) ;
#216538=DIRECTION ( 'NONE',  ( 0.000000000000000000, 0.000000000000000000, 1.000000000000000000 ) ) ;
#216543=VERTEX_POINT ( 'NONE', #135767 ) ;
#216578=ADVANCED_FACE ( 'NONE', ( #156665 ), #22270, .F. ) ;
#216587=ADVANCED_FACE ( 'NONE', ( #36713 ), #57506, .T. ) ;
#216597=ORIENTED_EDGE ( 'NONE', *, *, #7343, .F. ) ;
#216599=CARTESIAN_POINT ( 'NONE',  ( 23.14999999999999503, 64.35000000001221565, -148.2731074845243882 ) ) ;
#216613=ORIENTED_EDGE ( 'NONE', *, *, #199779, .F. ) ;
#216656=CARTESIAN_POINT ( 'NONE',  ( 23.15000000000000213, 85.60000000001197407, -112.9170766071766820 ) ) ;
#216659=CARTESIAN_POINT ( 'NONE',  ( 22.49066049874202022, 75.94365674847999514, -148.1731197220414060 ) ) ;
#216673=CARTESIAN_POINT ( 'NONE',  ( -23.24999999999999645, 85.60000000001186038, -96.42291809330220076 ) ) ;
#216701=CARTESIAN_POINT ( 'NONE',  ( -22.39999999999999858, 76.10000000001222986, -148.1726782920690937 ) ) ;
#216715=AXIS2_PLACEMENT_3D ( 'NONE', #36487, #212546, #191714 ) ;
#216721=CARTESIAN_POINT ( 'NONE',  ( -18.55121869061588669, 65.67252876774529113, -97.44570419949944551 ) ) ;
#216726=CARTESIAN_POINT ( 'NONE',  ( -23.25000000000000000, 77.25000000001185185, -95.22262673010921219 ) ) ;
#216737=LINE ( 'NONE', #38125, #69589 ) ;
#216745=CARTESIAN_POINT ( 'NONE',  ( 20.94999999999999574, 74.83729825007408465, -128.6231074845242972 ) ) ;
#216751=CARTESIAN_POINT ( 'NONE',  ( -21.46681500597191672, 76.00000000001219291, -143.3806186439590533 ) ) ;
#216773=DIRECTION ( 'NONE',  ( 0.000000000000000000, 6.938893903907511105E-14, -1.000000000000000000 ) ) ;
#216775=DIRECTION ( 'NONE',  ( 0.000000000000000000, 6.982962677686266711E-15, -1.000000000000000000 ) ) ;
#216784=ADVANCED_FACE ( 'NONE', ( #224297 ), #105608, .F. ) ;
#216805=DIRECTION ( 'NONE',  ( -0.000000000000000000, -6.982962677686266711E-15, 1.000000000000000000 ) ) ;
#216816=ADVANCED_FACE ( 'NONE', ( #134175 ), #22315, .F. ) ;
#216827=DIRECTION ( 'NONE',  ( 1.000000000000000000, -2.952720810173289112E-16, -2.061873921506763405E-30 ) ) ;
#216844=CARTESIAN_POINT ( 'NONE',  ( -20.00857864376270001, 66.75000000001199396, -115.2731074845243597 ) ) ;
#216852=CARTESIAN_POINT ( 'NONE',  ( -18.51555513499414474, 85.35265705451615759, -129.3279375888285188 ) ) ;
#216882=DIRECTION ( 'NONE',  ( 0.000000000000000000, 6.982962677686266711E-15, -1.000000000000000000 ) ) ;
#216887=ORIENTED_EDGE ( 'NONE', *, *, #253791, .F. ) ;
#216891=AXIS2_PLACEMENT_3D ( 'NONE', #247493, #126251, #10176 ) ;
#216906=EDGE_LOOP ( 'NONE', ( #234001, #17704, #78766 ) ) ;
#216928=AXIS2_PLACEMENT_3D ( 'NONE', #216726, #137191, #38112 ) ;
#216939=VECTOR ( 'NONE', #105438, 1000.000000000000000 ) ;
#216943=DIRECTION ( 'NONE',  ( 1.000000000000000000, -3.469446951953718318E-14, 2.003086131649645455E-14 ) ) ;
#216954=CARTESIAN_POINT ( 'NONE',  ( 20.85000000000000142, 76.00000000001190870, -103.0231074845243029 ) ) ;
#216955=VERTEX_POINT ( 'NONE', #196720 ) ;
#216974=DIRECTION ( 'NONE',  ( 1.000000000000000000, 0.000000000000000000, 0.000000000000000000 ) ) ;
#217016=FACE_OUTER_BOUND ( 'NONE', #16481, .T. ) ;
#217017=CARTESIAN_POINT ( 'NONE',  ( -20.94999999999999929, 77.83585931145546510, -91.51866831572576189 ) ) ;
#217061=EDGE_CURVE ( 'NONE', #10477, #199333, #186154, .T. ) ;
#217063=CARTESIAN_POINT ( 'NONE',  ( 20.94999999999999574, 77.16270174995010223, -128.5231074845242745 ) ) ;
#217080=CARTESIAN_POINT ( 'NONE',  ( -21.45000000000000284, 68.29142135624935861, -124.1731074845243512 ) ) ;
#217114=EDGE_CURVE ( 'NONE', #220552, #60670, #147006, .T. ) ;
#217131=CIRCLE ( 'NONE', #150713, 0.1000000000000028644 ) ;
#217189=VERTEX_POINT ( 'NONE', #107893 ) ;
#217209=EDGE_LOOP ( 'NONE', ( #174558, #46418, #207665, #213077 ) ) ;
#217215=VERTEX_POINT ( 'NONE', #207001 ) ;
#217218=CARTESIAN_POINT ( 'NONE',  ( -21.05000000000000071, 85.51932773110452501, -129.5501311079648872 ) ) ;
#217222=DIRECTION ( 'NONE',  ( -3.265361837132813093E-16, -1.000000000000000000, 7.445645354460596589E-46 ) ) ;
#217224=VERTEX_POINT ( 'NONE', #113034 ) ;
#217231=EDGE_CURVE ( 'NONE', #6807, #214648, #80898, .T. ) ;
#217239=LINE ( 'NONE', #97270, #157187 ) ;
#217265=DIRECTION ( 'NONE',  ( 0.7070776581708965169, 4.937903618720407826E-15, -0.7071359030027827286 ) ) ;
#217272=DIRECTION ( 'NONE',  ( -1.000000000000000000, 3.265361837132813093E-16, 2.280189983783949500E-30 ) ) ;
#217274=DIRECTION ( 'NONE',  ( 0.000000000000000000, -0.6728971962617172897, 0.7397360091702445128 ) ) ;
#217311=DIRECTION ( 'NONE',  ( 0.000000000000000000, -6.982962677686266711E-15, 1.000000000000000000 ) ) ;
#217321=CARTESIAN_POINT ( 'NONE',  ( -18.59999999999999787, 77.14957036958755054, -95.20719500002232394 ) ) ;
#217350=VECTOR ( 'NONE', #38400, 1000.000000000000000 ) ;
#217372=EDGE_CURVE ( 'NONE', #139747, #227184, #97451, .T. ) ;
#217426=DIRECTION ( 'NONE',  ( -1.000000000000000000, -0.000000000000000000, -0.000000000000000000 ) ) ;
#217431=EDGE_LOOP ( 'NONE', ( #12082, #75062, #73573, #128401 ) ) ;
#217462=DIRECTION ( 'NONE',  ( 0.000000000000000000, 0.000000000000000000, -1.000000000000000000 ) ) ;
#217466=AXIS2_PLACEMENT_3D ( 'NONE', #137532, #179274, #235356 ) ;
#217477=DIRECTION ( 'NONE',  ( 0.000000000000000000, 0.000000000000000000, 1.000000000000000000 ) ) ;
#217480=EDGE_CURVE ( 'NONE', #67927, #190104, #89277, .T. ) ;
#217497=DIRECTION ( 'NONE',  ( 0.000000000000000000, 0.1298341882519953583, 0.9915357197604862671 ) ) ;
#217523=TOROIDAL_SURFACE ( 'NONE', #130230, 0.2000000000000000111, 0.1000000000000000056 ) ;
#217533=AXIS2_PLACEMENT_3D ( 'NONE', #79421, #117292, #165074 ) ;
#217558=VERTEX_POINT ( 'NONE', #127155 ) ;
#217564=DIRECTION ( 'NONE',  ( -1.000000000000000000, -0.000000000000000000, -0.000000000000000000 ) ) ;
#217571=AXIS2_PLACEMENT_3D ( 'NONE', #22997, #222412, #88039 ) ;
#217573=EDGE_LOOP ( 'NONE', ( #247095, #227702, #44051, #138268 ) ) ;
#217590=PLANE ( 'NONE',  #87102 ) ;
#217607=FACE_OUTER_BOUND ( 'NONE', #116302, .T. ) ;
#217609=ADVANCED_FACE ( 'NONE', ( #231404 ), #68473, .F. ) ;
#217639=ORIENTED_EDGE ( 'NONE', *, *, #190076, .F. ) ;
#217645=DIRECTION ( 'NONE',  ( 1.000000000000000000, 0.000000000000000000, 0.000000000000000000 ) ) ;
#217666=CARTESIAN_POINT ( 'NONE',  ( 18.50000000000000000, 85.40000000001208491, -129.2258477248609267 ) ) ;
#217682=CIRCLE ( 'NONE', #105228, 0.09999999999999939493 ) ;
#217708=EDGE_CURVE ( 'NONE', #26810, #34583, #230103, .T. ) ;
#217752=DIRECTION ( 'NONE',  ( 1.000000000000000000, 0.000000000000000000, 0.000000000000000000 ) ) ;
#217811=CARTESIAN_POINT ( 'NONE',  ( -20.94999999999999929, 64.40000000001209912, -129.5949042542488314 ) ) ;
#217852=CIRCLE ( 'NONE', #126292, 0.1000000000000011990 ) ;
#217859=ORIENTED_EDGE ( 'NONE', *, *, #150823, .F. ) ;
#217864=EDGE_LOOP ( 'NONE', ( #228394, #119010, #178219, #64934 ) ) ;
#217879=VECTOR ( 'NONE', #107505, 1000.000000000000000 ) ;
#217895=ORIENTED_EDGE ( 'NONE', *, *, #127185, .F. ) ;
#217931=ORIENTED_EDGE ( 'NONE', *, *, #183866, .T. ) ;
#217980=CIRCLE ( 'NONE', #80606, 0.1000000000000026007 ) ;
#217984=DIRECTION ( 'NONE',  ( 0.000000000000000000, 0.000000000000000000, -1.000000000000000000 ) ) ;
#218038=CARTESIAN_POINT ( 'NONE',  ( -22.39999999999999858, 76.00000000001213607, -136.5231074845242745 ) ) ;
#218090=EDGE_CURVE ( 'NONE', #155941, #182465, #243021, .T. ) ;
#218110=FACE_OUTER_BOUND ( 'NONE', #157956, .T. ) ;
#218120=LINE ( 'NONE', #179053, #237865 ) ;
#218123=CARTESIAN_POINT ( 'NONE',  ( -18.52186455169011481, 85.48101848145478243, -129.4980910066099398 ) ) ;
#218125=CARTESIAN_POINT ( 'NONE',  ( -21.40925344232282512, 69.34148114062169554, -136.6220576731439849 ) ) ;
#218127=EDGE_CURVE ( 'NONE', #75842, #37875, #175020, .T. ) ;
#218152=DIRECTION ( 'NONE',  ( 0.000000000000000000, 0.000000000000000000, 1.000000000000000000 ) ) ;
#218218=CIRCLE ( 'NONE', #122396, 0.09999999999999939493 ) ;
#218244=DIRECTION ( 'NONE',  ( 0.000000000000000000, 0.000000000000000000, 1.000000000000000000 ) ) ;
#218251=AXIS2_PLACEMENT_3D ( 'NONE', #193663, #6344, #205844 ) ;
#218252=CARTESIAN_POINT ( 'NONE',  ( -18.46919391072061956, 85.67072438828961367, -96.34930395272469639 ) ) ;
#218274=DIRECTION ( 'NONE',  ( 1.000000000000000000, 0.000000000000000000, 0.000000000000000000 ) ) ;
#218289=CARTESIAN_POINT ( 'NONE',  ( 21.05000000000000426, 75.94851711813041106, -142.8232873024375351 ) ) ;
#218305=FACE_OUTER_BOUND ( 'NONE', #171049, .T. ) ;
#218309=VECTOR ( 'NONE', #231303, 1000.000000000000000 ) ;
#218310=CYLINDRICAL_SURFACE ( 'NONE', #211727, 2.000000000000001776 ) ;
#218339=CARTESIAN_POINT ( 'NONE',  ( -21.05000000000000071, 61.95000000001210338, -131.0094124137634140 ) ) ;
#218345=DIRECTION ( 'NONE',  ( -1.000000000000000000, 0.000000000000000000, 0.000000000000000000 ) ) ;
#218368=DIRECTION ( 'NONE',  ( 1.000000000000000000, 0.000000000000000000, 0.000000000000000000 ) ) ;
#218396=CARTESIAN_POINT ( 'NONE',  ( -18.59999999999999787, 64.35000000001208775, -129.5083017138703667 ) ) ;
#218413=ORIENTED_EDGE ( 'NONE', *, *, #51699, .T. ) ;
#218442=VECTOR ( 'NONE', #117852, 1000.000000000000000 ) ;
#218444=ORIENTED_EDGE ( 'NONE', *, *, #223029, .F. ) ;
#218471=CARTESIAN_POINT ( 'NONE',  ( 20.94999999999999929, 71.00000000001199396, -115.0283735034374359 ) ) ;
#218495=DIRECTION ( 'NONE',  ( -1.000000000000000000, -0.000000000000000000, -0.000000000000000000 ) ) ;
#218509=EDGE_CURVE ( 'NONE', #17154, #26810, #10131, .T. ) ;
#218559=CYLINDRICAL_SURFACE ( 'NONE', #178653, 0.09999999999998898659 ) ;
#218577=ORIENTED_EDGE ( 'NONE', *, *, #24733, .T. ) ;
#218581=ORIENTED_EDGE ( 'NONE', *, *, #184450, .F. ) ;
#218592=ORIENTED_EDGE ( 'NONE', *, *, #119745, .F. ) ;
#218625=EDGE_LOOP ( 'NONE', ( #232865, #179021, #4034, #157191, #182414 ) ) ;
#218637=DIRECTION ( 'NONE',  ( 0.000000000000000000, 6.982962677686266711E-15, -1.000000000000000000 ) ) ;
#218648=EDGE_LOOP ( 'NONE', ( #18805, #104037, #220023, #38432 ) ) ;
#218650=CARTESIAN_POINT ( 'NONE',  ( 21.13461538461538325, 67.11458296203758778, -124.1731074845243512 ) ) ;
#218657=DIRECTION ( 'NONE',  ( 0.000000000000000000, 6.982962677686266711E-15, -1.000000000000000000 ) ) ;
#218662=AXIS2_PLACEMENT_3D ( 'NONE', #25531, #65931, #28112 ) ;
#218688=CARTESIAN_POINT ( 'NONE',  ( 21.05000000000000071, 85.00000000001197975, -112.9170766071766820 ) ) ;
#218692=DIRECTION ( 'NONE',  ( 0.000000000000000000, -6.982962677686266711E-15, 1.000000000000000000 ) ) ;
#218730=FACE_OUTER_BOUND ( 'NONE', #49795, .T. ) ;
#218732=ORIENTED_EDGE ( 'NONE', *, *, #253753, .T. ) ;
#218762=DIRECTION ( 'NONE',  ( 1.000000000000000000, 0.000000000000000000, 0.000000000000000000 ) ) ;
#218783=DIRECTION ( 'NONE',  ( 1.000000000000000000, 0.000000000000000000, 0.000000000000000000 ) ) ;
#218824=ORIENTED_EDGE ( 'NONE', *, *, #207622, .T. ) ;
#218878=ORIENTED_EDGE ( 'NONE', *, *, #40001, .T. ) ;
#218916=DIRECTION ( 'NONE',  ( -1.000000000000000000, -0.000000000000000000, -0.000000000000000000 ) ) ;
#218924=ORIENTED_EDGE ( 'NONE', *, *, #225598, .T. ) ;
#218947=FACE_OUTER_BOUND ( 'NONE', #220144, .T. ) ;
#218952=CARTESIAN_POINT ( 'NONE',  ( -21.05000000000000071, 64.25000000001196554, -110.0379132551783243 ) ) ;
#218971=ORIENTED_EDGE ( 'NONE', *, *, #233497, .F. ) ;
#218973=AXIS2_PLACEMENT_3D ( 'NONE', #241037, #102768, #81909 ) ;
#218988=EDGE_CURVE ( 'NONE', #139774, #162824, #226828, .T. ) ;
#218989=CIRCLE ( 'NONE', #160770, 0.09999999999999939493 ) ;
#218998=CARTESIAN_POINT ( 'NONE',  ( 23.24999999999999645, 79.90000000001190017, -103.0231074845242745 ) ) ;
#219013=CARTESIAN_POINT ( 'NONE',  ( -23.15000000000000213, 64.25000000001196554, -110.0379132551783243 ) ) ;
#219049=CARTESIAN_POINT ( 'NONE',  ( 20.97107704358301916, 67.12452184799079191, -127.9641342551351215 ) ) ;
#219050=ORIENTED_EDGE ( 'NONE', *, *, #199680, .T. ) ;
#219059=DIRECTION ( 'NONE',  ( 0.000000000000000000, 0.000000000000000000, -1.000000000000000000 ) ) ;
#219060=CARTESIAN_POINT ( 'NONE',  ( 18.59999999999999787, 77.83534155023646406, -124.9679561919613064 ) ) ;
#219167=CIRCLE ( 'NONE', #31780, 4.150000000000001243 ) ;
#219170=ORIENTED_EDGE ( 'NONE', *, *, #149795, .F. ) ;
#219182=CIRCLE ( 'NONE', #215105, 11.65000000000000746 ) ;
#219218=DIRECTION ( 'NONE',  ( 1.000000000000000000, 0.000000000000000000, 0.000000000000000000 ) ) ;
#219236=( NAMED_UNIT ( * ) PLANE_ANGLE_UNIT ( ) SI_UNIT ( $, .RADIAN. ) );
#219239=EDGE_CURVE ( 'NONE', #140955, #207631, #24818, .T. ) ;
#219248=LINE ( 'NONE', #61475, #19630 ) ;
#219254=EDGE_LOOP ( 'NONE', ( #133714, #157787, #198339, #229899 ) ) ;
#219257=DIRECTION ( 'NONE',  ( 0.7071067811865127117, 0.7071067811865821007, 0.000000000000000000 ) ) ;
#219259=DIRECTION ( 'NONE',  ( -0.000000000000000000, -6.982962677686266711E-15, 1.000000000000000000 ) ) ;
#219269=B_SPLINE_CURVE_WITH_KNOTS ( 'NONE', 3,
 ( #30872, #205609, #90796, #145633 ),
 .UNSPECIFIED., .F., .F.,
 ( 4, 4 ),
 ( 0.000000000000000000, 0.001767853679387143117 ),
 .UNSPECIFIED. ) ;
#219280=CIRCLE ( 'NONE', #202709, 0.09999999999999939493 ) ;
#219293=DIRECTION ( 'NONE',  ( -0.000000000000000000, 0.7397360091702708251, 0.6728971962616883129 ) ) ;
#219317=AXIS2_PLACEMENT_3D ( 'NONE', #192572, #252525, #54325 ) ;
#219318=CARTESIAN_POINT ( 'NONE',  ( -22.39999999999999503, 76.00000000001219291, -144.3138870828977076 ) ) ;
#219322=CARTESIAN_POINT ( 'NONE',  ( -22.50000000000000000, 64.35012909624795441, -136.6056273753972903 ) ) ;
#219328=DIRECTION ( 'NONE',  ( 0.000000000000000000, -0.008583690987162452199, 0.9999631594459053030 ) ) ;
#219397=DIRECTION ( 'NONE',  ( 0.000000000000000000, -6.982962677686266711E-15, 1.000000000000000000 ) ) ;
#219410=FACE_OUTER_BOUND ( 'NONE', #217864, .T. ) ;
#219428=DIRECTION ( 'NONE',  ( 0.000000000000000000, -2.775557561562888827E-14, 1.000000000000000000 ) ) ;
#219435=CARTESIAN_POINT ( 'NONE',  ( 23.14999999999999147, 76.00000000001213607, -136.5231074845242745 ) ) ;
#219466=EDGE_LOOP ( 'NONE', ( #214787, #156330, #75950, #156155 ) ) ;
#219477=DIRECTION ( 'NONE',  ( 2.952720810173289112E-16, 1.000000000000000000, 6.467318590049456648E-15 ) ) ;
#219482=ORIENTED_EDGE ( 'NONE', *, *, #57355, .T. ) ;
#219486=VERTEX_POINT ( 'NONE', #250249 ) ;
#219524=CARTESIAN_POINT ( 'NONE',  ( -23.15000000000000213, 87.48912529308798014, -106.0231074845242176 ) ) ;
#219529=CIRCLE ( 'NONE', #44765, 2.000000000000001776 ) ;
#219531=CARTESIAN_POINT ( 'NONE',  ( 23.15000000000000213, 87.75000000001205080, -124.3731074845242119 ) ) ;
#219543=CARTESIAN_POINT ( 'NONE',  ( -18.54260524012588007, 85.62421939008567051, -96.28233443875350872 ) ) ;
#219551=DIRECTION ( 'NONE',  ( 0.000000000000000000, 0.000000000000000000, 1.000000000000000000 ) ) ;
#219584=ADVANCED_FACE ( 'NONE', ( #181155 ), #65034, .T. ) ;
#219586=CARTESIAN_POINT ( 'NONE',  ( 21.05000000000000071, 75.96798630682417297, -142.7819502080616303 ) ) ;
#219596=VERTEX_POINT ( 'NONE', #125026 ) ;
#219598=DIRECTION ( 'NONE',  ( -0.000000000000000000, 0.9876197685951241256, 0.1568667991644932258 ) ) ;
#219617=CYLINDRICAL_SURFACE ( 'NONE', #34262, 0.09999999999999939493 ) ;
#219631=CIRCLE ( 'NONE', #107206, 0.1000000000000064587 ) ;
#219659=DIRECTION ( 'NONE',  ( -0.000000000000000000, 7.272083257015735086E-15, -1.000000000000000000 ) ) ;
#219662=VECTOR ( 'NONE', #91280, 1000.000000000000000 ) ;
#219665=ORIENTED_EDGE ( 'NONE', *, *, #208396, .F. ) ;
#219698=ORIENTED_EDGE ( 'NONE', *, *, #154423, .F. ) ;
#219761=ORIENTED_EDGE ( 'NONE', *, *, #100583, .T. ) ;
#219779=CIRCLE ( 'NONE', #203037, 11.74999999999999645 ) ;
#219797=CARTESIAN_POINT ( 'NONE',  ( -20.85000000000000142, 64.35000000001191722, -103.0231074845243882 ) ) ;
#219802=DIRECTION ( 'NONE',  ( -0.000000000000000000, 1.000000000000000000, 6.982962677686266711E-15 ) ) ;
#219808=ORIENTED_EDGE ( 'NONE', *, *, #68806, .F. ) ;
#219829=ORIENTED_EDGE ( 'NONE', *, *, #37379, .F. ) ;
#219831=TOROIDAL_SURFACE ( 'NONE', #132352, 12.77500000000000036, 0.1000000000000000056 ) ;
#219845=ORIENTED_EDGE ( 'NONE', *, *, #194600, .F. ) ;
#219867=ORIENTED_EDGE ( 'NONE', *, *, #250454, .T. ) ;
#219922=EDGE_CURVE ( 'NONE', #189431, #213725, #252303, .T. ) ;
#219929=DIRECTION ( 'NONE',  ( 0.000000000000000000, -6.853228547068871147E-15, 1.000000000000000000 ) ) ;
#219931=LINE ( 'NONE', #36184, #215469 ) ;
#219969=( BOUNDED_CURVE ( )  B_SPLINE_CURVE ( 3, ( #36850, #175093, #116367, #155515 ),
 .UNSPECIFIED., .F., .F. ) 
 B_SPLINE_CURVE_WITH_KNOTS ( ( 4, 4 ),
 ( 4.712388980384689674, 6.283185307179586232 ),
 .UNSPECIFIED. ) 
 CURVE ( )  GEOMETRIC_REPRESENTATION_ITEM ( )  RATIONAL_B_SPLINE_CURVE ( ( 1.000000000000000000, 0.8047378541243649375, 0.8047378541243649375, 1.000000000000000000 ) ) 
 REPRESENTATION_ITEM ( '' )  );
#220023=ORIENTED_EDGE ( 'NONE', *, *, #60219, .F. ) ;
#220034=FACE_OUTER_BOUND ( 'NONE', #139884, .T. ) ;
#220051=DIRECTION ( 'NONE',  ( -1.000000000000000000, 0.000000000000000000, -0.000000000000000000 ) ) ;
#220078=CARTESIAN_POINT ( 'NONE',  ( -22.39999999999999858, 68.20922040163873135, -136.6231074845243540 ) ) ;
#220081=CARTESIAN_POINT ( 'NONE',  ( -23.15000000000000213, 87.65000000001192859, -106.1231074845242262 ) ) ;
#220105=EDGE_CURVE ( 'NONE', #125207, #47181, #143973, .T. ) ;
#220141=EDGE_CURVE ( 'NONE', #62035, #255544, #114949, .T. ) ;
#220144=EDGE_LOOP ( 'NONE', ( #23286, #234904, #123583, #43879 ) ) ;
#220201=VERTEX_POINT ( 'NONE', #14732 ) ;
#220216=CARTESIAN_POINT ( 'NONE',  ( 18.59999999999999076, 61.95000000001208917, -131.0094124137634140 ) ) ;
#220260=DIRECTION ( 'NONE',  ( -1.000000000000000000, 7.304098846218134667E-16, 5.100424963727256530E-30 ) ) ;
#220293=FACE_OUTER_BOUND ( 'NONE', #192789, .T. ) ;
#220302=DIRECTION ( 'NONE',  ( 0.000000000000000000, 0.1350103645451835865, 0.9908441862701605762 ) ) ;
#220336=EDGE_CURVE ( 'NONE', #31313, #170158, #119243, .T. ) ;
#220351=DIRECTION ( 'NONE',  ( 1.000000000000000000, 0.000000000000000000, 0.000000000000000000 ) ) ;
#220352=ADVANCED_FACE ( 'NONE', ( #167089 ), #223160, .T. ) ;
#220362=CARTESIAN_POINT ( 'NONE',  ( 20.86036036209898015, 65.37895722344113381, -128.8567590660221356 ) ) ;
#220393=CARTESIAN_POINT ( 'NONE',  ( -20.94999999999999929, 68.87972903831429505, -99.36354444268502561 ) ) ;
#220397=VERTEX_POINT ( 'NONE', #224449 ) ;
#220419=LINE ( 'NONE', #22224, #122089 ) ;
#220426=VERTEX_POINT ( 'NONE', #5379 ) ;
#220462=ORIENTED_EDGE ( 'NONE', *, *, #30172, .F. ) ;
#220510=CARTESIAN_POINT ( 'NONE',  ( 23.14999999999999858, 76.00000000001190870, -103.0231074845243029 ) ) ;
#220552=VERTEX_POINT ( 'NONE', #233471 ) ;
#220566=ORIENTED_EDGE ( 'NONE', *, *, #219922, .F. ) ;
#220577=EDGE_CURVE ( 'NONE', #49989, #162629, #190496, .T. ) ;
#220584=DIRECTION ( 'NONE',  ( 0.000000000000000000, 0.000000000000000000, 1.000000000000000000 ) ) ;
#220585=CARTESIAN_POINT ( 'NONE',  ( -18.52643265882458579, 65.68026841930900162, -97.47257401318891823 ) ) ;
#220615=DIRECTION ( 'NONE',  ( -1.000000000000000000, 0.000000000000000000, 0.000000000000000000 ) ) ;
#220625=EDGE_CURVE ( 'NONE', #144144, #176263, #59919, .T. ) ;
#220639=EDGE_CURVE ( 'NONE', #85598, #200718, #200739, .T. ) ;
#220674=ADVANCED_FACE ( 'NONE', ( #18253 ), #179909, .F. ) ;
#220679=CARTESIAN_POINT ( 'NONE',  ( 21.00000000000000000, 66.25000000001206502, -124.1731074845243654 ) ) ;
#220683=CIRCLE ( 'NONE', #187362, 12.87499999999999822 ) ;
#220689=AXIS2_PLACEMENT_3D ( 'NONE', #196545, #53191, #191460 ) ;
#220709=ORIENTED_EDGE ( 'NONE', *, *, #251581, .F. ) ;
#220711=CARTESIAN_POINT ( 'NONE',  ( 23.14999999999999147, 80.15000000001214175, -136.5231074845242460 ) ) ;
#220715=CARTESIAN_POINT ( 'NONE',  ( -18.40000000000000213, 85.50000000001209344, -129.5237453873441211 ) ) ;
#220722=ORIENTED_EDGE ( 'NONE', *, *, #130609, .F. ) ;
#220780=ORIENTED_EDGE ( 'NONE', *, *, #196870, .T. ) ;
#220788=CARTESIAN_POINT ( 'NONE',  ( -20.64999999999999858, 73.50000000001199396, -116.2477294072864140 ) ) ;
#220805=FACE_OUTER_BOUND ( 'NONE', #19767, .T. ) ;
#220825=AXIS2_PLACEMENT_3D ( 'NONE', #48175, #110723, #28675 ) ;
#220882=ORIENTED_EDGE ( 'NONE', *, *, #24733, .F. ) ;
#220906=DIRECTION ( 'NONE',  ( 0.000000000000000000, 7.109473446599835262E-15, -1.000000000000000000 ) ) ;
#220916=ORIENTED_EDGE ( 'NONE', *, *, #64609, .F. ) ;
#220947=ADVANCED_FACE ( 'NONE', ( #71524 ), #174510, .F. ) ;
#220953=LINE ( 'NONE', #201398, #149963 ) ;
#220956=ADVANCED_FACE ( 'NONE', ( #229299 ), #14113, .F. ) ;
#220972=CIRCLE ( 'NONE', #146522, 4.000000000000003553 ) ;
#220999=DIRECTION ( 'NONE',  ( 0.000000000000000000, 1.000000000000000000, 6.853228547068871147E-15 ) ) ;
#221007=ORIENTED_EDGE ( 'NONE', *, *, #20013, .F. ) ;
#221011=EDGE_CURVE ( 'NONE', #56619, #35302, #219529, .T. ) ;
#221058=VECTOR ( 'NONE', #154563, 1000.000000000000000 ) ;
#221091=AXIS2_PLACEMENT_3D ( 'NONE', #155209, #254252, #37823 ) ;
#221093=AXIS2_PLACEMENT_3D ( 'NONE', #4108, #83607, #44534 ) ;
#221149=VERTEX_POINT ( 'NONE', #156198 ) ;
#221207=DIRECTION ( 'NONE',  ( 1.000000000000000000, -0.000000000000000000, 0.000000000000000000 ) ) ;
#221227=CARTESIAN_POINT ( 'NONE',  ( -20.00857864376270001, 66.85000000001205933, -124.2731074845243597 ) ) ;
#221232=DIRECTION ( 'NONE',  ( 0.000000000000000000, -6.467318590049456648E-15, 1.000000000000000000 ) ) ;
#221243=ADVANCED_FACE ( 'NONE', ( #248536 ), #249828, .T. ) ;
#221246=DIRECTION ( 'NONE',  ( -0.000000000000000000, 6.982962677686266711E-15, -1.000000000000000000 ) ) ;
#221249=ORIENTED_EDGE ( 'NONE', *, *, #37055, .T. ) ;
#221259=DIRECTION ( 'NONE',  ( 0.000000000000000000, -6.982962677686266711E-15, 1.000000000000000000 ) ) ;
#221260=CARTESIAN_POINT ( 'NONE',  ( 20.85000000000000142, 64.35000000001190301, -103.0231074845243882 ) ) ;
#221289=DIRECTION ( 'NONE',  ( 1.000000000000000000, 0.000000000000000000, 0.000000000000000000 ) ) ;
#221292=FACE_OUTER_BOUND ( 'NONE', #189673, .T. ) ;
#221320=EDGE_LOOP ( 'NONE', ( #4679, #304, #1322, #254909 ) ) ;
#221336=FACE_OUTER_BOUND ( 'NONE', #197876, .T. ) ;
#221342=CARTESIAN_POINT ( 'NONE',  ( 18.49999999999999645, 70.05000000001213323, -126.2174051794894893 ) ) ;
#221343=ORIENTED_EDGE ( 'NONE', *, *, #152912, .T. ) ;
#221347=EDGE_CURVE ( 'NONE', #154466, #160229, #244662, .T. ) ;
#221360=DIRECTION ( 'NONE',  ( -0.000000000000000000, 1.000000000000000000, 6.982962677686267499E-15 ) ) ;
#221399=DIRECTION ( 'NONE',  ( -1.000000000000000000, -7.304098846218164250E-16, 4.217023435051628197E-16 ) ) ;
#221400=DIRECTION ( 'NONE',  ( 0.000000000000000000, -1.000000000000000000, -6.982962677686265922E-15 ) ) ;
#221411=VERTEX_POINT ( 'NONE', #115440 ) ;
#221429=CARTESIAN_POINT ( 'NONE',  ( 23.14999999999999503, 64.35000000001204512, -124.2731074845243739 ) ) ;
#221454=DIRECTION ( 'NONE',  ( 1.000000000000000000, 0.000000000000000000, 0.000000000000000000 ) ) ;
#221464=AXIS2_PLACEMENT_3D ( 'NONE', #164878, #67060, #51311 ) ;
#221491=CARTESIAN_POINT ( 'NONE',  ( 20.94999999999999574, 74.75000000001207923, -128.5231074845243029 ) ) ;
#221509=DIRECTION ( 'NONE',  ( 0.000000000000000000, 0.000000000000000000, 1.000000000000000000 ) ) ;
#221518=ORIENTED_EDGE ( 'NONE', *, *, #257505, .T. ) ;
#221533=ORIENTED_EDGE ( 'NONE', *, *, #171165, .F. ) ;
#221546=CARTESIAN_POINT ( 'NONE',  ( 21.05000000000000071, 65.27628289530463235, -136.5231074845243597 ) ) ;
#221548=EDGE_CURVE ( 'NONE', #34583, #254300, #125719, .T. ) ;
#221570=VERTEX_POINT ( 'NONE', #1902 ) ;
#221606=CARTESIAN_POINT ( 'NONE',  ( 20.75572585718182950, 67.11768327161469472, -128.0258490858113021 ) ) ;
#221617=CARTESIAN_POINT ( 'NONE',  ( 21.14999999999999858, 76.00000000001219291, -143.0637644362255401 ) ) ;
#221621=CARTESIAN_POINT ( 'NONE',  ( -20.54999999999999716, 73.50000000001199396, -116.2477294072864140 ) ) ;
#221648=CARTESIAN_POINT ( 'NONE',  ( 18.59999999999999432, 85.48068669529082797, -96.08199231576637089 ) ) ;
#221657=CARTESIAN_POINT ( 'NONE',  ( -18.59999999999999787, 70.05000000001213323, -126.2174051794894893 ) ) ;
#221665=DIRECTION ( 'NONE',  ( -1.000000000000000000, 0.000000000000000000, 0.000000000000000000 ) ) ;
#221682=DIRECTION ( 'NONE',  ( 0.000000000000000000, 6.982962677686267499E-15, -1.000000000000000000 ) ) ;
#221689=ADVANCED_FACE ( 'NONE', ( #167449 ), #149165, .F. ) ;
#221696=CARTESIAN_POINT ( 'NONE',  ( -23.25000000000000000, 76.00000000001210765, -132.4731074845242915 ) ) ;
#221698=DIRECTION ( 'NONE',  ( -1.000000000000000000, 0.000000000000000000, -0.000000000000000000 ) ) ;
#221720=CARTESIAN_POINT ( 'NONE',  ( -20.54999999999999716, 74.00000000001205080, -123.7984855617622060 ) ) ;
#221774=EDGE_CURVE ( 'NONE', #69086, #18420, #99084, .T. ) ;
#221776=VECTOR ( 'NONE', #231394, 1000.000000000000000 ) ;
#221788=CIRCLE ( 'NONE', #105240, 0.1000000000000028644 ) ;
#221796=EDGE_CURVE ( 'NONE', #201070, #226700, #237346, .T. ) ;
#221819=VECTOR ( 'NONE', #197210, 1000.000000000000000 ) ;
#221833=VERTEX_POINT ( 'NONE', #216487 ) ;
#221841=EDGE_CURVE ( 'NONE', #126698, #85598, #39163, .T. ) ;
#221844=DIRECTION ( 'NONE',  ( 0.000000000000000000, 1.000000000000000000, 6.982962677686266711E-15 ) ) ;
#221855=DIRECTION ( 'NONE',  ( 0.000000000000000000, 0.000000000000000000, 1.000000000000000000 ) ) ;
#221876=CARTESIAN_POINT ( 'NONE',  ( -21.03922262424648082, 64.37609936600730975, -129.6638994416306616 ) ) ;
#221917=ORIENTED_EDGE ( 'NONE', *, *, #166847, .T. ) ;
#221957=ORIENTED_EDGE ( 'NONE', *, *, #107367, .T. ) ;
#222000=ADVANCED_FACE ( 'NONE', ( #49410 ), #36796, .F. ) ;
#222014=CIRCLE ( 'NONE', #188716, 4.150000000000001243 ) ;
#222018=EDGE_CURVE ( 'NONE', #155807, #98643, #107484, .T. ) ;
#222028=DIRECTION ( 'NONE',  ( 0.000000000000000000, -0.1575844902526687130, -0.9875055080513762684 ) ) ;
#222058=DIRECTION ( 'NONE',  ( 0.000000000000000000, 0.000000000000000000, -1.000000000000000000 ) ) ;
#222113=ORIENTED_EDGE ( 'NONE', *, *, #241856, .T. ) ;
#222120=ORIENTED_EDGE ( 'NONE', *, *, #245502, .T. ) ;
#222122=AXIS2_PLACEMENT_3D ( 'NONE', #42027, #236358, #141122 ) ;
#222132=CARTESIAN_POINT ( 'NONE',  ( 18.39999999999999858, 85.51932773110452501, -129.5501311079648872 ) ) ;
#222180=FACE_OUTER_BOUND ( 'NONE', #194210, .T. ) ;
#222203=DIRECTION ( 'NONE',  ( 2.952720810173289112E-16, 1.000000000000000000, -6.088138035986627436E-46 ) ) ;
#222251=AXIS2_PLACEMENT_3D ( 'NONE', #247318, #64830, #186078 ) ;
#222269=CIRCLE ( 'NONE', #143172, 0.09999999999999939493 ) ;
#222300=ORIENTED_EDGE ( 'NONE', *, *, #133410, .T. ) ;
#222303=EDGE_CURVE ( 'NONE', #175608, #217189, #3607, .T. ) ;
#222315=DIRECTION ( 'NONE',  ( -1.000000000000000000, 0.000000000000000000, -0.000000000000000000 ) ) ;
#222317=VECTOR ( 'NONE', #59578, 1000.000000000000000 ) ;
#222365=DIRECTION ( 'NONE',  ( 0.000000000000000000, 1.000000000000000000, 6.853228547068871147E-15 ) ) ;
#222366=DIRECTION ( 'NONE',  ( 0.000000000000000000, 1.000000000000000000, 6.938893903907222067E-15 ) ) ;
#222367=VECTOR ( 'NONE', #231310, 1000.000000000000000 ) ;
#222412=DIRECTION ( 'NONE',  ( -1.000000000000000000, 0.000000000000000000, -0.000000000000000000 ) ) ;
#222435=AXIS2_PLACEMENT_3D ( 'NONE', #15208, #17739, #212124 ) ;
#222436=DIRECTION ( 'NONE',  ( 0.000000000000000000, 0.000000000000000000, 1.000000000000000000 ) ) ;
#222493=DIRECTION ( 'NONE',  ( 0.000000000000000000, 0.000000000000000000, -1.000000000000000000 ) ) ;
#222574=DIRECTION ( 'NONE',  ( 0.000000000000000000, -1.000000000000000000, 0.000000000000000000 ) ) ;
#222593=CARTESIAN_POINT ( 'NONE',  ( -20.64999999999999858, 76.00000000001205080, -123.6481074845242887 ) ) ;
#222637=EDGE_CURVE ( 'NONE', #69624, #157880, #58057, .T. ) ;
#222643=AXIS2_PLACEMENT_3D ( 'NONE', #164593, #43361, #5476 ) ;
#222663=EDGE_CURVE ( 'NONE', #231485, #135981, #18942, .T. ) ;
#222706=EDGE_CURVE ( 'NONE', #220552, #73178, #223799, .T. ) ;
#222720=CARTESIAN_POINT ( 'NONE',  ( 21.05000000000000071, 71.18691588786246882, -114.9646252410481537 ) ) ;
#222766=AXIS2_PLACEMENT_3D ( 'NONE', #227027, #147499, #204886 ) ;
#222769=FACE_OUTER_BOUND ( 'NONE', #169638, .T. ) ;
#222803=CARTESIAN_POINT ( 'NONE',  ( -20.85000000000000142, 65.66751761918668251, -97.42826094061121012 ) ) ;
#222805=AXIS2_PLACEMENT_3D ( 'NONE', #129799, #110230, #230184 ) ;
#222818=DIRECTION ( 'NONE',  ( 1.000000000000000000, 0.000000000000000000, 0.000000000000000000 ) ) ;
#222838=CARTESIAN_POINT ( 'NONE',  ( -22.49072729836729678, 75.94351806727860321, -148.1731157336792535 ) ) ;
#222849=VECTOR ( 'NONE', #25164, 1000.000000000000000 ) ;
#222873=DIRECTION ( 'NONE',  ( 0.000000000000000000, 0.000000000000000000, 1.000000000000000000 ) ) ;
#222896=AXIS2_PLACEMENT_3D ( 'NONE', #56314, #75899, #25889 ) ;
#222917=DIRECTION ( 'NONE',  ( 0.000000000000000000, 6.982962677686267499E-15, -1.000000000000000000 ) ) ;
#222948=ORIENTED_EDGE ( 'NONE', *, *, #106028, .F. ) ;
#222964=DIRECTION ( 'NONE',  ( -1.000000000000000000, -0.000000000000000000, -0.000000000000000000 ) ) ;
#223014=ORIENTED_EDGE ( 'NONE', *, *, #88743, .F. ) ;
#223020=VECTOR ( 'NONE', #26026, 1000.000000000000000 ) ;
#223029=EDGE_CURVE ( 'NONE', #73178, #207360, #172650, .T. ) ;
#223037=AXIS2_PLACEMENT_3D ( 'NONE', #74732, #231217, #214207 ) ;
#223078=VECTOR ( 'NONE', #130302, 1000.000000000000000 ) ;
#223090=DIRECTION ( 'NONE',  ( 1.000000000000000000, -0.000000000000000000, 0.000000000000000000 ) ) ;
#223112=CARTESIAN_POINT ( 'NONE',  ( 19.97071067811864609, 64.27928932189330169, -111.7731074845243739 ) ) ;
#223136=CIRCLE ( 'NONE', #6480, 0.09999999999999939493 ) ;
#223146=CARTESIAN_POINT ( 'NONE',  ( 21.05000000000000071, 67.22371735104096047, -128.0355151060064145 ) ) ;
#223153=DIRECTION ( 'NONE',  ( 1.000000000000000000, 0.000000000000000000, 0.000000000000000000 ) ) ;
#223159=DIRECTION ( 'NONE',  ( -0.000000000000000000, 1.000000000000000000, 6.982962677686266711E-15 ) ) ;
#223160=CYLINDRICAL_SURFACE ( 'NONE', #198331, 0.1000000000000106914 ) ;
#223184=CARTESIAN_POINT ( 'NONE',  ( 21.13461538461538325, 65.38541703798651383, -124.1731074845243654 ) ) ;
#223200=ORIENTED_EDGE ( 'NONE', *, *, #66518, .F. ) ;
#223212=CARTESIAN_POINT ( 'NONE',  ( -18.50000000000000000, 66.75000000001205080, -124.1731074845243654 ) ) ;
#223214=LINE ( 'NONE', #257163, #198082 ) ;
#223254=AXIS2_PLACEMENT_3D ( 'NONE', #36379, #178459, #79305 ) ;
#223290=ORIENTED_EDGE ( 'NONE', *, *, #244257, .T. ) ;
#223304=CARTESIAN_POINT ( 'NONE',  ( 21.05000000000000071, 69.45934304831089889, -136.5231074845243313 ) ) ;
#223316=CARTESIAN_POINT ( 'NONE',  ( -23.25000000000000000, 71.65000000001207070, -124.3731074845243256 ) ) ;
#223366=DIRECTION ( 'NONE',  ( -1.000000000000000000, -7.304098846218105085E-16, -4.217023435051676515E-16 ) ) ;
#223372=ORIENTED_EDGE ( 'NONE', *, *, #113015, .F. ) ;
#223373=CIRCLE ( 'NONE', #110968, 0.09999999999998898659 ) ;
#223377=AXIS2_PLACEMENT_3D ( 'NONE', #94651, #115498, #212057 ) ;
#223383=VECTOR ( 'NONE', #256023, 999.9999999999998863 ) ;
#223388=AXIS2_PLACEMENT_3D ( 'NONE', #46462, #221246, #81718 ) ;
#223409=EDGE_CURVE ( 'NONE', #101582, #174818, #157587, .T. ) ;
#223438=DIRECTION ( 'NONE',  ( -0.000000000000000000, 1.000000000000000000, 6.982962677686267499E-15 ) ) ;
#223448=ORIENTED_EDGE ( 'NONE', *, *, #43215, .T. ) ;
#223455=CARTESIAN_POINT ( 'NONE',  ( 20.94999999999999929, 85.00000000001207923, -126.6291383618717816 ) ) ;
#223458=DIRECTION ( 'NONE',  ( 0.000000000000000000, 0.000000000000000000, 1.000000000000000000 ) ) ;
#223459=ORIENTED_EDGE ( 'NONE', *, *, #190725, .T. ) ;
#223575=EDGE_CURVE ( 'NONE', #28671, #86933, #99263, .T. ) ;
#223584=CARTESIAN_POINT ( 'NONE',  ( 21.05000000000000071, 70.15000000001198543, -113.1556047088022581 ) ) ;
#223590=ORIENTED_EDGE ( 'NONE', *, *, #161018, .T. ) ;
#223596=CIRCLE ( 'NONE', #57003, 4.000000000000003553 ) ;
#223615=AXIS2_PLACEMENT_3D ( 'NONE', #32406, #173219, #208466 ) ;
#223619=DIRECTION ( 'NONE',  ( 0.000000000000000000, -1.000000000000000000, -6.982962677686265922E-15 ) ) ;
#223620=CARTESIAN_POINT ( 'NONE',  ( -23.25000000000000000, 77.83585931145546510, -91.51866831572576189 ) ) ;
#223628=ADVANCED_FACE ( 'NONE', ( #108808 ), #186785, .T. ) ;
#223641=ORIENTED_EDGE ( 'NONE', *, *, #1930, .F. ) ;
#223650=ADVANCED_FACE ( 'NONE', ( #9711 ), #133520, .F. ) ;
#223657=EDGE_CURVE ( 'NONE', #79346, #224301, #249507, .T. ) ;
#223703=AXIS2_PLACEMENT_3D ( 'NONE', #78856, #158449, #121874 ) ;
#223710=TOROIDAL_SURFACE ( 'NONE', #7231, 0.2000000000000000111, 0.1000000000000000056 ) ;
#223739=AXIS2_PLACEMENT_3D ( 'NONE', #221657, #40517, #99140 ) ;
#223759=AXIS2_PLACEMENT_3D ( 'NONE', #96786, #77244, #135928 ) ;
#223768=DIRECTION ( 'NONE',  ( 0.000000000000000000, 7.147358527629759053E-15, -1.000000000000000000 ) ) ;
#223789=DIRECTION ( 'NONE',  ( -1.000000000000000000, 0.000000000000000000, -0.000000000000000000 ) ) ;
#223799=CIRCLE ( 'NONE', #19826, 0.09999999999998898659 ) ;
#223812=VECTOR ( 'NONE', #185706, 1000.000000000000000 ) ;
#223829=AXIS2_PLACEMENT_3D ( 'NONE', #57325, #62495, #142013 ) ;
#223835=ORIENTED_EDGE ( 'NONE', *, *, #119745, .T. ) ;
#223870=DIRECTION ( 'NONE',  ( 0.000000000000000000, 6.982962677686267499E-15, -1.000000000000000000 ) ) ;
#223917=AXIS2_PLACEMENT_3D ( 'NONE', #50492, #51781, #93489 ) ;
#223922=VECTOR ( 'NONE', #48474, 1000.000000000000000 ) ;
#223943=CLOSED_SHELL ( 'NONE', ( #9645, #196690, #132798, #135225, #252168, #47332, #190203, #65019, #175176, #216816, #194308, #198202, #229337, #28729, #143139, #124558, #228692, #130696, #54008, #232475, #214690, #188788, #221689, #220956, #109176, #28279, #45564, #10067, #7628, #98478, #120223, #160650, #19321, #132150, #196919, #65907, #10550, #152488, #151254, #232142, #132266, #9955, #91459, #235125, #156871, #112942, #226248, #212314, #179252, #4652, #160747, #236014, #184553, #71098, #129398, #133517, #240437, #130427, #129608, #45195, #152171, #32324, #52262, #109452, #80782, #6090, #195295, #124768, #179572, #93836, #68801, #109664, #77124, #145902, #91069, #232276, #85002, #121528, #43777, #255958, #141717, #132196, #212265, #203390, #201607, #231328, #240832, #88283, #104455, #116326, #199617, #194098, #66340, #239013, #99549, #167758, #56138, #204292, #104738, #136543, #33532, #210684, #220674, #113402, #216784, #217609, #135435, #94379, #134428, #248065, #136136, #15593, #135419, #117715, #45625, #37083, #247289, #165447, #57944, #28324, #165542, #24917, #224281, #102655, #82220, #244567, #102608, #210847, #167436, #53957, #78205, #201262, #3515, #240692, #156286, #191584, #110752, #62298, #129075, #223650, #8479, #185941, #106836, #29794, #154109, #141388, #208417, #152391, #28927, #178556, #222000, #124219, #177766, #62015, #100026, #160801, #100893, #229260, #113037, #33840, #17375, #77354, #249489, #143892, #162976, #31097, #256948, #27479, #243266, #243032, #52603, #130362, #147571, #146876, #189907, #189313, #34895, #182831, #71542, #57545, #212579, #55415, #21042, #111152, #174206, #180356, #30551, #172047, #170852, #99262, #90666, #104288, #49066, #119744, #185156, #215433, #127307, #72381, #137441, #21731, #62240, #83786, #128132, #2311, #41047, #85275, #166505, #132594, #242244, #173653, #221243, #34640, #43330, #100215, #159027, #90849, #25807, #126017, #230337, #87865, #216587, #84866, #9907, #60435, #38277, #246243, #228100, #88901, #21458, #91790, #148511, #82651, #59833, #114928, #70312, #226697, #48815, #178650, #119259, #173122, #67107, #36504, #93718, #142226, #252542, #160775, #247594, #203509, #60533, #37881, #80093, #200613, #94387, #194249, #219584, #52257, #141452, #12305, #226837, #235682, #100342, #91265, #12889, #37584, #9638, #47262, #164786, #252635, #157675, #141885, #257001, #251580, #19993, #78995, #1899, #223628, #83978, #140796, #121531, #118637, #42621, #192136, #155248, #239215, #147927, #33317, #31459, #210244, #133056, #220947, #146589, #31998, #172382, #240354, #44007, #138016, #200675, #178747, #164527, #245209, #224492, #249949, #211900, #209748, #74373, #21229, #52043, #26933, #8615, #88188, #6680, #251791, #15524, #243970, #19739, #1987, #241648, #220352, #181050, #37299, #193956, #44163, #90618, #140951, #142120, #135850, #36113, #162941, #151153, #48406, #171152, #37014, #163065, #235008, #194530, #227909, #39660, #68438, #232067, #152330, #254549, #28402, #109442, #184533, #256687, #201494, #118236, #120840, #136740, #216578, #103821, #109146, #166353, #206445, #257071, #211146, #65856, #106744, #4894, #31267, #16018, #24365, #182916, #229948, #32993, #208209, #256626, #63607, #36230, #245852, #257260, #176624, #87903, #42955, #84791, #236310, #117683, #96668, #228241, #90339, #102597, #17079, #100168, #203024, #89362, #53129, #182413, #124213, #236109, #101744, #178902, #92329, #65232, #45896, #231173, #30800, #160469, #254553, #64615, #182604, #27673, #4729, #16343, #183966, #140341, #110326, #118619, #171043, #244814, #104415, #68827, #241244, #16411, #122119, #211318, #159309, #150375, #109802, #29255, #39317, #121642, #162351, #45869, #106116, #258008, #145015, #21580, #140763, #185053, #166361, #210948, #20049, #94103, #107637, #77547, #159425, #18997, #52409, #179271, #37785, #34142, #120535, #16142, #5768, #46056, #119061, #70590, #257075, #233347, #150977, #144249, #22598, #126001, #248441, #135692, #127064, #39135, #231170, #59028, #14361, #60720, #55973, #170295, #149835, #78462, #115162, #203707, #251820, #164830, #42116, #39085, #27662, #99346, #53870, #213555, #197231, #187507, #207452 ) ) ;
#223953=EDGE_LOOP ( 'NONE', ( #181870, #146994 ) ) ;
#223971=VECTOR ( 'NONE', #230516, 1000.000000000000000 ) ;
#223979=DIRECTION ( 'NONE',  ( 0.000000000000000000, -1.000000000000000000, -6.982962677686265922E-15 ) ) ;
#223997=ORIENTED_EDGE ( 'NONE', *, *, #92571, .F. ) ;
#224008=CARTESIAN_POINT ( 'NONE',  ( 23.24999999999999645, 78.10000000001190301, -103.0231074845242887 ) ) ;
#224150=DIRECTION ( 'NONE',  ( 1.000000000000000000, 0.000000000000000000, -0.000000000000000000 ) ) ;
#224153=EDGE_LOOP ( 'NONE', ( #171097, #65405, #47423 ) ) ;
#224154=LINE ( 'NONE', #102909, #202592 ) ;
#224168=AXIS2_PLACEMENT_3D ( 'NONE', #150345, #79753, #255803 ) ;
#224170=AXIS2_PLACEMENT_3D ( 'NONE', #228784, #65834, #187098 ) ;
#224184=EDGE_CURVE ( 'NONE', #147639, #56206, #171112, .T. ) ;
#224224=VERTEX_POINT ( 'NONE', #198320 ) ;
#224225=CARTESIAN_POINT ( 'NONE',  ( 23.14999999999998437, 71.95000000001213891, -136.5231074845243029 ) ) ;
#224242=DIRECTION ( 'NONE',  ( -1.000000000000000000, -0.000000000000000000, -0.000000000000000000 ) ) ;
#224248=LINE ( 'NONE', #83433, #30120 ) ;
#224249=LINE ( 'NONE', #120060, #126638 ) ;
#224260=VERTEX_POINT ( 'NONE', #19704 ) ;
#224281=ADVANCED_FACE ( 'NONE', ( #177519 ), #121400, .T. ) ;
#224283=DIRECTION ( 'NONE',  ( -1.000000000000000000, 0.000000000000000000, -0.000000000000000000 ) ) ;
#224288=CIRCLE ( 'NONE', #36904, 0.09999999999999939493 ) ;
#224297=FACE_OUTER_BOUND ( 'NONE', #86270, .T. ) ;
#224301=VERTEX_POINT ( 'NONE', #111 ) ;
#224315=ORIENTED_EDGE ( 'NONE', *, *, #79129, .T. ) ;
#224336=ORIENTED_EDGE ( 'NONE', *, *, #219239, .F. ) ;
#224361=CARTESIAN_POINT ( 'NONE',  ( -20.64999999999999858, 76.00000000001192291, -104.9231074845242944 ) ) ;
#224412=CIRCLE ( 'NONE', #149435, 0.1000000000000028644 ) ;
#224423=PLANE ( 'NONE',  #141206 ) ;
#224430=VERTEX_POINT ( 'NONE', #89919 ) ;
#224434=CARTESIAN_POINT ( 'NONE',  ( 21.04999999999999716, 67.12872031401643369, -127.9644784893834100 ) ) ;
#224442=DIRECTION ( 'NONE',  ( -1.000000000000000000, -0.000000000000000000, -0.000000000000000000 ) ) ;
#224445=ORIENTED_EDGE ( 'NONE', *, *, #229048, .T. ) ;
#224449=CARTESIAN_POINT ( 'NONE',  ( -20.94999999999999929, 74.14897176987119565, -124.8691942151018139 ) ) ;
#224492=ADVANCED_FACE ( 'NONE', ( #75527 ), #50780, .T. ) ;
#224494=CARTESIAN_POINT ( 'NONE',  ( 21.95218792049437795, 68.79849243876547860, -136.6221359243242546 ) ) ;
#224498=EDGE_CURVE ( 'NONE', #74752, #158778, #71676, .T. ) ;
#224500=DIRECTION ( 'NONE',  ( 0.000000000000000000, -0.008583690987135041833, 0.9999631594459055250 ) ) ;
#224504=DIRECTION ( 'NONE',  ( 1.000000000000000000, 0.000000000000000000, 0.000000000000000000 ) ) ;
#224513=CARTESIAN_POINT ( 'NONE',  ( -23.15000000000000213, 76.00000000001213607, -136.5231074845242745 ) ) ;
#224537=VECTOR ( 'NONE', #151526, 1000.000000000000000 ) ;
#224546=SPHERICAL_SURFACE ( 'NONE', #222643, 0.1000000000000000056 ) ;
#224574=CIRCLE ( 'NONE', #112194, 0.09999999999998712696 ) ;
#224578=ORIENTED_EDGE ( 'NONE', *, *, #28237, .T. ) ;
#224590=DIRECTION ( 'NONE',  ( 0.000000000000000000, -6.467318590049456648E-15, 1.000000000000000000 ) ) ;
#224603=ORIENTED_EDGE ( 'NONE', *, *, #67104, .F. ) ;
#224611=CARTESIAN_POINT ( 'NONE',  ( 18.49999999999999289, 65.74999999739293344, -111.8359355348920872 ) ) ;
#224616=ORIENTED_EDGE ( 'NONE', *, *, #177503, .F. ) ;
#224620=TOROIDAL_SURFACE ( 'NONE', #137314, 0.2000000000000000111, 0.1000000000000000056 ) ;
#224637=TOROIDAL_SURFACE ( 'NONE', #245507, 11.65000000000000036, 0.1000000000000000056 ) ;
#224638=CARTESIAN_POINT ( 'NONE',  ( -18.52139480978221542, 85.48135884507900073, -129.4985509174051685 ) ) ;
#224641=EDGE_CURVE ( 'NONE', #113334, #257983, #249850, .T. ) ;
#224653=DIRECTION ( 'NONE',  ( -0.000000000000000000, 0.4791956752371485107, 0.8777080977375185666 ) ) ;
#224662=DIRECTION ( 'NONE',  ( -0.000000000000000000, 6.982962677686266711E-15, -1.000000000000000000 ) ) ;
#224668=CARTESIAN_POINT ( 'NONE',  ( 21.00000000000000000, 66.25000000001206502, -124.2731074845243597 ) ) ;
#224672=CIRCLE ( 'NONE', #257954, 11.74999999999999645 ) ;
#224687=DIRECTION ( 'NONE',  ( 0.000000000000000000, 0.000000000000000000, -1.000000000000000000 ) ) ;
#224692=CIRCLE ( 'NONE', #62215, 0.1000000000000028644 ) ;
#224700=CARTESIAN_POINT ( 'NONE',  ( -20.85000000000000142, 68.97833521811179480, -99.18954208262705663 ) ) ;
#224711=DIRECTION ( 'NONE',  ( 0.000000000000000000, -6.982962677686266711E-15, 1.000000000000000000 ) ) ;
#224712=ORIENTED_EDGE ( 'NONE', *, *, #94759, .F. ) ;
#224716=CARTESIAN_POINT ( 'NONE',  ( -20.54999999999999716, 73.60000000001204512, -123.2984855617622202 ) ) ;
#224726=LINE ( 'NONE', #46094, #28325 ) ;
#224741=PLANE ( 'NONE',  #203299 ) ;
#224763=CARTESIAN_POINT ( 'NONE',  ( -23.15000000000000213, 85.60000000001221565, -148.2731074845242176 ) ) ;
#224775=DIRECTION ( 'NONE',  ( 0.000000000000000000, 0.000000000000000000, 1.000000000000000000 ) ) ;
#224803=LINE ( 'NONE', #227381, #252863 ) ;
#224808=CIRCLE ( 'NONE', #162471, 0.09999999999998898659 ) ;
#224814=VERTEX_POINT ( 'NONE', #203150 ) ;
#224834=AXIS2_PLACEMENT_3D ( 'NONE', #257392, #176657, #80061 ) ;
#224841=AXIS2_PLACEMENT_3D ( 'NONE', #211879, #52767, #216974 ) ;
#224844=ORIENTED_EDGE ( 'NONE', *, *, #232940, .F. ) ;
#224855=FACE_OUTER_BOUND ( 'NONE', #94838, .T. ) ;
#224865=ORIENTED_EDGE ( 'NONE', *, *, #53836, .T. ) ;
#224891=EDGE_LOOP ( 'NONE', ( #178603, #218577 ) ) ;
#224892=( BOUNDED_SURFACE ( )  B_SPLINE_SURFACE ( 3, 2, ( 
 ( #243673, #85845, #188832 ),
 ( #246246, #91016, #66327 ),
 ( #205829, #244951, #31085 ),
 ( #6333, #145843, #10214 ) ),
 .UNSPECIFIED., .F., .F., .T. ) 
 B_SPLINE_SURFACE_WITH_KNOTS ( ( 4, 4 ),
 ( 3, 3 ),
 ( 0.04058434257139457990, 0.04256401539001584966 ),
 ( 0.000000000000000000, 1.000000000000000000 ),
 .UNSPECIFIED. ) 
 GEOMETRIC_REPRESENTATION_ITEM ( )  RATIONAL_B_SPLINE_SURFACE ( (
 ( 1.000000000000000000, 0.7103081912007894738, 1.000000000000000000),
 ( 1.000000000000000000, 0.7104998333556562518, 1.000000000000000000),
 ( 1.000000000000000000, 0.7107238315754180746, 1.000000000000000000),
 ( 1.000000000000000000, 0.7110073749539692622, 1.000000000000000000) ) ) 
 REPRESENTATION_ITEM ( '' )  SURFACE ( )  );
#224898=DIRECTION ( 'NONE',  ( 0.000000000000000000, 0.01283462868040404978, 0.9999176327611370985 ) ) ;
#224952=VERTEX_POINT ( 'NONE', #233011 ) ;
#224992=AXIS2_PLACEMENT_3D ( 'NONE', #107043, #105743, #148769 ) ;
#225016=DIRECTION ( 'NONE',  ( 1.000000000000000000, 0.000000000000000000, 0.000000000000000000 ) ) ;
#225045=ORIENTED_EDGE ( 'NONE', *, *, #52022, .F. ) ;
#225051=DIRECTION ( 'NONE',  ( 1.000000000000000000, 0.000000000000000000, 0.000000000000000000 ) ) ;
#225060=FACE_OUTER_BOUND ( 'NONE', #87120, .T. ) ;
#225083=EDGE_CURVE ( 'NONE', #183267, #14291, #85101, .T. ) ;
#225088=EDGE_CURVE ( 'NONE', #59827, #255696, #76474, .T. ) ;
#225119=ORIENTED_EDGE ( 'NONE', *, *, #96506, .T. ) ;
#225149=SPHERICAL_SURFACE ( 'NONE', #202052, 0.1000000000000000056 ) ;
#225197=AXIS2_PLACEMENT_3D ( 'NONE', #91610, #37767, #57279 ) ;
#225251=CARTESIAN_POINT ( 'NONE',  ( -23.25000000000000000, 64.25000000001196554, -110.0379132551783243 ) ) ;
#225254=CARTESIAN_POINT ( 'NONE',  ( -22.60000000000094289, 75.89914163091371790, -148.2726746080137161 ) ) ;
#225275=ORIENTED_EDGE ( 'NONE', *, *, #250943, .T. ) ;
#225279=EDGE_LOOP ( 'NONE', ( #61648, #104737, #175895, #123386 ) ) ;
#225311=AXIS2_PLACEMENT_3D ( 'NONE', #53515, #250426, #152649 ) ;
#225384=DIRECTION ( 'NONE',  ( -1.000000000000000000, 0.000000000000000000, -0.000000000000000000 ) ) ;
#225439=DIRECTION ( 'NONE',  ( 0.000000000000000000, 7.026728003956683390E-15, -1.000000000000000000 ) ) ;
#225455=DIRECTION ( 'NONE',  ( 0.000000000000000000, 0.000000000000000000, -1.000000000000000000 ) ) ;
#225460=DIRECTION ( 'NONE',  ( 1.000000000000000000, 0.000000000000000000, 0.000000000000000000 ) ) ;
#225477=CARTESIAN_POINT ( 'NONE',  ( 21.08376601933332495, 69.65805272873649301, -136.5868834954543445 ) ) ;
#225483=DIRECTION ( 'NONE',  ( 0.000000000000000000, -7.026728003956683390E-15, 1.000000000000000000 ) ) ;
#225492=LINE ( 'NONE', #216844, #182793 ) ;
#225502=DIRECTION ( 'NONE',  ( 0.000000000000000000, -6.982962677686266711E-15, 1.000000000000000000 ) ) ;
#225516=ORIENTED_EDGE ( 'NONE', *, *, #72087, .F. ) ;
#225520=DIRECTION ( 'NONE',  ( 0.000000000000000000, 0.000000000000000000, -1.000000000000000000 ) ) ;
#225540=VECTOR ( 'NONE', #109821, 999.9999999999998863 ) ;
#225551=ORIENTED_EDGE ( 'NONE', *, *, #191005, .F. ) ;
#225598=EDGE_CURVE ( 'NONE', #162629, #157579, #166987, .T. ) ;
#225611=DIRECTION ( 'NONE',  ( 1.000000000000000000, 0.000000000000000000, 0.000000000000000000 ) ) ;
#225632=DIRECTION ( 'NONE',  ( 0.000000000000000000, -0.6728971962617102953, -0.7397360091702507301 ) ) ;
#225654=CARTESIAN_POINT ( 'NONE',  ( -20.94999999999999929, 76.00000000001213607, -136.5231074845242745 ) ) ;
#225674=ORIENTED_EDGE ( 'NONE', *, *, #231410, .T. ) ;
#225706=CARTESIAN_POINT ( 'NONE',  ( -23.15000000000000213, 74.00000000001199396, -116.2477294072864140 ) ) ;
#225714=AXIS2_PLACEMENT_3D ( 'NONE', #235303, #213174, #172821 ) ;
#225724=CARTESIAN_POINT ( 'NONE',  ( 21.05000000000000071, 76.00000000001205080, -124.3731074845242972 ) ) ;
#225759=VERTEX_POINT ( 'NONE', #113397 ) ;
#225775=ORIENTED_EDGE ( 'NONE', *, *, #21938, .F. ) ;
#225789=CARTESIAN_POINT ( 'NONE',  ( 21.14999999999999858, 67.21339244341194785, -124.2731074845243597 ) ) ;
#225799=AXIS2_PLACEMENT_3D ( 'NONE', #84238, #118300, #40071 ) ;
#225812=CARTESIAN_POINT ( 'NONE',  ( -21.45000000000000284, 68.29142135624930177, -115.3731074845243540 ) ) ;
#225841=DIRECTION ( 'NONE',  ( 0.000000000000000000, -0.9908441862701791170, 0.1350103645450472789 ) ) ;
#225870=CARTESIAN_POINT ( 'NONE',  ( 18.49999999999999289, 65.50857864377465489, -111.7731074845243597 ) ) ;
#225871=CIRCLE ( 'NONE', #171770, 11.65000000000000746 ) ;
#225890=PLANE ( 'NONE',  #119122 ) ;
#225917=VERTEX_POINT ( 'NONE', #122382 ) ;
#225951=CARTESIAN_POINT ( 'NONE',  ( 21.05000000000000071, 76.00000000001190870, -103.0231074845243029 ) ) ;
#225994=CIRCLE ( 'NONE', #126049, 7.720710678118663850 ) ;
#225999=ORIENTED_EDGE ( 'NONE', *, *, #113844, .F. ) ;
#226010=AXIS2_PLACEMENT_3D ( 'NONE', #244741, #102650, #161389 ) ;
#226075=ORIENTED_EDGE ( 'NONE', *, *, #192546, .T. ) ;
#226094=CIRCLE ( 'NONE', #242685, 0.09999999999998898659 ) ;
#226108=DIRECTION ( 'NONE',  ( 0.000000000000000000, 1.000000000000000000, 6.938893903907222067E-15 ) ) ;
#226121=DIRECTION ( 'NONE',  ( 1.000000000000000000, 0.000000000000000000, 0.000000000000000000 ) ) ;
#226153=VECTOR ( 'NONE', #189909, 1000.000000000000000 ) ;
#226159=CARTESIAN_POINT ( 'NONE',  ( 21.05000000000000071, 87.65000000001214175, -136.5231074845242176 ) ) ;
#226166=AXIS2_PLACEMENT_3D ( 'NONE', #244486, #205347, #80242 ) ;
#226169=CARTESIAN_POINT ( 'NONE',  ( 20.95392731769792150, 67.11693852082331091, -128.0008795049530761 ) ) ;
#226248=ADVANCED_FACE ( 'NONE', ( #102468 ), #101171, .F. ) ;
#226364=CIRCLE ( 'NONE', #43065, 6.329289321881370611 ) ;
#226392=DIRECTION ( 'NONE',  ( 0.000000000000000000, -6.982962677686266711E-15, 1.000000000000000000 ) ) ;
#226398=DIRECTION ( 'NONE',  ( 0.000000000000000000, 0.4999999999999689138, 0.8660254037844565822 ) ) ;
#226404=EDGE_CURVE ( 'NONE', #205485, #21653, #18116, .T. ) ;
#226405=VECTOR ( 'NONE', #95890, 1000.000000000000000 ) ;
#226414=SPHERICAL_SURFACE ( 'NONE', #247795, 0.1000000000000000056 ) ;
#226452=EDGE_LOOP ( 'NONE', ( #160413, #253216, #219867, #170484 ) ) ;
#226521=EDGE_LOOP ( 'NONE', ( #103471, #246911, #174003, #155144 ) ) ;
#226540=LINE ( 'NONE', #49210, #37032 ) ;
#226541=ORIENTED_EDGE ( 'NONE', *, *, #133333, .F. ) ;
#226559=DIRECTION ( 'NONE',  ( 0.000000000000000000, 0.000000000000000000, 1.000000000000000000 ) ) ;
#226588=EDGE_CURVE ( 'NONE', #107664, #165453, #234594, .T. ) ;
#226614=CARTESIAN_POINT ( 'NONE',  ( 22.59999985501178799, 64.25013020700916400, -136.5887061543241998 ) ) ;
#226627=VECTOR ( 'NONE', #238933, 1000.000000000000000 ) ;
#226633=CARTESIAN_POINT ( 'NONE',  ( 20.94999999999999929, 69.45000000001205365, -124.2731074845243597 ) ) ;
#226650=DIRECTION ( 'NONE',  ( -1.000000000000000000, 0.000000000000000000, -0.000000000000000000 ) ) ;
#226691=EDGE_LOOP ( 'NONE', ( #222300, #151008, #254657, #165617 ) ) ;
#226695=VERTEX_POINT ( 'NONE', #121781 ) ;
#226697=ADVANCED_FACE ( 'NONE', ( #3077 ), #59980, .T. ) ;
#226700=VERTEX_POINT ( 'NONE', #183035 ) ;
#226716=CIRCLE ( 'NONE', #143515, 0.1000000000000028644 ) ;
#226761=ORIENTED_EDGE ( 'NONE', *, *, #106220, .F. ) ;
#226780=CARTESIAN_POINT ( 'NONE',  ( 21.14999999999999858, 69.35000000001205933, -124.3731074845243540 ) ) ;
#226783=CARTESIAN_POINT ( 'NONE',  ( -20.94999999999999929, 74.63912941282003999, -128.4501095574333647 ) ) ;
#226789=DIRECTION ( 'NONE',  ( 0.000000000000000000, -7.272083257015735086E-15, 1.000000000000000000 ) ) ;
#226792=CARTESIAN_POINT ( 'NONE',  ( -23.15000000000000213, 64.35000000001195986, -110.0379132551783243 ) ) ;
#226802=DIRECTION ( 'NONE',  ( 0.000000000000000000, 0.000000000000000000, 1.000000000000000000 ) ) ;
#226828=CIRCLE ( 'NONE', #155939, 0.1000000000000028644 ) ;
#226829=VERTEX_POINT ( 'NONE', #19667 ) ;
#226837=ADVANCED_FACE ( 'NONE', ( #238699 ), #201452, .T. ) ;
#226855=VERTEX_POINT ( 'NONE', #96593 ) ;
#226861=ORIENTED_EDGE ( 'NONE', *, *, #166078, .F. ) ;
#226869=EDGE_CURVE ( 'NONE', #224430, #88161, #130724, .T. ) ;
#226960=DIRECTION ( 'NONE',  ( 0.000000000000000000, -0.1350103645451807555, -0.9908441862701610203 ) ) ;
#226969=AXIS2_PLACEMENT_3D ( 'NONE', #147632, #172384, #128076 ) ;
#227013=ORIENTED_EDGE ( 'NONE', *, *, #165874, .F. ) ;
#227015=ORIENTED_EDGE ( 'NONE', *, *, #177803, .F. ) ;
#227018=CARTESIAN_POINT ( 'NONE',  ( 18.49505816908824229, 85.43787255322298790, -96.24545028285334070 ) ) ;
#227019=DIRECTION ( 'NONE',  ( 0.000000000000000000, 0.4999999999999608646, -0.8660254037844612451 ) ) ;
#227027=CARTESIAN_POINT ( 'NONE',  ( 20.84999999999999432, 77.16412189325305349, -95.10825939895268277 ) ) ;
#227030=TOROIDAL_SURFACE ( 'NONE', #23054, 12.97499999999999609, 0.1000000000000000056 ) ;
#227073=CARTESIAN_POINT ( 'NONE',  ( -20.64999999999999858, 68.85000000001205933, -124.1731074845243370 ) ) ;
#227077=ORIENTED_EDGE ( 'NONE', *, *, #124760, .T. ) ;
#227087=CIRCLE ( 'NONE', #239575, 0.1000000000000028644 ) ;
#227092=ORIENTED_EDGE ( 'NONE', *, *, #131840, .F. ) ;
#227174=CYLINDRICAL_SURFACE ( 'NONE', #88888, 0.1000000000000028644 ) ;
#227179=CARTESIAN_POINT ( 'NONE',  ( -20.94999999999999929, 76.00000000001190870, -103.0231074845243029 ) ) ;
#227184=VERTEX_POINT ( 'NONE', #215908 ) ;
#227194=ORIENTED_EDGE ( 'NONE', *, *, #64832, .F. ) ;
#227251=CARTESIAN_POINT ( 'NONE',  ( 23.25000000000000000, 64.25000000001199396, -115.1731074845243796 ) ) ;
#227253=EDGE_CURVE ( 'NONE', #86736, #121418, #251717, .T. ) ;
#227307=DIRECTION ( 'NONE',  ( 0.000000000000000000, 0.000000000000000000, -1.000000000000000000 ) ) ;
#227319=AXIS2_PLACEMENT_3D ( 'NONE', #193372, #14746, #233775 ) ;
#227320=DIRECTION ( 'NONE',  ( 0.000000000000000000, 0.000000000000000000, 1.000000000000000000 ) ) ;
#227322=ORIENTED_EDGE ( 'NONE', *, *, #221774, .F. ) ;
#227356=CIRCLE ( 'NONE', #239843, 11.80000000000000426 ) ;
#227381=CARTESIAN_POINT ( 'NONE',  ( -23.25000000000000000, 69.06610602788553877, -99.23746165015076315 ) ) ;
#227436=EDGE_CURVE ( 'NONE', #235860, #194536, #31190, .T. ) ;
#227456=ORIENTED_EDGE ( 'NONE', *, *, #188039, .T. ) ;
#227469=VECTOR ( 'NONE', #245053, 1000.000000000000000 ) ;
#227477=CARTESIAN_POINT ( 'NONE',  ( 20.94999999999999574, 87.48912529308817909, -133.5231074845242176 ) ) ;
#227501=CIRCLE ( 'NONE', #198291, 0.1000000000000028644 ) ;
#227534=AXIS2_PLACEMENT_3D ( 'NONE', #29043, #219802, #179420 ) ;
#227651=DIRECTION ( 'NONE',  ( 0.000000000000000000, 0.000000000000000000, 1.000000000000000000 ) ) ;
#227702=ORIENTED_EDGE ( 'NONE', *, *, #118833, .F. ) ;
#227728=CARTESIAN_POINT ( 'NONE',  ( -23.15000000000000213, 76.00000000001213607, -136.5231074845242745 ) ) ;
#227731=ORIENTED_EDGE ( 'NONE', *, *, #46379, .T. ) ;
#227732=ORIENTED_EDGE ( 'NONE', *, *, #150642, .F. ) ;
#227748=DIRECTION ( 'NONE',  ( 1.000000000000000000, 0.000000000000000000, 0.000000000000000000 ) ) ;
#227776=DIRECTION ( 'NONE',  ( 2.952720810173289112E-16, 1.000000000000000000, 6.982962677686266711E-15 ) ) ;
#227784=CIRCLE ( 'NONE', #198560, 0.09999999999999820144 ) ;
#227797=DIRECTION ( 'NONE',  ( 1.000000000000000000, 0.000000000000000000, 0.000000000000000000 ) ) ;
#227884=CIRCLE ( 'NONE', #19803, 0.6000000000000033085 ) ;
#227909=ADVANCED_FACE ( 'NONE', ( #94391 ), #134785, .T. ) ;
#227935=DIRECTION ( 'NONE',  ( -1.836970198721029934E-16, -1.000000000000000000, -6.982962677686266711E-15 ) ) ;
#227937=DIRECTION ( 'NONE',  ( 0.000000000000000000, -1.000000000000000000, -6.982962677686266711E-15 ) ) ;
#227952=CARTESIAN_POINT ( 'NONE',  ( -22.57320508075687115, 64.25000000001215028, -136.5231074845243597 ) ) ;
#227956=FACE_OUTER_BOUND ( 'NONE', #74074, .T. ) ;
#227980=AXIS2_PLACEMENT_3D ( 'NONE', #167490, #129625, #204014 ) ;
#227990=ORIENTED_EDGE ( 'NONE', *, *, #72051, .F. ) ;
#228041=EDGE_CURVE ( 'NONE', #254300, #17154, #42151, .T. ) ;
#228058=ORIENTED_EDGE ( 'NONE', *, *, #138946, .F. ) ;
#228080=EDGE_CURVE ( 'NONE', #56789, #62705, #4273, .T. ) ;
#228090=CARTESIAN_POINT ( 'NONE',  ( -20.94999999999999929, 76.00000000001188027, -99.02310748452428868 ) ) ;
#228094=EDGE_CURVE ( 'NONE', #114115, #121586, #31367, .T. ) ;
#228100=ADVANCED_FACE ( 'NONE', ( #160824 ), #56175, .T. ) ;
#228109=ORIENTED_EDGE ( 'NONE', *, *, #88278, .T. ) ;
#228122=DIRECTION ( 'NONE',  ( 0.000000000000000000, 0.000000000000000000, 1.000000000000000000 ) ) ;
#228151=EDGE_LOOP ( 'NONE', ( #198708, #165609, #141962, #93530 ) ) ;
#228164=DIRECTION ( 'NONE',  ( 0.000000000000000000, 0.000000000000000000, 1.000000000000000000 ) ) ;
#228167=CYLINDRICAL_SURFACE ( 'NONE', #109365, 12.87499999999999822 ) ;
#228189=ORIENTED_EDGE ( 'NONE', *, *, #128080, .T. ) ;
#228207=ORIENTED_EDGE ( 'NONE', *, *, #136340, .T. ) ;
#228241=ADVANCED_FACE ( 'NONE', ( #256636 ), #179740, .T. ) ;
#228245=DIRECTION ( 'NONE',  ( 0.000000000000000000, -1.000000000000000000, -6.982962677686266711E-15 ) ) ;
#228273=VECTOR ( 'NONE', #59817, 1000.000000000000000 ) ;
#228275=DIRECTION ( 'NONE',  ( 1.000000000000000000, 0.000000000000000000, 0.000000000000000000 ) ) ;
#228340=CARTESIAN_POINT ( 'NONE',  ( 19.75857864376269291, 64.25000000001196554, -111.6731074845243796 ) ) ;
#228359=( BOUNDED_SURFACE ( )  B_SPLINE_SURFACE ( 3, 2, ( 
 ( #194882, #18780, #159593 ),
 ( #59159, #60468, #74943 ),
 ( #97000, #56596, #98286 ),
 ( #140000, #176603, #219543 ),
 ( #17498, #120491, #177882 ),
 ( #16252, #95738, #257338 ),
 ( #175329, #254781, #218252 ),
 ( #14958, #76181, #136137 ),
 ( #94464, #174059, #185569 ),
 ( #6929, #3059, #82579 ) ),
 .UNSPECIFIED., .F., .F., .F. ) 
 B_SPLINE_SURFACE_WITH_KNOTS ( ( 4, 2, 2, 2, 4 ),
 ( 3, 3 ),
 ( 0.0001836757140119223738, 0.0004000170051583654498, 0.0005081876507315870014, 0.0005622729735181977500, 0.0006163582963048084987 ),
 ( 0.000000000000000000, 1.000000000000000000 ),
 .UNSPECIFIED. ) 
 GEOMETRIC_REPRESENTATION_ITEM ( )  RATIONAL_B_SPLINE_SURFACE ( (
 ( 1.000000000000000000, 0.7071067811865475727, 1.000000000000000000),
 ( 1.000000000000000000, 0.6461995200004808648, 1.000000000000000000),
 ( 1.000000000000000000, 0.5776453529583049917, 1.000000000000000000),
 ( 1.000000000000000000, 0.4585233068334871875, 1.000000000000000000),
 ( 1.000000000000000000, 0.4154092989933438895, 1.000000000000000000),
 ( 1.000000000000000000, 0.3550093145839735009, 1.000000000000000000),
 ( 1.000000000000000000, 0.3354498651682673582, 1.000000000000000000),
 ( 1.000000000000000000, 0.3060347992259510042, 1.000000000000000000),
 ( 1.000000000000000000, 0.2963555829621785653, 1.000000000000000000),
 ( 1.000000000000000000, 0.2966190024561813354, 1.000000000000000000) ) ) 
 REPRESENTATION_ITEM ( '' )  SURFACE ( )  );
#228369=VERTEX_POINT ( 'NONE', #184850 ) ;
#228371=DIRECTION ( 'NONE',  ( -1.000000000000000000, 3.265361837132813093E-16, 2.280189983783949500E-30 ) ) ;
#228394=ORIENTED_EDGE ( 'NONE', *, *, #222018, .F. ) ;
#228396=DIRECTION ( 'NONE',  ( 0.000000000000000000, 0.000000000000000000, 1.000000000000000000 ) ) ;
#228401=CARTESIAN_POINT ( 'NONE',  ( 18.57399277249656322, 65.66887361445331805, -97.43298459182690863 ) ) ;
#228428=FACE_OUTER_BOUND ( 'NONE', #61367, .T. ) ;
#228471=DIRECTION ( 'NONE',  ( 1.000000000000000000, 0.000000000000000000, 0.000000000000000000 ) ) ;
#228481=ORIENTED_EDGE ( 'NONE', *, *, #40341, .F. ) ;
#228486=ORIENTED_EDGE ( 'NONE', *, *, #211791, .F. ) ;
#228488=ORIENTED_EDGE ( 'NONE', *, *, #176655, .F. ) ;
#228489=DIRECTION ( 'NONE',  ( -1.000000000000000000, 0.000000000000000000, 0.000000000000000000 ) ) ;
#228528=DIRECTION ( 'NONE',  ( 0.000000000000000000, 0.000000000000000000, -1.000000000000000000 ) ) ;
#228542=ORIENTED_EDGE ( 'NONE', *, *, #130505, .F. ) ;
#228543=DIRECTION ( 'NONE',  ( 1.000000000000000000, 0.000000000000000000, 0.000000000000000000 ) ) ;
#228550=LINE ( 'NONE', #129437, #129248 ) ;
#228579=CARTESIAN_POINT ( 'NONE',  ( -21.12230431290520016, 69.54243334671915022, -136.5283173362133482 ) ) ;
#228608=CARTESIAN_POINT ( 'NONE',  ( -18.59999999999999787, 85.40000000001204228, -129.2258477248609552 ) ) ;
#228619=FACE_OUTER_BOUND ( 'NONE', #224153, .T. ) ;
#228629=DIRECTION ( 'NONE',  ( 0.000000000000000000, -6.982962677686267499E-15, 1.000000000000000000 ) ) ;
#228649=CARTESIAN_POINT ( 'NONE',  ( -20.93302460841142931, 65.68434038414356735, -97.48668807260655456 ) ) ;
#228650=CIRCLE ( 'NONE', #232739, 4.049999999999998046 ) ;
#228671=DIRECTION ( 'NONE',  ( -1.000000000000000000, 0.000000000000000000, 0.000000000000000000 ) ) ;
#228692=ADVANCED_FACE ( 'NONE', ( #59427 ), #185804, .T. ) ;
#228703=VERTEX_POINT ( 'NONE', #215955 ) ;
#228754=CYLINDRICAL_SURFACE ( 'NONE', #151901, 0.09999999999998898659 ) ;
#228764=CARTESIAN_POINT ( 'NONE',  ( -21.05000000000000071, 76.00000000001193712, -107.1231074845243114 ) ) ;
#228773=CARTESIAN_POINT ( 'NONE',  ( 18.50000000000000355, 85.42145614550719301, -129.2811254005048340 ) ) ;
#228784=CARTESIAN_POINT ( 'NONE',  ( 23.15000000000000213, 87.65000000001192859, -106.1231074845242262 ) ) ;
#228791=DIRECTION ( 'NONE',  ( 0.000000000000000000, 1.000000000000000000, 6.982962677686267499E-15 ) ) ;
#228794=CARTESIAN_POINT ( 'NONE',  ( 20.94999999999999574, 77.36087058720413268, -128.4501095574333362 ) ) ;
#228849=ORIENTED_EDGE ( 'NONE', *, *, #124760, .F. ) ;
#228866=TOROIDAL_SURFACE ( 'NONE', #124632, 1.900000000000002576, 0.1000000000000000056 ) ;
#228916=CIRCLE ( 'NONE', #116490, 0.1000000000000021289 ) ;
#228992=CARTESIAN_POINT ( 'NONE',  ( 23.24999999999999289, 64.35000000001204512, -124.3731074845243825 ) ) ;
#229021=CARTESIAN_POINT ( 'NONE',  ( 21.09610168723073187, 75.96641049312069072, -142.9020631997490796 ) ) ;
#229048=EDGE_CURVE ( 'NONE', #40840, #8640, #139961, .T. ) ;
#229051=CARTESIAN_POINT ( 'NONE',  ( -21.05000000000000071, 76.00000000001207923, -128.6231074845242972 ) ) ;
#229071=CIRCLE ( 'NONE', #137464, 11.74999999999999645 ) ;
#229076=FACE_OUTER_BOUND ( 'NONE', #103529, .T. ) ;
#229097=ORIENTED_EDGE ( 'NONE', *, *, #212527, .F. ) ;
#229103=VERTEX_POINT ( 'NONE', #242930 ) ;
#229115=VERTEX_POINT ( 'NONE', #47280 ) ;
#229117=CYLINDRICAL_SURFACE ( 'NONE', #159670, 11.80000000000000426 ) ;
#229118=CIRCLE ( 'NONE', #120815, 0.09999999999999976963 ) ;
#229125=VERTEX_POINT ( 'NONE', #143821 ) ;
#229189=EDGE_LOOP ( 'NONE', ( #186184, #249615, #157268, #167607 ) ) ;
#229247=CARTESIAN_POINT ( 'NONE',  ( -22.59080734064477625, 64.25000000001215028, -136.5538571926213933 ) ) ;
#229255=CYLINDRICAL_SURFACE ( 'NONE', #86452, 0.09999999999999939493 ) ;
#229260=ADVANCED_FACE ( 'NONE', ( #251925 ), #231106, .F. ) ;
#229261=LINE ( 'NONE', #135261, #184857 ) ;
#229299=FACE_OUTER_BOUND ( 'NONE', #66345, .T. ) ;
#229337=ADVANCED_FACE ( 'NONE', ( #126844 ), #77633, .F. ) ;
#229388=CARTESIAN_POINT ( 'NONE',  ( 23.24999999999999289, 64.35000000001195986, -110.0379132551783243 ) ) ;
#229416=DIRECTION ( 'NONE',  ( -0.000000000000000000, 6.982962677686266711E-15, -1.000000000000000000 ) ) ;
#229439=ORIENTED_EDGE ( 'NONE', *, *, #246905, .F. ) ;
#229459=FACE_OUTER_BOUND ( 'NONE', #129986, .T. ) ;
#229470=VECTOR ( 'NONE', #57639, 1000.000000000000000 ) ;
#229480=FACE_OUTER_BOUND ( 'NONE', #31349, .T. ) ;
#229531=ORIENTED_EDGE ( 'NONE', *, *, #10501, .F. ) ;
#229550=ORIENTED_EDGE ( 'NONE', *, *, #30098, .T. ) ;
#229560=CARTESIAN_POINT ( 'NONE',  ( 23.25000000000000355, 98.45632476063501315, -129.7292090367925255 ) ) ;
#229611=DIRECTION ( 'NONE',  ( 1.000000000000000000, 0.000000000000000000, 0.000000000000000000 ) ) ;
#229618=LINE ( 'NONE', #164518, #53344 ) ;
#229623=CARTESIAN_POINT ( 'NONE',  ( 19.87657994472052536, 64.25000000001196554, -111.7573193598979628 ) ) ;
#229677=CARTESIAN_POINT ( 'NONE',  ( 18.59117750673696179, 65.66751761918668251, -97.42826094061121012 ) ) ;
#229680=AXIS2_PLACEMENT_3D ( 'NONE', #210665, #89424, #32059 ) ;
#229685=CARTESIAN_POINT ( 'NONE',  ( 18.50000000000000000, 85.40000000001208491, -129.2258477248609267 ) ) ;
#229694=LINE ( 'NONE', #49763, #223922 ) ;
#229720=DIRECTION ( 'NONE',  ( -0.000000000000000000, 1.000000000000000000, 6.982962677686266711E-15 ) ) ;
#229759=CIRCLE ( 'NONE', #167255, 0.09999999999999938105 ) ;
#229771=EDGE_CURVE ( 'NONE', #132227, #113334, #50831, .T. ) ;
#229802=CARTESIAN_POINT ( 'NONE',  ( -18.59999999999999787, 76.00000000001213607, -136.5231074845242745 ) ) ;
#229821=EDGE_CURVE ( 'NONE', #67101, #187259, #90669, .T. ) ;
#229857=ORIENTED_EDGE ( 'NONE', *, *, #196561, .T. ) ;
#229862=AXIS2_PLACEMENT_3D ( 'NONE', #58192, #217265, #115625 ) ;
#229886=ORIENTED_EDGE ( 'NONE', *, *, #127769, .F. ) ;
#229899=ORIENTED_EDGE ( 'NONE', *, *, #82380, .T. ) ;
#229900=CARTESIAN_POINT ( 'NONE',  ( -20.85000000000000142, 77.36242903720516040, -95.13422623660308375 ) ) ;
#229917=DIRECTION ( 'NONE',  ( 0.000000000000000000, -0.8660254037844377084, -0.5000000000000016653 ) ) ;
#229934=ORIENTED_EDGE ( 'NONE', *, *, #60205, .F. ) ;
#229948=ADVANCED_FACE ( 'NONE', ( #217607 ), #15619, .F. ) ;
#229963=DIRECTION ( 'NONE',  ( -1.000000000000000000, 0.000000000000000000, -0.000000000000000000 ) ) ;
#229983=EDGE_CURVE ( 'NONE', #216369, #182088, #143216, .T. ) ;
#230000=CARTESIAN_POINT ( 'NONE',  ( 23.14999999999999503, 64.25000000001199396, -115.1731074845243796 ) ) ;
#230045=FACE_OUTER_BOUND ( 'NONE', #19712, .T. ) ;
#230059=DIRECTION ( 'NONE',  ( 0.000000000000000000, -6.454785026890489601E-15, 1.000000000000000000 ) ) ;
#230073=CARTESIAN_POINT ( 'NONE',  ( -21.05000000000000071, 76.00000000001190870, -103.0231074845243029 ) ) ;
#230074=FACE_OUTER_BOUND ( 'NONE', #5777, .T. ) ;
#230097=CARTESIAN_POINT ( 'NONE',  ( 18.49999999999999289, 65.67426406872390032, -111.6731074845243796 ) ) ;
#230103=LINE ( 'NONE', #95717, #218442 ) ;
#230146=DIRECTION ( 'NONE',  ( 1.000000000000000000, 0.000000000000000000, 0.000000000000000000 ) ) ;
#230154=FACE_BOUND ( 'NONE', #71591, .T. ) ;
#230157=CARTESIAN_POINT ( 'NONE',  ( 20.94999999999999929, 87.65000000001192859, -106.0231074845242176 ) ) ;
#230165=EDGE_LOOP ( 'NONE', ( #171370, #253438, #128710, #252549 ) ) ;
#230184=DIRECTION ( 'NONE',  ( 1.000000000000000000, 4.758098676964952635E-14, 0.000000000000000000 ) ) ;
#230224=VERTEX_POINT ( 'NONE', #231443 ) ;
#230237=DIRECTION ( 'NONE',  ( 1.000000000000000000, 0.000000000000000000, 0.000000000000000000 ) ) ;
#230290=UNCERTAINTY_MEASURE_WITH_UNIT (LENGTH_MEASURE( 1.000000000000000082E-05 ), #198401, 'distance_accuracy_value', 'NONE');
#230303=DIRECTION ( 'NONE',  ( 0.000000000000000000, -0.8700118002898356018, 0.4930308989875170078 ) ) ;
#230335=AXIS2_PLACEMENT_3D ( 'NONE', #255871, #77270, #57706 ) ;
#230337=ADVANCED_FACE ( 'NONE', ( #120496 ), #257342, .T. ) ;
#230350=AXIS2_PLACEMENT_3D ( 'NONE', #108564, #203803, #186830 ) ;
#230368=VERTEX_POINT ( 'NONE', #194886 ) ;
#230374=EDGE_CURVE ( 'NONE', #93761, #82698, #98290, .T. ) ;
#230378=ORIENTED_EDGE ( 'NONE', *, *, #62731, .T. ) ;
#230388=VERTEX_POINT ( 'NONE', #179185 ) ;
#230422=ORIENTED_EDGE ( 'NONE', *, *, #97216, .F. ) ;
#230431=EDGE_LOOP ( 'NONE', ( #233, #255546, #191802, #94399, #8132, #93479 ) ) ;
#230443=EDGE_CURVE ( 'NONE', #148174, #198296, #185977, .T. ) ;
#230482=VECTOR ( 'NONE', #81474, 1000.000000000000000 ) ;
#230502=EDGE_CURVE ( 'NONE', #35302, #29489, #108604, .T. ) ;
#230510=DIRECTION ( 'NONE',  ( 1.000000000000000000, 0.000000000000000000, 0.000000000000000000 ) ) ;
#230516=DIRECTION ( 'NONE',  ( 0.000000000000000000, -6.982962677686266711E-15, 1.000000000000000000 ) ) ;
#230546=VERTEX_POINT ( 'NONE', #29118 ) ;
#230592=CARTESIAN_POINT ( 'NONE',  ( -21.05000000000000071, 76.00000000001213607, -136.5231074845242745 ) ) ;
#230613=CIRCLE ( 'NONE', #97274, 4.100000000000006750 ) ;
#230624=DIRECTION ( 'NONE',  ( 1.000000000000000000, -0.000000000000000000, 0.000000000000000000 ) ) ;
#230647=CARTESIAN_POINT ( 'NONE',  ( 21.05000000000000071, 76.00000000001190870, -103.0231074845243029 ) ) ;
#230657=ORIENTED_EDGE ( 'NONE', *, *, #14881, .F. ) ;
#230671=DIRECTION ( 'NONE',  ( -1.000000000000000000, 0.000000000000000000, -0.000000000000000000 ) ) ;
#230781=CARTESIAN_POINT ( 'NONE',  ( 18.41815437325348626, 85.49870985315328653, -96.41916164572225512 ) ) ;
#230823=DIRECTION ( 'NONE',  ( 1.000000000000000000, 0.000000000000000000, 0.000000000000000000 ) ) ;
#230825=ORIENTED_EDGE ( 'NONE', *, *, #59916, .F. ) ;
#230874=VECTOR ( 'NONE', #257590, 1000.000000000000114 ) ;
#230891=ORIENTED_EDGE ( 'NONE', *, *, #79951, .T. ) ;
#230893=DIRECTION ( 'NONE',  ( 1.000000000000000000, 0.000000000000000000, 0.000000000000000000 ) ) ;
#230906=CARTESIAN_POINT ( 'NONE',  ( 18.50000000000000000, 86.35479209693734504, -109.2665665014504697 ) ) ;
#230921=CARTESIAN_POINT ( 'NONE',  ( 19.96984138294275368, 64.25000000001196554, -111.7985354133235063 ) ) ;
#230929=CIRCLE ( 'NONE', #143414, 0.1000000000000028644 ) ;
#231044=EDGE_CURVE ( 'NONE', #57517, #1482, #48264, .T. ) ;
#231048=FACE_OUTER_BOUND ( 'NONE', #231058, .T. ) ;
#231051=DIRECTION ( 'NONE',  ( 1.000000000000000000, 0.000000000000000000, 0.000000000000000000 ) ) ;
#231058=EDGE_LOOP ( 'NONE', ( #71624, #257004, #53291, #252586 ) ) ;
#231061=ORIENTED_EDGE ( 'NONE', *, *, #237450, .T. ) ;
#231068=CIRCLE ( 'NONE', #6169, 0.1000000000000028644 ) ;
#231073=ORIENTED_EDGE ( 'NONE', *, *, #82380, .F. ) ;
#231074=AXIS2_PLACEMENT_3D ( 'NONE', #182735, #242679, #180164 ) ;
#231079=DIRECTION ( 'NONE',  ( 0.000000000000000000, 0.000000000000000000, 1.000000000000000000 ) ) ;
#231087=CIRCLE ( 'NONE', #2085, 0.1000000000000028644 ) ;
#231092=DIRECTION ( 'NONE',  ( 1.000000000000000000, 0.000000000000000000, 0.000000000000000000 ) ) ;
#231096=DIRECTION ( 'NONE',  ( -1.000000000000000000, 2.952720810173289112E-16, 2.061873921506763405E-30 ) ) ;
#231106=CYLINDRICAL_SURFACE ( 'NONE', #165147, 0.1000000000000028644 ) ;
#231138=EDGE_LOOP ( 'NONE', ( #216016, #22073, #219845, #68237 ) ) ;
#231151=CARTESIAN_POINT ( 'NONE',  ( -20.85000000000000142, 76.00000000001185185, -95.12310748452429721 ) ) ;
#231163=ORIENTED_EDGE ( 'NONE', *, *, #144790, .T. ) ;
#231170=ADVANCED_FACE ( 'NONE', ( #247749 ), #144633, .T. ) ;
#231173=ADVANCED_FACE ( 'NONE', ( #229480 ), #215555, .F. ) ;
#231203=EDGE_LOOP ( 'NONE', ( #171712, #102199, #48104, #176814 ) ) ;
#231217=DIRECTION ( 'NONE',  ( 7.589415207398576792E-15, 1.000000000000000000, 6.982962677686266711E-15 ) ) ;
#231218=AXIS2_PLACEMENT_3D ( 'NONE', #69635, #172626, #212980 ) ;
#231303=DIRECTION ( 'NONE',  ( 1.000000000000000000, 0.000000000000000000, 0.000000000000000000 ) ) ;
#231310=DIRECTION ( 'NONE',  ( 0.000000000000000000, 1.000000000000000000, 6.982962677686266711E-15 ) ) ;
#231313=EDGE_LOOP ( 'NONE', ( #256039, #203785, #209803 ) ) ;
#231316=EDGE_CURVE ( 'NONE', #125361, #43436, #111335, .T. ) ;
#231328=ADVANCED_FACE ( 'NONE', ( #40292 ), #19415, .F. ) ;
#231335=ORIENTED_EDGE ( 'NONE', *, *, #80854, .T. ) ;
#231338=DIRECTION ( 'NONE',  ( 1.000000000000000000, 0.000000000000000000, 0.000000000000000000 ) ) ;
#231344=CARTESIAN_POINT ( 'NONE',  ( -20.54999999999999716, 68.85000000001205933, -124.2731074845243455 ) ) ;
#231352=AXIS2_PLACEMENT_3D ( 'NONE', #235259, #57896, #38362 ) ;
#231371=AXIS2_PLACEMENT_3D ( 'NONE', #47574, #145398, #46293 ) ;
#231373=DIRECTION ( 'NONE',  ( 0.000000000000000000, -7.109473446599835262E-15, 1.000000000000000000 ) ) ;
#231394=DIRECTION ( 'NONE',  ( -1.000000000000000000, -0.000000000000000000, -0.000000000000000000 ) ) ;
#231404=FACE_OUTER_BOUND ( 'NONE', #74257, .T. ) ;
#231410=EDGE_CURVE ( 'NONE', #148843, #88364, #124933, .T. ) ;
#231430=VERTEX_POINT ( 'NONE', #143189 ) ;
#231443=CARTESIAN_POINT ( 'NONE',  ( -23.15000000000000213, 73.50000000001199396, -116.2477294072864140 ) ) ;
#231470=EDGE_LOOP ( 'NONE', ( #104643, #163387 ) ) ;
#231481=CARTESIAN_POINT ( 'NONE',  ( 22.59999999999999432, 75.95218160930740225, -148.2731299035715153 ) ) ;
#231485=VERTEX_POINT ( 'NONE', #221429 ) ;
#231504=DIRECTION ( 'NONE',  ( 1.000000000000000000, -0.000000000000000000, 0.000000000000000000 ) ) ;
#231541=DIRECTION ( 'NONE',  ( -1.000000000000000000, 0.000000000000000000, -0.000000000000000000 ) ) ;
#231552=EDGE_CURVE ( 'NONE', #91270, #156274, #113064, .T. ) ;
#231558=ORIENTED_EDGE ( 'NONE', *, *, #129486, .T. ) ;
#231588=CARTESIAN_POINT ( 'NONE',  ( -20.94999999999999929, 87.65000000001212754, -133.6231074845242119 ) ) ;
#231621=EDGE_CURVE ( 'NONE', #245292, #20295, #53252, .T. ) ;
#231647=CIRCLE ( 'NONE', #135765, 0.8750000000000007772 ) ;
#231682=AXIS2_PLACEMENT_3D ( 'NONE', #206688, #87994, #241953 ) ;
#231690=CYLINDRICAL_SURFACE ( 'NONE', #64256, 0.09999999999999939493 ) ;
#231692=ORIENTED_EDGE ( 'NONE', *, *, #203822, .T. ) ;
#231702=VERTEX_POINT ( 'NONE', #157358 ) ;
#231717=EDGE_LOOP ( 'NONE', ( #201431, #152981, #181372, #206502 ) ) ;
#231745=CARTESIAN_POINT ( 'NONE',  ( 20.94999999999999574, 87.48912529308817909, -133.6231074845242119 ) ) ;
#231756=AXIS2_PLACEMENT_3D ( 'NONE', #104803, #163533, #25330 ) ;
#231766=VERTEX_POINT ( 'NONE', #16544 ) ;
#231779=VECTOR ( 'NONE', #158343, 1000.000000000000000 ) ;
#231786=EDGE_CURVE ( 'NONE', #112033, #111084, #246800, .T. ) ;
#231791=DIRECTION ( 'NONE',  ( 1.000000000000000000, 0.000000000000000000, 0.000000000000000000 ) ) ;
#231809=VERTEX_POINT ( 'NONE', #126866 ) ;
#231819=CARTESIAN_POINT ( 'NONE',  ( -20.94999999999999929, 77.83534155023646406, -124.8679561919612979 ) ) ;
#231875=CARTESIAN_POINT ( 'NONE',  ( 21.05000000000000071, 76.00000000001213607, -136.5231074845242745 ) ) ;
#231913=CARTESIAN_POINT ( 'NONE',  ( 21.14999999999999858, 67.21339244341194785, -124.2731074845243597 ) ) ;
#231942=VERTEX_POINT ( 'NONE', #194575 ) ;
#231951=EDGE_CURVE ( 'NONE', #139103, #171429, #232411, .T. ) ;
#231958=CIRCLE ( 'NONE', #248682, 4.049999999999998046 ) ;
#231993=PLANE ( 'NONE',  #34345 ) ;
#232004=DIRECTION ( 'NONE',  ( 0.000000000000000000, 0.000000000000000000, 1.000000000000000000 ) ) ;
#232005=ORIENTED_EDGE ( 'NONE', *, *, #244257, .F. ) ;
#232055=ORIENTED_EDGE ( 'NONE', *, *, #111010, .T. ) ;
#232066=LINE ( 'NONE', #53409, #145367 ) ;
#232067=ADVANCED_FACE ( 'NONE', ( #139682 ), #62743, .T. ) ;
#232069=VECTOR ( 'NONE', #251696, 1000.000000000000000 ) ;
#232084=FACE_OUTER_BOUND ( 'NONE', #155464, .T. ) ;
#232133=FACE_OUTER_BOUND ( 'NONE', #62842, .T. ) ;
#232142=ADVANCED_FACE ( 'NONE', ( #78438 ), #166073, .F. ) ;
#232156=FACE_OUTER_BOUND ( 'NONE', #34665, .T. ) ;
#232195=ORIENTED_EDGE ( 'NONE', *, *, #257165, .F. ) ;
#232216=DIRECTION ( 'NONE',  ( 1.000000000000000000, 0.000000000000000000, 0.000000000000000000 ) ) ;
#232220=AXIS2_PLACEMENT_3D ( 'NONE', #54349, #90912, #173073 ) ;
#232246=CARTESIAN_POINT ( 'NONE',  ( 21.05000000000000071, 65.52661458509918191, -128.9444530202758301 ) ) ;
#232262=CARTESIAN_POINT ( 'NONE',  ( 18.59999999999996945, 65.66751761918668251, -97.42826094061121012 ) ) ;
#232276=ADVANCED_FACE ( 'NONE', ( #32642 ), #74333, .F. ) ;
#232277=EDGE_LOOP ( 'NONE', ( #114877, #142925, #120771, #60103 ) ) ;
#232287=DIRECTION ( 'NONE',  ( -3.265361837132813093E-16, -1.000000000000000000, -6.938893903907229955E-15 ) ) ;
#232297=VERTEX_POINT ( 'NONE', #10474 ) ;
#232324=SPHERICAL_SURFACE ( 'NONE', #192187, 0.1000000000000000056 ) ;
#232363=CARTESIAN_POINT ( 'NONE',  ( -20.64999999999999858, 74.00000000001205080, -123.2984855617622060 ) ) ;
#232376=VECTOR ( 'NONE', #229917, 1000.000000000000000 ) ;
#232390=DIRECTION ( 'NONE',  ( 0.7071067811865475727, -0.7071067811865475727, -4.937700262164531476E-15 ) ) ;
#232411=LINE ( 'NONE', #212834, #199177 ) ;
#232415=AXIS2_PLACEMENT_3D ( 'NONE', #29874, #45557, #5106 ) ;
#232420=ORIENTED_EDGE ( 'NONE', *, *, #151544, .T. ) ;
#232445=AXIS2_PLACEMENT_3D ( 'NONE', #105088, #85524, #86824 ) ;
#232451=ORIENTED_EDGE ( 'NONE', *, *, #174455, .T. ) ;
#232458=EDGE_LOOP ( 'NONE', ( #115930, #194050, #28280, #140973 ) ) ;
#232459=EDGE_CURVE ( 'NONE', #67694, #144364, #61144, .T. ) ;
#232475=ADVANCED_FACE ( 'NONE', ( #222769 ), #62183, .F. ) ;
#232496=DIRECTION ( 'NONE',  ( -0.000000000000000000, -1.000000000000000000, -6.982962677686266711E-15 ) ) ;
#232556=CARTESIAN_POINT ( 'NONE',  ( 20.95512820512820440, 65.37615131630019505, -128.8581939154367717 ) ) ;
#232562=ORIENTED_EDGE ( 'NONE', *, *, #182746, .T. ) ;
#232596=CARTESIAN_POINT ( 'NONE',  ( 21.05000000000000071, 85.00000000001197975, -112.9170766071766820 ) ) ;
#232696=AXIS2_PLACEMENT_3D ( 'NONE', #216673, #255757, #43182 ) ;
#232711=PRODUCT_DEFINITION_SHAPE ( 'NONE', 'NONE',  #2194 ) ;
#232739=AXIS2_PLACEMENT_3D ( 'NONE', #150616, #230146, #21396 ) ;
#232742=ORIENTED_EDGE ( 'NONE', *, *, #6766, .T. ) ;
#232764=CARTESIAN_POINT ( 'NONE',  ( 20.95000000000000284, 64.40000000001194280, -109.9513107147998880 ) ) ;
#232814=DIRECTION ( 'NONE',  ( 0.000000000000000000, -6.982962677686266711E-15, 1.000000000000000000 ) ) ;
#232817=CARTESIAN_POINT ( 'NONE',  ( -18.59999999999999787, 64.35000000001208775, -129.6083017138703610 ) ) ;
#232836=CYLINDRICAL_SURFACE ( 'NONE', #71603, 11.80000000000000426 ) ;
#232862=AXIS2_PLACEMENT_3D ( 'NONE', #209355, #33332, #251035 ) ;
#232865=ORIENTED_EDGE ( 'NONE', *, *, #105393, .F. ) ;
#232940=EDGE_CURVE ( 'NONE', #31427, #155438, #166445, .T. ) ;
#232951=ORIENTED_EDGE ( 'NONE', *, *, #125702, .F. ) ;
#233011=CARTESIAN_POINT ( 'NONE',  ( 20.94999999999999929, 64.35000000001195986, -109.8069731475024753 ) ) ;
#233069=ORIENTED_EDGE ( 'NONE', *, *, #171634, .T. ) ;
#233088=EDGE_CURVE ( 'NONE', #17154, #112979, #78890, .T. ) ;
#233108=DIRECTION ( 'NONE',  ( 0.000000000000000000, 0.000000000000000000, 1.000000000000000000 ) ) ;
#233133=AXIS2_PLACEMENT_3D ( 'NONE', #22773, #42314, #201380 ) ;
#233138=CARTESIAN_POINT ( 'NONE',  ( 21.08832698747859169, 67.22463560659483051, -124.2943900180602128 ) ) ;
#233228=DIRECTION ( 'NONE',  ( 1.000000000000000000, 0.000000000000000000, 0.000000000000000000 ) ) ;
#233231=FACE_OUTER_BOUND ( 'NONE', #247264, .T. ) ;
#233234=DIRECTION ( 'NONE',  ( 0.000000000000000000, -0.9908441862701420355, -0.1350103645453197554 ) ) ;
#233237=CARTESIAN_POINT ( 'NONE',  ( -23.25000000000000000, 85.60000000001198828, -112.9170766071766820 ) ) ;
#233316=CIRCLE ( 'NONE', #141702, 0.1000000000000028644 ) ;
#233322=CARTESIAN_POINT ( 'NONE',  ( -20.94999999999999929, 87.48912529308817909, -133.6231074845242119 ) ) ;
#233333=AXIS2_PLACEMENT_3D ( 'NONE', #56897, #253836, #12704 ) ;
#233347=ADVANCED_FACE ( 'NONE', ( #72098 ), #109910, .F. ) ;
#233354=ORIENTED_EDGE ( 'NONE', *, *, #18065, .T. ) ;
#233375=ORIENTED_EDGE ( 'NONE', *, *, #110845, .T. ) ;
#233379=DIRECTION ( 'NONE',  ( -1.000000000000000000, -0.000000000000000000, -0.000000000000000000 ) ) ;
#233393=DIRECTION ( 'NONE',  ( 1.000000000000000000, 7.304098846218134667E-16, 5.100424963727256530E-30 ) ) ;
#233405=DIRECTION ( 'NONE',  ( 0.000000000000000000, 0.000000000000000000, -1.000000000000000000 ) ) ;
#233409=ORIENTED_EDGE ( 'NONE', *, *, #228094, .T. ) ;
#233412=CARTESIAN_POINT ( 'NONE',  ( 18.49999999999999645, 76.00000000001213607, -136.5231074845242745 ) ) ;
#233415=DIRECTION ( 'NONE',  ( 0.000000000000000000, -1.000000000000000000, -6.352154140967427193E-15 ) ) ;
#233424=CARTESIAN_POINT ( 'NONE',  ( -21.14999999999999858, 64.25000000001210765, -129.7392418215462158 ) ) ;
#233431=CIRCLE ( 'NONE', #154350, 0.1000000000000028644 ) ;
#233436=CARTESIAN_POINT ( 'NONE',  ( 20.94999999999999929, 76.00000000001190870, -103.0231074845243029 ) ) ;
#233443=CARTESIAN_POINT ( 'NONE',  ( 20.94999999999999574, 62.00000000001210054, -131.0960149541418502 ) ) ;
#233464=CARTESIAN_POINT ( 'NONE',  ( -20.94999999999999929, 77.16270174995010223, -128.6231074845242972 ) ) ;
#233471=CARTESIAN_POINT ( 'NONE',  ( 21.14999999999999503, 64.35000000001213039, -136.5231074845243597 ) ) ;
#233493=ORIENTED_EDGE ( 'NONE', *, *, #187401, .F. ) ;
#233497=EDGE_CURVE ( 'NONE', #74720, #225917, #42625, .T. ) ;
#233511=CYLINDRICAL_SURFACE ( 'NONE', #199739, 0.8750000000000007772 ) ;
#233538=ORIENTED_EDGE ( 'NONE', *, *, #137590, .F. ) ;
#233593=ORIENTED_EDGE ( 'NONE', *, *, #111678, .F. ) ;
#233605=ORIENTED_EDGE ( 'NONE', *, *, #64222, .T. ) ;
#233606=EDGE_CURVE ( 'NONE', #16075, #224301, #148439, .T. ) ;
#233620=ORIENTED_EDGE ( 'NONE', *, *, #179866, .T. ) ;
#233628=CARTESIAN_POINT ( 'NONE',  ( 20.94999999999999929, 77.83534155023646406, -124.9679561919612922 ) ) ;
#233636=ORIENTED_EDGE ( 'NONE', *, *, #31450, .T. ) ;
#233642=CARTESIAN_POINT ( 'NONE',  ( -21.05000000000000071, 76.00000000001199396, -114.8231074845243000 ) ) ;
#233651=CARTESIAN_POINT ( 'NONE',  ( 21.05000000000000071, 61.95000000001194707, -108.5368025552853197 ) ) ;
#233670=CARTESIAN_POINT ( 'NONE',  ( 23.25000000000000000, 85.60000000001222986, -148.2731074845242460 ) ) ;
#233737=CARTESIAN_POINT ( 'NONE',  ( 18.45068634130097962, 85.48650607335487450, -129.4543290533561901 ) ) ;
#233739=DIRECTION ( 'NONE',  ( 1.000000000000000000, 0.000000000000000000, 0.000000000000000000 ) ) ;
#233775=DIRECTION ( 'NONE',  ( 1.000000000000000000, 0.000000000000000000, 0.000000000000000000 ) ) ;
#233785=CARTESIAN_POINT ( 'NONE',  ( 22.47071067811864609, 68.27992525551410097, -136.6221999392269595 ) ) ;
#233838=CYLINDRICAL_SURFACE ( 'NONE', #183509, 2.000000000000001776 ) ;
#233865=ORIENTED_EDGE ( 'NONE', *, *, #186537, .F. ) ;
#233887=ORIENTED_EDGE ( 'NONE', *, *, #14115, .F. ) ;
#233894=ORIENTED_EDGE ( 'NONE', *, *, #174578, .T. ) ;
#233903=DIRECTION ( 'NONE',  ( 0.000000000000000000, -6.982962677686266711E-15, 1.000000000000000000 ) ) ;
#233920=CARTESIAN_POINT ( 'NONE',  ( 18.59999999999999076, 69.35000000001200249, -115.1731074845243512 ) ) ;
#233924=DIRECTION ( 'NONE',  ( 1.000000000000000000, -0.000000000000000000, 0.000000000000000000 ) ) ;
#233937=CIRCLE ( 'NONE', #109023, 0.1000000000000028644 ) ;
#233940=DIRECTION ( 'NONE',  ( 0.000000000000000000, 0.000000000000000000, -1.000000000000000000 ) ) ;
#233967=CARTESIAN_POINT ( 'NONE',  ( 21.05000000000000071, 70.60000000001198828, -112.9170766071767815 ) ) ;
#234001=ORIENTED_EDGE ( 'NONE', *, *, #144833, .T. ) ;
#234033=AXIS2_PLACEMENT_3D ( 'NONE', #75217, #34813, #114315 ) ;
#234066=LINE ( 'NONE', #138781, #71843 ) ;
#234103=CARTESIAN_POINT ( 'NONE',  ( 23.25000000000000000, 87.75000000001205080, -124.3731074845242119 ) ) ;
#234115=VECTOR ( 'NONE', #236583, 999.9999999999998863 ) ;
#234168=ORIENTED_EDGE ( 'NONE', *, *, #50743, .F. ) ;
#234180=ORIENTED_EDGE ( 'NONE', *, *, #190359, .F. ) ;
#234192=CARTESIAN_POINT ( 'NONE',  ( -20.85000000000000142, 64.35000000001191722, -103.0231074845243882 ) ) ;
#234215=FACE_OUTER_BOUND ( 'NONE', #94668, .T. ) ;
#234224=CIRCLE ( 'NONE', #67830, 0.3999999999999975797 ) ;
#234233=VERTEX_POINT ( 'NONE', #136221 ) ;
#234253=ORIENTED_EDGE ( 'NONE', *, *, #7653, .T. ) ;
#234272=CIRCLE ( 'NONE', #188502, 0.09999999999999939493 ) ;
#234281=VERTEX_POINT ( 'NONE', #239206 ) ;
#234306=CARTESIAN_POINT ( 'NONE',  ( 20.94999999999999929, 65.70729864261004138, -97.56574559737244101 ) ) ;
#234326=CARTESIAN_POINT ( 'NONE',  ( -20.94999999999999929, 87.75000000001212186, -133.4231074845242233 ) ) ;
#234342=EDGE_CURVE ( 'NONE', #170795, #154304, #82664, .T. ) ;
#234351=DIRECTION ( 'NONE',  ( 2.952720810173289112E-16, 1.000000000000000000, -6.088138035986627436E-46 ) ) ;
#234354=FACE_OUTER_BOUND ( 'NONE', #32746, .T. ) ;
#234383=ORIENTED_EDGE ( 'NONE', *, *, #190693, .F. ) ;
#234397=DIRECTION ( 'NONE',  ( 2.952720810173289112E-16, 1.000000000000000000, 6.982962677686266711E-15 ) ) ;
#234403=CARTESIAN_POINT ( 'NONE',  ( 23.24999999999999645, 76.00000000001190870, -103.0231074845243029 ) ) ;
#234406=CARTESIAN_POINT ( 'NONE',  ( -18.59999999999999787, 76.00000000001190870, -103.0231074845243029 ) ) ;
#234445=CARTESIAN_POINT ( 'NONE',  ( 21.04999999999999716, 67.12872031401640527, -124.3731074845243540 ) ) ;
#234449=LINE ( 'NONE', #115802, #39024 ) ;
#234482=ORIENTED_EDGE ( 'NONE', *, *, #58447, .F. ) ;
#234523=CARTESIAN_POINT ( 'NONE',  ( 20.85000000000000142, 77.13501884592203339, -95.30613060109196510 ) ) ;
#234536=CARTESIAN_POINT ( 'NONE',  ( -21.14999999999999858, 64.35000000001214460, -136.4231074845243938 ) ) ;
#234547=VECTOR ( 'NONE', #20928, 1000.000000000000000 ) ;
#234594=CIRCLE ( 'NONE', #188808, 0.09999999999999939493 ) ;
#234618=DIRECTION ( 'NONE',  ( -0.000000000000000000, 7.109473446599835262E-15, -1.000000000000000000 ) ) ;
#234647=DIRECTION ( 'NONE',  ( -1.000000000000000000, 0.000000000000000000, -0.000000000000000000 ) ) ;
#234689=CIRCLE ( 'NONE', #122255, 0.3999999999999975797 ) ;
#234716=B_SPLINE_CURVE_WITH_KNOTS ( 'NONE', 3,
 ( #83392, #6446, #20915, #242491, #161703, #203378, #142110, #165544, #245064, #66433, #2590, #225477, #200811, #63863, #46845, #179974, #1302, #80837, #160428 ),
 .UNSPECIFIED., .F., .F.,
 ( 4, 3, 3, 3, 3, 3, 4 ),
 ( 0.000000000000000000, 7.110282409890467483E-05, 0.0001508797727291509062, 0.0002027344179858535443, 0.0002343294522349110036, 0.0002454816334821511518, 0.0002619873080085817312 ),
 .UNSPECIFIED. ) ;
#234742=AXIS2_PLACEMENT_3D ( 'NONE', #105480, #122529, #127893 ) ;
#234747=DIRECTION ( 'NONE',  ( 0.000000000000000000, 0.3738317757009942399, -0.9274965247785252886 ) ) ;
#234774=CARTESIAN_POINT ( 'NONE',  ( -23.15000000000000213, 71.85000000001205933, -124.1731074845243228 ) ) ;
#234834=CARTESIAN_POINT ( 'NONE',  ( -21.00857864376268935, 64.40000000001208491, -129.5949042542488314 ) ) ;
#234870=AXIS2_PLACEMENT_3D ( 'NONE', #125500, #146333, #148932 ) ;
#234895=DIRECTION ( 'NONE',  ( 0.000000000000000000, 0.000000000000000000, -1.000000000000000000 ) ) ;
#234904=ORIENTED_EDGE ( 'NONE', *, *, #195691, .F. ) ;
#234921=DIRECTION ( 'NONE',  ( 0.000000000000000000, 7.147358527629759053E-15, -1.000000000000000000 ) ) ;
#234967=AXIS2_PLACEMENT_3D ( 'NONE', #19581, #220351, #62554 ) ;
#234971=DIRECTION ( 'NONE',  ( 0.000000000000000000, -1.000000000000000000, -6.860497997771532351E-15 ) ) ;
#234991=FACE_OUTER_BOUND ( 'NONE', #132950, .T. ) ;
#235008=ADVANCED_FACE ( 'NONE', ( #70940 ), #90456, .F. ) ;
#235010=CARTESIAN_POINT ( 'NONE',  ( -23.25000000000000000, 71.75000000001205080, -124.3731074845243256 ) ) ;
#235025=AXIS2_PLACEMENT_3D ( 'NONE', #146528, #85255, #188247 ) ;
#235044=CARTESIAN_POINT ( 'NONE',  ( 18.59999999999999432, 74.83729825007408465, -128.4231074845243086 ) ) ;
#235046=AXIS2_PLACEMENT_3D ( 'NONE', #22947, #159883, #222366 ) ;
#235072=CARTESIAN_POINT ( 'NONE',  ( -18.52328366898032996, 85.64232108905312657, -96.30828814695416895 ) ) ;
#235112=FACE_OUTER_BOUND ( 'NONE', #127499, .T. ) ;
#235125=ADVANCED_FACE ( 'NONE', ( #252104 ), #233838, .F. ) ;
#235145=CIRCLE ( 'NONE', #201809, 0.09999999999999971412 ) ;
#235173=EDGE_LOOP ( 'NONE', ( #153824, #165397, #4977, #91755 ) ) ;
#235185=ORIENTED_EDGE ( 'NONE', *, *, #140021, .F. ) ;
#235186=CARTESIAN_POINT ( 'NONE',  ( 18.40000000000000213, 85.50000000001209344, -129.5237453873440927 ) ) ;
#235190=ORIENTED_EDGE ( 'NONE', *, *, #90033, .T. ) ;
#235201=DIRECTION ( 'NONE',  ( 0.000000000000000000, 0.000000000000000000, 1.000000000000000000 ) ) ;
#235209=LINE ( 'NONE', #193524, #62018 ) ;
#235242=ORIENTED_EDGE ( 'NONE', *, *, #1938, .F. ) ;
#235257=DIRECTION ( 'NONE',  ( -1.000000000000000000, -0.000000000000000000, 0.000000000000000000 ) ) ;
#235259=CARTESIAN_POINT ( 'NONE',  ( 18.59999999999999076, 69.55000000001199112, -115.3731074845243398 ) ) ;
#235267=CARTESIAN_POINT ( 'NONE',  ( 18.59999999999999787, 76.00000000001213607, -136.5231074845242745 ) ) ;
#235268=CARTESIAN_POINT ( 'NONE',  ( 18.59999999999999076, 74.25000000001205080, -124.8535959266226598 ) ) ;
#235291=ORIENTED_EDGE ( 'NONE', *, *, #130525, .F. ) ;
#235303=CARTESIAN_POINT ( 'NONE',  ( -21.14999999999999858, 87.65000000001212754, -133.6231074845242119 ) ) ;
#235350=LINE ( 'NONE', #252343, #23494 ) ;
#235356=DIRECTION ( 'NONE',  ( 1.000000000000000000, 0.000000000000000000, 0.000000000000000000 ) ) ;
#235405=ORIENTED_EDGE ( 'NONE', *, *, #88253, .F. ) ;
#235409=CIRCLE ( 'NONE', #231352, 0.09999999999999939493 ) ;
#235424=VERTEX_POINT ( 'NONE', #28957 ) ;
#235443=EDGE_LOOP ( 'NONE', ( #96505, #162708, #217895, #184070 ) ) ;
#235500=CIRCLE ( 'NONE', #210414, 0.1000000000000028644 ) ;
#235513=FACE_OUTER_BOUND ( 'NONE', #73028, .T. ) ;
#235532=AXIS2_PLACEMENT_3D ( 'NONE', #220081, #30895, #129938 ) ;
#235536=CARTESIAN_POINT ( 'NONE',  ( -21.14999999999999858, 69.45934304831089889, -136.5231074845243313 ) ) ;
#235551=VERTEX_POINT ( 'NONE', #131854 ) ;
#235573=LINE ( 'NONE', #16556, #31591 ) ;
#235583=ORIENTED_EDGE ( 'NONE', *, *, #108523, .T. ) ;
#235621=ORIENTED_EDGE ( 'NONE', *, *, #90496, .F. ) ;
#235658=CARTESIAN_POINT ( 'NONE',  ( 21.09706851349342216, 67.22415748653864398, -124.2875412681247127 ) ) ;
#235659=DIRECTION ( 'NONE',  ( 0.7071067811865487940, 4.851104656540973741E-15, -0.7071067811865463515 ) ) ;
#235682=ADVANCED_FACE ( 'NONE', ( #20924 ), #239955, .T. ) ;
#235699=CARTESIAN_POINT ( 'NONE',  ( -23.25000000000000000, 87.65000000001212754, -133.4231074845242233 ) ) ;
#235777=ORIENTED_EDGE ( 'NONE', *, *, #24690, .T. ) ;
#235847=ORIENTED_EDGE ( 'NONE', *, *, #24399, .F. ) ;
#235857=ORIENTED_EDGE ( 'NONE', *, *, #163974, .T. ) ;
#235860=VERTEX_POINT ( 'NONE', #243792 ) ;
#235865=VERTEX_POINT ( 'NONE', #26042 ) ;
#235891=ORIENTED_EDGE ( 'NONE', *, *, #103332, .F. ) ;
#235895=ORIENTED_EDGE ( 'NONE', *, *, #172099, .F. ) ;
#235925=ORIENTED_EDGE ( 'NONE', *, *, #146571, .F. ) ;
#235938=ORIENTED_EDGE ( 'NONE', *, *, #73038, .T. ) ;
#235940=CYLINDRICAL_SURFACE ( 'NONE', #119778, 0.1000000000000028644 ) ;
#235957=VECTOR ( 'NONE', #192323, 999.9999999999998863 ) ;
#235969=AXIS2_PLACEMENT_3D ( 'NONE', #119885, #45453, #140700 ) ;
#235971=DIRECTION ( 'NONE',  ( 0.000000000000000000, 0.8660254037844377084, 0.5000000000000016653 ) ) ;
#235997=EDGE_CURVE ( 'NONE', #178804, #213344, #114129, .T. ) ;
#236014=ADVANCED_FACE ( 'NONE', ( #178401 ), #79245, .F. ) ;
#236017=EDGE_CURVE ( 'NONE', #5563, #71875, #209268, .T. ) ;
#236034=ORIENTED_EDGE ( 'NONE', *, *, #202244, .F. ) ;
#236037=DIRECTION ( 'NONE',  ( 0.000000000000000000, 0.000000000000000000, 1.000000000000000000 ) ) ;
#236057=ORIENTED_EDGE ( 'NONE', *, *, #69902, .T. ) ;
#236069=CARTESIAN_POINT ( 'NONE',  ( -20.54999999999999716, 73.60000000001200249, -116.2477294072864140 ) ) ;
#236075=DIRECTION ( 'NONE',  ( 1.000000000000000000, 0.000000000000000000, 0.000000000000000000 ) ) ;
#236109=ADVANCED_FACE ( 'NONE', ( #8722 ), #159951, .T. ) ;
#236124=ORIENTED_EDGE ( 'NONE', *, *, #33124, .F. ) ;
#236143=AXIS2_PLACEMENT_3D ( 'NONE', #64212, #60345, #4220 ) ;
#236162=DIRECTION ( 'NONE',  ( 0.000000000000000000, -1.000000000000000000, -6.982962677686266711E-15 ) ) ;
#236219=CARTESIAN_POINT ( 'NONE',  ( 22.60000000000000142, 75.89914163091351895, -148.2726746080136877 ) ) ;
#236265=EDGE_CURVE ( 'NONE', #56206, #12375, #18279, .T. ) ;
#236271=ORIENTED_EDGE ( 'NONE', *, *, #245769, .F. ) ;
#236278=CIRCLE ( 'NONE', #98868, 0.09999999999998898659 ) ;
#236289=LINE ( 'NONE', #53807, #229470 ) ;
#236302=VERTEX_POINT ( 'NONE', #133795 ) ;
#236310=ADVANCED_FACE ( 'NONE', ( #112961 ), #168177, .T. ) ;
#236340=LINE ( 'NONE', #96798, #221819 ) ;
#236358=DIRECTION ( 'NONE',  ( 2.659396599871503635E-15, -0.6132151058540604716, 0.7899159663865477077 ) ) ;
#236370=ORIENTED_EDGE ( 'NONE', *, *, #178339, .T. ) ;
#236377=DIRECTION ( 'NONE',  ( 2.694716079187273439E-16, 1.000000000000000000, 6.467318590049456648E-15 ) ) ;
#236405=AXIS2_PLACEMENT_3D ( 'NONE', #170151, #50142, #29351 ) ;
#236408=VECTOR ( 'NONE', #164060, 1000.000000000000000 ) ;
#236422=CARTESIAN_POINT ( 'NONE',  ( -18.51991288638513211, 85.39243678968493612, -129.3798410805650576 ) ) ;
#236426=AXIS2_PLACEMENT_3D ( 'NONE', #114092, #214478, #192361 ) ;
#236437=AXIS2_PLACEMENT_3D ( 'NONE', #4430, #104790, #65699 ) ;
#236445=VERTEX_POINT ( 'NONE', #246695 ) ;
#236451=EDGE_CURVE ( 'NONE', #82698, #99212, #114316, .T. ) ;
#236454=CARTESIAN_POINT ( 'NONE',  ( 20.94999999999999929, 85.00000000001197975, -112.9170766071766820 ) ) ;
#236456=TOROIDAL_SURFACE ( 'NONE', #240752, 11.65000000000000036, 0.1000000000000000056 ) ;
#236477=ORIENTED_EDGE ( 'NONE', *, *, #95180, .T. ) ;
#236482=FACE_OUTER_BOUND ( 'NONE', #106934, .T. ) ;
#236484=AXIS2_PLACEMENT_3D ( 'NONE', #87245, #127686, #143383 ) ;
#236491=ORIENTED_EDGE ( 'NONE', *, *, #181227, .T. ) ;
#236533=AXIS2_PLACEMENT_3D ( 'NONE', #101593, #183745, #126327 ) ;
#236535=CARTESIAN_POINT ( 'NONE',  ( -20.54999999999999716, 71.65000000001207070, -124.1731074845243228 ) ) ;
#236542=AXIS2_PLACEMENT_3D ( 'NONE', #218038, #156839, #39465 ) ;
#236557=TOROIDAL_SURFACE ( 'NONE', #78341, 0.4000000000000010214, 0.1000000000000000056 ) ;
#236565=ORIENTED_EDGE ( 'NONE', *, *, #47798, .T. ) ;
#236583=DIRECTION ( 'NONE',  ( -0.000000000000000000, 0.1298341882519953583, 0.9915357197604862671 ) ) ;
#236605=DIRECTION ( 'NONE',  ( -1.000000000000000000, 0.000000000000000000, -0.000000000000000000 ) ) ;
#236629=AXIS2_PLACEMENT_3D ( 'NONE', #126863, #51145, #125571 ) ;
#236631=FACE_OUTER_BOUND ( 'NONE', #34106, .T. ) ;
#236635=LINE ( 'NONE', #94558, #154679 ) ;
#236669=ORIENTED_EDGE ( 'NONE', *, *, #99661, .F. ) ;
#236760=DIRECTION ( 'NONE',  ( 0.000000000000000000, -6.982962677686266711E-15, 1.000000000000000000 ) ) ;
#236770=ORIENTED_EDGE ( 'NONE', *, *, #128832, .F. ) ;
#236779=AXIS2_PLACEMENT_3D ( 'NONE', #225706, #223153, #27577 ) ;
#236797=ORIENTED_EDGE ( 'NONE', *, *, #238272, .T. ) ;
#236806=EDGE_CURVE ( 'NONE', #225917, #226855, #99162, .T. ) ;
#236812=AXIS2_PLACEMENT_3D ( 'NONE', #79462, #78177, #153935 ) ;
#236828=EDGE_CURVE ( 'NONE', #180506, #16182, #255915, .T. ) ;
#236843=DIRECTION ( 'NONE',  ( 1.000000000000000000, 0.000000000000000000, 0.000000000000000000 ) ) ;
#236851=ORIENTED_EDGE ( 'NONE', *, *, #115843, .T. ) ;
#236852=CARTESIAN_POINT ( 'NONE',  ( 18.59999999999999787, 77.25000000001185185, -95.22262673010921219 ) ) ;
#236864=VECTOR ( 'NONE', #225611, 1000.000000000000000 ) ;
#236876=DIRECTION ( 'NONE',  ( 0.000000000000000000, -6.938893903907222067E-15, 1.000000000000000000 ) ) ;
#236888=VECTOR ( 'NONE', #205916, 1000.000000000000000 ) ;
#236901=DIRECTION ( 'NONE',  ( 0.000000000000000000, 0.9908441862701605762, 0.1350103645451835310 ) ) ;
#236918=VERTEX_POINT ( 'NONE', #207297 ) ;
#236924=CARTESIAN_POINT ( 'NONE',  ( 19.75857864376268935, 64.35000000001197407, -111.7731074845243739 ) ) ;
#236937=VECTOR ( 'NONE', #15662, 1000.000000000000000 ) ;
#236945=CARTESIAN_POINT ( 'NONE',  ( 20.97239005616515684, 67.12515615866193741, -124.2729546823712070 ) ) ;
#237006=CARTESIAN_POINT ( 'NONE',  ( -18.39999999999999858, 85.60000000001186038, -96.32291809330219223 ) ) ;
#237022=CARTESIAN_POINT ( 'NONE',  ( 23.15000000000000213, 87.65000000001214175, -136.5231074845242176 ) ) ;
#237037=CARTESIAN_POINT ( 'NONE',  ( 20.85000000000000142, 87.75000000001190870, -105.9231074845242091 ) ) ;
#237044=ORIENTED_EDGE ( 'NONE', *, *, #9305, .T. ) ;
#237064=DIRECTION ( 'NONE',  ( 1.000000000000000000, 0.000000000000000000, 0.000000000000000000 ) ) ;
#237069=CARTESIAN_POINT ( 'NONE',  ( 18.52928932188133970, 65.72071067813062939, -111.8731074845243683 ) ) ;
#237073=DIRECTION ( 'NONE',  ( 0.000000000000000000, -0.1495327102803078179, 0.9887567792719429427 ) ) ;
#237131=CIRCLE ( 'NONE', #212211, 12.87499999999999822 ) ;
#237154=DIRECTION ( 'NONE',  ( -1.000000000000000000, 3.265361837132813093E-16, 2.280189983783949500E-30 ) ) ;
#237157=ORIENTED_EDGE ( 'NONE', *, *, #92473, .T. ) ;
#237179=DIRECTION ( 'NONE',  ( 0.000000000000000000, -2.771150684185008344E-14, -1.000000000000000000 ) ) ;
#237189=DIRECTION ( 'NONE',  ( -1.000000000000000000, -0.000000000000000000, 0.000000000000000000 ) ) ;
#237200=ORIENTED_EDGE ( 'NONE', *, *, #178390, .F. ) ;
#237203=ORIENTED_EDGE ( 'NONE', *, *, #96563, .F. ) ;
#237308=CARTESIAN_POINT ( 'NONE',  ( 23.14999999999999503, 64.35000000001195986, -110.0379132551783243 ) ) ;
#237319=DIRECTION ( 'NONE',  ( 0.000000000000000000, -1.000000000000000000, 0.000000000000000000 ) ) ;
#237346=LINE ( 'NONE', #59958, #61699 ) ;
#237358=ORIENTED_EDGE ( 'NONE', *, *, #44504, .F. ) ;
#237417=DIRECTION ( 'NONE',  ( -1.000000000000000000, -0.000000000000000000, -0.000000000000000000 ) ) ;
#237423=FACE_OUTER_BOUND ( 'NONE', #237453, .T. ) ;
#237436=DIRECTION ( 'NONE',  ( 0.000000000000000000, 0.000000000000000000, -1.000000000000000000 ) ) ;
#237450=EDGE_CURVE ( 'NONE', #216955, #197068, #189537, .T. ) ;
#237453=EDGE_LOOP ( 'NONE', ( #42310, #128813, #148929, #72994 ) ) ;
#237479=ORIENTED_EDGE ( 'NONE', *, *, #157776, .T. ) ;
#237482=VECTOR ( 'NONE', #186913, 1000.000000000000000 ) ;
#237554=FACE_OUTER_BOUND ( 'NONE', #157164, .T. ) ;
#237588=CARTESIAN_POINT ( 'NONE',  ( -23.15000000000000213, 84.59626168225496201, -112.4732350016745102 ) ) ;
#237594=CARTESIAN_POINT ( 'NONE',  ( 18.59999999999999076, 77.83585931145546510, -91.51866831572576189 ) ) ;
#237603=DIRECTION ( 'NONE',  ( -1.000000000000000000, -0.000000000000000000, -0.000000000000000000 ) ) ;
#237609=DIRECTION ( 'NONE',  ( 0.9880948137434723000, -0.1538461538461484146, -1.074301950413233906E-15 ) ) ;
#237612=CARTESIAN_POINT ( 'NONE',  ( 21.05000000000000071, 71.00000000001199396, -115.4283735034374274 ) ) ;
#237624=ORIENTED_EDGE ( 'NONE', *, *, #38548, .F. ) ;
#237648=CARTESIAN_POINT ( 'NONE',  ( -20.54999999999999716, 71.65000000001202807, -119.7731074845243313 ) ) ;
#237668=FACE_OUTER_BOUND ( 'NONE', #185257, .T. ) ;
#237684=CARTESIAN_POINT ( 'NONE',  ( 21.05000000000000071, 64.40000000001194280, -109.9513107147998880 ) ) ;
#237735=FACE_OUTER_BOUND ( 'NONE', #178059, .T. ) ;
#237769=CARTESIAN_POINT ( 'NONE',  ( 20.94999999999999574, 87.65000000001212754, -133.5231074845242176 ) ) ;
#237775=ORIENTED_EDGE ( 'NONE', *, *, #80478, .F. ) ;
#237778=EDGE_CURVE ( 'NONE', #73683, #19112, #85790, .T. ) ;
#237794=VECTOR ( 'NONE', #240231, 1000.000000000000000 ) ;
#237800=AXIS2_PLACEMENT_3D ( 'NONE', #7010, #126964, #103524 ) ;
#237813=EDGE_CURVE ( 'NONE', #8134, #115956, #9729, .T. ) ;
#237816=EDGE_LOOP ( 'NONE', ( #213594, #234383, #112056, #1310 ) ) ;
#237841=DIRECTION ( 'NONE',  ( 1.000000000000000000, -0.000000000000000000, 0.000000000000000000 ) ) ;
#237865=VECTOR ( 'NONE', #79882, 1000.000000000000000 ) ;
#237888=VERTEX_POINT ( 'NONE', #86241 ) ;
#237919=ORIENTED_EDGE ( 'NONE', *, *, #174402, .T. ) ;
#237959=CYLINDRICAL_SURFACE ( 'NONE', #242333, 0.09999999999999939493 ) ;
#237962=AXIS2_PLACEMENT_3D ( 'NONE', #20557, #167774, #4789 ) ;
#237965=VECTOR ( 'NONE', #8614, 1000.000000000000000 ) ;
#237968=FACE_OUTER_BOUND ( 'NONE', #171980, .T. ) ;
#237974=FACE_OUTER_BOUND ( 'NONE', #179029, .T. ) ;
#237993=CARTESIAN_POINT ( 'NONE',  ( -18.50000000000000000, 74.13328508995475374, -124.7704322382423072 ) ) ;
#238010=CARTESIAN_POINT ( 'NONE',  ( 18.59999999999999076, 69.55000000001207638, -126.5060803140843291 ) ) ;
#238033=AXIS2_PLACEMENT_3D ( 'NONE', #136673, #94988, #174594 ) ;
#238076=DIRECTION ( 'NONE',  ( 1.000000000000000000, 0.000000000000000000, 0.000000000000000000 ) ) ;
#238094=DIRECTION ( 'NONE',  ( -1.000000000000000000, 3.265361837132813093E-16, 2.280189983783949500E-30 ) ) ;
#238097=CARTESIAN_POINT ( 'NONE',  ( -21.05000000000000071, 76.01771943332060744, -142.9641921729960075 ) ) ;
#238134=ORIENTED_EDGE ( 'NONE', *, *, #61241, .T. ) ;
#238135=DIRECTION ( 'NONE',  ( 1.000000000000000000, 0.000000000000000000, 0.000000000000000000 ) ) ;
#238151=ORIENTED_EDGE ( 'NONE', *, *, #199429, .F. ) ;
#238168=CARTESIAN_POINT ( 'NONE',  ( -20.54999999999999716, 85.00000000001207923, -126.6291383618717816 ) ) ;
#238173=CARTESIAN_POINT ( 'NONE',  ( 20.94999999999999574, 74.15091558138504979, -124.8670969630771879 ) ) ;
#238178=VERTEX_POINT ( 'NONE', #63106 ) ;
#238204=ORIENTED_EDGE ( 'NONE', *, *, #236017, .T. ) ;
#238206=CARTESIAN_POINT ( 'NONE',  ( -20.64999999999999858, 68.85000000001205933, -124.2731074845243455 ) ) ;
#238216=DIRECTION ( 'NONE',  ( 0.000000000000000000, 0.6728971962617172897, -0.7397360091702445128 ) ) ;
#238230=LINE ( 'NONE', #180843, #193958 ) ;
#238232=EDGE_CURVE ( 'NONE', #47571, #181753, #219280, .T. ) ;
#238256=ORIENTED_EDGE ( 'NONE', *, *, #122902, .F. ) ;
#238258=DIRECTION ( 'NONE',  ( 1.000000000000000000, 0.000000000000000000, 0.000000000000000000 ) ) ;
#238272=EDGE_CURVE ( 'NONE', #246496, #17682, #90272, .T. ) ;
#238274=ORIENTED_EDGE ( 'NONE', *, *, #69153, .T. ) ;
#238338=CARTESIAN_POINT ( 'NONE',  ( 20.94999999999999929, 85.00000000001197975, -112.9170766071766820 ) ) ;
#238341=CARTESIAN_POINT ( 'NONE',  ( -20.94999999999999929, 87.48912529308817909, -133.4231074845242233 ) ) ;
#238390=EDGE_CURVE ( 'NONE', #154962, #102511, #215194, .T. ) ;
#238391=AXIS2_PLACEMENT_3D ( 'NONE', #212225, #213481, #110529 ) ;
#238400=DIRECTION ( 'NONE',  ( 0.000000000000000000, 0.000000000000000000, 1.000000000000000000 ) ) ;
#238463=DIRECTION ( 'NONE',  ( 1.000000000000000000, 7.304098846218135653E-16, 5.311601492717085047E-30 ) ) ;
#238518=DIRECTION ( 'NONE',  ( 1.000000000000000000, 0.000000000000000000, 0.000000000000000000 ) ) ;
#238519=CARTESIAN_POINT ( 'NONE',  ( -21.53551880898957904, 75.90103026544052511, -143.3079052459406171 ) ) ;
#238533=VERTEX_POINT ( 'NONE', #95519 ) ;
#238546=EDGE_CURVE ( 'NONE', #21653, #25805, #136053, .T. ) ;
#238551=CARTESIAN_POINT ( 'NONE',  ( 21.33487959338958717, 69.27444184810096317, -136.5231074845243313 ) ) ;
#238578=DIRECTION ( 'NONE',  ( -0.000000000000000000, -6.982962677686266711E-15, 1.000000000000000000 ) ) ;
#238598=EDGE_CURVE ( 'NONE', #80343, #113334, #123616, .T. ) ;
#238631=CARTESIAN_POINT ( 'NONE',  ( 20.51284917709620359, 65.68911337716677679, -128.8506342989326470 ) ) ;
#238645=DIRECTION ( 'NONE',  ( 1.000000000000000000, -2.952720810173289112E-16, -2.061873921506763405E-30 ) ) ;
#238685=DIRECTION ( 'NONE',  ( 1.000000000000000000, 0.000000000000000000, 0.000000000000000000 ) ) ;
#238695=CARTESIAN_POINT ( 'NONE',  ( 20.85000000000000142, 76.00000000001190870, -103.0231074845243029 ) ) ;
#238696=ORIENTED_EDGE ( 'NONE', *, *, #204840, .T. ) ;
#238699=FACE_OUTER_BOUND ( 'NONE', #59671, .T. ) ;
#238702=CARTESIAN_POINT ( 'NONE',  ( 23.24999999999999289, 64.35000000001213039, -136.4231074845243938 ) ) ;
#238709=AXIS2_PLACEMENT_3D ( 'NONE', #15743, #232216, #95243 ) ;
#238729=EDGE_LOOP ( 'NONE', ( #77250, #54530, #12030, #45072 ) ) ;
#238732=EDGE_CURVE ( 'NONE', #107540, #226855, #124536, .T. ) ;
#238747=DIRECTION ( 'NONE',  ( 0.000000000000000000, -6.853228547068871147E-15, 1.000000000000000000 ) ) ;
#238749=CIRCLE ( 'NONE', #39045, 0.1000000000000028644 ) ;
#238762=ORIENTED_EDGE ( 'NONE', *, *, #245809, .T. ) ;
#238805=AXIS2_PLACEMENT_3D ( 'NONE', #189948, #11308, #186097 ) ;
#238860=DIRECTION ( 'NONE',  ( 3.469446951953635015E-14, 6.982962677686266711E-15, -1.000000000000000000 ) ) ;
#238867=DIRECTION ( 'NONE',  ( -0.7071067811865127117, -0.7071067811865821007, 0.000000000000000000 ) ) ;
#238903=CARTESIAN_POINT ( 'NONE',  ( -22.50000000000000000, 64.35042919246734527, -136.6231074845243825 ) ) ;
#238933=DIRECTION ( 'NONE',  ( -0.000000000000000000, 6.982962677686266711E-15, -1.000000000000000000 ) ) ;
#238949=ORIENTED_EDGE ( 'NONE', *, *, #215239, .F. ) ;
#238990=CARTESIAN_POINT ( 'NONE',  ( -23.15000000000000213, 64.35000000001222986, -148.2731074845243882 ) ) ;
#239007=VERTEX_POINT ( 'NONE', #62517 ) ;
#239013=ADVANCED_FACE ( 'NONE', ( #1229 ), #239877, .F. ) ;
#239031=EDGE_LOOP ( 'NONE', ( #110078, #11911, #191852, #60588, #132704 ) ) ;
#239045=DIRECTION ( 'NONE',  ( -0.000000000000000000, 1.000000000000000000, 6.982962677686266711E-15 ) ) ;
#239081=CIRCLE ( 'NONE', #43444, 11.70000000000000284 ) ;
#239107=DIRECTION ( 'NONE',  ( 4.239556034732057360E-17, 0.1298341882519953860, 0.9915357197604862671 ) ) ;
#239115=DIRECTION ( 'NONE',  ( 0.000000000000000000, 6.982962677686266711E-15, -1.000000000000000000 ) ) ;
#239123=CARTESIAN_POINT ( 'NONE',  ( -20.94999999999999929, 64.35000000001195986, -109.8069731475024753 ) ) ;
#239138=CARTESIAN_POINT ( 'NONE',  ( -18.59999999999999787, 69.01799029515544248, -99.32695536626806643 ) ) ;
#239140=B_SPLINE_CURVE_WITH_KNOTS ( 'NONE', 3,
 ( #28515, #108007, #229247, #227952 ),
 .UNSPECIFIED., .F., .F.,
 ( 4, 4 ),
 ( 0.000000000000000000, 0.0001048066582182473756 ),
 .UNSPECIFIED. ) ;
#239155=ORIENTED_EDGE ( 'NONE', *, *, #177503, .T. ) ;
#239160=CARTESIAN_POINT ( 'NONE',  ( -20.54999999999999716, 68.85000000001200249, -115.3731074845243540 ) ) ;
#239172=CARTESIAN_POINT ( 'NONE',  ( 20.99999999999997868, 76.00000000001213607, -136.5231074845242745 ) ) ;
#239173=ORIENTED_EDGE ( 'NONE', *, *, #23579, .T. ) ;
#239183=CARTESIAN_POINT ( 'NONE',  ( -20.54999999999999716, 76.00000000001190870, -103.0231074845243029 ) ) ;
#239198=TOROIDAL_SURFACE ( 'NONE', #89339, 0.2000000000000000111, 0.1000000000000000056 ) ;
#239206=CARTESIAN_POINT ( 'NONE',  ( 21.05000000000000071, 85.50000000001207923, -126.6291383618717816 ) ) ;
#239215=ADVANCED_FACE ( 'NONE', ( #46778 ), #82252, .T. ) ;
#239266=CARTESIAN_POINT ( 'NONE',  ( 20.04142135623730070, 64.35000000001197407, -111.8731074845243825 ) ) ;
#239290=VERTEX_POINT ( 'NONE', #94897 ) ;
#239292=CARTESIAN_POINT ( 'NONE',  ( 23.15000000000000213, 87.75000000001205080, -124.2731074845242176 ) ) ;
#239306=ORIENTED_EDGE ( 'NONE', *, *, #80030, .T. ) ;
#239351=CARTESIAN_POINT ( 'NONE',  ( 20.94999999999999929, 85.00000000001197975, -112.5170766071766764 ) ) ;
#239366=CIRCLE ( 'NONE', #126941, 0.09999999999998898659 ) ;
#239371=ORIENTED_EDGE ( 'NONE', *, *, #132784, .T. ) ;
#239403=CARTESIAN_POINT ( 'NONE',  ( -21.05000000000000071, 76.09999996531173849, -143.0006596670174019 ) ) ;
#239410=AXIS2_PLACEMENT_3D ( 'NONE', #111946, #72831, #54513 ) ;
#239448=DIRECTION ( 'NONE',  ( 0.000000000000000000, 0.000000000000000000, -1.000000000000000000 ) ) ;
#239450=DIRECTION ( 'NONE',  ( 1.000000000000000000, -0.000000000000000000, -0.000000000000000000 ) ) ;
#239467=AXIS2_PLACEMENT_3D ( 'NONE', #74205, #113288, #192840 ) ;
#239476=DIRECTION ( 'NONE',  ( 0.000000000000000000, 0.01283462868040404978, 0.9999176327611370985 ) ) ;
#239515=DIRECTION ( 'NONE',  ( -1.000000000000000000, -0.000000000000000000, -0.000000000000000000 ) ) ;
#239539=EDGE_CURVE ( 'NONE', #191527, #131402, #149130, .T. ) ;
#239549=EDGE_CURVE ( 'NONE', #20295, #245292, #207390, .T. ) ;
#239551=VECTOR ( 'NONE', #225384, 1000.000000000000000 ) ;
#239553=EDGE_LOOP ( 'NONE', ( #74237, #147159, #62936, #172044 ) ) ;
#239575=AXIS2_PLACEMENT_3D ( 'NONE', #211611, #92923, #169957 ) ;
#239585=EDGE_CURVE ( 'NONE', #156311, #68456, #40768, .T. ) ;
#239612=ORIENTED_EDGE ( 'NONE', *, *, #195787, .T. ) ;
#239618=DIRECTION ( 'NONE',  ( -0.7070776581708965169, 0.7071359030027827286, 4.937903618720407826E-15 ) ) ;
#239621=FACE_OUTER_BOUND ( 'NONE', #173514, .T. ) ;
#239720=DIRECTION ( 'NONE',  ( 1.000000000000000000, 0.000000000000000000, 0.000000000000000000 ) ) ;
#239722=DIRECTION ( 'NONE',  ( 0.000000000000000000, 0.000000000000000000, 1.000000000000000000 ) ) ;
#239724=DIRECTION ( 'NONE',  ( -1.000000000000000000, 0.000000000000000000, -0.000000000000000000 ) ) ;
#239729=DIRECTION ( 'NONE',  ( 0.000000000000000000, 0.000000000000000000, 1.000000000000000000 ) ) ;
#239754=VERTEX_POINT ( 'NONE', #202374 ) ;
#239770=CARTESIAN_POINT ( 'NONE',  ( -23.15000000000000213, 64.25000000001215028, -136.5231074845243597 ) ) ;
#239784=CIRCLE ( 'NONE', #173193, 0.3999999999999975797 ) ;
#239835=CARTESIAN_POINT ( 'NONE',  ( 18.50000000000000000, 85.41920976342134963, -129.2753380217652648 ) ) ;
#239843=AXIS2_PLACEMENT_3D ( 'NONE', #57246, #216337, #37736 ) ;
#239860=CARTESIAN_POINT ( 'NONE',  ( -22.41119224318417125, 76.00000000001222134, -148.1726782920690937 ) ) ;
#239875=DIRECTION ( 'NONE',  ( 0.000000000000000000, 0.000000000000000000, 1.000000000000000000 ) ) ;
#239877=PLANE ( 'NONE',  #240503 ) ;
#239878=DIRECTION ( 'NONE',  ( 0.000000000000000000, -1.000000000000000000, -6.352154140967427193E-15 ) ) ;
#239907=FACE_OUTER_BOUND ( 'NONE', #120396, .T. ) ;
#239926=CARTESIAN_POINT ( 'NONE',  ( 20.87631937322877462, 65.52850496324631990, -128.9433616099437359 ) ) ;
#239936=DIRECTION ( 'NONE',  ( 0.000000000000000000, 0.000000000000000000, 1.000000000000000000 ) ) ;
#239941=LINE ( 'NONE', #221621, #10659 ) ;
#239949=DIRECTION ( 'NONE',  ( 0.000000000000000000, 7.026728003956683390E-15, -1.000000000000000000 ) ) ;
#239955=SPHERICAL_SURFACE ( 'NONE', #1166, 0.1000000000000000056 ) ;
#239966=ORIENTED_EDGE ( 'NONE', *, *, #4198, .F. ) ;
#239968=CARTESIAN_POINT ( 'NONE',  ( 22.50000000000000000, 64.35042919246734527, -136.6231074845243825 ) ) ;
#239972=SPHERICAL_SURFACE ( 'NONE', #112793, 0.1000000000000000056 ) ;
#239984=DIRECTION ( 'NONE',  ( 1.000000000000000000, 0.000000000000000000, 0.000000000000000000 ) ) ;
#239993=DIRECTION ( 'NONE',  ( 0.000000000000000000, 0.9908441862701605762, 0.1350103645451835310 ) ) ;
#240006=ORIENTED_EDGE ( 'NONE', *, *, #213875, .T. ) ;
#240046=ORIENTED_EDGE ( 'NONE', *, *, #37060, .F. ) ;
#240054=VERTEX_POINT ( 'NONE', #99082 ) ;
#240070=ORIENTED_EDGE ( 'NONE', *, *, #186278, .F. ) ;
#240085=CARTESIAN_POINT ( 'NONE',  ( 18.59999999999999076, 64.35000000001197407, -111.7731074845243739 ) ) ;
#240108=DIRECTION ( 'NONE',  ( 0.000000000000000000, 6.938893903907222067E-15, -1.000000000000000000 ) ) ;
#240125=FACE_OUTER_BOUND ( 'NONE', #121377, .T. ) ;
#240128=DIRECTION ( 'NONE',  ( -1.000000000000000000, 0.000000000000000000, 0.000000000000000000 ) ) ;
#240149=CIRCLE ( 'NONE', #61062, 0.1000000000000028644 ) ;
#240153=FACE_OUTER_BOUND ( 'NONE', #71837, .T. ) ;
#240167=CARTESIAN_POINT ( 'NONE',  ( 18.59999999999999076, 65.79142135624927334, -111.7731074845243739 ) ) ;
#240182=EDGE_CURVE ( 'NONE', #105588, #54007, #45556, .T. ) ;
#240187=EDGE_CURVE ( 'NONE', #186897, #128325, #253336, .T. ) ;
#240199=EDGE_CURVE ( 'NONE', #180506, #253291, #195100, .T. ) ;
#240213=AXIS2_PLACEMENT_3D ( 'NONE', #98195, #18699, #136049 ) ;
#240231=DIRECTION ( 'NONE',  ( -1.000000000000000000, 0.000000000000000000, 0.000000000000000000 ) ) ;
#240278=AXIS2_PLACEMENT_3D ( 'NONE', #200175, #81466, #220999 ) ;
#240349=DIRECTION ( 'NONE',  ( -0.000000000000000000, -1.000000000000000000, -6.982962677686266711E-15 ) ) ;
#240354=ADVANCED_FACE ( 'NONE', ( #134061 ), #163296, .F. ) ;
#240362=EDGE_LOOP ( 'NONE', ( #211483, #164354, #200608, #143680 ) ) ;
#240393=ORIENTED_EDGE ( 'NONE', *, *, #191005, .T. ) ;
#240423=DIRECTION ( 'NONE',  ( 0.000000000000000000, 0.000000000000000000, -1.000000000000000000 ) ) ;
#240437=ADVANCED_FACE ( 'NONE', ( #197887 ), #19260, .T. ) ;
#240451=DIRECTION ( 'NONE',  ( 0.000000000000000000, 5.880418562633242623E-15, -1.000000000000000000 ) ) ;
#240491=AXIS2_PLACEMENT_3D ( 'NONE', #102499, #120851, #158692 ) ;
#240503=AXIS2_PLACEMENT_3D ( 'NONE', #241163, #238578, #84591 ) ;
#240514=( BOUNDED_SURFACE ( )  B_SPLINE_SURFACE ( 3, 2, ( 
 ( #183792, #242467, #219049 ),
 ( #41734, #221606, #1282 ),
 ( #204621, #5115, #243764 ),
 ( #199525, #62566, #144648 ),
 ( #181245, #20896, #95588 ),
 ( #82091, #6, #43005 ),
 ( #175183, #79532, #159121 ),
 ( #238631, #140817, #59967 ),
 ( #100372, #161683, #80815 ),
 ( #142086, #121292, #160407 ),
 ( #239926, #61277, #220362 ),
 ( #128960, #187665, #88514 ) ),
 .UNSPECIFIED., .F., .F., .F. ) 
 B_SPLINE_SURFACE_WITH_KNOTS ( ( 4, 2, 2, 2, 2, 4 ),
 ( 3, 3 ),
 ( 3.174653483277205090, 3.943930578431714018, 4.713207673586222946, 5.482484768740731873, 5.867123316317986337, 6.251761863895240801 ),
 ( 0.000000000000000000, 1.000000000000000000 ),
 .UNSPECIFIED. ) 
 GEOMETRIC_REPRESENTATION_ITEM ( )  RATIONAL_B_SPLINE_SURFACE ( (
 ( 1.000000000000000000, 0.8659465255642114778, 1.000000000000000000),
 ( 1.000000000000000000, 0.8648614068487411322, 1.000000000000000000),
 ( 1.000000000000000000, 0.8489031841324523597, 1.000000000000000000),
 ( 1.000000000000000000, 0.7927507630160768315, 1.000000000000000000),
 ( 1.000000000000000000, 0.7523013859006951742, 1.000000000000000000),
 ( 1.000000000000000000, 0.6616226951198839190, 1.000000000000000000),
 ( 1.000000000000000000, 0.6112214368721479163, 1.000000000000000000),
 ( 1.000000000000000000, 0.5507684314500016498, 1.000000000000000000),
 ( 1.000000000000000000, 0.5333267243152196579, 1.000000000000000000),
 ( 1.000000000000000000, 0.5084565446481067452, 1.000000000000000000),
 ( 1.000000000000000000, 0.5010722703450574134, 1.000000000000000000),
 ( 1.000000000000000000, 0.5001234037138888588, 1.000000000000000000) ) ) 
 REPRESENTATION_ITEM ( '' )  SURFACE ( )  );
#240526=CIRCLE ( 'NONE', #140556, 0.1000000000000028644 ) ;
#240533=ORIENTED_EDGE ( 'NONE', *, *, #34489, .F. ) ;
#240633=ORIENTED_EDGE ( 'NONE', *, *, #110319, .T. ) ;
#240663=AXIS2_PLACEMENT_3D ( 'NONE', #247278, #90769, #166503 ) ;
#240666=CIRCLE ( 'NONE', #15849, 0.09999999999999520384 ) ;
#240692=ADVANCED_FACE ( 'NONE', ( #149504 ), #189890, .T. ) ;
#240694=ORIENTED_EDGE ( 'NONE', *, *, #175041, .T. ) ;
#240714=CARTESIAN_POINT ( 'NONE',  ( 20.94999999999999929, 69.55000000001207638, -126.5060803140843291 ) ) ;
#240716=FACE_OUTER_BOUND ( 'NONE', #55334, .T. ) ;
#240750=AXIS2_PLACEMENT_3D ( 'NONE', #105819, #224504, #165843 ) ;
#240752=AXIS2_PLACEMENT_3D ( 'NONE', #245590, #183054, #46084 ) ;
#240795=CIRCLE ( 'NONE', #2881, 12.77499999999999503 ) ;
#240801=DIRECTION ( 'NONE',  ( -1.000000000000000000, 0.000000000000000000, -0.000000000000000000 ) ) ;
#240809=DIRECTION ( 'NONE',  ( 1.000000000000000000, 0.000000000000000000, 0.000000000000000000 ) ) ;
#240810=ORIENTED_EDGE ( 'NONE', *, *, #23083, .T. ) ;
#240824=CARTESIAN_POINT ( 'NONE',  ( 23.24999999999999645, 76.00000000001213607, -136.5231074845242745 ) ) ;
#240832=ADVANCED_FACE ( 'NONE', ( #253698 ), #176761, .F. ) ;
#240880=CARTESIAN_POINT ( 'NONE',  ( -21.05000000000000071, 76.00000000001213607, -136.5231074845242745 ) ) ;
#240900=DIRECTION ( 'NONE',  ( 0.7071359030027593029, 0.7070776581709197206, 0.000000000000000000 ) ) ;
#240904=CYLINDRICAL_SURFACE ( 'NONE', #135721, 0.1000000000000028644 ) ;
#240912=DIRECTION ( 'NONE',  ( -1.000000000000000000, -0.000000000000000000, -0.000000000000000000 ) ) ;
#240923=AXIS2_PLACEMENT_3D ( 'NONE', #164550, #47130, #48431 ) ;
#240965=ORIENTED_EDGE ( 'NONE', *, *, #11236, .F. ) ;
#240989=CIRCLE ( 'NONE', #103765, 0.6000000000000033085 ) ;
#241001=CARTESIAN_POINT ( 'NONE',  ( -22.50000000000088463, 75.95463834342453424, -148.1736163187296995 ) ) ;
#241032=AXIS2_PLACEMENT_3D ( 'NONE', #50952, #69277, #151386 ) ;
#241037=CARTESIAN_POINT ( 'NONE',  ( 23.24999999999999289, 64.25000000001220712, -148.2731074845243882 ) ) ;
#241038=DIRECTION ( 'NONE',  ( 0.000000000000000000, 0.000000000000000000, 1.000000000000000000 ) ) ;
#241045=ORIENTED_EDGE ( 'NONE', *, *, #108656, .T. ) ;
#241068=AXIS2_PLACEMENT_3D ( 'NONE', #235267, #133603, #137444 ) ;
#241076=AXIS2_PLACEMENT_3D ( 'NONE', #35207, #254193, #233393 ) ;
#241118=DIRECTION ( 'NONE',  ( -2.915501640297152804E-16, -1.000000000000000000, -6.997203936713167125E-15 ) ) ;
#241137=CYLINDRICAL_SURFACE ( 'NONE', #138142, 0.09999999999998898659 ) ;
#241138=AXIS2_PLACEMENT_3D ( 'NONE', #175259, #253455, #213049 ) ;
#241163=CARTESIAN_POINT ( 'NONE',  ( -21.05000000000000071, 74.75000000001207923, -128.5231074845243029 ) ) ;
#241179=DIRECTION ( 'NONE',  ( 0.000000000000000000, -6.938893903907222067E-15, 1.000000000000000000 ) ) ;
#241188=EDGE_CURVE ( 'NONE', #47601, #56965, #103457, .T. ) ;
#241207=CARTESIAN_POINT ( 'NONE',  ( -23.25000000000000000, 87.75000000001190870, -103.0231074845242176 ) ) ;
#241228=CIRCLE ( 'NONE', #24764, 0.2000000000000057288 ) ;
#241232=FACE_OUTER_BOUND ( 'NONE', #16961, .T. ) ;
#241237=AXIS2_PLACEMENT_3D ( 'NONE', #247192, #129816, #29480 ) ;
#241244=ADVANCED_FACE ( 'NONE', ( #155637 ), #236557, .F. ) ;
#241260=CARTESIAN_POINT ( 'NONE',  ( 23.15000000000000213, 84.59626168225506149, -127.0729799673739677 ) ) ;
#241286=CARTESIAN_POINT ( 'NONE',  ( 18.39999999999999858, 85.50000000001185185, -96.10844914155455854 ) ) ;
#241293=EDGE_CURVE ( 'NONE', #185168, #82597, #225492, .T. ) ;
#241297=AXIS2_PLACEMENT_3D ( 'NONE', #109863, #49899, #31662 ) ;
#241328=CARTESIAN_POINT ( 'NONE',  ( -20.15000000000000568, 66.70857864377468616, -115.3731074845243683 ) ) ;
#241341=VERTEX_POINT ( 'NONE', #224225 ) ;
#241350=VERTEX_POINT ( 'NONE', #221648 ) ;
#241357=( BOUNDED_CURVE ( )  B_SPLINE_CURVE ( 3, ( #217811, #234834, #176166, #135716 ),
 .UNSPECIFIED., .F., .F. ) 
 B_SPLINE_CURVE_WITH_KNOTS ( ( 4, 4 ),
 ( 3.141592653589793116, 4.712388980384689674 ),
 .UNSPECIFIED. ) 
 CURVE ( )  GEOMETRIC_REPRESENTATION_ITEM ( )  RATIONAL_B_SPLINE_CURVE ( ( 1.000000000000000000, 0.8047378541243649375, 0.8047378541243649375, 1.000000000000000000 ) ) 
 REPRESENTATION_ITEM ( '' )  );
#241360=VERTEX_POINT ( 'NONE', #182563 ) ;
#241411=DIRECTION ( 'NONE',  ( 0.000000000000000000, 0.000000000000000000, 1.000000000000000000 ) ) ;
#241413=CARTESIAN_POINT ( 'NONE',  ( -23.25000000000000000, 64.35000000001214460, -136.5231074845243597 ) ) ;
#241414=CARTESIAN_POINT ( 'NONE',  ( -23.15000000000000213, 71.85000000001198828, -115.3731074845243256 ) ) ;
#241429=EDGE_CURVE ( 'NONE', #215387, #217189, #7817, .T. ) ;
#241439=CIRCLE ( 'NONE', #249807, 7.791421356237310469 ) ;
#241443=DIRECTION ( 'NONE',  ( -1.000000000000000000, 0.000000000000000000, 0.000000000000000000 ) ) ;
#241448=ORIENTED_EDGE ( 'NONE', *, *, #245502, .F. ) ;
#241452=ORIENTED_EDGE ( 'NONE', *, *, #111010, .F. ) ;
#241483=CARTESIAN_POINT ( 'NONE',  ( 20.97224591636398472, 65.37484658384840941, -124.2731815798607897 ) ) ;
#241485=DIRECTION ( 'NONE',  ( 1.000000000000000000, -7.304098846218134667E-16, -5.100424963727255829E-30 ) ) ;
#241518=ORIENTED_EDGE ( 'NONE', *, *, #191870, .F. ) ;
#241592=CIRCLE ( 'NONE', #187438, 11.90000000000000746 ) ;
#241601=CARTESIAN_POINT ( 'NONE',  ( 21.11833042828134310, 69.55435530615692130, -136.5302079935837867 ) ) ;
#241626=EDGE_CURVE ( 'NONE', #22494, #154603, #86882, .T. ) ;
#241648=ADVANCED_FACE ( 'NONE', ( #9873 ), #166235, .T. ) ;
#241656=CYLINDRICAL_SURFACE ( 'NONE', #111121, 0.09999999999998898659 ) ;
#241672=EDGE_CURVE ( 'NONE', #186227, #210448, #53779, .T. ) ;
#241676=ORIENTED_EDGE ( 'NONE', *, *, #61860, .F. ) ;
#241743=CIRCLE ( 'NONE', #16911, 0.09999999999999938105 ) ;
#241755=AXIS2_PLACEMENT_3D ( 'NONE', #205559, #123476, #103884 ) ;
#241765=CARTESIAN_POINT ( 'NONE',  ( -20.94999999999999929, 76.00000000001193712, -107.1231074845243114 ) ) ;
#241779=DIRECTION ( 'NONE',  ( 1.000000000000000000, 0.000000000000000000, 0.000000000000000000 ) ) ;
#241820=DIRECTION ( 'NONE',  ( -1.000000000000000000, 3.265361837132813093E-16, 2.280189983783949500E-30 ) ) ;
#241856=EDGE_CURVE ( 'NONE', #23447, #156427, #170542, .T. ) ;
#241859=DIRECTION ( 'NONE',  ( 0.7071067811865475727, 0.7071067811865475727, 4.937700262164531476E-15 ) ) ;
#241899=DIRECTION ( 'NONE',  ( -1.000000000000000000, 3.265361837132813093E-16, 2.280189983783949500E-30 ) ) ;
#241903=DIRECTION ( 'NONE',  ( 1.000000000000000000, -0.000000000000000000, 0.000000000000000000 ) ) ;
#241913=EDGE_CURVE ( 'NONE', #4010, #94457, #189525, .T. ) ;
#241915=CARTESIAN_POINT ( 'NONE',  ( -18.59999999999999787, 69.06610602788553877, -99.23746165015076315 ) ) ;
#241916=ORIENTED_EDGE ( 'NONE', *, *, #141713, .F. ) ;
#241953=DIRECTION ( 'NONE',  ( 0.000000000000000000, -1.000000000000000000, -7.272083257015735086E-15 ) ) ;
#242003=DIRECTION ( 'NONE',  ( 0.000000000000000000, 0.000000000000000000, -1.000000000000000000 ) ) ;
#242022=AXIS2_PLACEMENT_3D ( 'NONE', #86741, #47613, #124614 ) ;
#242055=DIRECTION ( 'NONE',  ( -0.000000000000000000, -6.982962677686266711E-15, 1.000000000000000000 ) ) ;
#242065=VERTEX_POINT ( 'NONE', #58953 ) ;
#242073=DIRECTION ( 'NONE',  ( -1.000000000000000000, -0.000000000000000000, -0.000000000000000000 ) ) ;
#242075=AXIS2_PLACEMENT_3D ( 'NONE', #113179, #234397, #14097 ) ;
#242104=VERTEX_POINT ( 'NONE', #105783 ) ;
#242105=DIRECTION ( 'NONE',  ( 0.000000000000000000, -1.000000000000000000, 0.000000000000000000 ) ) ;
#242120=DIRECTION ( 'NONE',  ( 1.000000000000000000, 0.000000000000000000, 0.000000000000000000 ) ) ;
#242190=EDGE_CURVE ( 'NONE', #16840, #17539, #83644, .T. ) ;
#242203=ORIENTED_EDGE ( 'NONE', *, *, #253753, .F. ) ;
#242213=FACE_OUTER_BOUND ( 'NONE', #251177, .T. ) ;
#242244=ADVANCED_FACE ( 'NONE', ( #50950 ), #3318, .T. ) ;
#242333=AXIS2_PLACEMENT_3D ( 'NONE', #143994, #613, #102273 ) ;
#242396=CARTESIAN_POINT ( 'NONE',  ( 22.39999999999999503, 68.20922040163875977, -136.5231074845243313 ) ) ;
#242410=LINE ( 'NONE', #221546, #146670 ) ;
#242429=DIRECTION ( 'NONE',  ( 0.000000000000000000, 0.000000000000000000, -1.000000000000000000 ) ) ;
#242452=AXIS2_PLACEMENT_3D ( 'NONE', #75530, #41544, #204097 ) ;
#242459=VECTOR ( 'NONE', #53160, 1000.000000000000000 ) ;
#242464=EDGE_CURVE ( 'NONE', #64483, #45900, #125074, .T. ) ;
#242467=CARTESIAN_POINT ( 'NONE',  ( 20.97217846901852312, 67.12455827530239105, -128.0218798005871577 ) ) ;
#242473=ORIENTED_EDGE ( 'NONE', *, *, #27708, .T. ) ;
#242491=CARTESIAN_POINT ( 'NONE',  ( 21.12757541349815682, 69.52661942876069645, -136.5282687003340811 ) ) ;
#242559=LINE ( 'NONE', #221696, #129039 ) ;
#242573=CARTESIAN_POINT ( 'NONE',  ( 21.05000000000000071, 87.65000000001192859, -106.0231074845242176 ) ) ;
#242614=ORIENTED_EDGE ( 'NONE', *, *, #93950, .T. ) ;
#242615=EDGE_CURVE ( 'NONE', #73178, #136488, #158409, .T. ) ;
#242618=ORIENTED_EDGE ( 'NONE', *, *, #205128, .T. ) ;
#242673=DIRECTION ( 'NONE',  ( 1.000000000000000000, 0.000000000000000000, 0.000000000000000000 ) ) ;
#242679=DIRECTION ( 'NONE',  ( -1.000000000000000000, -0.000000000000000000, -0.000000000000000000 ) ) ;
#242680=CARTESIAN_POINT ( 'NONE',  ( -21.29999999999995808, 76.00000000001213607, -136.5231074845242745 ) ) ;
#242681=DIRECTION ( 'NONE',  ( -0.7071067811865214825, -0.7071067811865735520, 0.000000000000000000 ) ) ;
#242685=AXIS2_PLACEMENT_3D ( 'NONE', #99152, #79591, #58736 ) ;
#242689=EDGE_CURVE ( 'NONE', #194615, #247013, #120805, .T. ) ;
#242699=CARTESIAN_POINT ( 'NONE',  ( -18.56579813702275672, 65.66974365629666011, -97.43601455626047425 ) ) ;
#242722=ORIENTED_EDGE ( 'NONE', *, *, #89125, .T. ) ;
#242728=CARTESIAN_POINT ( 'NONE',  ( 18.59999999999999432, 74.26374286841466699, -124.9544551555068068 ) ) ;
#242732=CARTESIAN_POINT ( 'NONE',  ( -22.59999985501179154, 64.25013020700916400, -136.5887061543240009 ) ) ;
#242734=AXIS2_PLACEMENT_3D ( 'NONE', #52566, #10897, #228671 ) ;
#242737=CARTESIAN_POINT ( 'NONE',  ( -21.00250684356850073, 64.25000000001209344, -129.5083017157663789 ) ) ;
#242738=CARTESIAN_POINT ( 'NONE',  ( -18.59999999999999787, 77.83534155023646406, -124.9679561919613064 ) ) ;
#242740=LINE ( 'NONE', #199801, #15970 ) ;
#242744=CARTESIAN_POINT ( 'NONE',  ( -18.50000000000000000, 72.08710075277861051, -125.0412845115133678 ) ) ;
#242820=CARTESIAN_POINT ( 'NONE',  ( -21.05000000000000071, 74.83729825007408465, -128.5231074845243029 ) ) ;
#242839=CIRCLE ( 'NONE', #130408, 0.1000000000000052097 ) ;
#242854=ORIENTED_EDGE ( 'NONE', *, *, #125698, .T. ) ;
#242856=VECTOR ( 'NONE', #132509, 999.9999999999998863 ) ;
#242881=ORIENTED_EDGE ( 'NONE', *, *, #48330, .T. ) ;
#242882=CARTESIAN_POINT ( 'NONE',  ( 21.07954763557393818, 69.67070900997488536, -136.5889834031427768 ) ) ;
#242897=CARTESIAN_POINT ( 'NONE',  ( 18.52928932188133970, 65.72071067813061518, -111.8731074845243683 ) ) ;
#242919=CIRCLE ( 'NONE', #134580, 0.1000000000000028644 ) ;
#242930=CARTESIAN_POINT ( 'NONE',  ( -20.15000000000000568, 66.70857864377474300, -124.2731074845243597 ) ) ;
#242940=ORIENTED_EDGE ( 'NONE', *, *, #159230, .T. ) ;
#242949=VERTEX_POINT ( 'NONE', #42652 ) ;
#242975=CARTESIAN_POINT ( 'NONE',  ( 20.94999999999999574, 74.75000000001207923, -128.6231074845242972 ) ) ;
#242976=CARTESIAN_POINT ( 'NONE',  ( -18.59999999999999787, 77.85102823015292017, -124.8691942151017855 ) ) ;
#242997=CARTESIAN_POINT ( 'NONE',  ( -23.15000000000000213, 85.60000000001208775, -126.6291383618717816 ) ) ;
#242999=DIRECTION ( 'NONE',  ( -1.000000000000000000, 0.000000000000000000, 0.000000000000000000 ) ) ;
#243005=CARTESIAN_POINT ( 'NONE',  ( 23.24999999999999645, 70.40000000001222702, -148.2731074845243313 ) ) ;
#243021=CIRCLE ( 'NONE', #251404, 0.09999999999999976963 ) ;
#243030=EDGE_CURVE ( 'NONE', #147164, #7536, #120990, .T. ) ;
#243032=ADVANCED_FACE ( 'NONE', ( #106445 ), #162614, .F. ) ;
#243046=CIRCLE ( 'NONE', #47216, 0.1000000000000026007 ) ;
#243083=DIRECTION ( 'NONE',  ( 0.000000000000000000, 0.000000000000000000, 1.000000000000000000 ) ) ;
#243094=CARTESIAN_POINT ( 'NONE',  ( 21.05563370358598263, 65.27576964416554972, -124.3400166685613044 ) ) ;
#243096=CARTESIAN_POINT ( 'NONE',  ( 21.05000000000000071, 71.00000000001199396, -114.9283735034374274 ) ) ;
#243105=CARTESIAN_POINT ( 'NONE',  ( -23.25000000000000000, 64.35000000001198828, -115.2731074845243739 ) ) ;
#243112=DIRECTION ( 'NONE',  ( 0.000000000000000000, -1.000000000000000000, -6.982962677686265922E-15 ) ) ;
#243122=EDGE_CURVE ( 'NONE', #217224, #152168, #154340, .T. ) ;
#243139=CARTESIAN_POINT ( 'NONE',  ( -18.41353343127310538, 85.50000000001207923, -129.4910380878245064 ) ) ;
#243150=DIRECTION ( 'NONE',  ( 1.000000000000000000, 0.000000000000000000, 0.000000000000000000 ) ) ;
#243152=DIRECTION ( 'NONE',  ( 0.000000000000000000, 0.000000000000000000, 1.000000000000000000 ) ) ;
#243159=CARTESIAN_POINT ( 'NONE',  ( -20.85000000000000142, 87.75000000001190870, -103.0231074845242176 ) ) ;
#243187=LINE ( 'NONE', #24169, #169775 ) ;
#243227=ORIENTED_EDGE ( 'NONE', *, *, #201265, .F. ) ;
#243230=CARTESIAN_POINT ( 'NONE',  ( -23.15000000000000213, 64.25000000001205080, -124.3731074845243825 ) ) ;
#243258=CARTESIAN_POINT ( 'NONE',  ( 20.94999675878240808, 65.70692517833232671, -97.56446533783034170 ) ) ;
#243260=VERTEX_POINT ( 'NONE', #153356 ) ;
#243265=ORIENTED_EDGE ( 'NONE', *, *, #106361, .F. ) ;
#243266=ADVANCED_FACE ( 'NONE', ( #237968 ), #193725, .F. ) ;
#243334=AXIS2_PLACEMENT_3D ( 'NONE', #234523, #175860, #97551 ) ;
#243339=DIRECTION ( 'NONE',  ( 1.000000000000000000, 0.000000000000000000, 0.000000000000000000 ) ) ;
#243381=CIRCLE ( 'NONE', #235025, 0.09999999999999938105 ) ;
#243383=EDGE_CURVE ( 'NONE', #145844, #85966, #103580, .T. ) ;
#243403=DIRECTION ( 'NONE',  ( -1.000000000000000000, 0.000000000000000000, 0.000000000000000000 ) ) ;
#243404=FACE_OUTER_BOUND ( 'NONE', #212643, .T. ) ;
#243413=EDGE_CURVE ( 'NONE', #20391, #95961, #71279, .T. ) ;
#243432=ORIENTED_EDGE ( 'NONE', *, *, #85939, .F. ) ;
#243447=EDGE_LOOP ( 'NONE', ( #46896, #17662, #124085, #211145 ) ) ;
#243453=DIRECTION ( 'NONE',  ( 0.000000000000000000, -7.124650136758317602E-15, 1.000000000000000000 ) ) ;
#243500=CIRCLE ( 'NONE', #239410, 0.09999999999999799327 ) ;
#243534=VERTEX_POINT ( 'NONE', #118716 ) ;
#243545=CIRCLE ( 'NONE', #239467, 0.1000000000000043771 ) ;
#243550=AXIS2_PLACEMENT_3D ( 'NONE', #30543, #8400, #125752 ) ;
#243551=EDGE_CURVE ( 'NONE', #217224, #189431, #179611, .T. ) ;
#243592=ORIENTED_EDGE ( 'NONE', *, *, #2341, .F. ) ;
#243623=DIRECTION ( 'NONE',  ( -1.000000000000000000, 0.000000000000000000, -0.000000000000000000 ) ) ;
#243660=CARTESIAN_POINT ( 'NONE',  ( 20.94999999999999929, 85.50000000001197975, -112.9170766071766820 ) ) ;
#243662=LINE ( 'NONE', #61173, #195846 ) ;
#243671=( BOUNDED_SURFACE ( )  B_SPLINE_SURFACE ( 3, 2, ( 
 ( #111706, #215917, #133831 ),
 ( #252484, #76416, #115548 ),
 ( #173012, #17718, #251198 ),
 ( #112996, #171715, #37321 ),
 ( #92140, #72601, #195121 ),
 ( #73897, #213358, #116841 ) ),
 .UNSPECIFIED., .F., .F., .T. ) 
 B_SPLINE_SURFACE_WITH_KNOTS ( ( 4, 2, 4 ),
 ( 3, 3 ),
 ( 1.570796326794897668, 2.356194490192346169, 3.141592653589794448 ),
 ( 0.000000000000000000, 1.000000000000000000 ),
 .UNSPECIFIED. ) 
 GEOMETRIC_REPRESENTATION_ITEM ( )  RATIONAL_B_SPLINE_SURFACE ( (
 ( 1.000000000000000000, 0.7071067811865597852, 1.000000000000000000),
 ( 1.000000000000000000, 0.6611148371798263312, 1.000000000000000000),
 ( 1.000000000000000000, 0.6092287576670563087, 1.000000000000000000),
 ( 1.000000000000000000, 0.5278258667083555178, 1.000000000000000000),
 ( 1.000000000000000000, 0.4993418825314846488, 1.000000000000000000),
 ( 1.000000000000000000, 0.5000000000000154321, 1.000000000000000000) ) ) 
 REPRESENTATION_ITEM ( '' )  SURFACE ( )  );
#243673=CARTESIAN_POINT ( 'NONE',  ( -22.39999999999999503, 68.20922040163873135, -136.5231074845243597 ) ) ;
#243723=DIRECTION ( 'NONE',  ( -0.000000000000000000, -0.8660254037844468122, -0.4999999999999860112 ) ) ;
#243730=DIRECTION ( 'NONE',  ( -0.000000000000000000, 6.982962677686266711E-15, -1.000000000000000000 ) ) ;
#243750=ORIENTED_EDGE ( 'NONE', *, *, #104662, .T. ) ;
#243764=CARTESIAN_POINT ( 'NONE',  ( 20.52683494730046476, 67.01946918171073264, -128.0178547619901508 ) ) ;
#243768=CARTESIAN_POINT ( 'NONE',  ( 18.59999999999999432, 77.63717271298244782, -124.9409541190522788 ) ) ;
#243792=CARTESIAN_POINT ( 'NONE',  ( 18.59999999999999076, 77.83585931145546510, -91.41866831572575336 ) ) ;
#243803=ORIENTED_EDGE ( 'NONE', *, *, #76738, .F. ) ;
#243808=CARTESIAN_POINT ( 'NONE',  ( 18.59999999999999432, 77.16270174995010223, -128.4231074845242802 ) ) ;
#243811=CARTESIAN_POINT ( 'NONE',  ( -21.05000000000000071, 88.41227409416160299, -105.9231074845242091 ) ) ;
#243836=PLANE ( 'NONE',  #214694 ) ;
#243851=FACE_OUTER_BOUND ( 'NONE', #251911, .T. ) ;
#243860=ORIENTED_EDGE ( 'NONE', *, *, #153874, .T. ) ;
#243894=DIRECTION ( 'NONE',  ( 0.000000000000000000, -5.551115123125777653E-14, 1.000000000000000000 ) ) ;
#243908=APPLICATION_CONTEXT ( 'automotive_design' ) ;
#243921=AXIS2_PLACEMENT_3D ( 'NONE', #72946, #110746, #232004 ) ;
#243970=ADVANCED_FACE ( 'NONE', ( #239621 ), #38319, .T. ) ;
#243992=ORIENTED_EDGE ( 'NONE', *, *, #117599, .F. ) ;
#243995=CARTESIAN_POINT ( 'NONE',  ( 21.05000000000000071, 67.07338541492498507, -128.0514244653012383 ) ) ;
#244005=CARTESIAN_POINT ( 'NONE',  ( 21.13461538461538680, 65.38541703798651383, -124.1731074845243654 ) ) ;
#244017=CARTESIAN_POINT ( 'NONE',  ( 23.14999999999998437, 64.25000000001215028, -136.5231074845243597 ) ) ;
#244018=LINE ( 'NONE', #225724, #88839 ) ;
#244024=CARTESIAN_POINT ( 'NONE',  ( -20.94684162521793525, 64.25000000001209344, -129.6814634907268271 ) ) ;
#244042=EDGE_LOOP ( 'NONE', ( #49986, #56140, #49934, #254609, #83600, #212742, #243750, #183621, #158389, #162916, #31907 ) ) ;
#244049=ORIENTED_EDGE ( 'NONE', *, *, #201092, .T. ) ;
#244051=FACE_OUTER_BOUND ( 'NONE', #28928, .T. ) ;
#244075=EDGE_LOOP ( 'NONE', ( #70832, #178123, #164168, #197898 ) ) ;
#244076=CARTESIAN_POINT ( 'NONE',  ( 20.94999999999999929, 85.50000000001207923, -126.6291383618717816 ) ) ;
#244096=AXIS2_PLACEMENT_3D ( 'NONE', #204375, #221360, #24492 ) ;
#244136=ORIENTED_EDGE ( 'NONE', *, *, #176981, .F. ) ;
#244141=ORIENTED_EDGE ( 'NONE', *, *, #67489, .F. ) ;
#244152=ORIENTED_EDGE ( 'NONE', *, *, #173557, .T. ) ;
#244162=DIRECTION ( 'NONE',  ( 1.000000000000000000, 0.000000000000000000, 0.000000000000000000 ) ) ;
#244170=DIRECTION ( 'NONE',  ( -0.000000000000000000, 1.000000000000000000, 6.982962677686266711E-15 ) ) ;
#244183=ORIENTED_EDGE ( 'NONE', *, *, #252346, .T. ) ;
#244186=FACE_OUTER_BOUND ( 'NONE', #145349, .T. ) ;
#244196=CARTESIAN_POINT ( 'NONE',  ( 21.14999999999999858, 76.00000000001219291, -143.0637644362255401 ) ) ;
#244237=CIRCLE ( 'NONE', #223388, 0.09999999999999939493 ) ;
#244255=CARTESIAN_POINT ( 'NONE',  ( 18.54116936837188589, 85.46356419838456020, -129.4745649936359939 ) ) ;
#244257=EDGE_CURVE ( 'NONE', #14889, #31859, #233937, .T. ) ;
#244273=CIRCLE ( 'NONE', #90146, 0.1000000000000028644 ) ;
#244278=CIRCLE ( 'NONE', #227534, 0.1000000000000028644 ) ;
#244363=DIRECTION ( 'NONE',  ( 1.000000000000000000, -7.304098846218134667E-16, -4.639676173203993355E-30 ) ) ;
#244470=CARTESIAN_POINT ( 'NONE',  ( 18.59999999999999076, 76.00000000001190870, -103.0231074845243029 ) ) ;
#244471=DIRECTION ( 'NONE',  ( -0.000000000000000000, 6.982962677686266711E-15, -1.000000000000000000 ) ) ;
#244479=ORIENTED_EDGE ( 'NONE', *, *, #130505, .T. ) ;
#244486=CARTESIAN_POINT ( 'NONE',  ( -23.15000000000000213, 74.08971962618026907, -123.8917396293253717 ) ) ;
#244513=ORIENTED_EDGE ( 'NONE', *, *, #245838, .F. ) ;
#244529=EDGE_CURVE ( 'NONE', #140683, #34419, #26032, .T. ) ;
#244541=ORIENTED_EDGE ( 'NONE', *, *, #206427, .T. ) ;
#244555=CYLINDRICAL_SURFACE ( 'NONE', #218662, 0.1000000000000028644 ) ;
#244567=ADVANCED_FACE ( 'NONE', ( #181905 ), #26703, .F. ) ;
#244585=AXIS2_PLACEMENT_3D ( 'NONE', #234406, #132776, #115757 ) ;
#244619=LINE ( 'NONE', #183381, #198604 ) ;
#244662=CIRCLE ( 'NONE', #65602, 0.1000000000000028644 ) ;
#244668=VERTEX_POINT ( 'NONE', #187061 ) ;
#244691=CARTESIAN_POINT ( 'NONE',  ( -21.29999999999995808, 76.00000000001210765, -132.4731074845242915 ) ) ;
#244694=CARTESIAN_POINT ( 'NONE',  ( -23.25000000000000000, 77.85161776048073534, -91.41991776492061206 ) ) ;
#244703=AXIS2_PLACEMENT_3D ( 'NONE', #233436, #255490, #133044 ) ;
#244731=FACE_OUTER_BOUND ( 'NONE', #73341, .T. ) ;
#244741=CARTESIAN_POINT ( 'NONE',  ( -21.59142135623730852, 68.15000000001205649, -124.1731074845243512 ) ) ;
#244748=AXIS2_PLACEMENT_3D ( 'NONE', #239172, #197465, #215738 ) ;
#244778=DIRECTION ( 'NONE',  ( -0.000000000000000000, -0.9876197685951290106, 0.1568667991644625281 ) ) ;
#244781=CARTESIAN_POINT ( 'NONE',  ( 18.59999999999999787, 77.83585931145546510, -91.51866831572576189 ) ) ;
#244799=DIRECTION ( 'NONE',  ( 1.000000000000000000, -2.952720810173289112E-16, -2.061873921506763405E-30 ) ) ;
#244814=ADVANCED_FACE ( 'NONE', ( #36980 ), #168380, .F. ) ;
#244832=CARTESIAN_POINT ( 'NONE',  ( -22.50875500270928953, 76.10085791378683950, -148.2726746119222128 ) ) ;
#244841=CARTESIAN_POINT ( 'NONE',  ( -21.05000000000000071, 69.55922910635067069, -136.5055102975167927 ) ) ;
#244849=ORIENTED_EDGE ( 'NONE', *, *, #161018, .F. ) ;
#244850=EDGE_LOOP ( 'NONE', ( #8589, #141778, #82253, #38604 ) ) ;
#244892=ORIENTED_EDGE ( 'NONE', *, *, #178945, .F. ) ;
#244903=ORIENTED_EDGE ( 'NONE', *, *, #206162, .F. ) ;
#244926=AXIS2_PLACEMENT_3D ( 'NONE', #238173, #77815, #236901 ) ;
#244948=CIRCLE ( 'NONE', #170162, 0.09999999999999939493 ) ;
#244951=CARTESIAN_POINT ( 'NONE',  ( -21.53699400380209283, 69.21228820681638183, -136.5231074845243597 ) ) ;
#244982=ORIENTED_EDGE ( 'NONE', *, *, #246090, .T. ) ;
#245008=EDGE_LOOP ( 'NONE', ( #36322, #153385, #130225, #98301 ) ) ;
#245035=DIRECTION ( 'NONE',  ( 1.000000000000000000, 0.000000000000000000, 0.000000000000000000 ) ) ;
#245039=DIRECTION ( 'NONE',  ( 0.000000000000000000, 0.1568667991644355497, -0.9876197685951332295 ) ) ;
#245053=DIRECTION ( 'NONE',  ( -0.000000000000000000, 6.982962677686266711E-15, -1.000000000000000000 ) ) ;
#245064=CARTESIAN_POINT ( 'NONE',  ( 21.09316766718127667, 69.62984668753773576, -136.5623708868390338 ) ) ;
#245066=ORIENTED_EDGE ( 'NONE', *, *, #58095, .T. ) ;
#245072=DIRECTION ( 'NONE',  ( 1.000000000000000000, 0.000000000000000000, 0.000000000000000000 ) ) ;
#245091=DIRECTION ( 'NONE',  ( -1.000000000000000000, 0.000000000000000000, -0.000000000000000000 ) ) ;
#245120=DIRECTION ( 'NONE',  ( -1.000000000000000000, -0.000000000000000000, 0.000000000000000000 ) ) ;
#245156=DIRECTION ( 'NONE',  ( 0.000000000000000000, -6.352154140967427193E-15, 1.000000000000000000 ) ) ;
#245209=ADVANCED_FACE ( 'NONE', ( #13245 ), #39362, .T. ) ;
#245239=CARTESIAN_POINT ( 'NONE',  ( -21.09316766718153247, 75.96073659769751885, -142.8932607969990158 ) ) ;
#245250=DIRECTION ( 'NONE',  ( 0.000000000000000000, -0.9908441862701610203, 0.1350103645451807555 ) ) ;
#245270=CARTESIAN_POINT ( 'NONE',  ( 21.05000000000000071, 71.14953271029236248, -115.0573748935260028 ) ) ;
#245292=VERTEX_POINT ( 'NONE', #170634 ) ;
#245323=CARTESIAN_POINT ( 'NONE',  ( -22.57320508075686405, 64.25000000001213607, -136.5231074845243313 ) ) ;
#245407=LINE ( 'NONE', #242820, #152179 ) ;
#245414=CARTESIAN_POINT ( 'NONE',  ( -18.50000000000000000, 66.75000000001199396, -115.1731074845243654 ) ) ;
#245452=EDGE_LOOP ( 'NONE', ( #193964, #248258, #234482, #210997 ) ) ;
#245468=VERTEX_POINT ( 'NONE', #34251 ) ;
#245502=EDGE_CURVE ( 'NONE', #225759, #104197, #217980, .T. ) ;
#245507=AXIS2_PLACEMENT_3D ( 'NONE', #133114, #130532, #171003 ) ;
#245533=DIRECTION ( 'NONE',  ( 1.000000000000000000, -0.000000000000000000, 0.000000000000000000 ) ) ;
#245577=CARTESIAN_POINT ( 'NONE',  ( 18.59999999999999432, 77.16270174995010223, -128.4231074845242802 ) ) ;
#245590=CARTESIAN_POINT ( 'NONE',  ( 20.85000000000000142, 76.00000000001190870, -103.0231074845243029 ) ) ;
#245602=ORIENTED_EDGE ( 'NONE', *, *, #225083, .F. ) ;
#245625=CARTESIAN_POINT ( 'NONE',  ( -20.89878130938411616, 65.67252876774529113, -97.44570419949944551 ) ) ;
#245645=AXIS2_PLACEMENT_3D ( 'NONE', #165570, #245091, #69043 ) ;
#245670=CARTESIAN_POINT ( 'NONE',  ( 21.08750232978087524, 65.27513661400190870, -124.2942493115248084 ) ) ;
#245687=AXIS2_PLACEMENT_3D ( 'NONE', #157851, #58678, #198209 ) ;
#245722=DIRECTION ( 'NONE',  ( 1.000000000000000000, 0.000000000000000000, 0.000000000000000000 ) ) ;
#245732=EDGE_CURVE ( 'NONE', #13011, #40840, #159746, .T. ) ;
#245769=EDGE_CURVE ( 'NONE', #190104, #245292, #51961, .T. ) ;
#245789=CARTESIAN_POINT ( 'NONE',  ( 21.05000000000000071, 76.00000000001190870, -103.0231074845243029 ) ) ;
#245809=EDGE_CURVE ( 'NONE', #20391, #140683, #211968, .T. ) ;
#245824=DIRECTION ( 'NONE',  ( 0.000000000000000000, 1.000000000000000000, 6.982962677686266711E-15 ) ) ;
#245829=CARTESIAN_POINT ( 'NONE',  ( -20.64999999999999858, 76.00000000001213607, -136.5231074845242745 ) ) ;
#245836=AXIS2_PLACEMENT_3D ( 'NONE', #232596, #138563, #94326 ) ;
#245838=EDGE_CURVE ( 'NONE', #128716, #119361, #86150, .T. ) ;
#245852=ADVANCED_FACE ( 'NONE', ( #183999 ), #126596, .F. ) ;
#245891=ORIENTED_EDGE ( 'NONE', *, *, #187947, .F. ) ;
#245897=LINE ( 'NONE', #149383, #48339 ) ;
#245928=CARTESIAN_POINT ( 'NONE',  ( 19.99999999999998934, 64.25000000001199396, -115.1731074845243796 ) ) ;
#245981=DIRECTION ( 'NONE',  ( -1.000000000000000000, 7.304098846218134667E-16, 5.100424963727256530E-30 ) ) ;
#246042=CARTESIAN_POINT ( 'NONE',  ( -20.00857864376270001, 66.85000000001200249, -115.3731074845243683 ) ) ;
#246060=EDGE_LOOP ( 'NONE', ( #75313, #179482, #213373, #93615 ) ) ;
#246082=ORIENTED_EDGE ( 'NONE', *, *, #50270, .F. ) ;
#246090=EDGE_CURVE ( 'NONE', #161343, #3082, #145481, .T. ) ;
#246107=DIRECTION ( 'NONE',  ( 0.000000000000000000, -7.026728003956683390E-15, 1.000000000000000000 ) ) ;
#246111=CARTESIAN_POINT ( 'NONE',  ( -20.85000000000000142, 77.16412189325305349, -95.10825939895268277 ) ) ;
#246140=ORIENTED_EDGE ( 'NONE', *, *, #242464, .T. ) ;
#246144=CARTESIAN_POINT ( 'NONE',  ( -21.05000000000000426, 69.65527659592147813, -136.5378253410474940 ) ) ;
#246151=CARTESIAN_POINT ( 'NONE',  ( -23.15000000000000213, 74.00000000001205080, -123.2984855617622060 ) ) ;
#246153=VERTEX_POINT ( 'NONE', #3773 ) ;
#246183=ORIENTED_EDGE ( 'NONE', *, *, #41763, .F. ) ;
#246199=FACE_OUTER_BOUND ( 'NONE', #194868, .T. ) ;
#246209=ORIENTED_EDGE ( 'NONE', *, *, #3317, .F. ) ;
#246224=ORIENTED_EDGE ( 'NONE', *, *, #187945, .T. ) ;
#246243=ADVANCED_FACE ( 'NONE', ( #227956 ), #27221, .T. ) ;
#246246=CARTESIAN_POINT ( 'NONE',  ( -21.93340585972176981, 68.67585297715999104, -136.5231074845243597 ) ) ;
#246265=ORIENTED_EDGE ( 'NONE', *, *, #74097, .F. ) ;
#246287=CYLINDRICAL_SURFACE ( 'NONE', #79887, 7.900000000000003908 ) ;
#246307=CYLINDRICAL_SURFACE ( 'NONE', #39533, 4.000000000000003553 ) ;
#246310=DIRECTION ( 'NONE',  ( 0.000000000000000000, 1.000000000000000000, 0.000000000000000000 ) ) ;
#246320=AXIS2_PLACEMENT_3D ( 'NONE', #115435, #247584, #68969 ) ;
#246340=ORIENTED_EDGE ( 'NONE', *, *, #11708, .F. ) ;
#246341=VERTEX_POINT ( 'NONE', #92285 ) ;
#246343=FACE_OUTER_BOUND ( 'NONE', #131158, .T. ) ;
#246441=ORIENTED_EDGE ( 'NONE', *, *, #81939, .F. ) ;
#246449=FACE_OUTER_BOUND ( 'NONE', #123827, .T. ) ;
#246453=AXIS2_PLACEMENT_3D ( 'NONE', #58859, #208025, #29408 ) ;
#246488=CARTESIAN_POINT ( 'NONE',  ( -20.94999999999999929, 61.95000000001194707, -108.5368025552853197 ) ) ;
#246489=EDGE_CURVE ( 'NONE', #33295, #176263, #208052, .T. ) ;
#246496=VERTEX_POINT ( 'NONE', #201657 ) ;
#246506=CARTESIAN_POINT ( 'NONE',  ( -21.08376601933334271, 75.93622398908230764, -142.8650547558000312 ) ) ;
#246534=CARTESIAN_POINT ( 'NONE',  ( -20.94999999999999929, 77.83534155023646406, -124.9679561919612922 ) ) ;
#246537=ORIENTED_EDGE ( 'NONE', *, *, #198539, .T. ) ;
#246553=LINE ( 'NONE', #147467, #163204 ) ;
#246562=CARTESIAN_POINT ( 'NONE',  ( -21.05000000000000071, 69.45934304831089889, -136.4231074845243654 ) ) ;
#246577=CARTESIAN_POINT ( 'NONE',  ( 23.25000000000000000, 87.75000000001192291, -106.1231074845242262 ) ) ;
#246610=CARTESIAN_POINT ( 'NONE',  ( -21.05000000000000071, 74.26374286841466699, -124.9544551555068068 ) ) ;
#246622=EDGE_CURVE ( 'NONE', #56206, #104197, #202938, .T. ) ;
#246625=DIRECTION ( 'NONE',  ( 0.000000000000000000, 6.982962677686266711E-15, -1.000000000000000000 ) ) ;
#246632=EDGE_LOOP ( 'NONE', ( #60382, #149724, #213471, #139519 ) ) ;
#246640=CARTESIAN_POINT ( 'NONE',  ( 21.05000000000000071, 65.27628318601242086, -128.9287082486403051 ) ) ;
#246642=EDGE_CURVE ( 'NONE', #167228, #128962, #128542, .T. ) ;
#246646=DIRECTION ( 'NONE',  ( 1.000000000000000000, -2.952720810173289112E-16, -2.061873921506763405E-30 ) ) ;
#246650=CYLINDRICAL_SURFACE ( 'NONE', #18631, 0.5000000000000004441 ) ;
#246695=CARTESIAN_POINT ( 'NONE',  ( 21.05000000000000071, 87.65000000001214175, -136.5231074845242176 ) ) ;
#246706=EDGE_CURVE ( 'NONE', #174077, #155848, #229071, .T. ) ;
#246712=ORIENTED_EDGE ( 'NONE', *, *, #3119, .T. ) ;
#246720=FACE_OUTER_BOUND ( 'NONE', #34108, .T. ) ;
#246721=ORIENTED_EDGE ( 'NONE', *, *, #213846, .T. ) ;
#246732=DIRECTION ( 'NONE',  ( 0.000000000000000000, 0.000000000000000000, -1.000000000000000000 ) ) ;
#246734=ORIENTED_EDGE ( 'NONE', *, *, #8735, .F. ) ;
#246737=DIRECTION ( 'NONE',  ( 0.000000000000000000, 0.000000000000000000, 1.000000000000000000 ) ) ;
#246757=LINE ( 'NONE', #220788, #181363 ) ;
#246800=LINE ( 'NONE', #147716, #161789 ) ;
#246810=DIRECTION ( 'NONE',  ( 0.000000000000000000, 0.000000000000000000, -1.000000000000000000 ) ) ;
#246822=ORIENTED_EDGE ( 'NONE', *, *, #140855, .F. ) ;
#246832=CARTESIAN_POINT ( 'NONE',  ( 18.39999999999999858, 85.51932773110452501, -129.5501311079648872 ) ) ;
#246842=ORIENTED_EDGE ( 'NONE', *, *, #105393, .T. ) ;
#246853=AXIS2_PLACEMENT_3D ( 'NONE', #145495, #225016, #82929 ) ;
#246881=CARTESIAN_POINT ( 'NONE',  ( 21.05000000000000071, 76.00000000001213607, -136.5231074845242745 ) ) ;
#246895=ORIENTED_EDGE ( 'NONE', *, *, #232459, .T. ) ;
#246905=EDGE_CURVE ( 'NONE', #239007, #127805, #179377, .T. ) ;
#246911=ORIENTED_EDGE ( 'NONE', *, *, #180403, .T. ) ;
#246921=TOROIDAL_SURFACE ( 'NONE', #51267, 0.2000000000000000111, 0.1000000000000000056 ) ;
#246926=AXIS2_PLACEMENT_3D ( 'NONE', #108810, #86656, #224898 ) ;
#246936=AXIS2_PLACEMENT_3D ( 'NONE', #176802, #21572, #256241 ) ;
#246964=CARTESIAN_POINT ( 'NONE',  ( 23.14999999999999503, 69.35000000001205933, -124.2731074845243455 ) ) ;
#246976=ORIENTED_EDGE ( 'NONE', *, *, #10049, .F. ) ;
#246989=CARTESIAN_POINT ( 'NONE',  ( -20.54999999999999716, 85.00000000001197975, -112.9170766071766820 ) ) ;
#246997=CIRCLE ( 'NONE', #184460, 0.1000000000000017680 ) ;
#247013=VERTEX_POINT ( 'NONE', #87487 ) ;
#247019=CARTESIAN_POINT ( 'NONE',  ( 21.05000000000000071, 75.90220970870339556, -142.7809220950004203 ) ) ;
#247056=CARTESIAN_POINT ( 'NONE',  ( -22.39999999999999858, 76.00000000001222134, -148.1726782920690937 ) ) ;
#247066=EDGE_CURVE ( 'NONE', #206536, #156363, #58542, .T. ) ;
#247095=ORIENTED_EDGE ( 'NONE', *, *, #20013, .T. ) ;
#247118=VERTEX_POINT ( 'NONE', #66666 ) ;
#247159=DIRECTION ( 'NONE',  ( 0.000000000000000000, -7.189901751995743170E-15, 1.000000000000000000 ) ) ;
#247190=EDGE_CURVE ( 'NONE', #17539, #153145, #171221, .T. ) ;
#247192=CARTESIAN_POINT ( 'NONE',  ( -18.59999999999999787, 77.83534155023646406, -124.9679561919613064 ) ) ;
#247211=FACE_OUTER_BOUND ( 'NONE', #46461, .T. ) ;
#247242=CARTESIAN_POINT ( 'NONE',  ( 18.49999999999998934, 64.35000000001197407, -111.7731074845243739 ) ) ;
#247255=CARTESIAN_POINT ( 'NONE',  ( 23.14999999999999858, 70.05000000001197691, -113.3288097895591591 ) ) ;
#247264=EDGE_LOOP ( 'NONE', ( #214589, #224336, #20451, #40576 ) ) ;
#247275=DIRECTION ( 'NONE',  ( 0.000000000000000000, -1.000000000000000000, 1.387778780781406043E-13 ) ) ;
#247278=CARTESIAN_POINT ( 'NONE',  ( -20.54999999999999716, 71.75000000001205080, -124.2731074845243313 ) ) ;
#247289=ADVANCED_FACE ( 'NONE', ( #52215 ), #32716, .F. ) ;
#247306=LINE ( 'NONE', #68688, #144606 ) ;
#247318=CARTESIAN_POINT ( 'NONE',  ( 21.14999999999999503, 76.00000000001213607, -136.5231074845242745 ) ) ;
#247325=ORIENTED_EDGE ( 'NONE', *, *, #250346, .T. ) ;
#247332=DIRECTION ( 'NONE',  ( 2.694716079187273439E-16, 1.000000000000000000, 6.467318590049456648E-15 ) ) ;
#247369=VERTEX_POINT ( 'NONE', #218998 ) ;
#247379=DIRECTION ( 'NONE',  ( 0.000000000000000000, -7.056502275159890832E-15, 1.000000000000000000 ) ) ;
#247392=CARTESIAN_POINT ( 'NONE',  ( 22.47071067811865319, 75.90090754530959316, -144.2431822290223522 ) ) ;
#247394=CARTESIAN_POINT ( 'NONE',  ( 20.94999999999999929, 76.00000000001190870, -103.0231074845243029 ) ) ;
#247399=ORIENTED_EDGE ( 'NONE', *, *, #234342, .T. ) ;
#247400=CIRCLE ( 'NONE', #222435, 0.09999999999998898659 ) ;
#247413=AXIS2_PLACEMENT_3D ( 'NONE', #219060, #20905, #247275 ) ;
#247427=CARTESIAN_POINT ( 'NONE',  ( 18.59999999999999076, 64.35000000001197407, -111.6731074845243796 ) ) ;
#247453=ORIENTED_EDGE ( 'NONE', *, *, #238232, .F. ) ;
#247463=EDGE_CURVE ( 'NONE', #3601, #159137, #127615, .T. ) ;
#247464=DIRECTION ( 'NONE',  ( -1.000000000000000000, 1.875376730785737719E-16, 1.309568571767809260E-30 ) ) ;
#247493=CARTESIAN_POINT ( 'NONE',  ( -18.59999999999999787, 77.16412189325305349, -95.10825939895268277 ) ) ;
#247559=EDGE_LOOP ( 'NONE', ( #240810, #107442, #171292, #26134 ) ) ;
#247576=DIRECTION ( 'NONE',  ( 0.000000000000000000, 6.982962677686266711E-15, -1.000000000000000000 ) ) ;
#247584=DIRECTION ( 'NONE',  ( 1.000000000000000000, 0.000000000000000000, 0.000000000000000000 ) ) ;
#247594=ADVANCED_FACE ( 'NONE', ( #154903 ), #175745, .T. ) ;
#247601=CARTESIAN_POINT ( 'NONE',  ( 18.59999999999999076, 64.35000000001197407, -111.6731074845243796 ) ) ;
#247622=CYLINDRICAL_SURFACE ( 'NONE', #236484, 0.09999999999999939493 ) ;
#247668=CARTESIAN_POINT ( 'NONE',  ( -18.39999999999999858, 85.50000000001186606, -96.42291809330220076 ) ) ;
#247707=ORIENTED_EDGE ( 'NONE', *, *, #53352, .T. ) ;
#247749=FACE_OUTER_BOUND ( 'NONE', #215978, .T. ) ;
#247757=VECTOR ( 'NONE', #215928, 1000.000000000000000 ) ;
#247759=AXIS2_PLACEMENT_3D ( 'NONE', #226783, #48146, #233234 ) ;
#247795=AXIS2_PLACEMENT_3D ( 'NONE', #197273, #169074, #116465 ) ;
#247812=CARTESIAN_POINT ( 'NONE',  ( 21.05000000000000071, 69.45934304831089889, -136.4231074845243654 ) ) ;
#247816=CIRCLE ( 'NONE', #202024, 0.09999999999998898659 ) ;
#247827=DIRECTION ( 'NONE',  ( 0.000000000000000000, 0.000000000000000000, -1.000000000000000000 ) ) ;
#247864=DIRECTION ( 'NONE',  ( 0.000000000000000000, 0.000000000000000000, 1.000000000000000000 ) ) ;
#247884=AXIS2_PLACEMENT_3D ( 'NONE', #239266, #123171, #120620 ) ;
#247891=CARTESIAN_POINT ( 'NONE',  ( 19.86930884467576419, 64.31308993304084254, -111.7838848455855327 ) ) ;
#247902=ORIENTED_EDGE ( 'NONE', *, *, #133410, .F. ) ;
#247922=DIRECTION ( 'NONE',  ( -0.000000000000000000, -1.000000000000000000, -6.982962677686266711E-15 ) ) ;
#247925=CARTESIAN_POINT ( 'NONE',  ( 21.05000000000000071, 65.27628289530457550, -128.8581939154367717 ) ) ;
#247948=LINE ( 'NONE', #45906, #162011 ) ;
#247964=DIRECTION ( 'NONE',  ( 3.265361837132813093E-16, 1.000000000000000000, 6.982962677686266711E-15 ) ) ;
#247986=AXIS2_PLACEMENT_3D ( 'NONE', #183885, #1375, #80914 ) ;
#247987=TOROIDAL_SURFACE ( 'NONE', #156265, 0.6000000000000009770, 0.1000000000000000056 ) ;
#248030=CIRCLE ( 'NONE', #89800, 0.2000000000000057288 ) ;
#248064=CARTESIAN_POINT ( 'NONE',  ( -18.60000000000000853, 85.36424052760300185, -129.3428589026834743 ) ) ;
#248065=ADVANCED_FACE ( 'NONE', ( #210682 ), #232836, .F. ) ;
#248075=DIRECTION ( 'NONE',  ( -1.000000000000000000, 0.000000000000000000, 0.000000000000000000 ) ) ;
#248082=VECTOR ( 'NONE', #62216, 1000.000000000000000 ) ;
#248111=ORIENTED_EDGE ( 'NONE', *, *, #149449, .T. ) ;
#248125=VECTOR ( 'NONE', #166440, 1000.000000000000000 ) ;
#248181=CIRCLE ( 'NONE', #48262, 0.6000000000000033085 ) ;
#248235=CARTESIAN_POINT ( 'NONE',  ( 20.94999999999999929, 76.00000000001193712, -107.1231074845243114 ) ) ;
#248246=FACE_OUTER_BOUND ( 'NONE', #194248, .T. ) ;
#248258=ORIENTED_EDGE ( 'NONE', *, *, #213877, .F. ) ;
#248331=LINE ( 'NONE', #226159, #72173 ) ;
#248361=DIRECTION ( 'NONE',  ( 0.000000000000000000, 6.982962677686267499E-15, -1.000000000000000000 ) ) ;
#248366=ORIENTED_EDGE ( 'NONE', *, *, #82070, .F. ) ;
#248396=LINE ( 'NONE', #8508, #77616 ) ;
#248441=ADVANCED_FACE ( 'NONE', ( #73471 ), #153016, .T. ) ;
#248452=ORIENTED_EDGE ( 'NONE', *, *, #47655, .F. ) ;
#248489=CIRCLE ( 'NONE', #206797, 0.3999999999999975797 ) ;
#248514=ORIENTED_EDGE ( 'NONE', *, *, #130312, .F. ) ;
#248525=DIRECTION ( 'NONE',  ( 0.000000000000000000, -0.4999999999999088507, 0.8660254037844913322 ) ) ;
#248536=FACE_OUTER_BOUND ( 'NONE', #43317, .T. ) ;
#248543=EDGE_CURVE ( 'NONE', #175608, #40840, #160715, .T. ) ;
#248596=AXIS2_PLACEMENT_3D ( 'NONE', #129515, #190802, #227320 ) ;
#248603=LINE ( 'NONE', #229051, #39561 ) ;
#248607=AXIS2_PLACEMENT_3D ( 'NONE', #127906, #49641, #30106 ) ;
#248616=FACE_OUTER_BOUND ( 'NONE', #112078, .T. ) ;
#248638=CARTESIAN_POINT ( 'NONE',  ( 21.14999999999999858, 76.00000000001213607, -136.5231074845242745 ) ) ;
#248639=EDGE_CURVE ( 'NONE', #48194, #442, #36370, .T. ) ;
#248661=DIRECTION ( 'NONE',  ( -0.7071067811865474617, 0.7071067811865474617, 5.142139384388980375E-15 ) ) ;
#248667=VECTOR ( 'NONE', #115141, 1000.000000000000000 ) ;
#248682=AXIS2_PLACEMENT_3D ( 'NONE', #852, #161257, #219929 ) ;
#248687=EDGE_LOOP ( 'NONE', ( #34387, #185281, #211229, #115493 ) ) ;
#248703=DIRECTION ( 'NONE',  ( 1.000000000000000000, 0.000000000000000000, 0.000000000000000000 ) ) ;
#248716=ORIENTED_EDGE ( 'NONE', *, *, #18856, .F. ) ;
#248734=DIRECTION ( 'NONE',  ( 0.000000000000000000, 0.000000000000000000, 1.000000000000000000 ) ) ;
#248755=ORIENTED_EDGE ( 'NONE', *, *, #250454, .F. ) ;
#248770=ORIENTED_EDGE ( 'NONE', *, *, #202421, .F. ) ;
#248774=DIRECTION ( 'NONE',  ( 0.000000000000000000, 1.000000000000000000, 6.982962677686266711E-15 ) ) ;
#248792=EDGE_CURVE ( 'NONE', #254598, #19089, #54618, .T. ) ;
#248860=CARTESIAN_POINT ( 'NONE',  ( -18.50000000000000000, 74.65925378207852248, -146.7959699899454904 ) ) ;
#248869=CIRCLE ( 'NONE', #77968, 0.5000000000000004441 ) ;
#248898=EDGE_CURVE ( 'NONE', #8134, #176263, #83804, .T. ) ;
#248902=DIRECTION ( 'NONE',  ( 1.000000000000000000, 0.000000000000000000, 0.000000000000000000 ) ) ;
#248908=DIRECTION ( 'NONE',  ( -0.8660254037843277963, 0.000000000000000000, 0.5000000000001921796 ) ) ;
#248933=EDGE_CURVE ( 'NONE', #121418, #105325, #108783, .T. ) ;
#248985=EDGE_CURVE ( 'NONE', #219596, #54007, #46422, .T. ) ;
#248997=DIRECTION ( 'NONE',  ( -4.408576920032448588E-17, -0.1350103645451807832, -0.9908441862701610203 ) ) ;
#249004=( BOUNDED_SURFACE ( )  B_SPLINE_SURFACE ( 3, 2, ( 
 ( #238903, #60245, #139772 ),
 ( #219322, #105774, #242732 ),
 ( #207493, #125375, #49681 ),
 ( #187922, #203619, #245323 ) ),
 .UNSPECIFIED., .F., .F., .T. ) 
 B_SPLINE_SURFACE_WITH_KNOTS ( ( 4, 4 ),
 ( 3, 3 ),
 ( 0.0006461284895273765793, 0.0007503702773986201200 ),
 ( 0.000000000000000000, 1.000000000000000000 ),
 .UNSPECIFIED. ) 
 GEOMETRIC_REPRESENTATION_ITEM ( )  RATIONAL_B_SPLINE_SURFACE ( (
 ( 1.000000000000000000, 0.7071067811865475727, 1.000000000000000000),
 ( 1.000000000000000000, 0.7076476444648711617, 1.000000000000000000),
 ( 1.000000000000000000, 0.7075727925192061285, 1.000000000000000000),
 ( 1.000000000000000000, 0.7071067811865581199, 1.000000000000000000) ) ) 
 REPRESENTATION_ITEM ( '' )  SURFACE ( )  );
#249019=VERTEX_POINT ( 'NONE', #252394 ) ;
#249031=DIRECTION ( 'NONE',  ( 0.000000000000000000, -3.664813867694691995E-14, 1.000000000000000000 ) ) ;
#249053=CIRCLE ( 'NONE', #24192, 0.1000000000000028644 ) ;
#249070=ORIENTED_EDGE ( 'NONE', *, *, #192546, .F. ) ;
#249086=VECTOR ( 'NONE', #155583, 1000.000000000000000 ) ;
#249108=EDGE_CURVE ( 'NONE', #52643, #79334, #185513, .T. ) ;
#249129=VECTOR ( 'NONE', #61780, 1000.000000000000000 ) ;
#249143=DIRECTION ( 'NONE',  ( 0.000000000000000000, -1.000000000000000000, -6.982962677686265922E-15 ) ) ;
#249168=ORIENTED_EDGE ( 'NONE', *, *, #67122, .T. ) ;
#249172=DIRECTION ( 'NONE',  ( 1.000000000000000000, 0.000000000000000000, 0.000000000000000000 ) ) ;
#249198=EDGE_CURVE ( 'NONE', #231485, #181753, #142295, .T. ) ;
#249223=TOROIDAL_SURFACE ( 'NONE', #203430, 0.6000000000000004219, 0.1000000000000000056 ) ;
#249224=EDGE_LOOP ( 'NONE', ( #80318, #185076, #195926, #137389 ) ) ;
#249233=CARTESIAN_POINT ( 'NONE',  ( -23.15000000000000213, 76.00000000001199396, -115.8981074845243029 ) ) ;
#249243=DIRECTION ( 'NONE',  ( -1.000000000000000000, 0.000000000000000000, -0.000000000000000000 ) ) ;
#249245=CARTESIAN_POINT ( 'NONE',  ( 18.50596464788227280, 65.69367753730654158, -97.51892380663477411 ) ) ;
#249264=AXIS2_PLACEMENT_3D ( 'NONE', #73129, #52225, #212617 ) ;
#249283=CIRCLE ( 'NONE', #16071, 0.5000000000000004441 ) ;
#249304=AXIS2_PLACEMENT_3D ( 'NONE', #212525, #73033, #14333 ) ;
#249344=CYLINDRICAL_SURFACE ( 'NONE', #130529, 2.000000000000001776 ) ;
#249346=CARTESIAN_POINT ( 'NONE',  ( 20.94999999999999574, 65.52661458509918191, -128.9444530202758301 ) ) ;
#249389=ORIENTED_EDGE ( 'NONE', *, *, #11629, .F. ) ;
#249401=AXIS2_PLACEMENT_3D ( 'NONE', #178486, #237154, #201871 ) ;
#249442=ORIENTED_EDGE ( 'NONE', *, *, #183639, .F. ) ;
#249450=CARTESIAN_POINT ( 'NONE',  ( 21.05000000000000071, 76.00000000001213607, -136.4231074845243086 ) ) ;
#249452=DIRECTION ( 'NONE',  ( 1.000000000000000000, 0.000000000000000000, 0.000000000000000000 ) ) ;
#249487=ORIENTED_EDGE ( 'NONE', *, *, #190344, .F. ) ;
#249489=ADVANCED_FACE ( 'NONE', ( #13754 ), #54151, .F. ) ;
#249500=DIRECTION ( 'NONE',  ( -1.000000000000000000, -0.000000000000000000, -0.000000000000000000 ) ) ;
#249507=CIRCLE ( 'NONE', #241138, 0.2000000000000057288 ) ;
#249519=ORIENTED_EDGE ( 'NONE', *, *, #182746, .F. ) ;
#249540=EDGE_CURVE ( 'NONE', #122081, #121455, #150847, .T. ) ;
#249559=ORIENTED_EDGE ( 'NONE', *, *, #64832, .T. ) ;
#249605=CARTESIAN_POINT ( 'NONE',  ( -21.55000000000000071, 68.65000000001205649, -124.1731074845243512 ) ) ;
#249615=ORIENTED_EDGE ( 'NONE', *, *, #195361, .F. ) ;
#249624=VECTOR ( 'NONE', #55984, 1000.000000000000000 ) ;
#249626=VECTOR ( 'NONE', #137449, 1000.000000000000114 ) ;
#249680=DIRECTION ( 'NONE',  ( 1.000000000000000000, 0.000000000000000000, 0.000000000000000000 ) ) ;
#249718=DIRECTION ( 'NONE',  ( -1.000000000000000000, -0.000000000000000000, -0.000000000000000000 ) ) ;
#249733=EDGE_CURVE ( 'NONE', #139747, #148869, #124422, .T. ) ;
#249785=DIRECTION ( 'NONE',  ( 1.000000000000000000, 0.000000000000000000, 0.000000000000000000 ) ) ;
#249806=AXIS2_PLACEMENT_3D ( 'NONE', #173098, #93503, #178206 ) ;
#249807=AXIS2_PLACEMENT_3D ( 'NONE', #67390, #146903, #243453 ) ;
#249808=CARTESIAN_POINT ( 'NONE',  ( 21.14999999999998082, 87.75000000001213607, -136.5231074845242176 ) ) ;
#249828=CYLINDRICAL_SURFACE ( 'NONE', #103015, 0.09999999999999939493 ) ;
#249835=CYLINDRICAL_SURFACE ( 'NONE', #38173, 0.1000000000000028644 ) ;
#249836=AXIS2_PLACEMENT_3D ( 'NONE', #129046, #204707, #31266 ) ;
#249850=CIRCLE ( 'NONE', #116578, 0.09999999999999939493 ) ;
#249859=DIRECTION ( 'NONE',  ( -1.836970198721029934E-16, -1.000000000000000000, -6.982962677686266711E-15 ) ) ;
#249862=ORIENTED_EDGE ( 'NONE', *, *, #116787, .T. ) ;
#249889=ORIENTED_EDGE ( 'NONE', *, *, #66590, .T. ) ;
#249906=DIRECTION ( 'NONE',  ( -1.000000000000000000, 0.000000000000000000, 0.000000000000000000 ) ) ;
#249949=ADVANCED_FACE ( 'NONE', ( #23755 ), #185361, .F. ) ;
#249990=EDGE_LOOP ( 'NONE', ( #7919, #236370, #180103 ) ) ;
#250044=ORIENTED_EDGE ( 'NONE', *, *, #189286, .T. ) ;
#250047=CARTESIAN_POINT ( 'NONE',  ( 22.50014994444007144, 64.25028026812009330, -136.6061876412435367 ) ) ;
#250069=TOROIDAL_SURFACE ( 'NONE', #199995, 11.65000000000000036, 0.1000000000000000056 ) ;
#250110=CARTESIAN_POINT ( 'NONE',  ( -21.64999999999999858, 68.65000000001199965, -115.2731074845243455 ) ) ;
#250126=ORIENTED_EDGE ( 'NONE', *, *, #223575, .F. ) ;
#250134=CIRCLE ( 'NONE', #108481, 0.09999999999999939493 ) ;
#250148=DIRECTION ( 'NONE',  ( 0.000000000000000000, -0.9998779222360097974, 0.01562500000000363945 ) ) ;
#250151=DIRECTION ( 'NONE',  ( -6.938893903907224433E-15, -1.000000000000000000, -6.982962677686266711E-15 ) ) ;
#250162=AXIS2_PLACEMENT_3D ( 'NONE', #77217, #138458, #35567 ) ;
#250168=CARTESIAN_POINT ( 'NONE',  ( 22.32929514600007792, 68.42135243463566496, -136.6221831626382652 ) ) ;
#250201=EDGE_CURVE ( 'NONE', #147787, #182942, #73151, .T. ) ;
#250203=ORIENTED_EDGE ( 'NONE', *, *, #62141, .F. ) ;
#250213=AXIS2_PLACEMENT_3D ( 'NONE', #173128, #213479, #101191 ) ;
#250231=AXIS2_PLACEMENT_3D ( 'NONE', #84489, #7573, #64969 ) ;
#250236=CARTESIAN_POINT ( 'NONE',  ( -18.47690164073606667, 85.46484453802410997, -96.32172654468811857 ) ) ;
#250237=EDGE_LOOP ( 'NONE', ( #156014, #77969, #173592, #20258 ) ) ;
#250249=CARTESIAN_POINT ( 'NONE',  ( -20.64999999999999858, 74.00000000001199396, -115.7477294072863998 ) ) ;
#250250=FACE_OUTER_BOUND ( 'NONE', #170376, .T. ) ;
#250263=AXIS2_PLACEMENT_3D ( 'NONE', #29157, #108644, #215444 ) ;
#250265=FACE_OUTER_BOUND ( 'NONE', #12229, .T. ) ;
#250298=CARTESIAN_POINT ( 'NONE',  ( -21.64999999999999858, 68.75000000001199396, -115.3731074845243540 ) ) ;
#250322=CARTESIAN_POINT ( 'NONE',  ( 18.39999999999999858, 85.68240343348824695, -96.36626410711143365 ) ) ;
#250337=CARTESIAN_POINT ( 'NONE',  ( 23.24999999999997513, 64.35000000001195986, -110.0379132551783243 ) ) ;
#250346=EDGE_CURVE ( 'NONE', #105040, #121092, #184523, .T. ) ;
#250373=EDGE_LOOP ( 'NONE', ( #176893, #156506, #208550, #246734 ) ) ;
#250414=DIRECTION ( 'NONE',  ( -0.000000000000000000, 0.9908441862701591329, 0.1350103645451946055 ) ) ;
#250426=DIRECTION ( 'NONE',  ( -1.000000000000000000, 0.000000000000000000, -0.000000000000000000 ) ) ;
#250432=EDGE_LOOP ( 'NONE', ( #219829, #34756, #251885 ) ) ;
#250453=CARTESIAN_POINT ( 'NONE',  ( -18.50000000000000355, 77.26327546522911405, -95.12124281777788326 ) ) ;
#250454=EDGE_CURVE ( 'NONE', #60684, #4010, #92946, .T. ) ;
#250457=CARTESIAN_POINT ( 'NONE',  ( 19.75857864376269291, 64.35000000001197407, -111.7731074845243739 ) ) ;
#250471=CIRCLE ( 'NONE', #129844, 0.5000000000000004441 ) ;
#250498=CARTESIAN_POINT ( 'NONE',  ( -21.05000000000000071, 74.16465844978765176, -124.9679561919613207 ) ) ;
#250502=ORIENTED_EDGE ( 'NONE', *, *, #82074, .F. ) ;
#250576=ORIENTED_EDGE ( 'NONE', *, *, #64611, .T. ) ;
#250605=EDGE_LOOP ( 'NONE', ( #179738, #78542, #869, #131849 ) ) ;
#250607=ORIENTED_EDGE ( 'NONE', *, *, #76895, .T. ) ;
#250627=CARTESIAN_POINT ( 'NONE',  ( 20.94999999999999574, 74.83729825007408465, -128.5231074845243029 ) ) ;
#250655=AXIS2_PLACEMENT_3D ( 'NONE', #122808, #24998, #45817 ) ;
#250658=ORIENTED_EDGE ( 'NONE', *, *, #1938, .T. ) ;
#250675=CARTESIAN_POINT ( 'NONE',  ( 20.94999999999999929, 76.00000000001192291, -105.0231074845243029 ) ) ;
#250684=DIRECTION ( 'NONE',  ( 1.000000000000000000, 0.000000000000000000, 0.000000000000000000 ) ) ;
#250711=CARTESIAN_POINT ( 'NONE',  ( -22.39999999999999858, 75.90000000001219860, -144.3138870828977076 ) ) ;
#250723=ORIENTED_EDGE ( 'NONE', *, *, #118833, .T. ) ;
#250764=CARTESIAN_POINT ( 'NONE',  ( -23.25000000000000000, 77.14957036958755054, -95.20719500002232394 ) ) ;
#250780=CARTESIAN_POINT ( 'NONE',  ( 20.94999999999999929, 69.35000000001205933, -124.3731074845243540 ) ) ;
#250793=EDGE_LOOP ( 'NONE', ( #90260, #169681, #219808, #161811 ) ) ;
#250807=CIRCLE ( 'NONE', #184159, 0.1000000000000070832 ) ;
#250830=DIRECTION ( 'NONE',  ( 0.000000000000000000, 0.000000000000000000, 1.000000000000000000 ) ) ;
#250858=CARTESIAN_POINT ( 'NONE',  ( 20.94999999999999929, 71.14953271029236248, -115.0573748935260028 ) ) ;
#250872=VERTEX_POINT ( 'NONE', #6086 ) ;
#250877=CARTESIAN_POINT ( 'NONE',  ( 18.49713797159841633, 85.44648232759121242, -129.4516493629137983 ) ) ;
#250930=CARTESIAN_POINT ( 'NONE',  ( -23.15000000000000213, 80.83132476063495631, -119.5534105423255227 ) ) ;
#250943=EDGE_CURVE ( 'NONE', #61045, #6106, #213951, .T. ) ;
#250955=EDGE_CURVE ( 'NONE', #194536, #3363, #106451, .T. ) ;
#250982=PLANE ( 'NONE',  #180854 ) ;
#251019=DIRECTION ( 'NONE',  ( -3.265361837132813093E-16, -1.000000000000000000, -7.026728003956683390E-15 ) ) ;
#251030=ORIENTED_EDGE ( 'NONE', *, *, #88743, .T. ) ;
#251035=DIRECTION ( 'NONE',  ( -3.265361837132813093E-16, -1.000000000000000000, 7.445645354460596589E-46 ) ) ;
#251039=ORIENTED_EDGE ( 'NONE', *, *, #164192, .F. ) ;
#251047=CIRCLE ( 'NONE', #117969, 0.5000000000000004441 ) ;
#251057=CYLINDRICAL_SURFACE ( 'NONE', #90606, 0.09999999999999939493 ) ;
#251058=ORIENTED_EDGE ( 'NONE', *, *, #256472, .T. ) ;
#251097=DIRECTION ( 'NONE',  ( 1.000000000000000000, 0.000000000000000000, 0.000000000000000000 ) ) ;
#251140=LINE ( 'NONE', #51646, #226153 ) ;
#251177=EDGE_LOOP ( 'NONE', ( #59061, #66221, #55561, #170757 ) ) ;
#251181=AXIS2_PLACEMENT_3D ( 'NONE', #230073, #233924, #51401 ) ;
#251198=CARTESIAN_POINT ( 'NONE',  ( -20.87155475150660777, 64.25000000001195133, -109.9275209553671147 ) ) ;
#251215=EDGE_LOOP ( 'NONE', ( #143137, #170100, #13108, #31414, #227322 ) ) ;
#251258=EDGE_CURVE ( 'NONE', #16182, #151026, #83688, .T. ) ;
#251259=ORIENTED_EDGE ( 'NONE', *, *, #7963, .F. ) ;
#251269=CIRCLE ( 'NONE', #80566, 4.049999999999998046 ) ;
#251352=DIRECTION ( 'NONE',  ( 0.000000000000000000, -1.000000000000000000, -6.982962677686265922E-15 ) ) ;
#251365=ORIENTED_EDGE ( 'NONE', *, *, #187945, .F. ) ;
#251369=ORIENTED_EDGE ( 'NONE', *, *, #91321, .F. ) ;
#251370=DIRECTION ( 'NONE',  ( 0.000000000000000000, 6.982962677686266711E-15, -1.000000000000000000 ) ) ;
#251374=CARTESIAN_POINT ( 'NONE',  ( 20.94999999999999929, 76.00000000001185185, -95.22310748452429152 ) ) ;
#251379=CARTESIAN_POINT ( 'NONE',  ( 21.05000000000000071, 67.22371710471958295, -124.3731074845243683 ) ) ;
#251391=EDGE_CURVE ( 'NONE', #189431, #80026, #18318, .T. ) ;
#251404=AXIS2_PLACEMENT_3D ( 'NONE', #147705, #210257, #69465 ) ;
#251411=EDGE_CURVE ( 'NONE', #24859, #188797, #195701, .T. ) ;
#251439=CARTESIAN_POINT ( 'NONE',  ( -20.94999999999999929, 87.29603075034741266, -133.4752083248603469 ) ) ;
#251466=CARTESIAN_POINT ( 'NONE',  ( 21.14999999999999858, 64.35000000001204512, -124.3731074845243825 ) ) ;
#251486=DIRECTION ( 'NONE',  ( 0.000000000000000000, 0.000000000000000000, -1.000000000000000000 ) ) ;
#251488=CARTESIAN_POINT ( 'NONE',  ( 23.24999999999999645, 72.10000000001190301, -103.0231074845243313 ) ) ;
#251493=DIRECTION ( 'NONE',  ( 1.000000000000000000, 0.000000000000000000, 0.000000000000000000 ) ) ;
#251580=ADVANCED_FACE ( 'NONE', ( #241232 ), #145954, .T. ) ;
#251581=EDGE_CURVE ( 'NONE', #60670, #442, #234716, .T. ) ;
#251590=ORIENTED_EDGE ( 'NONE', *, *, #96311, .T. ) ;
#251598=ORIENTED_EDGE ( 'NONE', *, *, #193896, .F. ) ;
#251607=CARTESIAN_POINT ( 'NONE',  ( 18.44206774312970154, 85.49102735755195681, -96.39687997982596812 ) ) ;
#251614=VECTOR ( 'NONE', #91515, 1000.000000000000000 ) ;
#251619=ORIENTED_EDGE ( 'NONE', *, *, #40204, .F. ) ;
#251626=ORIENTED_EDGE ( 'NONE', *, *, #89409, .T. ) ;
#251646=DIRECTION ( 'NONE',  ( 0.000000000000000000, -6.454785026890406770E-15, 1.000000000000000000 ) ) ;
#251647=CARTESIAN_POINT ( 'NONE',  ( 21.00000000000000000, 66.25000000001206502, -124.1731074845243654 ) ) ;
#251653=CARTESIAN_POINT ( 'NONE',  ( 23.15000000000000213, 87.65000000001221281, -148.2731074845242176 ) ) ;
#251656=CARTESIAN_POINT ( 'NONE',  ( 21.05000000000000071, 76.00000000001192291, -104.9231074845242944 ) ) ;
#251696=DIRECTION ( 'NONE',  ( -1.000000000000000000, -0.000000000000000000, -0.000000000000000000 ) ) ;
#251704=PLANE ( 'NONE',  #137880 ) ;
#251709=VECTOR ( 'NONE', #5765, 1000.000000000000000 ) ;
#251711=CARTESIAN_POINT ( 'NONE',  ( 21.14999999999999858, 64.25000000001220712, -148.2731074845243882 ) ) ;
#251717=CIRCLE ( 'NONE', #243334, 0.1000000000000017680 ) ;
#251766=CARTESIAN_POINT ( 'NONE',  ( 21.22070241538126467, 75.90108096947716376, -142.9930537573939091 ) ) ;
#251767=DIRECTION ( 'NONE',  ( -1.000000000000000000, 0.000000000000000000, 0.000000000000000000 ) ) ;
#251783=CARTESIAN_POINT ( 'NONE',  ( 21.04999999999999716, 65.49746832288708731, -128.9642776674504887 ) ) ;
#251784=ORIENTED_EDGE ( 'NONE', *, *, #23048, .T. ) ;
#251791=ADVANCED_FACE ( 'NONE', ( #186394 ), #1905, .F. ) ;
#251799=CARTESIAN_POINT ( 'NONE',  ( 18.50211644919734866, 65.69792220476318789, -97.53355541284612684 ) ) ;
#251820=ADVANCED_FACE ( 'NONE', ( #233231 ), #114545, .T. ) ;
#251831=ORIENTED_EDGE ( 'NONE', *, *, #115968, .T. ) ;
#251885=ORIENTED_EDGE ( 'NONE', *, *, #257115, .F. ) ;
#251911=EDGE_LOOP ( 'NONE', ( #236271, #23553, #137778, #249168, #202451 ) ) ;
#251923=CARTESIAN_POINT ( 'NONE',  ( 20.95132126680579887, 65.51005012986530573, -128.9527829460898545 ) ) ;
#251925=FACE_OUTER_BOUND ( 'NONE', #146064, .T. ) ;
#251932=CARTESIAN_POINT ( 'NONE',  ( 22.48508240969612615, 75.95372358549531100, -148.1731182160978619 ) ) ;
#251934=CIRCLE ( 'NONE', #189591, 0.09999999999999976963 ) ;
#251945=DIRECTION ( 'NONE',  ( -1.000000000000000000, 2.952720810173289112E-16, 2.061873921506763405E-30 ) ) ;
#251958=DIRECTION ( 'NONE',  ( 1.000000000000000000, -2.952720810173289112E-16, -2.061873921506763405E-30 ) ) ;
#251964=CARTESIAN_POINT ( 'NONE',  ( 23.14999999999999858, 71.18691588786253988, -124.5815897280005089 ) ) ;
#251975=EDGE_CURVE ( 'NONE', #27724, #34583, #231087, .T. ) ;
#251996=DIRECTION ( 'NONE',  ( 1.000000000000000000, 7.304098846218134667E-16, 5.100424963727256530E-30 ) ) ;
#252006=DIRECTION ( 'NONE',  ( 0.000000000000000000, -7.056502275159890832E-15, 1.000000000000000000 ) ) ;
#252010=VERTEX_POINT ( 'NONE', #222593 ) ;
#252019=ORIENTED_EDGE ( 'NONE', *, *, #200597, .T. ) ;
#252024=DIRECTION ( 'NONE',  ( 0.000000000000000000, 0.000000000000000000, 1.000000000000000000 ) ) ;
#252029=CARTESIAN_POINT ( 'NONE',  ( 21.05000000000000071, 88.41227409416161720, -106.0231074845242176 ) ) ;
#252048=ORIENTED_EDGE ( 'NONE', *, *, #79439, .T. ) ;
#252068=VERTEX_POINT ( 'NONE', #189919 ) ;
#252092=AXIS2_PLACEMENT_3D ( 'NONE', #42395, #120674, #21559 ) ;
#252104=FACE_OUTER_BOUND ( 'NONE', #48711, .T. ) ;
#252109=EDGE_CURVE ( 'NONE', #114115, #7849, #248603, .T. ) ;
#252131=AXIS2_PLACEMENT_3D ( 'NONE', #161600, #62484, #3785 ) ;
#252153=CARTESIAN_POINT ( 'NONE',  ( 21.00000000000000000, 66.25000000001206502, -124.1731074845243654 ) ) ;
#252168=ADVANCED_FACE ( 'NONE', ( #128671 ), #247987, .T. ) ;
#252172=DIRECTION ( 'NONE',  ( 1.000000000000000000, 0.000000000000000000, 0.000000000000000000 ) ) ;
#252218=CARTESIAN_POINT ( 'NONE',  ( 18.49999999999999289, 65.50857864377465489, -111.6731074845243796 ) ) ;
#252251=TOROIDAL_SURFACE ( 'NONE', #98120, 0.2000000000000000111, 0.1000000000000000056 ) ;
#252303=CIRCLE ( 'NONE', #98164, 0.09999999999999971412 ) ;
#252305=CARTESIAN_POINT ( 'NONE',  ( -23.15000000000000213, 76.00000000001188027, -99.02310748452428868 ) ) ;
#252306=EDGE_CURVE ( 'NONE', #178773, #126698, #80198, .T. ) ;
#252343=CARTESIAN_POINT ( 'NONE',  ( -21.05000000000000071, 77.16270174995010223, -128.5231074845242745 ) ) ;
#252344=DIRECTION ( 'NONE',  ( 1.000000000000000000, 0.000000000000000000, 0.000000000000000000 ) ) ;
#252345=DIRECTION ( 'NONE',  ( 1.000000000000000000, 0.000000000000000000, 0.000000000000000000 ) ) ;
#252346=EDGE_CURVE ( 'NONE', #67694, #76270, #48076, .T. ) ;
#252350=DIRECTION ( 'NONE',  ( 1.000000000000000000, 0.000000000000000000, 0.000000000000000000 ) ) ;
#252370=CARTESIAN_POINT ( 'NONE',  ( 20.04142135623730070, 64.35000000001221565, -148.2731074845243882 ) ) ;
#252394=CARTESIAN_POINT ( 'NONE',  ( -18.59999999999999787, 68.97833521811179480, -99.28954208262706516 ) ) ;
#252397=ORIENTED_EDGE ( 'NONE', *, *, #157341, .F. ) ;
#252402=CARTESIAN_POINT ( 'NONE',  ( 21.08479644141221954, 75.94144555744806269, -142.8681461422562222 ) ) ;
#252416=FACE_OUTER_BOUND ( 'NONE', #99775, .T. ) ;
#252430=AXIS2_PLACEMENT_3D ( 'NONE', #3489, #6056, #242105 ) ;
#252432=EDGE_CURVE ( 'NONE', #156851, #220552, #87912, .T. ) ;
#252472=ORIENTED_EDGE ( 'NONE', *, *, #37662, .T. ) ;
#252484=CARTESIAN_POINT ( 'NONE',  ( -20.94999999999999929, 64.36312671090736615, -109.8448666978492838 ) ) ;
#252499=DIRECTION ( 'NONE',  ( -1.000000000000000000, 0.000000000000000000, 0.000000000000000000 ) ) ;
#252525=DIRECTION ( 'NONE',  ( 1.000000000000000000, 0.000000000000000000, 0.000000000000000000 ) ) ;
#252542=ADVANCED_FACE ( 'NONE', ( #120249 ), #61526, .T. ) ;
#252549=ORIENTED_EDGE ( 'NONE', *, *, #195574, .F. ) ;
#252580=ORIENTED_EDGE ( 'NONE', *, *, #212652, .T. ) ;
#252586=ORIENTED_EDGE ( 'NONE', *, *, #199872, .F. ) ;
#252635=ADVANCED_FACE ( 'NONE', ( #101900 ), #144509, .F. ) ;
#252641=ORIENTED_EDGE ( 'NONE', *, *, #155392, .F. ) ;
#252696=CIRCLE ( 'NONE', #106953, 0.8750000000000007772 ) ;
#252738=VECTOR ( 'NONE', #194225, 1000.000000000000000 ) ;
#252788=CIRCLE ( 'NONE', #94570, 4.000000000000003553 ) ;
#252798=DIRECTION ( 'NONE',  ( 0.000000000000000000, -0.1298341882519953860, -0.9915357197604862671 ) ) ;
#252836=DIRECTION ( 'NONE',  ( 0.000000000000000000, -6.982962677686266711E-15, 1.000000000000000000 ) ) ;
#252853=ORIENTED_EDGE ( 'NONE', *, *, #119507, .T. ) ;
#252863=VECTOR ( 'NONE', #26642, 1000.000000000000000 ) ;
#252882=CARTESIAN_POINT ( 'NONE',  ( 18.49362639424906263, 85.44260436789993207, -96.25866655101246749 ) ) ;
#252884=CARTESIAN_POINT ( 'NONE',  ( -21.05000000000000071, 75.90220970870339556, -142.7809220950004203 ) ) ;
#252903=CARTESIAN_POINT ( 'NONE',  ( -20.64999999999999858, 76.00000000001190870, -103.0231074845243029 ) ) ;
#252912=ORIENTED_EDGE ( 'NONE', *, *, #34578, .F. ) ;
#252915=ORIENTED_EDGE ( 'NONE', *, *, #208554, .F. ) ;
#252959=EDGE_CURVE ( 'NONE', #89242, #136488, #136897, .T. ) ;
#253030=EDGE_CURVE ( 'NONE', #54007, #243260, #102575, .T. ) ;
#253066=ORIENTED_EDGE ( 'NONE', *, *, #249198, .F. ) ;
#253079=EDGE_CURVE ( 'NONE', #111919, #105079, #23552, .T. ) ;
#253097=ORIENTED_EDGE ( 'NONE', *, *, #79613, .T. ) ;
#253141=ORIENTED_EDGE ( 'NONE', *, *, #180682, .F. ) ;
#253161=AXIS2_PLACEMENT_3D ( 'NONE', #248638, #205646, #131254 ) ;
#253188=DIRECTION ( 'NONE',  ( -0.000000000000000000, -6.982962677686266711E-15, 1.000000000000000000 ) ) ;
#253216=ORIENTED_EDGE ( 'NONE', *, *, #90496, .T. ) ;
#253258=CARTESIAN_POINT ( 'NONE',  ( -21.30740335185486245, 75.90106547423633288, -143.0797654065522977 ) ) ;
#253271=CARTESIAN_POINT ( 'NONE',  ( 20.94999999999999929, 77.34915357198789820, -95.23561014893439847 ) ) ;
#253291=VERTEX_POINT ( 'NONE', #215936 ) ;
#253302=EDGE_CURVE ( 'NONE', #135981, #121455, #227501, .T. ) ;
#253321=CARTESIAN_POINT ( 'NONE',  ( 20.94999999999999574, 65.37642973952928571, -129.0311622812938310 ) ) ;
#253324=CARTESIAN_POINT ( 'NONE',  ( 22.39999999999999147, 68.20922040163875977, -136.5231074845243597 ) ) ;
#253332=DIRECTION ( 'NONE',  ( 0.000000000000000000, 0.8700118002898356018, -0.4930308989875170078 ) ) ;
#253336=CIRCLE ( 'NONE', #140920, 6.329289321881370611 ) ;
#253344=CIRCLE ( 'NONE', #161614, 0.1000000000000026007 ) ;
#253388=VECTOR ( 'NONE', #124634, 1000.000000000000114 ) ;
#253430=DIRECTION ( 'NONE',  ( -1.000000000000000000, 2.952720810173289112E-16, 2.061873921506763405E-30 ) ) ;
#253434=DIRECTION ( 'NONE',  ( -1.000000000000000000, 0.000000000000000000, -0.000000000000000000 ) ) ;
#253438=ORIENTED_EDGE ( 'NONE', *, *, #91863, .T. ) ;
#253455=DIRECTION ( 'NONE',  ( -1.000000000000000000, 0.000000000000000000, -0.000000000000000000 ) ) ;
#253541=CIRCLE ( 'NONE', #128670, 0.09999999999999971412 ) ;
#253589=CARTESIAN_POINT ( 'NONE',  ( -21.14999999999999858, 69.45934304831089889, -136.5231074845243313 ) ) ;
#253608=DIRECTION ( 'NONE',  ( 0.000000000000000000, -6.982962677686266711E-15, 1.000000000000000000 ) ) ;
#253653=FACE_OUTER_BOUND ( 'NONE', #125407, .T. ) ;
#253698=FACE_OUTER_BOUND ( 'NONE', #231717, .T. ) ;
#253723=ORIENTED_EDGE ( 'NONE', *, *, #63741, .F. ) ;
#253738=CARTESIAN_POINT ( 'NONE',  ( 21.14999999999999503, 76.00000000001217870, -142.7731074845243029 ) ) ;
#253753=EDGE_CURVE ( 'NONE', #130620, #242949, #246757, .T. ) ;
#253791=EDGE_CURVE ( 'NONE', #206647, #93015, #73232, .T. ) ;
#253800=CARTESIAN_POINT ( 'NONE',  ( 21.00000000000000000, 66.25000000001206502, -124.2731074845243597 ) ) ;
#253803=B_SPLINE_CURVE_WITH_KNOTS ( 'NONE', 3,
 ( #31417, #47070, #107050, #190483, #71808, #129203, #110914, #246562 ),
 .UNSPECIFIED., .F., .F.,
 ( 4, 2, 2, 4 ),
 ( 0.000000000000000000, 9.550056980124347803E-05, 0.0001910011396024869561, 0.0003820022792049804173 ),
 .UNSPECIFIED. ) ;
#253808=CYLINDRICAL_SURFACE ( 'NONE', #101089, 0.1000000000000028644 ) ;
#253817=DIRECTION ( 'NONE',  ( 0.000000000000000000, -1.000000000000000000, -6.982962677686265922E-15 ) ) ;
#253819=ORIENTED_EDGE ( 'NONE', *, *, #144457, .T. ) ;
#253836=DIRECTION ( 'NONE',  ( 1.000000000000000000, 0.000000000000000000, 0.000000000000000000 ) ) ;
#253868=CARTESIAN_POINT ( 'NONE',  ( 20.94999999999999929, 87.65000000001192859, -105.9231074845242091 ) ) ;
#253883=CIRCLE ( 'NONE', #20687, 0.1000000000000021289 ) ;
#253900=CARTESIAN_POINT ( 'NONE',  ( 20.94999999999999929, 76.00000000001188027, -98.92310748452429436 ) ) ;
#253909=CARTESIAN_POINT ( 'NONE',  ( 23.14999999999999858, 69.35000000001205933, -124.1731074845243370 ) ) ;
#253936=DIRECTION ( 'NONE',  ( 1.000000000000000000, 0.000000000000000000, 0.000000000000000000 ) ) ;
#253950=EDGE_CURVE ( 'NONE', #3082, #105588, #89749, .T. ) ;
#253968=CARTESIAN_POINT ( 'NONE',  ( -21.05000000000000071, 77.83534155023646406, -124.9679561919613064 ) ) ;
#253980=AXIS2_PLACEMENT_3D ( 'NONE', #8881, #231791, #132685 ) ;
#253984=EDGE_CURVE ( 'NONE', #193833, #117705, #2446, .T. ) ;
#254000=DIRECTION ( 'NONE',  ( -1.000000000000000000, 0.000000000000000000, 0.000000000000000000 ) ) ;
#254004=DIRECTION ( 'NONE',  ( 1.000000000000000000, 0.000000000000000000, 0.000000000000000000 ) ) ;
#254014=CARTESIAN_POINT ( 'NONE',  ( -18.59999999999999787, 66.65000000001198543, -115.2731074845243597 ) ) ;
#254023=DIRECTION ( 'NONE',  ( 0.000000000000000000, 0.9908441862701420355, 0.1350103645453197554 ) ) ;
#254037=ORIENTED_EDGE ( 'NONE', *, *, #62538, .T. ) ;
#254039=CARTESIAN_POINT ( 'NONE',  ( 20.85000000000000142, 64.25000000001190870, -103.0231074845243882 ) ) ;
#254050=ORIENTED_EDGE ( 'NONE', *, *, #187017, .F. ) ;
#254071=AXIS2_PLACEMENT_3D ( 'NONE', #135564, #16929, #97702 ) ;
#254108=AXIS2_PLACEMENT_3D ( 'NONE', #206523, #164837, #146526 ) ;
#254127=VERTEX_POINT ( 'NONE', #144773 ) ;
#254134=ORIENTED_EDGE ( 'NONE', *, *, #24399, .T. ) ;
#254166=DIRECTION ( 'NONE',  ( 4.408576920032447355E-17, 0.1350103645451807555, 0.9908441862701610203 ) ) ;
#254171=ORIENTED_EDGE ( 'NONE', *, *, #249733, .T. ) ;
#254178=CARTESIAN_POINT ( 'NONE',  ( -18.59999999999999787, 76.00000000001190870, -103.0231074845243029 ) ) ;
#254193=DIRECTION ( 'NONE',  ( -7.304098846218134667E-16, 1.000000000000000000, 6.982962677686266711E-15 ) ) ;
#254194=CARTESIAN_POINT ( 'NONE',  ( 18.49999999999999645, 74.16465844978765176, -124.9679561919613207 ) ) ;
#254252=DIRECTION ( 'NONE',  ( -1.000000000000000000, 2.952720810173289112E-16, 2.061873921506763405E-30 ) ) ;
#254284=ORIENTED_EDGE ( 'NONE', *, *, #136116, .T. ) ;
#254285=DIRECTION ( 'NONE',  ( 0.000000000000000000, -0.1350103645451807555, -0.9908441862701610203 ) ) ;
#254296=ORIENTED_EDGE ( 'NONE', *, *, #73038, .F. ) ;
#254300=VERTEX_POINT ( 'NONE', #213753 ) ;
#254362=ORIENTED_EDGE ( 'NONE', *, *, #190344, .T. ) ;
#254368=ORIENTED_EDGE ( 'NONE', *, *, #59038, .F. ) ;
#254375=EDGE_LOOP ( 'NONE', ( #235190, #189324, #14233 ) ) ;
#254451=ORIENTED_EDGE ( 'NONE', *, *, #138946, .T. ) ;
#254453=VECTOR ( 'NONE', #217311, 1000.000000000000000 ) ;
#254454=ORIENTED_EDGE ( 'NONE', *, *, #174924, .T. ) ;
#254467=DIRECTION ( 'NONE',  ( -0.000000000000000000, 6.982962677686266711E-15, -1.000000000000000000 ) ) ;
#254474=ORIENTED_EDGE ( 'NONE', *, *, #217372, .T. ) ;
#254488=EDGE_CURVE ( 'NONE', #180506, #62035, #248396, .T. ) ;
#254537=CARTESIAN_POINT ( 'NONE',  ( -18.50000000000000000, 66.65000000001205649, -124.1731074845243654 ) ) ;
#254549=ADVANCED_FACE ( 'NONE', ( #171467 ), #72344, .T. ) ;
#254553=ADVANCED_FACE ( 'NONE', ( #74925 ), #148587, .F. ) ;
#254598=VERTEX_POINT ( 'NONE', #134837 ) ;
#254609=ORIENTED_EDGE ( 'NONE', *, *, #9864, .T. ) ;
#254617=CARTESIAN_POINT ( 'NONE',  ( -20.94999999999999929, 70.10000000001197407, -113.2422072491807086 ) ) ;
#254630=DIRECTION ( 'NONE',  ( 0.000000000000000000, 0.000000000000000000, 1.000000000000000000 ) ) ;
#254636=ORIENTED_EDGE ( 'NONE', *, *, #252432, .T. ) ;
#254657=ORIENTED_EDGE ( 'NONE', *, *, #156013, .T. ) ;
#254661=CYLINDRICAL_SURFACE ( 'NONE', #22515, 11.80000000000000426 ) ;
#254663=CARTESIAN_POINT ( 'NONE',  ( -21.22070241538126112, 69.53005372714252985, -136.6220265150593605 ) ) ;
#254675=AXIS2_PLACEMENT_3D ( 'NONE', #133688, #232814, #154573 ) ;
#254677=CARTESIAN_POINT ( 'NONE',  ( 20.94999999999999574, 69.65000000001205649, -126.6792853948412159 ) ) ;
#254694=CARTESIAN_POINT ( 'NONE',  ( 18.46947024752525479, 85.50929715716807777, -129.5364180358261592 ) ) ;
#254711=CIRCLE ( 'NONE', #42377, 11.80000000000000426 ) ;
#254715=DIRECTION ( 'NONE',  ( 1.000000000000000000, 0.000000000000000000, 0.000000000000000000 ) ) ;
#254742=CIRCLE ( 'NONE', #142363, 0.9750000000000036415 ) ;
#254776=CARTESIAN_POINT ( 'NONE',  ( 20.04142135623730070, 64.25000000001199396, -115.1731074845243796 ) ) ;
#254780=ORIENTED_EDGE ( 'NONE', *, *, #194321, .F. ) ;
#254781=CARTESIAN_POINT ( 'NONE',  ( -18.31331870001012163, 85.53629471919282423, -96.15452879353861704 ) ) ;
#254802=ORIENTED_EDGE ( 'NONE', *, *, #204840, .F. ) ;
#254895=DIRECTION ( 'NONE',  ( -0.000000000000000000, 1.000000000000000000, 6.982962677686267499E-15 ) ) ;
#254904=FACE_OUTER_BOUND ( 'NONE', #73611, .T. ) ;
#254909=ORIENTED_EDGE ( 'NONE', *, *, #203713, .F. ) ;
#254934=CYLINDRICAL_SURFACE ( 'NONE', #118494, 0.1000000000000028644 ) ;
#254940=FACE_OUTER_BOUND ( 'NONE', #168665, .T. ) ;
#254943=CARTESIAN_POINT ( 'NONE',  ( -20.94999999999999929, 74.73821383144705521, -128.4366085209788366 ) ) ;
#254949=CARTESIAN_POINT ( 'NONE',  ( -18.50000000000000000, 66.65000000001198543, -115.3731074845243683 ) ) ;
#254952=LINE ( 'NONE', #213312, #242856 ) ;
#254962=CARTESIAN_POINT ( 'NONE',  ( -20.64999999999999858, 74.00000000001199396, -116.2477294072864140 ) ) ;
#254984=DIRECTION ( 'NONE',  ( -1.000000000000000000, 0.000000000000000000, 0.000000000000000000 ) ) ;
#255001=ORIENTED_EDGE ( 'NONE', *, *, #104662, .F. ) ;
#255014=VECTOR ( 'NONE', #153282, 1000.000000000000000 ) ;
#255040=CARTESIAN_POINT ( 'NONE',  ( -21.70464131381649509, 68.90464198104429272, -136.5231074845243313 ) ) ;
#255067=AXIS2_PLACEMENT_3D ( 'NONE', #118313, #257755, #221232 ) ;
#255079=LINE ( 'NONE', #179473, #82555 ) ;
#255083=ORIENTED_EDGE ( 'NONE', *, *, #196998, .T. ) ;
#255094=CARTESIAN_POINT ( 'NONE',  ( -20.64999999999999858, 74.00000000001205080, -123.2984855617622060 ) ) ;
#255117=AXIS2_PLACEMENT_3D ( 'NONE', #186048, #8692, #188602 ) ;
#255124=DIRECTION ( 'NONE',  ( 0.000000000000000000, -6.308085367188367561E-15, 1.000000000000000000 ) ) ;
#255130=ORIENTED_EDGE ( 'NONE', *, *, #241672, .F. ) ;
#255141=CIRCLE ( 'NONE', #163626, 0.1000000000000028644 ) ;
#255149=ORIENTED_EDGE ( 'NONE', *, *, #31450, .F. ) ;
#255164=CARTESIAN_POINT ( 'NONE',  ( 20.95512820512820440, 67.12384868372393498, -124.3731074845243683 ) ) ;
#255166=LINE ( 'NONE', #38756, #171381 ) ;
#255167=CARTESIAN_POINT ( 'NONE',  ( 23.15000000000000213, 87.48912529308798014, -106.1231074845242262 ) ) ;
#255169=CARTESIAN_POINT ( 'NONE',  ( 23.15000000000000213, 87.65000000001192859, -106.1231074845242262 ) ) ;
#255215=CYLINDRICAL_SURFACE ( 'NONE', #93354, 0.1000000000000028644 ) ;
#255219=DIRECTION ( 'NONE',  ( 0.000000000000000000, 0.000000000000000000, 1.000000000000000000 ) ) ;
#255242=CYLINDRICAL_SURFACE ( 'NONE', #106117, 11.80000000000000426 ) ;
#255255=CIRCLE ( 'NONE', #167857, 0.1000000000000028644 ) ;
#255272=CARTESIAN_POINT ( 'NONE',  ( -23.25000000000000000, 76.00000000001190870, -103.0231074845243029 ) ) ;
#255299=DIRECTION ( 'NONE',  ( 0.000000000000000000, 7.056502275159890043E-15, -1.000000000000000000 ) ) ;
#255304=CARTESIAN_POINT ( 'NONE',  ( 21.87500000000000355, 66.25000000001205080, -124.1731074845243654 ) ) ;
#255345=ORIENTED_EDGE ( 'NONE', *, *, #28911, .T. ) ;
#255400=CIRCLE ( 'NONE', #142997, 0.1000000000000028644 ) ;
#255471=DIRECTION ( 'NONE',  ( 0.000000000000000000, 0.4930308989875575865, 0.8700118002898125091 ) ) ;
#255478=ORIENTED_EDGE ( 'NONE', *, *, #241856, .F. ) ;
#255486=DIRECTION ( 'NONE',  ( -0.000000000000000000, 1.000000000000000000, 6.982962677686266711E-15 ) ) ;
#255487=ORIENTED_EDGE ( 'NONE', *, *, #113708, .T. ) ;
#255490=DIRECTION ( 'NONE',  ( 1.000000000000000000, 0.000000000000000000, 0.000000000000000000 ) ) ;
#255495=CARTESIAN_POINT ( 'NONE',  ( -23.15000000000000213, 64.35000000001198828, -115.1731074845243938 ) ) ;
#255505=ORIENTED_EDGE ( 'NONE', *, *, #176363, .T. ) ;
#255544=VERTEX_POINT ( 'NONE', #205783 ) ;
#255546=ORIENTED_EDGE ( 'NONE', *, *, #193896, .T. ) ;
#255556=EDGE_LOOP ( 'NONE', ( #112599, #127514, #20996, #154637, #85993 ) ) ;
#255575=DIRECTION ( 'NONE',  ( -1.000000000000000000, -0.000000000000000000, -0.000000000000000000 ) ) ;
#255598=CARTESIAN_POINT ( 'NONE',  ( -18.59999999999999787, 74.83729825007408465, -128.4231074845243086 ) ) ;
#255613=ORIENTED_EDGE ( 'NONE', *, *, #47798, .F. ) ;
#255630=PLANE ( 'NONE',  #202723 ) ;
#255696=VERTEX_POINT ( 'NONE', #171837 ) ;
#255704=CARTESIAN_POINT ( 'NONE',  ( 18.59999999999999432, 77.13501884592203339, -95.30613060109196510 ) ) ;
#255706=ORIENTED_EDGE ( 'NONE', *, *, #243383, .F. ) ;
#255717=ORIENTED_EDGE ( 'NONE', *, *, #215082, .F. ) ;
#255723=DIRECTION ( 'NONE',  ( -1.000000000000000000, 0.000000000000000000, -0.000000000000000000 ) ) ;
#255734=DIRECTION ( 'NONE',  ( -1.000000000000000000, 0.000000000000000000, 0.000000000000000000 ) ) ;
#255748=CIRCLE ( 'NONE', #55849, 0.1000000000000052097 ) ;
#255757=DIRECTION ( 'NONE',  ( 1.000000000000000000, 0.000000000000000000, 0.000000000000000000 ) ) ;
#255779=AXIS2_PLACEMENT_3D ( 'NONE', #226780, #37587, #117113 ) ;
#255786=DIRECTION ( 'NONE',  ( 0.000000000000000000, 6.982962677686266711E-15, -1.000000000000000000 ) ) ;
#255801=VERTEX_POINT ( 'NONE', #178244 ) ;
#255803=DIRECTION ( 'NONE',  ( 0.000000000000000000, 0.000000000000000000, 1.000000000000000000 ) ) ;
#255817=CIRCLE ( 'NONE', #126870, 0.09999999999999939493 ) ;
#255830=ORIENTED_EDGE ( 'NONE', *, *, #138600, .T. ) ;
#255871=CARTESIAN_POINT ( 'NONE',  ( 18.59999999999999076, 64.35000000001221565, -148.2731074845243882 ) ) ;
#255914=CIRCLE ( 'NONE', #31159, 11.64999999999999325 ) ;
#255915=CIRCLE ( 'NONE', #164405, 0.1000000000000052097 ) ;
#255936=CARTESIAN_POINT ( 'NONE',  ( -18.46946985241234529, 85.50931722872354612, -129.5364449190244045 ) ) ;
#255958=ADVANCED_FACE ( 'NONE', ( #63384 ), #65969, .T. ) ;
#255972=CARTESIAN_POINT ( 'NONE',  ( 18.45036689428336274, 85.49018414334089755, -129.5104116570378778 ) ) ;
#255997=ORIENTED_EDGE ( 'NONE', *, *, #215082, .T. ) ;
#256015=VECTOR ( 'NONE', #169051, 1000.000000000000000 ) ;
#256023=DIRECTION ( 'NONE',  ( -0.000000000000000000, -0.8660254037844420383, 0.4999999999999943379 ) ) ;
#256039=ORIENTED_EDGE ( 'NONE', *, *, #198169, .F. ) ;
#256081=AXIS2_PLACEMENT_3D ( 'NONE', #30926, #55548, #50427 ) ;
#256093=ORIENTED_EDGE ( 'NONE', *, *, #239539, .T. ) ;
#256105=CARTESIAN_POINT ( 'NONE',  ( -20.94999999999999929, 74.83729825007408465, -128.4231074845243086 ) ) ;
#256114=LINE ( 'NONE', #56659, #192776 ) ;
#256117=VECTOR ( 'NONE', #201459, 1000.000000000000000 ) ;
#256134=DIRECTION ( 'NONE',  ( 0.000000000000000000, 6.982962677686266711E-15, -1.000000000000000000 ) ) ;
#256165=EDGE_LOOP ( 'NONE', ( #188206, #47567, #148380, #227194 ) ) ;
#256167=ORIENTED_EDGE ( 'NONE', *, *, #135861, .T. ) ;
#256204=CARTESIAN_POINT ( 'NONE',  ( 18.50000000000000000, 85.50000000001222134, -148.2731074845242460 ) ) ;
#256205=DIRECTION ( 'NONE',  ( -0.000000000000000000, 1.000000000000000000, 8.717686153663073805E-15 ) ) ;
#256241=DIRECTION ( 'NONE',  ( 0.000000000000000000, 0.000000000000000000, -1.000000000000000000 ) ) ;
#256257=DIRECTION ( 'NONE',  ( 0.000000000000000000, 7.086529944415894657E-15, -1.000000000000000000 ) ) ;
#256298=CYLINDRICAL_SURFACE ( 'NONE', #122533, 0.09999999999999939493 ) ;
#256302=CARTESIAN_POINT ( 'NONE',  ( -18.50000000000000000, 64.35000000001208775, -129.5083017138703667 ) ) ;
#256321=DIRECTION ( 'NONE',  ( 0.000000000000000000, -6.467318590049456648E-15, 1.000000000000000000 ) ) ;
#256350=ORIENTED_EDGE ( 'NONE', *, *, #57035, .T. ) ;
#256358=ORIENTED_EDGE ( 'NONE', *, *, #206780, .F. ) ;
#256372=VECTOR ( 'NONE', #74000, 1000.000000000000000 ) ;
#256373=DIRECTION ( 'NONE',  ( 0.000000000000000000, 8.770518838402102073E-15, -1.000000000000000000 ) ) ;
#256446=CARTESIAN_POINT ( 'NONE',  ( 21.10710606213542206, 67.22310597611885896, -124.2821109581249317 ) ) ;
#256455=DIRECTION ( 'NONE',  ( 0.000000000000000000, 0.1350103645451945777, -0.9908441862701589109 ) ) ;
#256472=EDGE_CURVE ( 'NONE', #198296, #252068, #119752, .T. ) ;
#256529=CIRCLE ( 'NONE', #69362, 0.09999999999998898659 ) ;
#256554=CYLINDRICAL_SURFACE ( 'NONE', #19741, 0.5000000000000004441 ) ;
#256580=DIRECTION ( 'NONE',  ( -1.000000000000000000, 0.000000000000000000, 0.000000000000000000 ) ) ;
#256584=CARTESIAN_POINT ( 'NONE',  ( -21.05000000000000071, 76.00000000001190870, -103.0231074845243029 ) ) ;
#256619=FACE_OUTER_BOUND ( 'NONE', #250432, .T. ) ;
#256626=ADVANCED_FACE ( 'NONE', ( #250265 ), #169489, .T. ) ;
#256636=FACE_OUTER_BOUND ( 'NONE', #177372, .T. ) ;
#256681=CARTESIAN_POINT ( 'NONE',  ( 21.05000000000000071, 76.00000000001213607, -136.5231074845242745 ) ) ;
#256687=ADVANCED_FACE ( 'NONE', ( #256619 ), #117178, .T. ) ;
#256748=CARTESIAN_POINT ( 'NONE',  ( 19.99999999999998934, 64.35000000001198828, -115.2731074845243739 ) ) ;
#256749=DIRECTION ( 'NONE',  ( 0.000000000000000000, 0.000000000000000000, -1.000000000000000000 ) ) ;
#256794=ORIENTED_EDGE ( 'NONE', *, *, #124347, .T. ) ;
#256815=CARTESIAN_POINT ( 'NONE',  ( -21.44999999999999929, 68.65000000001205649, -124.2731074845243455 ) ) ;
#256871=EDGE_CURVE ( 'NONE', #220201, #146363, #26677, .T. ) ;
#256875=CARTESIAN_POINT ( 'NONE',  ( 18.49999999999998934, 56.14960075277857499, -134.2428044267230689 ) ) ;
#256924=DIRECTION ( 'NONE',  ( -4.408576920032448588E-17, -0.1350103645451807555, -0.9908441862701609093 ) ) ;
#256941=ORIENTED_EDGE ( 'NONE', *, *, #35369, .T. ) ;
#256948=ADVANCED_FACE ( 'NONE', ( #145700 ), #127437, .F. ) ;
#256954=TOROIDAL_SURFACE ( 'NONE', #206937, 0.2000000000000000111, 0.1000000000000000056 ) ;
#256963=DIRECTION ( 'NONE',  ( 1.000000000000000000, 0.000000000000000000, 0.000000000000000000 ) ) ;
#256970=LINE ( 'NONE', #191952, #15142 ) ;
#256992=EDGE_CURVE ( 'NONE', #171429, #162828, #43408, .T. ) ;
#257001=ADVANCED_FACE ( 'NONE', ( #165278 ), #101629, .T. ) ;
#257004=ORIENTED_EDGE ( 'NONE', *, *, #76568, .F. ) ;
#257011=CARTESIAN_POINT ( 'NONE',  ( -20.85000000000000142, 77.13501884592203339, -95.30613060109196510 ) ) ;
#257045=TOROIDAL_SURFACE ( 'NONE', #223759, 0.6000000000000013101, 0.1000000000000000056 ) ;
#257071=ADVANCED_FACE ( 'NONE', ( #175570 ), #256298, .F. ) ;
#257075=ADVANCED_FACE ( 'NONE', ( #235513 ), #231690, .F. ) ;
#257090=DIRECTION ( 'NONE',  ( -0.7071067811865475727, 0.7071067811865475727, 4.937700262164531476E-15 ) ) ;
#257094=DIRECTION ( 'NONE',  ( -1.000000000000000000, 0.000000000000000000, 0.000000000000000000 ) ) ;
#257115=EDGE_CURVE ( 'NONE', #139103, #39149, #247400, .T. ) ;
#257139=CARTESIAN_POINT ( 'NONE',  ( -21.05000000000000071, 77.36087058720413268, -128.4501095574333362 ) ) ;
#257163=CARTESIAN_POINT ( 'NONE',  ( -20.54999999999999716, 84.66355140188112216, -112.5472086025915388 ) ) ;
#257165=EDGE_CURVE ( 'NONE', #234233, #147787, #255748, .T. ) ;
#257197=EDGE_CURVE ( 'NONE', #117705, #137344, #181977, .T. ) ;
#257238=CARTESIAN_POINT ( 'NONE',  ( -23.15000000000000213, 74.00000000001199396, -116.2477294072864140 ) ) ;
#257257=CARTESIAN_POINT ( 'NONE',  ( 18.41789779300686192, 85.50000000001209344, -129.4910378181635622 ) ) ;
#257259=ORIENTED_EDGE ( 'NONE', *, *, #94608, .F. ) ;
#257260=ADVANCED_FACE ( 'NONE', ( #197669 ), #147460, .T. ) ;
#257294=ORIENTED_EDGE ( 'NONE', *, *, #172491, .F. ) ;
#257326=AXIS2_PLACEMENT_3D ( 'NONE', #15313, #94821, #174420 ) ;
#257338=CARTESIAN_POINT ( 'NONE',  ( -18.48408745364680428, 85.66432225867497152, -96.34002895119586185 ) ) ;
#257342=CYLINDRICAL_SURFACE ( 'NONE', #52683, 0.09999999999999976963 ) ;
#257352=EDGE_LOOP ( 'NONE', ( #17521, #32258, #139615, #241518 ) ) ;
#257378=CARTESIAN_POINT ( 'NONE',  ( 21.05000000000000071, 76.08559286337410299, -142.9367702193934804 ) ) ;
#257379=CARTESIAN_POINT ( 'NONE',  ( -21.05000000000000071, 76.00000000001190870, -103.0231074845243029 ) ) ;
#257392=CARTESIAN_POINT ( 'NONE',  ( -18.59999999999999787, 77.16270174995010223, -128.4231074845242802 ) ) ;
#257399=FACE_OUTER_BOUND ( 'NONE', #81183, .T. ) ;
#257466=DIRECTION ( 'NONE',  ( 0.000000000000000000, 0.000000000000000000, 1.000000000000000000 ) ) ;
#257483=DIRECTION ( 'NONE',  ( 4.239556034732056743E-17, 0.1298341882519953860, 0.9915357197604862671 ) ) ;
#257505=EDGE_CURVE ( 'NONE', #13648, #38706, #160331, .T. ) ;
#257536=VECTOR ( 'NONE', #52224, 1000.000000000000227 ) ;
#257565=DIRECTION ( 'NONE',  ( 0.000000000000000000, -2.775557561563196798E-13, -1.000000000000000000 ) ) ;
#257573=AXIS2_PLACEMENT_3D ( 'NONE', #223620, #24175, #29337 ) ;
#257590=DIRECTION ( 'NONE',  ( 0.000000000000000000, 0.8700118002898356018, -0.4930308989875170078 ) ) ;
#257609=DIRECTION ( 'NONE',  ( -7.304098846217948299E-16, -1.000000000000000000, 0.000000000000000000 ) ) ;
#257634=EDGE_LOOP ( 'NONE', ( #48563, #40835, #61375 ) ) ;
#257640=CARTESIAN_POINT ( 'NONE',  ( -20.64999999999999858, 84.73084112150731073, -112.6211822035085675 ) ) ;
#257659=EDGE_LOOP ( 'NONE', ( #12377, #152059, #118615, #217931, #204708 ) ) ;
#257661=EDGE_CURVE ( 'NONE', #241341, #45688, #110401, .T. ) ;
#257690=DIRECTION ( 'NONE',  ( 0.000000000000000000, -7.086529944415894657E-15, 1.000000000000000000 ) ) ;
#257721=DIRECTION ( 'NONE',  ( 0.000000000000000000, 7.056502275159890832E-15, -1.000000000000000000 ) ) ;
#257739=DIRECTION ( 'NONE',  ( 0.000000000000000000, -7.147358527629766941E-15, 1.000000000000000000 ) ) ;
#257740=AXIS2_PLACEMENT_3D ( 'NONE', #127626, #207172, #28577 ) ;
#257751=VERTEX_POINT ( 'NONE', #87358 ) ;
#257755=DIRECTION ( 'NONE',  ( 1.000000000000000000, 0.000000000000000000, 0.000000000000000000 ) ) ;
#257761=CARTESIAN_POINT ( 'NONE',  ( 20.94999999999999929, 76.00000000001189449, -101.0231074845243029 ) ) ;
#257814=CARTESIAN_POINT ( 'NONE',  ( 18.59999999999999076, 74.16465844978765176, -124.9679561919613207 ) ) ;
#257874=CARTESIAN_POINT ( 'NONE',  ( 20.94999999999999929, 76.00000000001188027, -99.02310748452428868 ) ) ;
#257933=AXIS2_PLACEMENT_3D ( 'NONE', #180878, #81729, #243403 ) ;
#257946=CARTESIAN_POINT ( 'NONE',  ( -23.25000000000000000, 76.00000000001190870, -103.0231074845243029 ) ) ;
#257954=AXIS2_PLACEMENT_3D ( 'NONE', #254178, #93832, #53428 ) ;
#257970=ORIENTED_EDGE ( 'NONE', *, *, #141713, .T. ) ;
#257983=VERTEX_POINT ( 'NONE', #41551 ) ;
#257988=CARTESIAN_POINT ( 'NONE',  ( 21.05000000000000071, 76.00000000001213607, -136.5231074845242745 ) ) ;
#257989=DIRECTION ( 'NONE',  ( 0.000000000000000000, -1.000000000000000000, 6.938893903907030216E-14 ) ) ;
#258008=ADVANCED_FACE ( 'NONE', ( #42810 ), #147845, .T. ) ;
#258017=CARTESIAN_POINT ( 'NONE',  ( -20.54999999999999716, 76.00000000001213607, -136.5231074845242745 ) ) ;
#258043=CARTESIAN_POINT ( 'NONE',  ( 18.59999999999999787, 86.35479209693734504, -109.2665665014504697 ) ) ;
#258052=EDGE_CURVE ( 'NONE', #176995, #74814, #2235, .T. ) ;
#258069=DIRECTION ( 'NONE',  ( 0.000000000000000000, 1.000000000000000000, 0.000000000000000000 ) ) ;
#258083=CARTESIAN_POINT ( 'NONE',  ( 18.39999999999999858, 85.60000000001186038, -96.32291809330219223 ) ) ;
#258101=CARTESIAN_POINT ( 'NONE',  ( -23.15000000000000213, 73.40000000001205649, -123.2984855617622202 ) ) ;
ENDSEC;
END-ISO-10303-21;
